ISO-10303-21;
HEADER;
FILE_DESCRIPTION (('STEP AP214'),
    '1' );
FILE_NAME ('straight bevel gear(wobble out)_iso_ISO - Straight bevel gear 2M 48GT 47PT 20PA 5FW ---48O1H50MD20.0S1.step',
    '2026-10-08T08:02:49',
    ( '' ),
    ( '' ),
    'SwSTEP 2.0',
    'SolidWorks 2026',
    '' );
FILE_SCHEMA (( 'AUTOMOTIVE_DESIGN' ));
ENDSEC;

DATA;
#2=ORIENTED_EDGE ( 'NONE', *, *, #40135, .F. ) ;
#3=CARTESIAN_POINT ( 'NONE',  ( -6.017396004339686577, 14.95000090562881390, 11.47005965438143882 ) ) ;
#4=VERTEX_POINT ( 'NONE', #15118 ) ;
#18=ORIENTED_EDGE ( 'NONE', *, *, #60103, .F. ) ;
#32=ORIENTED_EDGE ( 'NONE', *, *, #35814, .T. ) ;
#36=DIRECTION ( 'NONE',  ( 0.000000000000000000, 0.000000000000000000, 1.000000000000000000 ) ) ;
#38=CARTESIAN_POINT ( 'NONE',  ( 1.827326673878743257, 6.839036141888570342, -42.50320212329573621 ) ) ;
#41=CARTESIAN_POINT ( 'NONE',  ( 0.1313383488274124655, -37.02311703718871883, 22.11173226734828745 ) ) ;
#42=CARTESIAN_POINT ( 'NONE',  ( 0.6025881611877910160, 48.10699274197334319, 0.2181813582440121635 ) ) ;
#51=CARTESIAN_POINT ( 'NONE',  ( -6.015611763856276717, -18.68122482568281839, 2.465697960550983225 ) ) ;
#52=ORIENTED_EDGE ( 'NONE', *, *, #55367, .T. ) ;
#55=DIRECTION ( 'NONE',  ( -1.000000000000000000, -0.000000000000000000, -0.000000000000000000 ) ) ;
#57=ORIENTED_EDGE ( 'NONE', *, *, #25597, .F. ) ;
#59=CONICAL_SURFACE ( 'NONE', #54074, 42.92674063221959813, 1.485477209440487556 ) ;
#73=CARTESIAN_POINT ( 'NONE',  ( 0.1073791018717483448, -30.83464511437118816, -30.14884492832378626 ) ) ;
#82=CARTESIAN_POINT ( 'NONE',  ( -6.015611763856276717, 17.40650793417854203, -7.216738110653091454 ) ) ;
#90=EDGE_CURVE ( 'NONE', #9871, #29097, #13329, .T. ) ;
#98=CARTESIAN_POINT ( 'NONE',  ( 0.1310142868023682072, 37.66054729763593656, -21.00772081177039041 ) ) ;
#116=CARTESIAN_POINT ( 'NONE',  ( 0.1102847568649952675, 42.76743495471822598, 5.537466591275816974 ) ) ;
#121=DIRECTION ( 'NONE',  ( 0.000000000000000000, 0.000000000000000000, 1.000000000000000000 ) ) ;
#127=CARTESIAN_POINT ( 'NONE',  ( -5.995132425357893702, -14.95525565067283047, 11.46484027925362170 ) ) ;
#134=EDGE_CURVE ( 'NONE', #31710, #59272, #52135, .T. ) ;
#137=B_SPLINE_CURVE_WITH_KNOTS ( 'NONE', 3,
 ( #31189, #25263, #45615, #30260, #59373, #21803, #54354, #49372, #40937, #34673 ),
 .UNSPECIFIED., .F., .F.,
 ( 4, 3, 3, 4 ),
 ( 2.027574016683678720E-17, 0.0002618515315864107518, 0.0003927756766341517500, 0.0005236741812375312905 ),
 .UNSPECIFIED. ) ;
#138=CARTESIAN_POINT ( 'NONE',  ( -6.015611763856276717, 11.46610900684744472, -14.95313250337417799 ) ) ;
#157=ORIENTED_EDGE ( 'NONE', *, *, #10599, .T. ) ;
#158=CARTESIAN_POINT ( 'NONE',  ( 0.6001305935487315502, 28.87057754790937381, -38.48510059944018735 ) ) ;
#163=CARTESIAN_POINT ( 'NONE',  ( 0.6001305935487422083, -46.33281397023073112, 12.95698906763730029 ) ) ;
#165=CARTESIAN_POINT ( 'NONE',  ( 5.880360259849739535, -21.25991003419923331, -43.00389496650606702 ) ) ;
#166=B_SPLINE_CURVE_WITH_KNOTS ( 'NONE', 3,
 ( #1737, #48445, #29959, #44100, #20871, #49069 ),
 .UNSPECIFIED., .F., .F.,
 ( 4, 2, 4 ),
 ( 1.764953265579307567E-18, 0.0002450742804987333630, 0.0004901485609974648829 ),
 .UNSPECIFIED. ) ;
#177=CARTESIAN_POINT ( 'NONE',  ( 0.3622758884714730732, 26.89560658783340585, 33.69533458712353280 ) ) ;
#178=CARTESIAN_POINT ( 'NONE',  ( 0.6009452777970410997, 28.93864923253898169, -38.43042656245044242 ) ) ;
#179=CARTESIAN_POINT ( 'NONE',  ( 0.1081432562775998252, 16.89351827868222600, -39.67792926340383985 ) ) ;
#182=CARTESIAN_POINT ( 'NONE',  ( -6.015611763856276717, 14.95313250337430055, 11.46610900684727952 ) ) ;
#184=ORIENTED_EDGE ( 'NONE', *, *, #61518, .T. ) ;
#186=LINE ( 'NONE', #38450, #30341 ) ;
#190=VECTOR ( 'NONE', #29724, 1000.000000000000114 ) ;
#195=CARTESIAN_POINT ( 'NONE',  ( 4.975801465491695552, -3.702618843597113685, -47.76942479135485087 ) ) ;
#198=FACE_OUTER_BOUND ( 'NONE', #52449, .T. ) ;
#199=VERTEX_POINT ( 'NONE', #3761 ) ;
#218=CARTESIAN_POINT ( 'NONE',  ( 0.6023143664670691511, 33.83148565876883396, 34.20175727332139815 ) ) ;
#220=CARTESIAN_POINT ( 'NONE',  ( -5.995132425357893702, -16.32377331145327304, 9.414704407577744405 ) ) ;
#226=VERTEX_POINT ( 'NONE', #61691 ) ;
#235=EDGE_CURVE ( 'NONE', #45826, #24987, #55024, .T. ) ;
#236=CARTESIAN_POINT ( 'NONE',  ( 0.1095718737110178281, -16.74012863188530531, 39.74279513315646284 ) ) ;
#246=B_SPLINE_CURVE_WITH_KNOTS ( 'NONE', 3,
 ( #22467, #55345, #2101, #3338, #21239, #30943 ),
 .UNSPECIFIED., .F., .F.,
 ( 4, 2, 4 ),
 ( 3.496446946337351263E-18, 0.0002450742804987353146, 0.0004901485609974671597 ),
 .UNSPECIFIED. ) ;
#253=CARTESIAN_POINT ( 'NONE',  ( 0.8751705887134553219, -34.63284514348562482, -33.37254303619542384 ) ) ;
#258=ORIENTED_EDGE ( 'NONE', *, *, #20245, .T. ) ;
#265=CARTESIAN_POINT ( 'NONE',  ( 4.549368137175248350, 0.000000000000000000, 0.000000000000000000 ) ) ;
#267=ORIENTED_EDGE ( 'NONE', *, *, #21360, .T. ) ;
#286=EDGE_CURVE ( 'NONE', #21806, #20018, #34185, .T. ) ;
#288=B_SPLINE_CURVE_WITH_KNOTS ( 'NONE', 3,
 ( #44380, #20544, #58724, #11151 ),
 .UNSPECIFIED., .F., .F.,
 ( 4, 4 ),
 ( 5.818439421673296370E-18, 0.004566006591234646368 ),
 .UNSPECIFIED. ) ;
#292=EDGE_CURVE ( 'NONE', #49088, #39212, #16990, .T. ) ;
#293=B_SPLINE_CURVE_WITH_KNOTS ( 'NONE', 3,
 ( #46059, #55716, #27232, #21301, #12534, #30685 ),
 .UNSPECIFIED., .F., .F.,
 ( 4, 2, 4 ),
 ( 9.842382305685178914E-18, 0.0002450742804987399766, 0.0004901485609974700871 ),
 .UNSPECIFIED. ) ;
#314=ADVANCED_FACE ( 'NONE', ( #10034 ), #32031, .F. ) ;
#327=CARTESIAN_POINT ( 'NONE',  ( 0.5998501479064708430, 5.759754759340140140, 47.76154736470759588 ) ) ;
#332=CARTESIAN_POINT ( 'NONE',  ( 0.5980894510889448457, 47.60453381548683893, 6.974827154144264796 ) ) ;
#333=EDGE_CURVE ( 'NONE', #28532, #55039, #19988, .T. ) ;
#334=CARTESIAN_POINT ( 'NONE',  ( 0.8760168074887090262, 44.09317760313751933, -19.22870327415257563 ) ) ;
#335=B_SPLINE_CURVE_WITH_KNOTS ( 'NONE', 3,
 ( #7423, #26237, #46002, #7741 ),
 .UNSPECIFIED., .F., .F.,
 ( 4, 4 ),
 ( 6.254634441385501517E-18, 0.004566006591234648103 ),
 .UNSPECIFIED. ) ;
#338=CARTESIAN_POINT ( 'NONE',  ( 2.301430502907644726, 19.56449039932732603, -43.86847929982167216 ) ) ;
#341=CARTESIAN_POINT ( 'NONE',  ( 0.6001305935487315502, 6.798494447611584057, 47.62765676940946236 ) ) ;
#344=CARTESIAN_POINT ( 'NONE',  ( 0.5998501479064699549, 48.10473956285920138, -0.5236536531309904374 ) ) ;
#351=VERTEX_POINT ( 'NONE', #43564 ) ;
#360=ORIENTED_EDGE ( 'NONE', *, *, #48950, .T. ) ;
#364=B_SPLINE_CURVE_WITH_KNOTS ( 'NONE', 3,
 ( #15023, #38221, #57268, #19406 ),
 .UNSPECIFIED., .F., .F.,
 ( 4, 4 ),
 ( 2.292215966409847280E-17, 0.004564976165746187711 ),
 .UNSPECIFIED. ) ;
#369=ORIENTED_EDGE ( 'NONE', *, *, #45796, .F. ) ;
#373=CARTESIAN_POINT ( 'NONE',  ( 0.8760168074886960365, -28.57146030081953114, -38.69913431881812471 ) ) ;
#374=CIRCLE ( 'NONE', #52438, 42.92674063221959813 ) ;
#375=DIRECTION ( 'NONE',  ( -0.1024043820194934368, 0.2447326578667261276, 0.9641676559171094008 ) ) ;
#379=ORIENTED_EDGE ( 'NONE', *, *, #18746, .F. ) ;
#389=CARTESIAN_POINT ( 'NONE',  ( 4.549368137175248350, 0.000000000000000000, 0.000000000000000000 ) ) ;
#400=EDGE_CURVE ( 'NONE', #39651, #55243, #39806, .T. ) ;
#408=CARTESIAN_POINT ( 'NONE',  ( 0.8751705887134423323, -13.30665218149394669, 46.21789262997734227 ) ) ;
#409=CARTESIAN_POINT ( 'NONE',  ( 0.8760168074887090262, 11.58706983520326084, -46.68716261866164530 ) ) ;
#411=DIRECTION ( 'NONE',  ( -1.000000000000000000, -0.000000000000000000, -0.000000000000000000 ) ) ;
#416=CARTESIAN_POINT ( 'NONE',  ( 0.1103310638050662013, 30.55179781597996680, -30.43528225250908648 ) ) ;
#418=B_SPLINE_CURVE_WITH_KNOTS ( 'NONE', 3,
 ( #44504, #16914, #36031, #25057, #6222, #26285 ),
 .UNSPECIFIED., .F., .F.,
 ( 4, 2, 4 ),
 ( 1.266823315017301927E-16, 0.0002450741128632354863, 0.0004901482257263442294 ),
 .UNSPECIFIED. ) ;
#420=ORIENTED_EDGE ( 'NONE', *, *, #21979, .T. ) ;
#426=VECTOR ( 'NONE', #13703, 1000.000000000000000 ) ;
#427=CARTESIAN_POINT ( 'NONE',  ( 2.643462169533613793, -17.09809940585690313, 44.89050350746123286 ) ) ;
#429=CARTESIAN_POINT ( 'NONE',  ( 0.6254087463353900089, 23.45485308995599993, -42.00124903776048058 ) ) ;
#431=CARTESIAN_POINT ( 'NONE',  ( 0.1073791018717578927, 21.98088480513665388, -37.10214135362866728 ) ) ;
#435=CARTESIAN_POINT ( 'NONE',  ( -6.016761891674564211, 4.880293656734964181, 18.20023637398600869 ) ) ;
#446=( BOUNDED_SURFACE ( )  B_SPLINE_SURFACE ( 3, 1, ( 
 ( #42165, #8925 ),
 ( #28037, #32125 ),
 ( #2978, #56829 ),
 ( #46231, #61218 ) ),
 .UNSPECIFIED., .F., .F., .F. ) 
 B_SPLINE_SURFACE_WITH_KNOTS ( ( 4, 4 ),
 ( 2, 2 ),
 ( 0.000000000000000000, 1.000000000000000000 ),
 ( 0.000000000000000000, 1.000000000000000000 ),
 .UNSPECIFIED. ) 
 GEOMETRIC_REPRESENTATION_ITEM ( )  RATIONAL_B_SPLINE_SURFACE ( (
 ( 1.000000000000000000, 1.000000000000000000),
 ( 0.9953040768229013402, 0.8617119497784988535),
 ( 0.9953040768229013402, 0.8617119497784988535),
 ( 1.000000000000000000, 1.000000000000000000) ) ) 
 REPRESENTATION_ITEM ( '' )  SURFACE ( )  );
#454=CARTESIAN_POINT ( 'NONE',  ( -2.569797478183790229, 14.55946937464483959, -1.464172661884012960 ) ) ;
#456=CARTESIAN_POINT ( 'NONE',  ( 0.6254087463353900089, -17.77193046492983441, 44.70339519268186024 ) ) ;
#467=CARTESIAN_POINT ( 'NONE',  ( 4.975801465491695552, 15.94009207552985252, 45.18341283946464415 ) ) ;
#469=CARTESIAN_POINT ( 'NONE',  ( 0.6030672727741701600, 46.44558360016994669, 12.53539249098730757 ) ) ;
#470=CARTESIAN_POINT ( 'NONE',  ( 4.549368137175248350, 0.000000000000000000, 0.000000000000000000 ) ) ;
#471=VECTOR ( 'NONE', #9116, 1000.000000000000114 ) ;
#476=CARTESIAN_POINT ( 'NONE',  ( 0.1073791018717483448, -37.58707531572191840, -21.14095454447545919 ) ) ;
#480=EDGE_CURVE ( 'NONE', #24850, #5676, #46177, .T. ) ;
#485=CARTESIAN_POINT ( 'NONE',  ( -6.017396004339687465, -4.878103249821196030, 18.20079405513548565 ) ) ;
#487=CARTESIAN_POINT ( 'NONE',  ( 0.6009453534118440743, -47.75104957283902962, 5.846398087358569029 ) ) ;
#488=CARTESIAN_POINT ( 'NONE',  ( 4.691466044806103852, -25.04870410140763326, -36.88741755356061702 ) ) ;
#490=ORIENTED_EDGE ( 'NONE', *, *, #26338, .F. ) ;
#495=CARTESIAN_POINT ( 'NONE',  ( 0.6031357023905875581, 29.32055886552322477, -38.13964912630303417 ) ) ;
#497=VERTEX_POINT ( 'NONE', #19290 ) ;
#512=AXIS2_PLACEMENT_3D ( 'NONE', #37885, #12518, #51011 ) ;
#513=CARTESIAN_POINT ( 'NONE',  ( 0.2885697896453121580, -26.88157175352913342, 33.71073718007492914 ) ) ;
#514=CARTESIAN_POINT ( 'NONE',  ( 5.880360259849739535, 21.17507050419515480, -43.04573319267424125 ) ) ;
#530=CARTESIAN_POINT ( 'NONE',  ( 4.975801465491695552, 0.000000000000000000, 0.000000000000000000 ) ) ;
#538=CARTESIAN_POINT ( 'NONE',  ( 4.549368137175248350, 40.58005590356670211, 13.99871866169379508 ) ) ;
#549=ORIENTED_EDGE ( 'NONE', *, *, #18643, .T. ) ;
#553=ADVANCED_FACE ( 'NONE', ( #4842 ), #51575, .F. ) ;
#554=ORIENTED_EDGE ( 'NONE', *, *, #59411, .T. ) ;
#560=FACE_OUTER_BOUND ( 'NONE', #30769, .T. ) ;
#565=ORIENTED_EDGE ( 'NONE', *, *, #41540, .F. ) ;
#577=CARTESIAN_POINT ( 'NONE',  ( 0.6017667736363749853, 12.11362382130071502, 46.55748817282779584 ) ) ;
#579=EDGE_CURVE ( 'NONE', #58789, #16193, #41322, .T. ) ;
#582=CARTESIAN_POINT ( 'NONE',  ( 3.680882792899938138, 43.58303137875407174, -20.05474345988764284 ) ) ;
#593=VERTEX_POINT ( 'NONE', #44049 ) ;
#599=DIRECTION ( 'NONE',  ( 0.1024043820194936449, 0.01315135725335150538, 0.9946559125373961585 ) ) ;
#601=EDGE_CURVE ( 'NONE', #54484, #21442, #16427, .T. ) ;
#602=CARTESIAN_POINT ( 'NONE',  ( 0.3622758884714730732, -15.73321244754880688, 40.13994584881756111 ) ) ;
#608=CARTESIAN_POINT ( 'NONE',  ( 0.7954196712028469562, -44.76287685048099263, 17.60078400783944019 ) ) ;
#611=ORIENTED_EDGE ( 'NONE', *, *, #25395, .F. ) ;
#612=B_SPLINE_CURVE_WITH_KNOTS ( 'NONE', 3,
 ( #46317, #36930, #27494, #13113, #46024, #8082 ),
 .UNSPECIFIED., .F., .F.,
 ( 4, 2, 4 ),
 ( 8.570390151981194323E-17, 0.0002293366620881429790, 0.0004586733241762002517 ),
 .UNSPECIFIED. ) ;
#615=EDGE_LOOP ( 'NONE', ( #60615, #22132, #37483, #15249 ) ) ;
#618=DIRECTION ( 'NONE',  ( 0.000000000000000000, 0.000000000000000000, 1.000000000000000000 ) ) ;
#621=CARTESIAN_POINT ( 'NONE',  ( 0.6001305935487315502, -12.95698906763778524, -46.33281397023059611 ) ) ;
#629=CARTESIAN_POINT ( 'NONE',  ( 4.322998006666179727, -8.359821156456151314, -47.25487450103533860 ) ) ;
#634=EDGE_CURVE ( 'NONE', #39212, #54056, #37548, .T. ) ;
#636=CARTESIAN_POINT ( 'NONE',  ( 3.238741278300275805, -38.98370040185414354, -18.12697907494881377 ) ) ;
#640=ORIENTED_EDGE ( 'NONE', *, *, #39428, .T. ) ;
#644=ORIENTED_EDGE ( 'NONE', *, *, #34344, .F. ) ;
#648=CARTESIAN_POINT ( 'NONE',  ( 0.1073791018717578927, -40.02496097243069784, 16.05399293000745686 ) ) ;
#658=CARTESIAN_POINT ( 'NONE',  ( 0.7048096507298635682, 41.23648859290927504, -24.78213711671556396 ) ) ;
#660=CARTESIAN_POINT ( 'NONE',  ( 4.549368137175248350, 8.166781970325731166, -42.14271863032826104 ) ) ;
#663=LINE ( 'NONE', #19802, #9200 ) ;
#664=CARTESIAN_POINT ( 'NONE',  ( 0.8751705887134423323, -42.09020928323391075, 23.27176129838352736 ) ) ;
#668=CARTESIAN_POINT ( 'NONE',  ( -6.015611763856276717, 4.882992715191300626, 18.19956619163659894 ) ) ;
#669=B_SPLINE_CURVE_WITH_KNOTS ( 'NONE', 3,
 ( #10160, #48987, #747, #24568, #6036, #20188, #4813, #39301, #58355, #34590, #53655, #52751, #10786, #33669, #29872, #25174 ),
 .UNSPECIFIED., .F., .F.,
 ( 4, 3, 3, 3, 3, 4 ),
 ( 2.221635811791082109E-17, 0.0002618515315864366642, 0.0003927756766341980997, 0.0005236998216950544205, 0.0007855159896329859956, 0.001047349442285927003 ),
 .UNSPECIFIED. ) ;
#675=CARTESIAN_POINT ( 'NONE',  ( -6.016761891674564211, -9.418621820384613486, 16.32039929810254009 ) ) ;
#682=ORIENTED_EDGE ( 'NONE', *, *, #17053, .F. ) ;
#687=EDGE_CURVE ( 'NONE', #54494, #4004, #28518, .T. ) ;
#692=ORIENTED_EDGE ( 'NONE', *, *, #16762, .T. ) ;
#693=CARTESIAN_POINT ( 'NONE',  ( 0.3622758884714730732, -42.84426538328728640, -4.808133778521729518 ) ) ;
#700=EDGE_CURVE ( 'NONE', #45191, #45197, #17329, .T. ) ;
#709=CARTESIAN_POINT ( 'NONE',  ( 4.691466044806102076, 19.42108863068321511, 40.13652286047901185 ) ) ;
#711=CARTESIAN_POINT ( 'NONE',  ( 0.6025881611877911270, -12.66175293297434656, 46.41131722377287616 ) ) ;
#712=CARTESIAN_POINT ( 'NONE',  ( 2.643462169533600914, 1.382267876918459315, -48.01657676222235693 ) ) ;
#718=LINE ( 'NONE', #58032, #49664 ) ;
#720=AXIS2_PLACEMENT_3D ( 'NONE', #46539, #27411, #3586 ) ;
#724=CARTESIAN_POINT ( 'NONE',  ( -2.569797478183783568, 2.353985772484557426, 14.44232325624827595 ) ) ;
#727=ADVANCED_FACE ( 'NONE', ( #41490 ), #47217, .F. ) ;
#728=B_SPLINE_CURVE_WITH_KNOTS ( 'NONE', 3,
 ( #16941, #36055, #21315, #30385 ),
 .UNSPECIFIED., .F., .F.,
 ( 4, 4 ),
 ( 0.000000000000000000, 0.005014147105413705591 ),
 .UNSPECIFIED. ) ;
#729=CARTESIAN_POINT ( 'NONE',  ( 4.975801465491695552, -14.85979367497206205, 45.55012473237727733 ) ) ;
#733=CARTESIAN_POINT ( 'NONE',  ( 3.238741278300276694, 31.66556122967958231, -29.07934833201334968 ) ) ;
#736=CARTESIAN_POINT ( 'NONE',  ( -6.015611763856276717, -13.32857883366842700, 13.31979030221794424 ) ) ;
#742=CARTESIAN_POINT ( 'NONE',  ( 3.238741278300273585, -19.89284324544667015, -38.11287256318055228 ) ) ;
#743=CARTESIAN_POINT ( 'NONE',  ( 0.1102144999581333162, -34.13606714958032740, -26.35238362727828232 ) ) ;
#744=PRODUCT_DEFINITION ( 'UNKNOWN', '', #56876, #15421 ) ;
#747=CARTESIAN_POINT ( 'NONE',  ( 0.6017667736363749853, -24.35549005323445471, 41.48674115080360281 ) ) ;
#756=CARTESIAN_POINT ( 'NONE',  ( 3.238931869106853600, -23.06038324659541772, -36.28407486357512823 ) ) ;
#758=CARTESIAN_POINT ( 'NONE',  ( 0.8751705887134423323, -23.27176129838396790, -42.09020928323367627 ) ) ;
#763=CARTESIAN_POINT ( 'NONE',  ( 0.3622758884714600280, 15.73321244754796666, 40.13994584881788086 ) ) ;
#768=B_SPLINE_CURVE_WITH_KNOTS ( 'NONE', 3,
 ( #39427, #58479, #39121, #52877, #25605, #20305 ),
 .UNSPECIFIED., .F., .F.,
 ( 4, 2, 4 ),
 ( 8.652891131202922673E-17, 0.0002293366620881455539, 0.0004586733241762045886 ),
 .UNSPECIFIED. ) ;
#772=ORIENTED_EDGE ( 'NONE', *, *, #60310, .T. ) ;
#774=EDGE_CURVE ( 'NONE', #35221, #43756, #59136, .T. ) ;
#782=CARTESIAN_POINT ( 'NONE',  ( 0.8751705887134423323, -17.57879340691512837, -44.76769609654229498 ) ) ;
#784=ORIENTED_EDGE ( 'NONE', *, *, #20649, .F. ) ;
#790=LINE ( 'NONE', #58093, #17538 ) ;
#797=CARTESIAN_POINT ( 'NONE',  ( -6.016761891674564211, 17.41015286184802946, 7.207804629151374876 ) ) ;
#808=CARTESIAN_POINT ( 'NONE',  ( 0.3622758884714730732, -25.58609868863794290, 34.70015533914785522 ) ) ;
#810=FACE_OUTER_BOUND ( 'NONE', #7730, .T. ) ;
#814=CARTESIAN_POINT ( 'NONE',  ( 0.6031356755773454870, 29.28593560184431510, -38.16621646312178484 ) ) ;
#819=MECHANICAL_DESIGN_GEOMETRIC_PRESENTATION_REPRESENTATION('',(#60818),#10854);
#823=CARTESIAN_POINT ( 'NONE',  ( 0.5998501479064708430, -0.5236536531318284338, 48.10473956285918717 ) ) ;
#828=CARTESIAN_POINT ( 'NONE',  ( 0.1073791018717483448, -0.4849339620930353534, -43.12183934961191056 ) ) ;
#830=CARTESIAN_POINT ( 'NONE',  ( 4.833616638992208614, -30.83411269743540473, -34.47248434257901550 ) ) ;
#836=ORIENTED_EDGE ( 'NONE', *, *, #601, .T. ) ;
#842=CARTESIAN_POINT ( 'NONE',  ( 4.691466044806102076, 25.04870410140789261, -36.88741755356043228 ) ) ;
#844=EDGE_CURVE ( 'NONE', #61266, #41784, #57084, .T. ) ;
#845=ORIENTED_EDGE ( 'NONE', *, *, #3724, .T. ) ;
#850=EDGE_LOOP ( 'NONE', ( #20238, #49927, #25803, #15835 ) ) ;
#852=B_SPLINE_CURVE_WITH_KNOTS ( 'NONE', 3,
 ( #40262, #11737, #26126, #30819 ),
 .UNSPECIFIED., .F., .F.,
 ( 4, 4 ),
 ( 2.204559228842524708E-17, 0.004444306975806115896 ),
 .UNSPECIFIED. ) ;
#859=DIRECTION ( 'NONE',  ( -0.1024043820194934368, -0.2701391291102854253, 0.9573600124648732335 ) ) ;
#860=EDGE_CURVE ( 'NONE', #44643, #7607, #39105, .T. ) ;
#861=CARTESIAN_POINT ( 'NONE',  ( 0.5980894510889457338, -46.65000524237077428, -11.77356634613301445 ) ) ;
#868=VERTEX_POINT ( 'NONE', #13911 ) ;
#870=CARTESIAN_POINT ( 'NONE',  ( 0.6031356219577719280, -0.08729769678277263245, -48.10744328000515679 ) ) ;
#881=ORIENTED_EDGE ( 'NONE', *, *, #47421, .F. ) ;
#896=CARTESIAN_POINT ( 'NONE',  ( 0.6030672727741701600, 12.36682345648116410, 46.49075153683476458 ) ) ;
#898=CARTESIAN_POINT ( 'NONE',  ( 2.643462169533600914, 43.83256147628706145, 19.65219740572204543 ) ) ;
#903=CARTESIAN_POINT ( 'NONE',  ( 4.549368137175248350, -42.84816078363928682, 2.596185425821780246 ) ) ;
#904=CARTESIAN_POINT ( 'NONE',  ( 3.238931869106854489, 23.06038324659516903, 36.28407486357528455 ) ) ;
#907=CARTESIAN_POINT ( 'NONE',  ( -6.016104459813374383, -18.20253432612970457, 4.871830707672994087 ) ) ;
#910=LINE ( 'NONE', #10019, #48650 ) ;
#913=ADVANCED_FACE ( 'NONE', ( #18291 ), #53578, .F. ) ;
#920=ORIENTED_EDGE ( 'NONE', *, *, #19893, .T. ) ;
#937=ORIENTED_EDGE ( 'NONE', *, *, #19804, .F. ) ;
#939=CARTESIAN_POINT ( 'NONE',  ( -2.569797478183790229, 10.65947181927839615, -10.02484965418630303 ) ) ;
#940=VERTEX_POINT ( 'NONE', #43035 ) ;
#942=EDGE_CURVE ( 'NONE', #12367, #49832, #46520, .T. ) ;
#943=ORIENTED_EDGE ( 'NONE', *, *, #26032, .F. ) ;
#944=CARTESIAN_POINT ( 'NONE',  ( 4.975801465491695552, 0.000000000000000000, 0.000000000000000000 ) ) ;
#952=CARTESIAN_POINT ( 'NONE',  ( -6.017396004339687465, 18.20079405513549631, 4.878103249821131193 ) ) ;
#953=FACE_OUTER_BOUND ( 'NONE', #61682, .T. ) ;
#956=ORIENTED_EDGE ( 'NONE', *, *, #27151, .T. ) ;
#957=CARTESIAN_POINT ( 'NONE',  ( -5.995132425357893702, 13.33084941932907519, 13.31880955509731734 ) ) ;
#966=EDGE_CURVE ( 'NONE', #10647, #6988, #36109, .T. ) ;
#968=B_SPLINE_CURVE_WITH_KNOTS ( 'NONE', 3,
 ( #26241, #55049, #43610, #44768 ),
 .UNSPECIFIED., .F., .F.,
 ( 4, 4 ),
 ( 0.000000000000000000, 0.004445488388166993383 ),
 .UNSPECIFIED. ) ;
#972=CARTESIAN_POINT ( 'NONE',  ( -6.010958268070873523, 14.94067681728549779, 11.48268200989202192 ) ) ;
#977=CARTESIAN_POINT ( 'NONE',  ( 0.8751705887134423323, -17.57879340691512837, -44.76769609654229498 ) ) ;
#978=CARTESIAN_POINT ( 'NONE',  ( 0.09136607875274982415, 0.000000000000000000, 0.000000000000000000 ) ) ;
#987=CARTESIAN_POINT ( 'NONE',  ( 0.3622758884714600280, 39.50828911766974016, 17.25816669465007891 ) ) ;
#997=ORIENTED_EDGE ( 'NONE', *, *, #53649, .T. ) ;
#1003=EDGE_LOOP ( 'NONE', ( #55950, #35313, #30459, #44447 ) ) ;
#1005=CARTESIAN_POINT ( 'NONE',  ( 4.975801465491695552, 47.76942479135485797, -3.702618843596948039 ) ) ;
#1007=CARTESIAN_POINT ( 'NONE',  ( 0.6041374136657476912, -41.74951251761557813, -23.90252055111306717 ) ) ;
#1008=ORIENTED_EDGE ( 'NONE', *, *, #22055, .F. ) ;
#1017=CARTESIAN_POINT ( 'NONE',  ( 0.1064266418746774995, 0.5615180042400674809, -43.12102053154802661 ) ) ;
#1020=CARTESIAN_POINT ( 'NONE',  ( 0.6017667736363748743, -12.78803812527920591, 46.37677940471275662 ) ) ;
#1021=CARTESIAN_POINT ( 'NONE',  ( -5.995132425357893702, 0.008513469642806619636, 18.84415457712583475 ) ) ;
#1023=CARTESIAN_POINT ( 'NONE',  ( 0.6041374136657475802, 6.452348380035901165, -47.67304777898693402 ) ) ;
#1024=ORIENTED_EDGE ( 'NONE', *, *, #19184, .T. ) ;
#1031=DIRECTION ( 'NONE',  ( 0.09835009131224564660, 0.2650256080583759943, -0.9592125346408693076 ) ) ;
#1044=AXIS2_PLACEMENT_3D ( 'NONE', #15501, #38707, #9874 ) ;
#1046=CARTESIAN_POINT ( 'NONE',  ( 4.549368137175248350, 0.000000000000000000, 0.000000000000000000 ) ) ;
#1049=CARTESIAN_POINT ( 'NONE',  ( 0.3622758884714600280, -20.83792692158946025, -37.74294673546579304 ) ) ;
#1051=CARTESIAN_POINT ( 'NONE',  ( 0.5980894510889448457, 38.59343625445447401, -28.72954109785563404 ) ) ;
#1052=CARTESIAN_POINT ( 'NONE',  ( 0.5998501479064708430, -47.62484632993683675, -6.798102206413969562 ) ) ;
#1057=EDGE_CURVE ( 'NONE', #15504, #24440, #40539, .T. ) ;
#1058=CARTESIAN_POINT ( 'NONE',  ( 4.549368137175248350, 0.000000000000000000, 0.000000000000000000 ) ) ;
#1070=CARTESIAN_POINT ( 'NONE',  ( 3.238931869106854933, -14.74782013370872846, 40.38337734129178358 ) ) ;
#1081=ADVANCED_FACE ( 'NONE', ( #35168 ), #6041, .F. ) ;
#1088=CARTESIAN_POINT ( 'NONE',  ( 4.691466044806103852, 20.01963481131604183, 39.84135254923144487 ) ) ;
#1091=CARTESIAN_POINT ( 'NONE',  ( 4.691466044806103852, 33.74235639413287657, 29.14742760351121831 ) ) ;
#1094=FACE_OUTER_BOUND ( 'NONE', #30509, .T. ) ;
#1098=ORIENTED_EDGE ( 'NONE', *, *, #1896, .F. ) ;
#1099=LINE ( 'NONE', #49642, #12543 ) ;
#1101=CARTESIAN_POINT ( 'NONE',  ( 4.322998006666165516, -22.13465289016597382, -42.57894920390120319 ) ) ;
#1103=ORIENTED_EDGE ( 'NONE', *, *, #51969, .F. ) ;
#1104=CARTESIAN_POINT ( 'NONE',  ( 0.6001305935487422083, 11.94532529598378012, -46.60388846085711378 ) ) ;
#1105=CARTESIAN_POINT ( 'NONE',  ( -6.010958268070873523, 16.32616437357112105, 9.409153349053642756 ) ) ;
#1111=CARTESIAN_POINT ( 'NONE',  ( 0.1064266379913943877, -21.07422113734189750, 37.62465837278038094 ) ) ;
#1112=( BOUNDED_SURFACE ( )  B_SPLINE_SURFACE ( 3, 1, ( 
 ( #25198, #24903 ),
 ( #39632, #58382 ),
 ( #35235, #54296 ),
 ( #15505, #44342 ) ),
 .UNSPECIFIED., .F., .F., .F. ) 
 B_SPLINE_SURFACE_WITH_KNOTS ( ( 4, 4 ),
 ( 2, 2 ),
 ( 0.000000000000000000, 1.000000000000000000 ),
 ( 0.000000000000000000, 1.000000000000000000 ),
 .UNSPECIFIED. ) 
 GEOMETRIC_REPRESENTATION_ITEM ( )  RATIONAL_B_SPLINE_SURFACE ( (
 ( 1.000000000000000000, 1.000000000000000000),
 ( 0.9751682680413298332, 0.9999560080971552356),
 ( 0.9751682680413298332, 0.9999560080971552356),
 ( 1.000000000000000000, 1.000000000000000000) ) ) 
 REPRESENTATION_ITEM ( '' )  SURFACE ( )  );
#1123=DIRECTION ( 'NONE',  ( 0.09835009131224550782, -0.9223318362920762681, -0.3736726418952285855 ) ) ;
#1128=CARTESIAN_POINT ( 'NONE',  ( 0.6031356219577718170, 38.11305734842063941, -29.35521383643418503 ) ) ;
#1140=CARTESIAN_POINT ( 'NONE',  ( 4.549368137175248350, -28.46244473166650479, -32.13400537129916046 ) ) ;
#1146=VERTEX_POINT ( 'NONE', #30749 ) ;
#1147=CARTESIAN_POINT ( 'NONE',  ( 4.549368137175248350, -28.14399996863474129, -32.41327393324131378 ) ) ;
#1151=B_SPLINE_CURVE_WITH_KNOTS ( 'NONE', 3,
 ( #11366, #25144, #44290, #30451 ),
 .UNSPECIFIED., .F., .F.,
 ( 4, 4 ),
 ( 2.100108283942811974E-17, 0.004444306975806115029 ),
 .UNSPECIFIED. ) ;
#1152=CARTESIAN_POINT ( 'NONE',  ( 0.1103744047535531458, -0.03874731383761919473, 43.12441516302519773 ) ) ;
#1156=CARTESIAN_POINT ( 'NONE',  ( 0.1073791018717483448, -21.14095454447585709, 37.58707531572169813 ) ) ;
#1159=CARTESIAN_POINT ( 'NONE',  ( 0.6028618097248863439, 34.14037999462324535, 33.89350006451839192 ) ) ;
#1166=CARTESIAN_POINT ( 'NONE',  ( -6.016761891674564211, -17.40752468084787452, 7.214149619366299504 ) ) ;
#1174=CARTESIAN_POINT ( 'NONE',  ( 0.1064266418746779297, 41.50637583369805128, 11.70292610004339195 ) ) ;
#1180=EDGE_CURVE ( 'NONE', #50113, #497, #50927, .T. ) ;
#1184=ADVANCED_FACE ( 'NONE', ( #46119 ), #59, .F. ) ;
#1192=CARTESIAN_POINT ( 'NONE',  ( 0.8751705887134423323, -28.56654290188627243, -38.69254731947824411 ) ) ;
#1199=CARTESIAN_POINT ( 'NONE',  ( 0.5998501479064699549, 12.95623334615437550, 46.33007877220744319 ) ) ;
#1201=DIRECTION ( 'NONE',  ( 1.000000000000000000, 0.000000000000000000, 0.000000000000000000 ) ) ;
#1210=CARTESIAN_POINT ( 'NONE',  ( 0.3622758884714730732, 34.70015533914794759, 25.58609868863780434 ) ) ;
#1212=CARTESIAN_POINT ( 'NONE',  ( -6.016761891674564211, -18.68153697670643609, 2.462934516563739518 ) ) ;
#1227=CARTESIAN_POINT ( 'NONE',  ( 0.1313383488274139088, -30.94058105930541558, -30.03864748494533643 ) ) ;
#1232=ORIENTED_EDGE ( 'NONE', *, *, #35856, .F. ) ;
#1234=ORIENTED_EDGE ( 'NONE', *, *, #11984, .F. ) ;
#1237=ORIENTED_EDGE ( 'NONE', *, *, #46578, .T. ) ;
#1240=CARTESIAN_POINT ( 'NONE',  ( 0.1313383488274124655, -41.48452234694106266, 11.77600546273697724 ) ) ;
#1242=ORIENTED_EDGE ( 'NONE', *, *, #56798, .F. ) ;
#1243=CARTESIAN_POINT ( 'NONE',  ( -2.569797478183790229, -12.44213550320647954, -7.701637110048636714 ) ) ;
#1245=LINE ( 'NONE', #5931, #30257 ) ;
#1248=CARTESIAN_POINT ( 'NONE',  ( -6.016761891674564211, 18.20201388312095503, 4.873659902332430960 ) ) ;
#1263=DIRECTION ( 'NONE',  ( -1.000000000000000000, -0.000000000000000000, -0.000000000000000000 ) ) ;
#1268=CARTESIAN_POINT ( 'NONE',  ( 4.549368137175248350, 0.000000000000000000, 0.000000000000000000 ) ) ;
#1270=CARTESIAN_POINT ( 'NONE',  ( 2.643462169533613793, -38.93558293168521089, -28.13401304854706808 ) ) ;
#1272=( BOUNDED_SURFACE ( )  B_SPLINE_SURFACE ( 3, 1, ( 
 ( #30931, #2410 ),
 ( #60340, #17453 ),
 ( #36891, #60048 ),
 ( #40361, #21532 ) ),
 .UNSPECIFIED., .F., .F., .F. ) 
 B_SPLINE_SURFACE_WITH_KNOTS ( ( 4, 4 ),
 ( 2, 2 ),
 ( 0.000000000000000000, 1.000000000000000000 ),
 ( 0.000000000000000000, 1.000000000000000000 ),
 .UNSPECIFIED. ) 
 GEOMETRIC_REPRESENTATION_ITEM ( )  RATIONAL_B_SPLINE_SURFACE ( (
 ( 1.000000000000000000, 1.000000000000000000),
 ( 0.9953040768229005630, 0.8617119497784937465),
 ( 0.9953040768229005630, 0.8617119497784937465),
 ( 1.000000000000000000, 1.000000000000000000) ) ) 
 REPRESENTATION_ITEM ( '' )  SURFACE ( )  );
#1276=CARTESIAN_POINT ( 'NONE',  ( 4.833616638992205949, -41.67905425467720448, 20.04871863793733056 ) ) ;
#1278=DIRECTION ( 'NONE',  ( -1.000000000000000000, -0.000000000000000000, -0.000000000000000000 ) ) ;
#1281=VECTOR ( 'NONE', #39244, 1000.000000000000114 ) ;
#1283=CARTESIAN_POINT ( 'NONE',  ( -2.708315649062910779, 3.532515819624157505, 14.20182604343561295 ) ) ;
#1291=ORIENTED_EDGE ( 'NONE', *, *, #54153, .T. ) ;
#1301=VECTOR ( 'NONE', #57417, 1000.000000000000114 ) ;
#1302=ADVANCED_FACE ( 'NONE', ( #22602 ), #50133, .F. ) ;
#1306=CARTESIAN_POINT ( 'NONE',  ( 3.238931869106854489, 41.01619136531527232, -12.88361013339121008 ) ) ;
#1307=ORIENTED_EDGE ( 'NONE', *, *, #52182, .F. ) ;
#1313=CARTESIAN_POINT ( 'NONE',  ( 0.5998501479064699549, 12.95623334615437550, 46.33007877220744319 ) ) ;
#1315=VERTEX_POINT ( 'NONE', #5004 ) ;
#1316=CARTESIAN_POINT ( 'NONE',  ( 0.6017666602106489515, -12.11361215600212304, 46.55749120190025536 ) ) ;
#1329=CARTESIAN_POINT ( 'NONE',  ( -2.708315649062916552, 11.76894112707800844, 8.698422600177160291 ) ) ;
#1330=EDGE_CURVE ( 'NONE', #4316, #49088, #60568, .T. ) ;
#1333=CARTESIAN_POINT ( 'NONE',  ( 0.1081432562775997974, 34.46918062033751085, -25.91533557232854790 ) ) ;
#1335=CARTESIAN_POINT ( 'NONE',  ( 0.1064266418746775689, -43.12102053154801951, -0.5615180042399171567 ) ) ;
#1338=CARTESIAN_POINT ( 'NONE',  ( 0.5980894510889457338, 37.73932204245519273, -29.84264441023739067 ) ) ;
#1339=CARTESIAN_POINT ( 'NONE',  ( 0.6031357023905875581, -18.36962560204189288, -44.46217339385164280 ) ) ;
#1353=CARTESIAN_POINT ( 'NONE',  ( 0.5988103622719989083, -47.61318311633120004, -6.880137819454693826 ) ) ;
#1355=CARTESIAN_POINT ( 'NONE',  ( 0.09136607875274982415, 0.000000000000000000, -3.000000000000000000 ) ) ;
#1362=EDGE_LOOP ( 'NONE', ( #20699, #3409, #36647, #9267 ) ) ;
#1364=CARTESIAN_POINT ( 'NONE',  ( 4.549368137175248350, -13.99871866169391765, 40.58005590356665948 ) ) ;
#1374=CARTESIAN_POINT ( 'NONE',  ( 0.7954190325252775695, 19.20649988843056732, 44.09776758977478295 ) ) ;
#1377=CARTESIAN_POINT ( 'NONE',  ( -6.016104459813371719, -7.206059014950207064, 17.41090761020834066 ) ) ;
#1381=EDGE_LOOP ( 'NONE', ( #46301, #55090, #25849, #33963 ) ) ;
#1383=CARTESIAN_POINT ( 'NONE',  ( -5.995132425357893702, -9.414704407577689338, -16.32377331145330501 ) ) ;
#1390=ORIENTED_EDGE ( 'NONE', *, *, #12134, .F. ) ;
#1398=VERTEX_POINT ( 'NONE', #34168 ) ;
#1401=EDGE_CURVE ( 'NONE', #59975, #52610, #57565, .T. ) ;
#1405=CARTESIAN_POINT ( 'NONE',  ( 0.6027935024548037868, -47.71838037711337677, 6.106197519200678769 ) ) ;
#1413=CARTESIAN_POINT ( 'NONE',  ( 3.238741278300274917, -9.350673766180513269, -41.96285461600078293 ) ) ;
#1418=EDGE_LOOP ( 'NONE', ( #55748, #32684, #10445, #30814 ) ) ;
#1427=CARTESIAN_POINT ( 'NONE',  ( 4.691466044806103852, -29.64918311951105778, -33.30232861642423359 ) ) ;
#1431=CARTESIAN_POINT ( 'NONE',  ( 0.1064266418746773746, -6.185136754498649303, 42.67882141624135528 ) ) ;
#1451=B_SPLINE_CURVE_WITH_KNOTS ( 'NONE', 3,
 ( #29436, #58233, #61695, #38560, #48254, #29136 ),
 .UNSPECIFIED., .F., .F.,
 ( 4, 2, 4 ),
 ( 1.870559545977334001E-17, 0.0002293319059085109570, 0.0004586638118170032114 ),
 .UNSPECIFIED. ) ;
#1452=CARTESIAN_POINT ( 'NONE',  ( 0.1073791018717483448, 37.10214135362888754, -21.98088480513627729 ) ) ;
#1456=ORIENTED_EDGE ( 'NONE', *, *, #1817, .F. ) ;
#1457=EDGE_CURVE ( 'NONE', #27177, #27976, #6745, .T. ) ;
#1461=EDGE_LOOP ( 'NONE', ( #5875, #47255, #11594, #58640 ) ) ;
#1467=DIRECTION ( 'NONE',  ( -0.1024043820194934507, -0.01315135725336535714, 0.9946559125373960475 ) ) ;
#1470=CARTESIAN_POINT ( 'NONE',  ( 0.3622758884714730732, -34.70015533914812522, -25.58609868863756276 ) ) ;
#1481=CARTESIAN_POINT ( 'NONE',  ( 0.6041374136657475802, -18.57118264377566774, 44.37863742124635991 ) ) ;
#1484=FACE_OUTER_BOUND ( 'NONE', #30690, .T. ) ;
#1490=CARTESIAN_POINT ( 'NONE',  ( 0.1073791018717578927, 30.14884492832347718, 30.83464511437148659 ) ) ;
#1492=CARTESIAN_POINT ( 'NONE',  ( 2.643462169533600914, 4.896978544601506833, 47.78621045426877600 ) ) ;
#1493=VECTOR ( 'NONE', #30697, 1000.000000000000114 ) ;
#1497=VECTOR ( 'NONE', #54986, 1000.000000000000000 ) ;
#1510=CARTESIAN_POINT ( 'NONE',  ( -2.708315649062910779, -9.116606751444415124, 11.44805714186556322 ) ) ;
#1512=CARTESIAN_POINT ( 'NONE',  ( -6.001507490154110336, -18.19774963328911710, 4.892199142591239891 ) ) ;
#1529=AXIS2_PLACEMENT_3D ( 'NONE', #38802, #53468, #57859 ) ;
#1530=EDGE_CURVE ( 'NONE', #7607, #11343, #58340, .T. ) ;
#1538=EDGE_CURVE ( 'NONE', #30127, #16034, #13558, .T. ) ;
#1549=ORIENTED_EDGE ( 'NONE', *, *, #2878, .F. ) ;
#1557=ADVANCED_FACE ( 'NONE', ( #14864 ), #21059, .F. ) ;
#1561=B_SPLINE_CURVE_WITH_KNOTS ( 'NONE', 3,
 ( #26472, #16166, #21162, #39996, #40921, #59985, #44997, #44682, #12097, #26164, #35277, #2032, #40606, #54337, #16462, #34974, #45922, #30860, #11461 ),
 .UNSPECIFIED., .F., .F.,
 ( 4, 3, 3, 3, 3, 3, 4 ),
 ( 1.144439277862597989E-16, 0.0002618519381806243447, 0.0003927759815485966800, 0.0005237000248299447311, 0.0006546240681324983672, 0.0007855481115631302155, 0.0009699050456655107250 ),
 .UNSPECIFIED. ) ;
#1572=CARTESIAN_POINT ( 'NONE',  ( 0.1073791018717578927, 42.81622261970994003, -5.147744207006430983 ) ) ;
#1579=CIRCLE ( 'NONE', #17620, 47.91270532121795611 ) ;
#1582=CARTESIAN_POINT ( 'NONE',  ( 0.8751705887134553219, 47.55935879196470495, -7.160166390003808168 ) ) ;
#1598=ORIENTED_EDGE ( 'NONE', *, *, #47462, .F. ) ;
#1617=ORIENTED_EDGE ( 'NONE', *, *, #32269, .T. ) ;
#1618=CARTESIAN_POINT ( 'NONE',  ( 0.6023143664670691511, -18.65155446683280260, 44.34466302085792222 ) ) ;
#1624=CARTESIAN_POINT ( 'NONE',  ( 0.7245667037590776127, 13.24050682223029618, 46.24390958543281727 ) ) ;
#1633=CARTESIAN_POINT ( 'NONE',  ( 0.2224561200757622370, 42.64482917976808807, 6.380320192202126428 ) ) ;
#1635=CARTESIAN_POINT ( 'NONE',  ( 0.6027935024548037868, -41.57475399306903796, -24.20473723001681776 ) ) ;
#1639=FACE_OUTER_BOUND ( 'NONE', #16266, .T. ) ;
#1642=CARTESIAN_POINT ( 'NONE',  ( 0.1092355843206037486, -39.95589129953380336, 16.22491322981557005 ) ) ;
#1644=CARTESIAN_POINT ( 'NONE',  ( 0.1102144999581333162, 34.28951223307529972, -26.15241010112988818 ) ) ;
#1648=DIRECTION ( 'NONE',  ( 0.000000000000000000, 0.000000000000000000, -1.000000000000000000 ) ) ;
#1649=CARTESIAN_POINT ( 'NONE',  ( 0.6009452777970412107, -5.846392105360883384, 47.75105029762382003 ) ) ;
#1651=CARTESIAN_POINT ( 'NONE',  ( 4.833616638992205949, 43.93936707042099954, -14.43699082351666085 ) ) ;
#1663=ORIENTED_EDGE ( 'NONE', *, *, #37491, .T. ) ;
#1665=CARTESIAN_POINT ( 'NONE',  ( 0.1103744047535531458, -43.12441516302519773, -0.03874731383716748662 ) ) ;
#1667=AXIS2_PLACEMENT_3D ( 'NONE', #61773, #37718, #61468 ) ;
#1669=ORIENTED_EDGE ( 'NONE', *, *, #1457, .T. ) ;
#1671=CARTESIAN_POINT ( 'NONE',  ( 0.1103878639767399278, -11.11454059769229374, 41.66755962011260550 ) ) ;
#1682=ADVANCED_FACE ( 'NONE', ( #45529 ), #50483, .F. ) ;
#1683=ORIENTED_EDGE ( 'NONE', *, *, #28104, .F. ) ;
#1686=CARTESIAN_POINT ( 'NONE',  ( 4.549368137175248350, 0.000000000000000000, 0.000000000000000000 ) ) ;
#1689=ORIENTED_EDGE ( 'NONE', *, *, #18590, .F. ) ;
#1690=ORIENTED_EDGE ( 'NONE', *, *, #41870, .F. ) ;
#1691=CARTESIAN_POINT ( 'NONE',  ( 4.691466044806102076, 2.583163953527854773, 44.51344083442440080 ) ) ;
#1703=VERTEX_POINT ( 'NONE', #13245 ) ;
#1711=ORIENTED_EDGE ( 'NONE', *, *, #11636, .F. ) ;
#1712=CARTESIAN_POINT ( 'NONE',  ( -6.016761891674565099, -4.880293656735092078, 18.20023637398597671 ) ) ;
#1714=CARTESIAN_POINT ( 'NONE',  ( 0.8760168074886960365, -41.20610493656892714, -24.81951362746063339 ) ) ;
#1717=( BOUNDED_SURFACE ( )  B_SPLINE_SURFACE ( 3, 1, ( 
 ( #12022, #22322 ),
 ( #21701, #45843 ),
 ( #17626, #36751 ),
 ( #17318, #56124 ) ),
 .UNSPECIFIED., .F., .F., .F. ) 
 B_SPLINE_SURFACE_WITH_KNOTS ( ( 4, 4 ),
 ( 2, 2 ),
 ( 0.000000000000000000, 1.000000000000000000 ),
 ( 0.000000000000000000, 1.000000000000000000 ),
 .UNSPECIFIED. ) 
 GEOMETRIC_REPRESENTATION_ITEM ( )  RATIONAL_B_SPLINE_SURFACE ( (
 ( 1.000000000000000000, 1.000000000000000000),
 ( 0.9751682680413298332, 0.9999560080971552356),
 ( 0.9751682680413298332, 0.9999560080971552356),
 ( 1.000000000000000000, 1.000000000000000000) ) ) 
 REPRESENTATION_ITEM ( '' )  SURFACE ( )  );
#1720=CARTESIAN_POINT ( 'NONE',  ( 4.322998006666165516, 8.359821156456478164, -47.25487450103527465 ) ) ;
#1721=CARTESIAN_POINT ( 'NONE',  ( 2.301430502907645170, -40.93949994354167643, -25.12309903330006122 ) ) ;
#1729=CARTESIAN_POINT ( 'NONE',  ( 4.975801465491695552, 0.000000000000000000, 0.000000000000000000 ) ) ;
#1731=CARTESIAN_POINT ( 'NONE',  ( 0.5998501479064699549, 33.64490850298844293, -34.38546660123262200 ) ) ;
#1737=CARTESIAN_POINT ( 'NONE',  ( 0.5998501479064699549, 46.60114184914301205, 11.94461217097485672 ) ) ;
#1748=CARTESIAN_POINT ( 'NONE',  ( 0.1073791018717578927, 16.05399293000759542, 40.02496097243063389 ) ) ;
#1755=CARTESIAN_POINT ( 'NONE',  ( -6.016489644550736315, 7.215050741358040476, 17.40716454747931152 ) ) ;
#1758=CARTESIAN_POINT ( 'NONE',  ( 0.1081432562775998252, -10.75186376283313372, -41.76274004527628847 ) ) ;
#1770=CARTESIAN_POINT ( 'NONE',  ( 0.1064266418746775411, -37.06314021531093772, -22.04679912212815296 ) ) ;
#1780=CARTESIAN_POINT ( 'NONE',  ( 4.975801465491695552, 8.787181743660156030, -47.10002938642133330 ) ) ;
#1785=EDGE_LOOP ( 'NONE', ( #26681, #47476, #7372, #29705, #50543, #46251, #13058, #12859, #29736, #56103, #18679, #28008, #61702, #49743, #44732, #23947, #15196, #56585, #20948, #52576, #29452, #10800, #50944, #42394, #56388, #23385, #32255, #16806, #15974, #42474, #50312, #5372, #4211, #57015, #23899, #59809, #29466, #7475, #15123, #54708, #28044, #50173, #11499, #49177, #34038, #61806, #8966, #55785, #44452, #1663, #17622, #35156, #54989, #24121, #24307, #4162, #20569, #14889, #57043, #3331, #57616, #35531, #26298, #29303, #25707, #36346, #49300, #21530, #36266, #19152, #40250, #8168, #52254, #31456, #56784, #1931, #44120, #997, #21672, #6018, #26943, #44572, #56485, #35657, #549, #27307, #24367, #50334, #56178, #44440, #28787, #6665, #43977, #19200, #16507, #47349, #36235, #24202, #16452, #4637, #35491, #55842, #44419, #60106, #13297, #27706, #15673, #19034, #36330, #7473, #45729, #53037, #32997, #53919, #4135, #17910, #8468, #3749, #1390, #30361, #48511, #58408, #17856, #61697, #27558, #35075, #19751, #17247, #45447, #58598, #30229, #24688, #22220, #20828, #28767, #12825, #33469, #18448, #45654, #640, #55681, #17785, #36157, #30142, #56925, #42819, #13909, #16379 ) ) ;
#1788=VERTEX_POINT ( 'NONE', #17629 ) ;
#1802=CARTESIAN_POINT ( 'NONE',  ( 0.1092565886968784733, 26.00565248013053221, -34.40108480122224677 ) ) ;
#1804=CARTESIAN_POINT ( 'NONE',  ( -5.995132425357893702, -2.468096378287997439, -18.68182899165013922 ) ) ;
#1805=ORIENTED_EDGE ( 'NONE', *, *, #29261, .T. ) ;
#1812=CARTESIAN_POINT ( 'NONE',  ( 0.8760168074886965917, -28.57146030081952759, -38.69913431881813182 ) ) ;
#1815=CARTESIAN_POINT ( 'NONE',  ( 4.549368137175248350, -19.17571786012296187, -38.40568845698270195 ) ) ;
#1816=FACE_OUTER_BOUND ( 'NONE', #9677, .T. ) ;
#1817=EDGE_CURVE ( 'NONE', #33784, #61780, #18663, .T. ) ;
#1819=LINE ( 'NONE', #59139, #34862 ) ;
#1822=EDGE_CURVE ( 'NONE', #46926, #29080, #14228, .T. ) ;
#1824=EDGE_CURVE ( 'NONE', #18698, #37177, #3642, .T. ) ;
#1828=CARTESIAN_POINT ( 'NONE',  ( 0.1073791018717483448, 0.4849339620927342054, 43.12183934961191767 ) ) ;
#1833=EDGE_CURVE ( 'NONE', #42044, #1398, #55236, .T. ) ;
#1836=ADVANCED_FACE ( 'NONE', ( #1816 ), #16105, .F. ) ;
#1855=CARTESIAN_POINT ( 'NONE',  ( 0.5998501479064699549, 41.39809967730487017, -24.50586714782561160 ) ) ;
#1856=ORIENTED_EDGE ( 'NONE', *, *, #3295, .F. ) ;
#1861=EDGE_CURVE ( 'NONE', #7602, #58429, #54453, .T. ) ;
#1865=CARTESIAN_POINT ( 'NONE',  ( 0.1100053167205931187, 5.806749312984545774, 42.73174076921946352 ) ) ;
#1866=CARTESIAN_POINT ( 'NONE',  ( -2.569797478183783568, 13.34095667500604776, -6.011723966604011871 ) ) ;
#1896=EDGE_CURVE ( 'NONE', #12539, #40478, #35684, .T. ) ;
#1897=VECTOR ( 'NONE', #41450, 1000.000000000000114 ) ;
#1898=EDGE_CURVE ( 'NONE', #54850, #49335, #4039, .T. ) ;
#1901=FACE_OUTER_BOUND ( 'NONE', #41118, .T. ) ;
#1909=AXIS2_PLACEMENT_3D ( 'NONE', #23583, #13584, #8547 ) ;
#1917=CARTESIAN_POINT ( 'NONE',  ( 0.6031356219577718170, -12.53544563195267436, -46.44562759437249611 ) ) ;
#1931=ORIENTED_EDGE ( 'NONE', *, *, #45023, .T. ) ;
#1940=CARTESIAN_POINT ( 'NONE',  ( 4.549368137175248350, 42.82045902618772715, -3.018832571116098151 ) ) ;
#1944=CARTESIAN_POINT ( 'NONE',  ( 0.1100053167205930632, 41.70112744323654397, 10.98799238780965659 ) ) ;
#1946=CARTESIAN_POINT ( 'NONE',  ( 0.2224561200757602386, -41.84032767736809433, 10.42482236669231099 ) ) ;
#1950=DIRECTION ( 'NONE',  ( -0.1024043820194934507, 0.7126273545981537394, -0.6940285268068185909 ) ) ;
#1951=CARTESIAN_POINT ( 'NONE',  ( 0.6030672727741701600, -41.61859040196966930, -24.12926094633971275 ) ) ;
#1954=VERTEX_POINT ( 'NONE', #16877 ) ;
#1955=CARTESIAN_POINT ( 'NONE',  ( 0.1064266418746774023, 15.98292515284405191, 40.05351192729366261 ) ) ;
#1956=CARTESIAN_POINT ( 'NONE',  ( 0.1092355843206037486, 34.02913268098554056, 26.49036028133793508 ) ) ;
#1957=CARTESIAN_POINT ( 'NONE',  ( -6.016104459813374383, 7.206059014950080943, 17.41090761020838329 ) ) ;
#1959=CARTESIAN_POINT ( 'NONE',  ( 0.1095718737110178004, 34.36877422440999652, -26.04820588677157289 ) ) ;
#1964=CARTESIAN_POINT ( 'NONE',  ( 4.691466044806102076, -19.42108863068351354, -40.13652286047886264 ) ) ;
#1965=CARTESIAN_POINT ( 'NONE',  ( 0.6028618097248862329, -6.106174977919399005, 47.71844004092977087 ) ) ;
#1968=CARTESIAN_POINT ( 'NONE',  ( 4.691466044806102076, 42.32811009116555567, -14.01607102724497977 ) ) ;
#1969=LINE ( 'NONE', #17635, #39073 ) ;
#1971=CARTESIAN_POINT ( 'NONE',  ( 0.5998501479064699549, -47.76154736470754614, -5.759754759340617092 ) ) ;
#1975=CARTESIAN_POINT ( 'NONE',  ( 0.3622758884714730732, 43.10531414739106282, -0.8252992914323589169 ) ) ;
#1978=CARTESIAN_POINT ( 'NONE',  ( -6.017396004339687465, -18.68211039806565310, 2.458362590802723791 ) ) ;
#1985=CARTESIAN_POINT ( 'NONE',  ( -6.016104459813371719, 18.68271063303494728, 2.454244026261157341 ) ) ;
#1987=EDGE_CURVE ( 'NONE', #50136, #9272, #47848, .T. ) ;
#1990=CARTESIAN_POINT ( 'NONE',  ( 0.7048096507298635682, -28.61383451045728066, 38.67623024743999594 ) ) ;
#1996=CARTESIAN_POINT ( 'NONE',  ( -6.016489644550737204, 2.455165042129735298, 18.68257207665197228 ) ) ;
#2000=EDGE_CURVE ( 'NONE', #19675, #29055, #27635, .T. ) ;
#2001=LINE ( 'NONE', #21129, #4931 ) ;
#2002=VERTEX_POINT ( 'NONE', #3970 ) ;
#2003=VERTEX_POINT ( 'NONE', #47530 ) ;
#2005=CARTESIAN_POINT ( 'NONE',  ( 0.8760168074887090262, -23.27577685234627580, 42.09738177923914293 ) ) ;
#2009=B_SPLINE_CURVE_WITH_KNOTS ( 'NONE', 3,
 ( #59423, #21848, #12458, #50044, #16854, #22158, #21227, #31871, #60051, #40672, #8048, #17156, #26852, #36269, #13080, #36894, #41281, #60341, #46287 ),
 .UNSPECIFIED., .F., .F.,
 ( 4, 3, 3, 3, 3, 3, 4 ),
 ( 1.138109825968292890E-16, 0.0002618519381806228810, 0.0003927759815485970052, 0.0005237000248299436469, 0.0006546240681325004272, 0.0007855481115631334681, 0.0009699050456655086650 ),
 .UNSPECIFIED. ) ;
#2016=DIRECTION ( 'NONE',  ( 0.1024043820194936449, 0.9946559125373961585, -0.01315135725335497656 ) ) ;
#2020=CARTESIAN_POINT ( 'NONE',  ( 0.1073791018717483448, 30.14884492832389284, -30.83464511437107447 ) ) ;
#2025=CARTESIAN_POINT ( 'NONE',  ( 0.1073791018717483448, -42.68962945260958008, 6.109314776651994627 ) ) ;
#2027=CARTESIAN_POINT ( 'NONE',  ( 0.1073791018717483448, 25.86618856530710531, -34.50606437925521419 ) ) ;
#2030=FACE_OUTER_BOUND ( 'NONE', #31689, .T. ) ;
#2032=CARTESIAN_POINT ( 'NONE',  ( 0.1102144999581332746, -41.62223437741661769, -11.28312052188132952 ) ) ;
#2037=ORIENTED_EDGE ( 'NONE', *, *, #46922, .T. ) ;
#2046=CARTESIAN_POINT ( 'NONE',  ( 0.6031356219577718170, -44.41207482560220399, 18.49057407199378034 ) ) ;
#2047=CARTESIAN_POINT ( 'NONE',  ( 0.6029303876144825880, 41.72757124235822346, -23.94027529185509451 ) ) ;
#2048=CARTESIAN_POINT ( 'NONE',  ( 0.7245667037590721726, -29.92941129926923693, -37.65687897229916103 ) ) ;
#2051=VERTEX_POINT ( 'NONE', #42236 ) ;
#2055=ADVANCED_FACE ( 'NONE', ( #22792 ), #5640, .F. ) ;
#2059=CARTESIAN_POINT ( 'NONE',  ( 0.1104177457020373010, 41.65375561851285369, -11.16615714989265484 ) ) ;
#2063=CARTESIAN_POINT ( 'NONE',  ( 0.1104177457020373426, -11.16615714989280050, -41.65375561851281816 ) ) ;
#2068=ORIENTED_EDGE ( 'NONE', *, *, #57480, .F. ) ;
#2076=CARTESIAN_POINT ( 'NONE',  ( 0.8751705887134423323, 23.27176129838367302, 42.09020928323383259 ) ) ;
#2079=CARTESIAN_POINT ( 'NONE',  ( 2.643462169533613793, -19.65219740572159424, -43.83256147628726040 ) ) ;
#2081=VERTEX_POINT ( 'NONE', #13101 ) ;
#2082=EDGE_CURVE ( 'NONE', #39212, #3487, #48118, .T. ) ;
#2084=CARTESIAN_POINT ( 'NONE',  ( 0.6025881611877910160, 44.52856035602907525, -18.20817581200370228 ) ) ;
#2085=ORIENTED_EDGE ( 'NONE', *, *, #15130, .F. ) ;
#2086=CARTESIAN_POINT ( 'NONE',  ( 0.2224561200757619595, -31.02237548791974220, 29.94832483817983970 ) ) ;
#2097=DIRECTION ( 'NONE',  ( -1.000000000000000000, -0.000000000000000000, -0.000000000000000000 ) ) ;
#2099=EDGE_LOOP ( 'NONE', ( #27603, #15245, #51859, #2349 ) ) ;
#2101=CARTESIAN_POINT ( 'NONE',  ( 0.6254087463353908971, -37.74264085326077378, 29.82831063981268116 ) ) ;
#2103=CARTESIAN_POINT ( 'NONE',  ( 4.833616638992205949, 25.31740731790842602, 38.70560126501871423 ) ) ;
#2118=CARTESIAN_POINT ( 'NONE',  ( 0.6254087463353916743, -47.60024110474256531, 6.960754339421005632 ) ) ;
#2119=ADVANCED_FACE ( 'NONE', ( #39080 ), #28893, .F. ) ;
#2123=CARTESIAN_POINT ( 'NONE',  ( -6.016761891674564211, -18.84319130225482297, 0.003433883959717882409 ) ) ;
#2125=CARTESIAN_POINT ( 'NONE',  ( 0.8751705887134423323, -44.76769609654249393, 17.57879340691464165 ) ) ;
#2132=LINE ( 'NONE', #15659, #58862 ) ;
#2136=ORIENTED_EDGE ( 'NONE', *, *, #9331, .F. ) ;
#2142=CARTESIAN_POINT ( 'NONE',  ( 1.827119703190777544, 17.60659059422121686, 39.28489939038895074 ) ) ;
#2147=EDGE_LOOP ( 'NONE', ( #59872, #5116, #9175, #58869 ) ) ;
#2162=ORIENTED_EDGE ( 'NONE', *, *, #27048, .T. ) ;
#2172=ORIENTED_EDGE ( 'NONE', *, *, #37571, .T. ) ;
#2176=ORIENTED_EDGE ( 'NONE', *, *, #54993, .F. ) ;
#2177=CARTESIAN_POINT ( 'NONE',  ( 2.643462169533600914, -32.97543604874651635, -34.93025802711714789 ) ) ;
#2181=CARTESIAN_POINT ( 'NONE',  ( 3.238931869106853600, -29.07925862215153501, 31.66562935062887263 ) ) ;
#2184=CARTESIAN_POINT ( 'NONE',  ( 0.6027935024548037868, -29.14731236071041920, -38.27223087442838079 ) ) ;
#2185=EDGE_CURVE ( 'NONE', #36718, #55958, #58742, .T. ) ;
#2187=CARTESIAN_POINT ( 'NONE',  ( -6.001507490154111224, 13.33564355450126904, -13.31361390284146218 ) ) ;
#2194=DIRECTION ( 'NONE',  ( -1.000000000000000000, -0.000000000000000000, -0.000000000000000000 ) ) ;
#2199=CARTESIAN_POINT ( 'NONE',  ( -2.708315649062910779, 12.54007339125004883, 7.544341609840020446 ) ) ;
#2206=ADVANCED_FACE ( 'NONE', ( #20868 ), #39724, .F. ) ;
#2207=CARTESIAN_POINT ( 'NONE',  ( 0.1073791018717578927, 33.91564619577771111, 26.63563652260178927 ) ) ;
#2214=CARTESIAN_POINT ( 'NONE',  ( 4.975801465491695552, 8.787181743660156030, -47.10002938642133330 ) ) ;
#2218=B_SPLINE_CURVE_WITH_KNOTS ( 'NONE', 3,
 ( #61618, #20213, #3990, #29589 ),
 .UNSPECIFIED., .F., .F.,
 ( 4, 4 ),
 ( 0.000000000000000000, 0.005014147105413705591 ),
 .UNSPECIFIED. ) ;
#2221=CARTESIAN_POINT ( 'NONE',  ( -6.016761891674565099, -13.32172022638582121, -13.32657647165369141 ) ) ;
#2227=EDGE_CURVE ( 'NONE', #41115, #11845, #26858, .T. ) ;
#2232=CARTESIAN_POINT ( 'NONE',  ( 2.301430502907646947, 43.86847929982158689, 19.56449039932746459 ) ) ;
#2240=CARTESIAN_POINT ( 'NONE',  ( 0.6017667736363750963, -18.73201910948690596, 44.31084570541168688 ) ) ;
#2245=EDGE_CURVE ( 'NONE', #24034, #37726, #33639, .T. ) ;
#2262=B_SPLINE_CURVE_WITH_KNOTS ( 'NONE', 3,
 ( #36958, #16595, #45731, #2781, #45125, #54784, #35722, #56023, #7159, #21913, #11919, #50703, #30675, #50104, #55401, #2474, #41646, #36035, #41348 ),
 .UNSPECIFIED., .F., .F.,
 ( 4, 3, 3, 3, 3, 3, 4 ),
 ( 1.138109825968292890E-16, 0.0002618519381806232063, 0.0003927759815485936442, 0.0005237000248299411532, 0.0006546240681324906694, 0.0007855481115631298902, 0.0009699050456655105082 ),
 .UNSPECIFIED. ) ;
#2270=CARTESIAN_POINT ( 'NONE',  ( 3.680882792899938138, 8.091276083384761009, 47.28852514876959390 ) ) ;
#2272=CARTESIAN_POINT ( 'NONE',  ( -2.569797478183783568, -12.89088113963431326, -6.924386868080802060 ) ) ;
#2279=EDGE_CURVE ( 'NONE', #31934, #58618, #41850, .T. ) ;
#2285=ORIENTED_EDGE ( 'NONE', *, *, #13474, .F. ) ;
#2286=ORIENTED_EDGE ( 'NONE', *, *, #16129, .F. ) ;
#2287=FACE_OUTER_BOUND ( 'NONE', #21187, .T. ) ;
#2288=CARTESIAN_POINT ( 'NONE',  ( 0.1310142868023675411, 30.94009702668472883, -30.03916697317183804 ) ) ;
#2294=CARTESIAN_POINT ( 'NONE',  ( 0.6031356755773454870, 6.279306815850185686, 47.69587413076375526 ) ) ;
#2297=ORIENTED_EDGE ( 'NONE', *, *, #20089, .T. ) ;
#2301=DIRECTION ( 'NONE',  ( 0.000000000000000000, 0.000000000000000000, 1.000000000000000000 ) ) ;
#2303=CARTESIAN_POINT ( 'NONE',  ( 4.691466044806102076, -29.64918311951151964, 33.30232861642381437 ) ) ;
#2308=CARTESIAN_POINT ( 'NONE',  ( 0.7954190325252773475, -24.79809930825956599, -41.21355377862690261 ) ) ;
#2314=CARTESIAN_POINT ( 'NONE',  ( -6.001507490154111224, -9.408444979392205809, -16.32705935667517139 ) ) ;
#2329=CARTESIAN_POINT ( 'NONE',  ( 4.549368137175248350, 42.84816078363926550, 2.596185425822091553 ) ) ;
#2331=CARTESIAN_POINT ( 'NONE',  ( 0.6001305935487315502, 11.94532529598378190, -46.60388846085711378 ) ) ;
#2332=EDGE_CURVE ( 'NONE', #34292, #14733, #50816, .T. ) ;
#2338=CARTESIAN_POINT ( 'NONE',  ( 0.1313383488274157129, 25.74310646082151877, -34.59671037481849254 ) ) ;
#2345=CARTESIAN_POINT ( 'NONE',  ( 0.8751705887134423323, -41.19904111682490822, -24.81530984069193480 ) ) ;
#2347=CARTESIAN_POINT ( 'NONE',  ( 0.6001305935487422083, -5.760103278697706664, -47.76436356026965768 ) ) ;
#2349=ORIENTED_EDGE ( 'NONE', *, *, #42345, .F. ) ;
#2357=CARTESIAN_POINT ( 'NONE',  ( 0.6254087463353934506, 17.77193046492952533, -44.70339519268195971 ) ) ;
#2366=ORIENTED_EDGE ( 'NONE', *, *, #45718, .F. ) ;
#2375=EDGE_LOOP ( 'NONE', ( #14900, #3773, #35253, #48613 ) ) ;
#2377=CARTESIAN_POINT ( 'NONE',  ( 0.1103878639767399417, -39.86034920885575872, -16.45816205842750080 ) ) ;
#2379=ORIENTED_EDGE ( 'NONE', *, *, #48886, .T. ) ;
#2387=CARTESIAN_POINT ( 'NONE',  ( 4.549368137175248350, 0.000000000000000000, 0.000000000000000000 ) ) ;
#2390=CARTESIAN_POINT ( 'NONE',  ( -5.995132425357893702, 18.68182899165011435, 2.468096378288185733 ) ) ;
#2391=LINE ( 'NONE', #21516, #32558 ) ;
#2399=CIRCLE ( 'NONE', #34448, 47.91270532121795611 ) ;
#2403=CARTESIAN_POINT ( 'NONE',  ( 0.5998501479064708430, 44.64337787626247689, -17.92509395669061689 ) ) ;
#2405=CARTESIAN_POINT ( 'NONE',  ( 0.3622758884714600280, -31.06363466427748321, 29.89648521331577058 ) ) ;
#2410=CARTESIAN_POINT ( 'NONE',  ( 0.8760168074887076939, -17.58183840866429293, 44.77533136581851636 ) ) ;
#2414=EDGE_CURVE ( 'NONE', #29913, #31002, #13896, .T. ) ;
#2421=CARTESIAN_POINT ( 'NONE',  ( 0.1084644655670282259, 25.93599432281498096, -34.45367667780541154 ) ) ;
#2426=CARTESIAN_POINT ( 'NONE',  ( 4.833616638992208614, -20.04871863793836084, 41.67905425467671421 ) ) ;
#2436=CARTESIAN_POINT ( 'NONE',  ( 0.6031356755773454870, 38.16621646312168536, 29.28593560184445010 ) ) ;
#2442=FACE_OUTER_BOUND ( 'NONE', #54471, .T. ) ;
#2444=DIRECTION ( 'NONE',  ( -1.000000000000000000, -0.000000000000000000, -0.000000000000000000 ) ) ;
#2446=CONICAL_SURFACE ( 'NONE', #51447, 42.92674063221959813, 1.485477209440487556 ) ;
#2449=ADVANCED_FACE ( 'NONE', ( #19265 ), #26897, .F. ) ;
#2450=VERTEX_POINT ( 'NONE', #48674 ) ;
#2451=EDGE_CURVE ( 'NONE', #41641, #27695, #17883, .T. ) ;
#2452=CARTESIAN_POINT ( 'NONE',  ( 0.1073791018717578927, 11.62916352156150346, -41.52698815987157133 ) ) ;
#2456=CARTESIAN_POINT ( 'NONE',  ( 0.1084644655670282953, -41.55047717876512792, 11.54510651093188933 ) ) ;
#2468=CARTESIAN_POINT ( 'NONE',  ( 0.6017666602106490625, -29.00829887116099570, 38.37783452831155984 ) ) ;
#2469=VERTEX_POINT ( 'NONE', #1052 ) ;
#2471=EDGE_CURVE ( 'NONE', #25842, #9574, #669, .T. ) ;
#2474=CARTESIAN_POINT ( 'NONE',  ( 0.1092355843206037486, -26.01340835034388732, -34.39511076960595659 ) ) ;
#2483=FACE_OUTER_BOUND ( 'NONE', #47134, .T. ) ;
#2487=CARTESIAN_POINT ( 'NONE',  ( 0.1102144999581332746, -16.61938362665576108, 39.79340763430480621 ) ) ;
#2489=ORIENTED_EDGE ( 'NONE', *, *, #15281, .F. ) ;
#2491=CARTESIAN_POINT ( 'NONE',  ( 0.8751705887134553219, 7.160166390003662507, 47.55935879196473337 ) ) ;
#2498=CARTESIAN_POINT ( 'NONE',  ( -5.995132425357893702, 2.451215106828613433, -18.68405145320021532 ) ) ;
#2500=VERTEX_POINT ( 'NONE', #35213 ) ;
#2501=CARTESIAN_POINT ( 'NONE',  ( 0.3622758884714730732, -29.89648521331652731, 31.06363466427676201 ) ) ;
#2502=CARTESIAN_POINT ( 'NONE',  ( -6.016761891674564211, -16.31696541414278911, 9.424569481870193499 ) ) ;
#2503=CARTESIAN_POINT ( 'NONE',  ( 0.6031357023905875581, -29.25135304925253976, -38.19275261685265122 ) ) ;
#2510=FILL_AREA_STYLE ('',( #39850 ) ) ;
#2517=CARTESIAN_POINT ( 'NONE',  ( 0.09136607875274982415, 5.281323502666703820E-15, -43.12527911185304674 ) ) ;
#2526=AXIS2_PLACEMENT_3D ( 'NONE', #21208, #54697, #59096 ) ;
#2536=VECTOR ( 'NONE', #27315, 1000.000000000000114 ) ;
#2537=CARTESIAN_POINT ( 'NONE',  ( 0.3622758884714730732, -39.50828911767010965, 17.25816669464924047 ) ) ;
#2543=( BOUNDED_SURFACE ( )  B_SPLINE_SURFACE ( 3, 1, ( 
 ( #21050, #54221 ),
 ( #11342, #40489 ),
 ( #13509, #56394 ),
 ( #45806, #42036 ) ),
 .UNSPECIFIED., .F., .F., .F. ) 
 B_SPLINE_SURFACE_WITH_KNOTS ( ( 4, 4 ),
 ( 2, 2 ),
 ( 0.000000000000000000, 1.000000000000000000 ),
 ( 0.000000000000000000, 1.000000000000000000 ),
 .UNSPECIFIED. ) 
 GEOMETRIC_REPRESENTATION_ITEM ( )  RATIONAL_B_SPLINE_SURFACE ( (
 ( 1.000000000000000000, 1.000000000000000000),
 ( 0.7223157951917480446, 0.9931996967497186413),
 ( 0.7223157951917480446, 0.9931996967497186413),
 ( 1.000000000000000000, 1.000000000000000000) ) ) 
 REPRESENTATION_ITEM ( '' )  SURFACE ( )  );
#2547=VERTEX_POINT ( 'NONE', #20794 ) ;
#2548=ORIENTED_EDGE ( 'NONE', *, *, #11307, .T. ) ;
#2550=ORIENTED_EDGE ( 'NONE', *, *, #51977, .F. ) ;
#2551=DIRECTION ( 'NONE',  ( 0.000000000000000000, 0.000000000000000000, -1.000000000000000000 ) ) ;
#2565=CARTESIAN_POINT ( 'NONE',  ( 0.1087620492084204749, 41.55994353650425666, 11.51076657762349598 ) ) ;
#2567=DIRECTION ( 'NONE',  ( 0.09835009131224567436, -0.7091251765524118067, 0.6981896185982600089 ) ) ;
#2575=B_SPLINE_CURVE_WITH_KNOTS ( 'NONE', 3,
 ( #11598, #35727, #21604, #54790, #11925, #20748, #48320, #5380, #24506, #29822, #58616, #10735, #53606, #38950, #25748, #48938, #5986, #25126, #30432 ),
 .UNSPECIFIED., .F., .F.,
 ( 4, 3, 3, 3, 3, 3, 4 ),
 ( 1.161276725443423652E-16, 0.0002618519381806236400, 0.0003927759815485981978, 0.0005237000248299445142, 0.0006546240681324981504, 0.0007855481115631340102, 0.0009699050456655115924 ),
 .UNSPECIFIED. ) ;
#2579=CARTESIAN_POINT ( 'NONE',  ( 3.238741278300274029, 12.88350628398740483, -41.01623499586001742 ) ) ;
#2581=CARTESIAN_POINT ( 'NONE',  ( 0.6027935024548038978, 6.452291758824724610, -47.67281620606625836 ) ) ;
#2584=CARTESIAN_POINT ( 'NONE',  ( 0.2230388203127609270, -6.380812898001274824, -42.64472907182728534 ) ) ;
#2590=CARTESIAN_POINT ( 'NONE',  ( 0.6254087463353908971, 5.596276562478328387, -47.77987801197956230 ) ) ;
#2596=CARTESIAN_POINT ( 'NONE',  ( 0.1064266379913940824, 43.12102052820963394, -0.5615183164813251082 ) ) ;
#2602=ORIENTED_EDGE ( 'NONE', *, *, #43973, .F. ) ;
#2610=CARTESIAN_POINT ( 'NONE',  ( 0.1101816497532063233, -37.27878591512690321, 21.67974746580484435 ) ) ;
#2611=ORIENTED_EDGE ( 'NONE', *, *, #3313, .T. ) ;
#2612=ORIENTED_EDGE ( 'NONE', *, *, #6390, .F. ) ;
#2617=CARTESIAN_POINT ( 'NONE',  ( -6.015611763856276717, 2.453375430804066504, 18.68284711750059301 ) ) ;
#2620=CARTESIAN_POINT ( 'NONE',  ( 0.8760168074886965917, 7.161346975773705381, -47.56749362999706676 ) ) ;
#2626=DIRECTION ( 'NONE',  ( 0.09835009131224567436, -0.2500873580884643288, -0.9632152266566414989 ) ) ;
#2636=CARTESIAN_POINT ( 'NONE',  ( 0.6009452777970409887, 18.81240106508465004, 44.27681866781112063 ) ) ;
#2641=EDGE_LOOP ( 'NONE', ( #28229, #27216, #27458, #6927 ) ) ;
#2642=DIRECTION ( 'NONE',  ( -1.000000000000000000, -0.000000000000000000, -0.000000000000000000 ) ) ;
#2643=CARTESIAN_POINT ( 'NONE',  ( 0.1313383488274121880, -4.995828979989775043, 42.83318330237614902 ) ) ;
#2644=FACE_OUTER_BOUND ( 'NONE', #50040, .T. ) ;
#2667=CARTESIAN_POINT ( 'NONE',  ( 0.6009452777970414328, -44.27681866781119169, 18.81240106508449372 ) ) ;
#2668=ADVANCED_FACE ( 'NONE', ( #8218 ), #60908, .F. ) ;
#2670=EDGE_CURVE ( 'NONE', #45306, #44423, #29090, .T. ) ;
#2672=CARTESIAN_POINT ( 'NONE',  ( 4.975801465491694664, 42.71626295676232843, 21.70134120755216145 ) ) ;
#2675=ORIENTED_EDGE ( 'NONE', *, *, #8604, .T. ) ;
#2682=CARTESIAN_POINT ( 'NONE',  ( 0.1073791018717578927, 37.58707531572206051, -21.14095454447521405 ) ) ;
#2685=VECTOR ( 'NONE', #12874, 1000.000000000000114 ) ;
#2689=CARTESIAN_POINT ( 'NONE',  ( 0.1104177457020373287, -39.84367193872667201, -16.49849172082149451 ) ) ;
#2690=DIRECTION ( 'NONE',  ( 0.000000000000000000, 0.000000000000000000, 1.000000000000000000 ) ) ;
#2693=CARTESIAN_POINT ( 'NONE',  ( 0.7246131072078549895, 0.8205838906003107835, -48.09507913767662757 ) ) ;
#2701=CONICAL_SURFACE ( 'NONE', #48729, 42.92674063221959813, 1.485477209440487556 ) ;
#2712=CARTESIAN_POINT ( 'NONE',  ( 0.2885700199627515561, 42.84523253167937185, 4.828949117911921718 ) ) ;
#2713=EDGE_CURVE ( 'NONE', #23990, #45978, #57117, .T. ) ;
#2719=CARTESIAN_POINT ( 'NONE',  ( 0.5998501479064699549, 44.24259072156085182, -18.89267974119621485 ) ) ;
#2723=CARTESIAN_POINT ( 'NONE',  ( 0.7048096507298635682, -44.11842270945987821, 19.18768066167044140 ) ) ;
#2725=VERTEX_POINT ( 'NONE', #10707 ) ;
#2727=CARTESIAN_POINT ( 'NONE',  ( 4.549368137175248350, 0.000000000000000000, 0.000000000000000000 ) ) ;
#2730=CARTESIAN_POINT ( 'NONE',  ( 0.1073791018717578927, -5.147744207006579309, -42.81622261970993293 ) ) ;
#2732=ORIENTED_EDGE ( 'NONE', *, *, #44512, .T. ) ;
#2745=CARTESIAN_POINT ( 'NONE',  ( 0.6017667736363750963, 37.95278695280770620, 29.56223180955344532 ) ) ;
#2746=EDGE_CURVE ( 'NONE', #32390, #56965, #43941, .T. ) ;
#2750=CARTESIAN_POINT ( 'NONE',  ( 0.1313383488274123545, -40.08066228784256424, -15.91164383651733161 ) ) ;
#2751=CARTESIAN_POINT ( 'NONE',  ( -6.001507490154110336, -17.40350523682700157, 7.225628667346519762 ) ) ;
#2760=( BOUNDED_SURFACE ( )  B_SPLINE_SURFACE ( 3, 1, ( 
 ( #34936, #53998 ),
 ( #11425, #25507 ),
 ( #6999, #30209 ),
 ( #6682, #35554 ) ),
 .UNSPECIFIED., .F., .F., .F. ) 
 B_SPLINE_SURFACE_WITH_KNOTS ( ( 4, 4 ),
 ( 2, 2 ),
 ( 0.000000000000000000, 1.000000000000000000 ),
 ( 0.000000000000000000, 1.000000000000000000 ),
 .UNSPECIFIED. ) 
 GEOMETRIC_REPRESENTATION_ITEM ( )  RATIONAL_B_SPLINE_SURFACE ( (
 ( 1.000000000000000000, 1.000000000000000000),
 ( 0.9953040768229005630, 0.8617119497784937465),
 ( 0.9953040768229005630, 0.8617119497784937465),
 ( 1.000000000000000000, 1.000000000000000000) ) ) 
 REPRESENTATION_ITEM ( '' )  SURFACE ( )  );
#2763=EDGE_CURVE ( 'NONE', #19329, #57918, #30119, .T. ) ;
#2764=CARTESIAN_POINT ( 'NONE',  ( 0.1095718737110178559, 37.21776476380626519, 21.78439022773168787 ) ) ;
#2775=EDGE_LOOP ( 'NONE', ( #35597, #49308, #3343, #42126 ) ) ;
#2776=CARTESIAN_POINT ( 'NONE',  ( 0.6028618097248862329, -29.14732267129602050, 38.27229381545001985 ) ) ;
#2780=CARTESIAN_POINT ( 'NONE',  ( 0.1073791018717483448, -33.91564619577824402, 26.63563652260111070 ) ) ;
#2781=CARTESIAN_POINT ( 'NONE',  ( 0.1097557419366048670, -26.42915440612308231, -34.07666148910637105 ) ) ;
#2795=ORIENTED_EDGE ( 'NONE', *, *, #50137, .F. ) ;
#2799=B_SPLINE_CURVE_WITH_KNOTS ( 'NONE', 3,
 ( #26999, #22926, #2865, #26375 ),
 .UNSPECIFIED., .F., .F.,
 ( 4, 4 ),
 ( 0.000000000000000000, 0.005014147105413707325 ),
 .UNSPECIFIED. ) ;
#2802=CARTESIAN_POINT ( 'NONE',  ( 0.1073791018717483448, -30.14884492832410601, 30.83464511437086841 ) ) ;
#2803=CARTESIAN_POINT ( 'NONE',  ( 0.3622758884714600280, -22.26738722580193652, 36.91764744403282350 ) ) ;
#2806=CARTESIAN_POINT ( 'NONE',  ( 0.1103878639767399555, -42.76182653383953891, -5.580746265796884487 ) ) ;
#2810=CARTESIAN_POINT ( 'NONE',  ( 0.6001305935487315502, 38.48510059944008077, 28.87057754790950881 ) ) ;
#2816=SURFACE_STYLE_FILL_AREA ( #25400 ) ;
#2823=DIRECTION ( 'NONE',  ( 0.000000000000000000, 0.000000000000000000, -1.000000000000000000 ) ) ;
#2824=CARTESIAN_POINT ( 'NONE',  ( 0.1104177457020373565, 21.55798761925387907, -37.34931850022147870 ) ) ;
#2830=CARTESIAN_POINT ( 'NONE',  ( 0.6001305935487315502, 28.87057754790885866, 38.48510059944057815 ) ) ;
#2833=CARTESIAN_POINT ( 'NONE',  ( 0.1064266418746771803, 33.86837517279509768, 26.69589626339724120 ) ) ;
#2839=CARTESIAN_POINT ( 'NONE',  ( -6.016104459813374383, 18.68271063303497925, -2.454244026260903766 ) ) ;
#2844=CARTESIAN_POINT ( 'NONE',  ( 3.238741278300274029, -42.82436441900176760, 3.793425828151925305 ) ) ;
#2849=ORIENTED_EDGE ( 'NONE', *, *, #33530, .F. ) ;
#2851=AXIS2_PLACEMENT_3D ( 'NONE', #1046, #53963, #58982 ) ;
#2865=CARTESIAN_POINT ( 'NONE',  ( 4.833616638992208614, 46.11947910922909699, -3.476827473557382753 ) ) ;
#2874=CARTESIAN_POINT ( 'NONE',  ( 3.238741278300273141, 18.12697907494894878, -38.98370040185407959 ) ) ;
#2877=CARTESIAN_POINT ( 'NONE',  ( 0.7048096507298579061, 11.63498350884271737, 46.68221792389243063 ) ) ;
#2878=EDGE_CURVE ( 'NONE', #38025, #24504, #50156, .T. ) ;
#2897=CARTESIAN_POINT ( 'NONE',  ( 0.3622758884714600280, -15.73321244754826509, -40.13994584881776007 ) ) ;
#2900=B_SPLINE_CURVE_WITH_KNOTS ( 'NONE', 3,
 ( #9818, #44284, #1020, #57399, #711, #28922, #5091, #43356, #48958, #48041, #6007, #24218, #38348, #1316, #34557, #53624 ),
 .UNSPECIFIED., .F., .F.,
 ( 4, 3, 3, 3, 3, 4 ),
 ( 2.030557555191247372E-17, 0.0002618515315864420852, 0.0003927756766342001596, 0.0005236998216950581068, 0.0007855159896329935850, 0.001047349442285931556 ),
 .UNSPECIFIED. ) ;
#2901=CARTESIAN_POINT ( 'NONE',  ( 0.6025881611877910160, -33.86250327239872604, -34.17105830828403157 ) ) ;
#2902=CARTESIAN_POINT ( 'NONE',  ( 4.549368137175248350, -2.596185425822241211, 42.84816078363925840 ) ) ;
#2903=CARTESIAN_POINT ( 'NONE',  ( 0.6031357023905875581, -6.236038527293725764, -47.70157053127527291 ) ) ;
#2907=DIRECTION ( 'NONE',  ( -1.000000000000000000, -0.000000000000000000, -0.000000000000000000 ) ) ;
#2908=( BOUNDED_SURFACE ( )  B_SPLINE_SURFACE ( 3, 1, ( 
 ( #3386, #22522 ),
 ( #41640, #56017 ),
 ( #13135, #861 ),
 ( #48473, #57540 ) ),
 .UNSPECIFIED., .F., .F., .F. ) 
 B_SPLINE_SURFACE_WITH_KNOTS ( ( 4, 4 ),
 ( 2, 2 ),
 ( 0.000000000000000000, 1.000000000000000000 ),
 ( 0.000000000000000000, 1.000000000000000000 ),
 .UNSPECIFIED. ) 
 GEOMETRIC_REPRESENTATION_ITEM ( )  RATIONAL_B_SPLINE_SURFACE ( (
 ( 1.000000000000000000, 1.000000000000000000),
 ( 0.9953040768229005630, 0.8617119497784937465),
 ( 0.9953040768229005630, 0.8617119497784937465),
 ( 1.000000000000000000, 1.000000000000000000) ) ) 
 REPRESENTATION_ITEM ( '' )  SURFACE ( )  );
#2909=CARTESIAN_POINT ( 'NONE',  ( 0.6029303876144825880, 46.50193792184025199, -12.32464004947830993 ) ) ;
#2911=VERTEX_POINT ( 'NONE', #30407 ) ;
#2915=CARTESIAN_POINT ( 'NONE',  ( -6.015611763856276717, -13.31979030221789984, -13.32857883366847318 ) ) ;
#2916=ORIENTED_EDGE ( 'NONE', *, *, #24565, .T. ) ;
#2924=ORIENTED_EDGE ( 'NONE', *, *, #38011, .T. ) ;
#2925=CARTESIAN_POINT ( 'NONE',  ( 0.8751705887134423323, -11.58504748649167837, -46.67919521768883584 ) ) ;
#2927=CONICAL_SURFACE ( 'NONE', #59943, 42.92674063221959813, 1.485477209440487556 ) ;
#2933=CARTESIAN_POINT ( 'NONE',  ( 4.833616638992205949, -30.83411269743588434, 34.47248434257857497 ) ) ;
#2935=CARTESIAN_POINT ( 'NONE',  ( 0.6031356755773454870, -48.10744332413212021, 2.564066922309144806E-05 ) ) ;
#2940=ORIENTED_EDGE ( 'NONE', *, *, #1538, .T. ) ;
#2941=CARTESIAN_POINT ( 'NONE',  ( 0.6041374136657476912, -12.28249295042078160, 46.51335992032597488 ) ) ;
#2942=LINE ( 'NONE', #22070, #32648 ) ;
#2950=CARTESIAN_POINT ( 'NONE',  ( 0.1081432562775998252, 40.00205417854812140, -16.11101151263784459 ) ) ;
#2951=ORIENTED_EDGE ( 'NONE', *, *, #35118, .F. ) ;
#2952=CARTESIAN_POINT ( 'NONE',  ( 0.1087620492084205442, 42.80136086877933366, -5.269740196867475746 ) ) ;
#2955=CARTESIAN_POINT ( 'NONE',  ( 0.7245667037590756143, 48.09508190954920082, -0.8205429720399597393 ) ) ;
#2962=CARTESIAN_POINT ( 'NONE',  ( -2.569797478183790229, 6.924386868080667945, 12.89088113963438431 ) ) ;
#2973=ORIENTED_EDGE ( 'NONE', *, *, #18346, .T. ) ;
#2978=CARTESIAN_POINT ( 'NONE',  ( -6.016104459813371719, 14.95258000663132236, 11.46679299034585675 ) ) ;
#2979=CARTESIAN_POINT ( 'NONE',  ( 2.643462169533613793, 1.382267876917792737, 48.01657676222237825 ) ) ;
#2981=CARTESIAN_POINT ( 'NONE',  ( 0.6029303876144825880, -44.49541906039141281, 18.28892193312784542 ) ) ;
#2986=ORIENTED_EDGE ( 'NONE', *, *, #38914, .F. ) ;
#2987=CIRCLE ( 'NONE', #34010, 42.92674063221959813 ) ;
#2995=CARTESIAN_POINT ( 'NONE',  ( 0.1084644655670283647, 41.55047717876504976, -11.54510651093217710 ) ) ;
#3006=( BOUNDED_SURFACE ( )  B_SPLINE_SURFACE ( 3, 1, ( 
 ( #9387, #61681 ),
 ( #18814, #37938 ),
 ( #51368, #52290 ),
 ( #4659, #56996 ) ),
 .UNSPECIFIED., .F., .F., .F. ) 
 B_SPLINE_SURFACE_WITH_KNOTS ( ( 4, 4 ),
 ( 2, 2 ),
 ( 0.000000000000000000, 1.000000000000000000 ),
 ( 0.000000000000000000, 1.000000000000000000 ),
 .UNSPECIFIED. ) 
 GEOMETRIC_REPRESENTATION_ITEM ( )  RATIONAL_B_SPLINE_SURFACE ( (
 ( 1.000000000000000000, 1.000000000000000000),
 ( 0.7223157951917476005, 0.9931996967497186413),
 ( 0.7223157951917476005, 0.9931996967497186413),
 ( 1.000000000000000000, 1.000000000000000000) ) ) 
 REPRESENTATION_ITEM ( '' )  SURFACE ( )  );
#3008=CARTESIAN_POINT ( 'NONE',  ( -6.016761891674565099, -7.214149619366484245, 17.40752468084780702 ) ) ;
#3016=CARTESIAN_POINT ( 'NONE',  ( -6.001507490154111224, 16.32705935667520336, -9.408444979392148966 ) ) ;
#3019=CARTESIAN_POINT ( 'NONE',  ( 0.6031356755773454870, 44.44547243635321365, -18.40994522247712695 ) ) ;
#3020=ADVANCED_FACE ( 'NONE', ( #56681 ), #33309, .F. ) ;
#3064=CARTESIAN_POINT ( 'NONE',  ( 0.3622758884714600280, 0.8252992914328071139, -43.10531414739104861 ) ) ;
#3071=CARTESIAN_POINT ( 'NONE',  ( 0.1103310638050662013, 11.24099191366999406, -41.63362651001254733 ) ) ;
#3072=B_SPLINE_CURVE_WITH_KNOTS ( 'NONE', 3,
 ( #52894, #29703, #48819, #10304 ),
 .UNSPECIFIED., .F., .F.,
 ( 4, 4 ),
 ( 2.180944827630287245E-17, 0.004564976165746189446 ),
 .UNSPECIFIED. ) ;
#3075=DIRECTION ( 'NONE',  ( -1.000000000000000000, 0.000000000000000000, 0.000000000000000000 ) ) ;
#3076=ORIENTED_EDGE ( 'NONE', *, *, #7655, .F. ) ;
#3079=CARTESIAN_POINT ( 'NONE',  ( 0.5998501479064699549, -29.69975237324587169, -37.84527566984847624 ) ) ;
#3098=EDGE_CURVE ( 'NONE', #12553, #38470, #4657, .T. ) ;
#3100=CARTESIAN_POINT ( 'NONE',  ( -6.017396004339687465, -9.420565012089314294, -16.31924478664284806 ) ) ;
#3101=CARTESIAN_POINT ( 'NONE',  ( 4.549368137175248350, 42.06008734272396765, -8.582197505783977221 ) ) ;
#3105=CARTESIAN_POINT ( 'NONE',  ( 0.6017666602106489515, 44.57804174182696499, 18.08695057064608136 ) ) ;
#3118=ORIENTED_EDGE ( 'NONE', *, *, #60033, .F. ) ;
#3119=CARTESIAN_POINT ( 'NONE',  ( 0.1095718737110178004, -42.72125633542930245, -5.883530294869984800 ) ) ;
#3120=CARTESIAN_POINT ( 'NONE',  ( -6.017396004339686577, -16.31807101179377284, 9.422598049764564720 ) ) ;
#3121=ADVANCED_FACE ( 'NONE', ( #26809 ), #46124, .F. ) ;
#3130=( BOUNDED_SURFACE ( )  B_SPLINE_SURFACE ( 3, 1, ( 
 ( #16809, #32138 ),
 ( #36536, #12733 ),
 ( #41239, #12117 ),
 ( #60607, #45947 ) ),
 .UNSPECIFIED., .F., .F., .F. ) 
 B_SPLINE_SURFACE_WITH_KNOTS ( ( 4, 4 ),
 ( 2, 2 ),
 ( 0.000000000000000000, 1.000000000000000000 ),
 ( 0.000000000000000000, 1.000000000000000000 ),
 .UNSPECIFIED. ) 
 GEOMETRIC_REPRESENTATION_ITEM ( )  RATIONAL_B_SPLINE_SURFACE ( (
 ( 1.000000000000000000, 1.000000000000000000),
 ( 0.7223157951917480446, 0.9931996967497186413),
 ( 0.7223157951917480446, 0.9931996967497186413),
 ( 1.000000000000000000, 1.000000000000000000) ) ) 
 REPRESENTATION_ITEM ( '' )  SURFACE ( )  );
#3135=CARTESIAN_POINT ( 'NONE',  ( 0.1100053167205930493, -16.66867746965619546, -39.77279469894207864 ) ) ;
#3136=LINE ( 'NONE', #36383, #4170 ) ;
#3140=CARTESIAN_POINT ( 'NONE',  ( -6.016489644550736315, -11.47450955518478111, -14.94663725562927503 ) ) ;
#3142=B_SPLINE_CURVE_WITH_KNOTS ( 'NONE', 3,
 ( #47852, #52841, #61907, #14962, #43792, #24031 ),
 .UNSPECIFIED., .F., .F.,
 ( 4, 2, 4 ),
 ( 1.253145692779649283E-17, 0.0002293319059085063491, 0.0004586638118170001757 ),
 .UNSPECIFIED. ) ;
#3156=ORIENTED_EDGE ( 'NONE', *, *, #58570, .F. ) ;
#3161=CARTESIAN_POINT ( 'NONE',  ( 0.6017667736363749853, 29.00830848931575900, 38.37782726569699321 ) ) ;
#3164=CARTESIAN_POINT ( 'NONE',  ( 4.975801465491695552, 42.71626295676264817, -21.70134120755155394 ) ) ;
#3168=CARTESIAN_POINT ( 'NONE',  ( 3.680882792899937250, 27.71664061799148371, -39.15943299201958894 ) ) ;
#3170=EDGE_CURVE ( 'NONE', #2911, #39295, #36852, .T. ) ;
#3188=CARTESIAN_POINT ( 'NONE',  ( -6.016104459813371719, -18.19977249352313819, 4.882138007282685876 ) ) ;
#3191=ORIENTED_EDGE ( 'NONE', *, *, #56927, .F. ) ;
#3197=CARTESIAN_POINT ( 'NONE',  ( 0.6031357023905875581, 6.322524267548581989, -47.69018446756502527 ) ) ;
#3207=CARTESIAN_POINT ( 'NONE',  ( -6.015611763856276717, 14.94556629257425584, 11.47596948473816170 ) ) ;
#3208=CARTESIAN_POINT ( 'NONE',  ( 0.6009452777970410997, -6.711700115493219876, -47.63713033690751786 ) ) ;
#3209=CARTESIAN_POINT ( 'NONE',  ( 0.8751705887134553219, 46.67919521768871505, 11.58504748649215976 ) ) ;
#3219=ORIENTED_EDGE ( 'NONE', *, *, #32047, .T. ) ;
#3222=CARTESIAN_POINT ( 'NONE',  ( 4.975801465491695552, 0.000000000000000000, 0.000000000000000000 ) ) ;
#3228=CARTESIAN_POINT ( 'NONE',  ( 0.6001305935487315502, -33.64689939321966250, 34.38748867424654776 ) ) ;
#3236=ORIENTED_EDGE ( 'NONE', *, *, #37708, .T. ) ;
#3242=CARTESIAN_POINT ( 'NONE',  ( -6.015611763856276717, -0.006214430185009750529, -18.84324252354755203 ) ) ;
#3254=CARTESIAN_POINT ( 'NONE',  ( -6.001507490154111224, 13.31361390284159896, 13.33564355450112870 ) ) ;
#3269=CARTESIAN_POINT ( 'NONE',  ( 4.549368137175248350, 0.000000000000000000, 0.000000000000000000 ) ) ;
#3270=CARTESIAN_POINT ( 'NONE',  ( 5.880360259849752858, 47.86623372148045519, 3.184717612778101614 ) ) ;
#3271=CARTESIAN_POINT ( 'NONE',  ( 0.7954196712028483995, -33.39101545667313076, -34.61997730204570445 ) ) ;
#3283=EDGE_LOOP ( 'NONE', ( #44355, #40516, #7947, #16615 ) ) ;
#3284=VERTEX_POINT ( 'NONE', #47777 ) ;
#3285=CARTESIAN_POINT ( 'NONE',  ( 4.322998006666165516, 46.85697641700708260, -10.36018990813264296 ) ) ;
#3294=CARTESIAN_POINT ( 'NONE',  ( 0.8751705887134423323, -29.98056538504989277, 37.60752970653777538 ) ) ;
#3295=EDGE_CURVE ( 'NONE', #42216, #55695, #21541, .T. ) ;
#3301=CARTESIAN_POINT ( 'NONE',  ( 0.6017666602106489515, 41.83584962818284225, 23.75081624637636679 ) ) ;
#3309=CARTESIAN_POINT ( 'NONE',  ( 3.238741278300274029, 41.96285461600081135, -9.350673766180365831 ) ) ;
#3313=EDGE_CURVE ( 'NONE', #37210, #47783, #43198, .T. ) ;
#3317=AXIS2_PLACEMENT_3D ( 'NONE', #53422, #40301, #59354 ) ;
#3324=CARTESIAN_POINT ( 'NONE',  ( -6.016761891674565099, -2.456125503350587991, -18.68243340030205246 ) ) ;
#3331=ORIENTED_EDGE ( 'NONE', *, *, #45884, .T. ) ;
#3337=VERTEX_POINT ( 'NONE', #19900 ) ;
#3338=CARTESIAN_POINT ( 'NONE',  ( 0.7245667037590732829, -37.65687897229943104, 29.92941129926883903 ) ) ;
#3339=CARTESIAN_POINT ( 'NONE',  ( -6.015611763856276717, 17.40650793417854203, -7.216738110653091454 ) ) ;
#3343=ORIENTED_EDGE ( 'NONE', *, *, #40535, .T. ) ;
#3351=CARTESIAN_POINT ( 'NONE',  ( 4.975801465491694664, -35.64402118370934147, -32.01766832630300286 ) ) ;
#3359=CARTESIAN_POINT ( 'NONE',  ( 0.8751705887134553219, -46.67919521768879321, -11.58504748649183647 ) ) ;
#3360=CARTESIAN_POINT ( 'NONE',  ( 4.549368137175248350, -42.14271863032838894, 8.166781970325002860 ) ) ;
#3366=CARTESIAN_POINT ( 'NONE',  ( 0.7245667037590747261, -42.06183421678311163, -23.33692989609096813 ) ) ;
#3367=EDGE_CURVE ( 'NONE', #49832, #38633, #26752, .T. ) ;
#3368=( BOUNDED_SURFACE ( )  B_SPLINE_SURFACE ( 3, 1, ( 
 ( #23535, #22619 ),
 ( #3486, #8194 ),
 ( #27313, #42661 ),
 ( #19170, #17932 ) ),
 .UNSPECIFIED., .F., .F., .F. ) 
 B_SPLINE_SURFACE_WITH_KNOTS ( ( 4, 4 ),
 ( 2, 2 ),
 ( 0.000000000000000000, 1.000000000000000000 ),
 ( 0.000000000000000000, 1.000000000000000000 ),
 .UNSPECIFIED. ) 
 GEOMETRIC_REPRESENTATION_ITEM ( )  RATIONAL_B_SPLINE_SURFACE ( (
 ( 1.000000000000000000, 1.000000000000000000),
 ( 0.9751682680413298332, 0.9999560080971552356),
 ( 0.9751682680413298332, 0.9999560080971552356),
 ( 1.000000000000000000, 1.000000000000000000) ) ) 
 REPRESENTATION_ITEM ( '' )  SURFACE ( )  );
#3373=CARTESIAN_POINT ( 'NONE',  ( 2.643462169533600914, -47.42536612906423699, -7.637863311827439716 ) ) ;
#3386=CARTESIAN_POINT ( 'NONE',  ( -6.015611763856276717, 18.19956619163658118, 4.882992715191364574 ) ) ;
#3392=CARTESIAN_POINT ( 'NONE',  ( 0.1310142868023676521, -15.91230901232197326, -40.08041389954875200 ) ) ;
#3394=CARTESIAN_POINT ( 'NONE',  ( 2.301529144917016101, -42.22700141647025873, -22.89307126379972601 ) ) ;
#3400=CARTESIAN_POINT ( 'NONE',  ( 4.833616638992208614, 45.27110352095247947, -9.466882727841657186 ) ) ;
#3403=CARTESIAN_POINT ( 'NONE',  ( 0.8760168074886965917, 41.20610493656875661, 24.81951362746092826 ) ) ;
#3409=ORIENTED_EDGE ( 'NONE', *, *, #18116, .F. ) ;
#3417=CARTESIAN_POINT ( 'NONE',  ( 0.1087620492084206275, -42.70684898916392314, -5.987629195157659900 ) ) ;
#3433=CARTESIAN_POINT ( 'NONE',  ( 1.827119703190780209, -1.232688548475726620, -43.03226500438893964 ) ) ;
#3439=ADVANCED_FACE ( 'NONE', ( #2287 ), #54493, .F. ) ;
#3440=CARTESIAN_POINT ( 'NONE',  ( 4.975801465491695552, 0.000000000000000000, 0.000000000000000000 ) ) ;
#3450=CARTESIAN_POINT ( 'NONE',  ( 4.322998006666165516, -10.36018990813280816, -46.85697641700704708 ) ) ;
#3460=CARTESIAN_POINT ( 'NONE',  ( 0.5988103622719993524, 46.30780754281414602, 13.03604477829307129 ) ) ;
#3464=CARTESIAN_POINT ( 'NONE',  ( 0.1073791018717483448, -42.81622261970991161, -5.147744207006710759 ) ) ;
#3478=CARTESIAN_POINT ( 'NONE',  ( 4.691466044806102076, -29.14742760351085593, -33.74235639413318211 ) ) ;
#3482=CARTESIAN_POINT ( 'NONE',  ( 0.1073791018717578927, 37.10214135362858912, 21.98088480513677823 ) ) ;
#3483=VECTOR ( 'NONE', #18982, 1000.000000000000000 ) ;
#3486=CARTESIAN_POINT ( 'NONE',  ( -6.017396004339687465, 11.47192209077608815, -14.94857180791981222 ) ) ;
#3487=VERTEX_POINT ( 'NONE', #42395 ) ;
#3492=ORIENTED_EDGE ( 'NONE', *, *, #34731, .T. ) ;
#3494=CARTESIAN_POINT ( 'NONE',  ( 4.975801465491694664, -8.787181743659814970, -47.10002938642139014 ) ) ;
#3498=CARTESIAN_POINT ( 'NONE',  ( 4.549368137175248350, -8.166781970326043805, 42.14271863032818999 ) ) ;
#3505=CARTESIAN_POINT ( 'NONE',  ( 0.2885700199627516671, -15.75356883787179108, 40.13549263616297935 ) ) ;
#3507=AXIS2_PLACEMENT_3D ( 'NONE', #48407, #48108, #18374 ) ;
#3513=EDGE_CURVE ( 'NONE', #58236, #2002, #33900, .T. ) ;
#3514=CARTESIAN_POINT ( 'NONE',  ( 0.6041374136657475802, -47.67304777898695534, -6.452348380035735076 ) ) ;
#3529=ORIENTED_EDGE ( 'NONE', *, *, #24899, .T. ) ;
#3536=ORIENTED_EDGE ( 'NONE', *, *, #37675, .T. ) ;
#3545=ORIENTED_EDGE ( 'NONE', *, *, #292, .F. ) ;
#3549=CARTESIAN_POINT ( 'NONE',  ( 4.549368137175248350, 23.67244292351640667, -35.80950303116076583 ) ) ;
#3550=CARTESIAN_POINT ( 'NONE',  ( 0.6017667736363750963, 34.26315558341190837, -33.76945004754880131 ) ) ;
#3553=B_SPLINE_CURVE_WITH_KNOTS ( 'NONE', 3,
 ( #37200, #13386, #37832, #43134, #37510, #24005 ),
 .UNSPECIFIED., .F., .F.,
 ( 4, 2, 4 ),
 ( 0.000000000000000000, 0.0002450742804987359109, 0.0004901485609974718218 ),
 .UNSPECIFIED. ) ;
#3555=DIRECTION ( 'NONE',  ( 0.000000000000000000, 0.000000000000000000, 1.000000000000000000 ) ) ;
#3558=CARTESIAN_POINT ( 'NONE',  ( -6.015611763856276717, -18.68284711750060367, 2.453375430804002111 ) ) ;
#3561=CARTESIAN_POINT ( 'NONE',  ( 0.1084644655670281704, 42.70194587816329346, -6.022910953206664253 ) ) ;
#3564=CARTESIAN_POINT ( 'NONE',  ( 0.8751705887134423323, 46.67919521768887847, -11.58504748649151317 ) ) ;
#3567=CARTESIAN_POINT ( 'NONE',  ( 0.6001305935487315502, -48.10757715638248300, -0.5236757026887732813 ) ) ;
#3568=CARTESIAN_POINT ( 'NONE',  ( 4.975801465491695552, -47.10002938642136883, -8.787181743659990829 ) ) ;
#3574=CARTESIAN_POINT ( 'NONE',  ( 0.7245667037590776127, 29.92941129926897759, 37.65687897229936709 ) ) ;
#3578=B_SPLINE_CURVE_WITH_KNOTS ( 'NONE', 3,
 ( #57343, #14175, #61428, #47360 ),
 .UNSPECIFIED., .F., .F.,
 ( 4, 4 ),
 ( 1.907487264466063683E-17, 0.004444306975806113294 ),
 .UNSPECIFIED. ) ;
#3581=CARTESIAN_POINT ( 'NONE',  ( -6.016489644550736315, -11.46752133529394868, 14.95199950534944122 ) ) ;
#3586=DIRECTION ( 'NONE',  ( 0.000000000000000000, 0.000000000000000000, -1.000000000000000000 ) ) ;
#3590=CARTESIAN_POINT ( 'NONE',  ( 0.6029303876144825880, -46.43417959025982356, -12.57751758557253652 ) ) ;
#3592=VERTEX_POINT ( 'NONE', #32367 ) ;
#3599=CARTESIAN_POINT ( 'NONE',  ( 0.5998501479064699549, 0.5236536531308225717, 48.10473956285920138 ) ) ;
#3601=CARTESIAN_POINT ( 'NONE',  ( 0.7954196712028469562, -29.96539649507113623, 37.62416450255238232 ) ) ;
#3603=ORIENTED_EDGE ( 'NONE', *, *, #52758, .F. ) ;
#3607=CARTESIAN_POINT ( 'NONE',  ( -6.016761891674564211, -18.20201388312091950, -4.873659902332557081 ) ) ;
#3608=CARTESIAN_POINT ( 'NONE',  ( 4.833616638992208614, 3.476827473557241976, 46.11947910922911120 ) ) ;
#3610=DIRECTION ( 'NONE',  ( -0.000000000000000000, 1.000000000000000000, 0.000000000000000000 ) ) ;
#3611=CARTESIAN_POINT ( 'NONE',  ( 0.6254311100348672881, -23.45480814408399084, -42.00127298835415246 ) ) ;
#3613=VERTEX_POINT ( 'NONE', #48606 ) ;
#3625=ORIENTED_EDGE ( 'NONE', *, *, #45679, .F. ) ;
#3627=ORIENTED_EDGE ( 'NONE', *, *, #53812, .T. ) ;
#3631=CARTESIAN_POINT ( 'NONE',  ( 0.6001305935487422083, 0.5236757026889211630, -48.10757715638248300 ) ) ;
#3639=EDGE_CURVE ( 'NONE', #45306, #9574, #34220, .T. ) ;
#3642=B_SPLINE_CURVE_WITH_KNOTS ( 'NONE', 3,
 ( #44171, #57897, #582, #53208 ),
 .UNSPECIFIED., .F., .F.,
 ( 4, 4 ),
 ( 2.081470520767878803E-17, 0.004444306975806114161 ),
 .UNSPECIFIED. ) ;
#3659=CARTESIAN_POINT ( 'NONE',  ( 0.1073791018717578927, -11.62916352156179123, 41.52698815987148606 ) ) ;
#3664=CARTESIAN_POINT ( 'NONE',  ( 0.5998501479064708430, 37.84527566984816360, 29.69975237324626605 ) ) ;
#3666=CARTESIAN_POINT ( 'NONE',  ( 4.549368137175248350, -42.06008734272402450, 8.582197505783685898 ) ) ;
#3669=CARTESIAN_POINT ( 'NONE',  ( 0.5998501479064699549, -46.60114184914309021, -11.94461217097453343 ) ) ;
#3677=CONICAL_SURFACE ( 'NONE', #49756, 42.92674063221959813, 1.485477209440487556 ) ;
#3684=EDGE_CURVE ( 'NONE', #1788, #14276, #43549, .T. ) ;
#3689=CARTESIAN_POINT ( 'NONE',  ( 0.8760168074887090262, 48.09529047980637984, -0.8912768426701217495 ) ) ;
#3691=B_SPLINE_CURVE_WITH_KNOTS ( 'NONE', 3,
 ( #6481, #53795, #49125, #35050 ),
 .UNSPECIFIED., .F., .F.,
 ( 4, 4 ),
 ( 6.254634441385501517E-18, 0.004566006591234646368 ),
 .UNSPECIFIED. ) ;
#3695=ORIENTED_EDGE ( 'NONE', *, *, #30939, .F. ) ;
#3699=VERTEX_POINT ( 'NONE', #24807 ) ;
#3707=DIRECTION ( 'NONE',  ( 0.09835009131224567436, -0.9951218349151971232, -0.007732607185427117953 ) ) ;
#3709=CARTESIAN_POINT ( 'NONE',  ( 0.1101816497532063233, -16.37745527993615013, 39.89358705406957029 ) ) ;
#3717=B_SPLINE_CURVE_WITH_KNOTS ( 'NONE', 3,
 ( #20324, #9674, #48818, #39444 ),
 .UNSPECIFIED., .F., .F.,
 ( 4, 4 ),
 ( 0.000000000000000000, 0.004445488388166992516 ),
 .UNSPECIFIED. ) ;
#3721=CARTESIAN_POINT ( 'NONE',  ( 0.8751705887134423323, 47.55935879196461968, 7.160166390004468973 ) ) ;
#3723=CARTESIAN_POINT ( 'NONE',  ( 0.6041374136657476912, 41.57494627055144321, -24.20487816031478800 ) ) ;
#3724=EDGE_CURVE ( 'NONE', #38743, #51844, #8884, .T. ) ;
#3727=CIRCLE ( 'NONE', #12758, 47.91270532121795611 ) ;
#3735=CARTESIAN_POINT ( 'NONE',  ( 0.3622758884714730732, 39.50828911766998175, -17.25816669464953534 ) ) ;
#3737=EDGE_CURVE ( 'NONE', #5739, #7607, #36122, .T. ) ;
#3742=CARTESIAN_POINT ( 'NONE',  ( 0.1081432562775997974, 21.92800090985269890, -37.13343246403903919 ) ) ;
#3749=ORIENTED_EDGE ( 'NONE', *, *, #40211, .T. ) ;
#3755=CARTESIAN_POINT ( 'NONE',  ( -6.015611763856276717, 4.882992715191300626, 18.19956619163659894 ) ) ;
#3759=CARTESIAN_POINT ( 'NONE',  ( 0.000000000000000000, 0.000000000000000000, 0.000000000000000000 ) ) ;
#3761=CARTESIAN_POINT ( 'NONE',  ( 0.3622758884714730732, -25.58609868863794290, 34.70015533914785522 ) ) ;
#3763=CARTESIAN_POINT ( 'NONE',  ( 0.6001305935487315502, -47.76436356026964347, -5.760103278697851437 ) ) ;
#3772=CARTESIAN_POINT ( 'NONE',  ( -2.708315649062910779, -14.47261168455368185, -2.171184472130632148 ) ) ;
#3773=ORIENTED_EDGE ( 'NONE', *, *, #43228, .F. ) ;
#3777=CARTESIAN_POINT ( 'NONE',  ( 0.8751705887134553219, 28.56654290188653178, -38.69254731947804515 ) ) ;
#3784=PLANE ( 'NONE',  #60246 ) ;
#3787=CARTESIAN_POINT ( 'NONE',  ( 4.549368137175248350, 0.000000000000000000, 0.000000000000000000 ) ) ;
#3795=CARTESIAN_POINT ( 'NONE',  ( 4.549368137175248350, -8.166781970325423856, -42.14271863032831078 ) ) ;
#3797=ORIENTED_EDGE ( 'NONE', *, *, #25454, .T. ) ;
#3801=CARTESIAN_POINT ( 'NONE',  ( -5.995132425357893702, -11.47834865841086049, -14.94489030678163033 ) ) ;
#3823=CARTESIAN_POINT ( 'NONE',  ( 0.6001305935487315502, -38.48510059944028683, -28.87057754790923880 ) ) ;
#3825=CARTESIAN_POINT ( 'NONE',  ( -6.016489644550736315, 16.32089497094061059, 9.417787539062304702 ) ) ;
#3827=CARTESIAN_POINT ( 'NONE',  ( 0.6023142530420679819, 46.39979989577480524, -12.70386526143724026 ) ) ;
#3828=CARTESIAN_POINT ( 'NONE',  ( 0.8751705887134423323, 24.81530984069208401, -41.19904111682483716 ) ) ;
#3831=VECTOR ( 'NONE', #33372, 999.9999999999998863 ) ;
#3850=CARTESIAN_POINT ( 'NONE',  ( 0.5988103622719985752, -18.96890139670021469, 44.21009254328972560 ) ) ;
#3853=CARTESIAN_POINT ( 'NONE',  ( 0.1073791018717578927, 0.4849339620933161288, -43.12183934961191056 ) ) ;
#3854=ORIENTED_EDGE ( 'NONE', *, *, #51096, .T. ) ;
#3866=CARTESIAN_POINT ( 'NONE',  ( 0.6001305935487422083, -24.50730504006484978, 41.40054608060251695 ) ) ;
#3867=CARTESIAN_POINT ( 'NONE',  ( 0.3622758884714600280, 40.13994584881781691, -15.73321244754812298 ) ) ;
#3871=CARTESIAN_POINT ( 'NONE',  ( 0.1102847568649952675, 42.74337176234129743, -5.720244683738159530 ) ) ;
#3875=CARTESIAN_POINT ( 'NONE',  ( 0.7954196712028464011, 46.67728755034884358, -11.60747899261471083 ) ) ;
#3878=EDGE_CURVE ( 'NONE', #24212, #18593, #18497, .T. ) ;
#3879=CARTESIAN_POINT ( 'NONE',  ( 0.1073791018717578927, -42.81622261970997556, 5.147744207006151207 ) ) ;
#3887=CARTESIAN_POINT ( 'NONE',  ( 0.5988103622719987973, -46.30780754281423128, -13.03604477829274444 ) ) ;
#3889=CARTESIAN_POINT ( 'NONE',  ( 4.975801465491695552, -40.15204426031515794, -26.14269827151666092 ) ) ;
#3896=CARTESIAN_POINT ( 'NONE',  ( -6.016761891674564211, -14.94721834528423088, 11.47373234755497862 ) ) ;
#3898=CARTESIAN_POINT ( 'NONE',  ( 0.1103744047535531458, 42.75042227379820048, 5.667281528142542157 ) ) ;
#3900=AXIS2_PLACEMENT_3D ( 'NONE', #3222, #37703, #22348 ) ;
#3902=CARTESIAN_POINT ( 'NONE',  ( 0.1064266418746773329, 6.185136754498332223, -42.67882141624139081 ) ) ;
#3908=CARTESIAN_POINT ( 'NONE',  ( 0.1103744047535531458, 39.82693656558409856, 16.53879706351786893 ) ) ;
#3913=CARTESIAN_POINT ( 'NONE',  ( 0.6254311100348628472, -29.82834996731721233, 37.74260849418442376 ) ) ;
#3920=CARTESIAN_POINT ( 'NONE',  ( 0.6023142530420679819, 41.79260242564367189, 23.82662387835881646 ) ) ;
#3928=CARTESIAN_POINT ( 'NONE',  ( 0.6009452777970413218, -47.75105029762388398, -5.846392105360362912 ) ) ;
#3943=CARTESIAN_POINT ( 'NONE',  ( 0.6041374136657475802, 0.1745662470644584741, -48.10739871142803992 ) ) ;
#3955=CARTESIAN_POINT ( 'NONE',  ( -6.016104459813371719, 17.40682403289259028, -7.215917642688879141 ) ) ;
#3956=CARTESIAN_POINT ( 'NONE',  ( 0.1100247026804066219, 26.38690693952957034, -34.10937070541719152 ) ) ;
#3959=CARTESIAN_POINT ( 'NONE',  ( 0.8760168074886960365, 23.27577685234539473, 42.09738177923962610 ) ) ;
#3961=CARTESIAN_POINT ( 'NONE',  ( -5.995132425357893702, 18.68405145320027572, -2.451215106828155577 ) ) ;
#3970=CARTESIAN_POINT ( 'NONE',  ( 4.549368137175248350, 13.59764261105751793, -40.71620287708331176 ) ) ;
#3980=CARTESIAN_POINT ( 'NONE',  ( 0.8751705887134423323, -48.08707113907595243, -0.8911681664086732457 ) ) ;
#3990=CARTESIAN_POINT ( 'NONE',  ( 4.691466044806102964, -14.64802401911257235, 42.11359095667464203 ) ) ;
#3992=CARTESIAN_POINT ( 'NONE',  ( 0.6031357023905874470, 24.09149424676616391, -41.64046004335391871 ) ) ;
#3993=ORIENTED_EDGE ( 'NONE', *, *, #54998, .F. ) ;
#4003=CARTESIAN_POINT ( 'NONE',  ( 0.1101816497532063233, 26.36013219694225640, 34.13008584880301299 ) ) ;
#4004=VERTEX_POINT ( 'NONE', #7853 ) ;
#4009=VERTEX_POINT ( 'NONE', #46100 ) ;
#4015=CARTESIAN_POINT ( 'NONE',  ( 0.6028618097248864549, -33.89350006451850561, 34.14037999462312456 ) ) ;
#4016=CARTESIAN_POINT ( 'NONE',  ( 0.5998501479064699549, 44.64337787626223530, 17.92509395669123862 ) ) ;
#4018=ORIENTED_EDGE ( 'NONE', *, *, #12134, .T. ) ;
#4021=CARTESIAN_POINT ( 'NONE',  ( 4.833616638992205949, -26.07076047129164564, 38.20222678111891668 ) ) ;
#4025=( BOUNDED_SURFACE ( )  B_SPLINE_SURFACE ( 3, 1, ( 
 ( #11605, #34486 ),
 ( #30074, #39828 ),
 ( #20995, #20689 ),
 ( #5932, #34180 ) ),
 .UNSPECIFIED., .F., .F., .F. ) 
 B_SPLINE_SURFACE_WITH_KNOTS ( ( 4, 4 ),
 ( 2, 2 ),
 ( 0.000000000000000000, 1.000000000000000000 ),
 ( 0.000000000000000000, 1.000000000000000000 ),
 .UNSPECIFIED. ) 
 GEOMETRIC_REPRESENTATION_ITEM ( )  RATIONAL_B_SPLINE_SURFACE ( (
 ( 1.000000000000000000, 1.000000000000000000),
 ( 0.9953040768229013402, 0.8617119497784988535),
 ( 0.9953040768229013402, 0.8617119497784988535),
 ( 1.000000000000000000, 1.000000000000000000) ) ) 
 REPRESENTATION_ITEM ( '' )  SURFACE ( )  );
#4028=CARTESIAN_POINT ( 'NONE',  ( 0.1084644655670283786, -33.96951444491441663, 26.56696682928998143 ) ) ;
#4030=ORIENTED_EDGE ( 'NONE', *, *, #20649, .T. ) ;
#4032=CARTESIAN_POINT ( 'NONE',  ( 0.3622758884714600280, -11.95365414648526148, 41.42293301073604539 ) ) ;
#4039=CIRCLE ( 'NONE', #51088, 47.91270532121795611 ) ;
#4048=CARTESIAN_POINT ( 'NONE',  ( 0.8751705887134423323, 44.76769609654235893, -17.57879340691497561 ) ) ;
#4051=EDGE_CURVE ( 'NONE', #41864, #46085, #40442, .T. ) ;
#4059=CARTESIAN_POINT ( 'NONE',  ( -6.010958268070873523, 4.891065400978385824, 18.19761767765831806 ) ) ;
#4064=CARTESIAN_POINT ( 'NONE',  ( 4.975801465491695552, 0.000000000000000000, 0.000000000000000000 ) ) ;
#4067=CARTESIAN_POINT ( 'NONE',  ( 4.833616638992205949, -8.578242093415418879, -45.44786513329594158 ) ) ;
#4071=ORIENTED_EDGE ( 'NONE', *, *, #61372, .T. ) ;
#4074=DIRECTION ( 'NONE',  ( 0.09835009131224567436, -0.9855991218957022015, -0.1375559175655256539 ) ) ;
#4088=EDGE_CURVE ( 'NONE', #21034, #9246, #47198, .T. ) ;
#4090=CARTESIAN_POINT ( 'NONE',  ( 0.7954196712028460681, 29.96539649507085201, -37.62416450255258837 ) ) ;
#4091=ORIENTED_EDGE ( 'NONE', *, *, #35439, .F. ) ;
#4092=CARTESIAN_POINT ( 'NONE',  ( 4.549368137175248350, 0.000000000000000000, 0.000000000000000000 ) ) ;
#4093=EDGE_CURVE ( 'NONE', #13939, #43595, #2132, .T. ) ;
#4095=ORIENTED_EDGE ( 'NONE', *, *, #6123, .T. ) ;
#4109=ADVANCED_FACE ( 'NONE', ( #6831, #16573 ), #6510, .F. ) ;
#4112=EDGE_CURVE ( 'NONE', #21617, #16942, #53162, .T. ) ;
#4113=CARTESIAN_POINT ( 'NONE',  ( 0.6041374136657476912, -29.42442150067172335, -38.05989626241419899 ) ) ;
#4114=LINE ( 'NONE', #56439, #53863 ) ;
#4117=CARTESIAN_POINT ( 'NONE',  ( 0.1064266379913939298, -37.06314005629928232, 22.04679939086769380 ) ) ;
#4119=CARTESIAN_POINT ( 'NONE',  ( 0.1100053167205931326, -21.40663161101019796, 37.43629428538725534 ) ) ;
#4120=CARTESIAN_POINT ( 'NONE',  ( 0.6041374136657476912, 29.42442150067147821, 38.05989626241439794 ) ) ;
#4125=CARTESIAN_POINT ( 'NONE',  ( -6.016761891674564211, 16.32039929810256851, 9.418621820384554866 ) ) ;
#4126=LINE ( 'NONE', #52365, #6213 ) ;
#4129=VERTEX_POINT ( 'NONE', #20964 ) ;
#4133=ORIENTED_EDGE ( 'NONE', *, *, #25324, .F. ) ;
#4135=ORIENTED_EDGE ( 'NONE', *, *, #35118, .T. ) ;
#4138=B_SPLINE_CURVE_WITH_KNOTS ( 'NONE', 3,
 ( #47300, #38778, #18488, #9079 ),
 .UNSPECIFIED., .F., .F.,
 ( 4, 4 ),
 ( 0.000000000000000000, 0.005014147105413699519 ),
 .UNSPECIFIED. ) ;
#4144=CARTESIAN_POINT ( 'NONE',  ( 0.6031357023905875581, -38.13964912630314075, -29.32055886552309332 ) ) ;
#4146=ADVANCED_FACE ( 'NONE', ( #37241 ), #45758, .F. ) ;
#4149=ADVANCED_FACE ( 'NONE', ( #50997 ), #27264, .F. ) ;
#4154=DIRECTION ( 'NONE',  ( 0.1024043820194936311, -0.2701391291102787640, -0.9573600124648750098 ) ) ;
#4157=ADVANCED_FACE ( 'NONE', ( #13124 ), #33679, .F. ) ;
#4159=ORIENTED_EDGE ( 'NONE', *, *, #51197, .F. ) ;
#4162=ORIENTED_EDGE ( 'NONE', *, *, #8999, .T. ) ;
#4164=CARTESIAN_POINT ( 'NONE',  ( 5.880360259849739535, -3.090325311465197178, 47.87242051977160173 ) ) ;
#4166=FACE_OUTER_BOUND ( 'NONE', #41028, .T. ) ;
#4170=VECTOR ( 'NONE', #22264, 1000.000000000000227 ) ;
#4190=CARTESIAN_POINT ( 'NONE',  ( 2.643462169533613793, -4.896978544602504257, 47.78621045426866232 ) ) ;
#4195=CARTESIAN_POINT ( 'NONE',  ( 0.7048096507298579061, 29.95256433478725455, -37.64898672361922394 ) ) ;
#4198=CARTESIAN_POINT ( 'NONE',  ( 4.975801465491695552, 45.18341283946458020, -15.94009207553003016 ) ) ;
#4199=CARTESIAN_POINT ( 'NONE',  ( 0.5980894510889448457, 44.17723055703925183, 19.05812566676522124 ) ) ;
#4204=CARTESIAN_POINT ( 'NONE',  ( 0.8751705887134423323, 42.09020928323375443, -23.27176129838382224 ) ) ;
#4209=CARTESIAN_POINT ( 'NONE',  ( 5.880360259849752858, 36.09847387447859290, -31.59460303415945148 ) ) ;
#4211=ORIENTED_EDGE ( 'NONE', *, *, #15130, .T. ) ;
#4214=CARTESIAN_POINT ( 'NONE',  ( 0.6023142530420679819, -44.54505940664473940, -18.16775455049929988 ) ) ;
#4215=CIRCLE ( 'NONE', #13240, 42.92674063221959813 ) ;
#4216=EDGE_CURVE ( 'NONE', #28210, #16902, #1561, .T. ) ;
#4218=B_SPLINE_CURVE_WITH_KNOTS ( 'NONE', 3,
 ( #38322, #28276, #18282, #14206, #22981, #19212, #56466, #13582, #4144, #32686, #27978, #47100, #23282, #52380, #33308, #42408 ),
 .UNSPECIFIED., .F., .F.,
 ( 4, 3, 3, 3, 3, 4 ),
 ( 1.962735358247463844E-17, 0.0002618515315864410552, 0.0003927756766341956060, 0.0005236998216950555047, 0.0007855159896329858872, 0.001047349442285930472 ),
 .UNSPECIFIED. ) ;
#4226=EDGE_CURVE ( 'NONE', #21310, #593, #21781, .T. ) ;
#4229=CARTESIAN_POINT ( 'NONE',  ( 0.1313383488274116884, 10.54394128763557781, -41.81465294768275243 ) ) ;
#4234=FACE_OUTER_BOUND ( 'NONE', #18941, .T. ) ;
#4245=CARTESIAN_POINT ( 'NONE',  ( 4.975801465491695552, -39.51822597168514051, 27.09127437476313816 ) ) ;
#4247=ORIENTED_EDGE ( 'NONE', *, *, #59597, .T. ) ;
#4248=CARTESIAN_POINT ( 'NONE',  ( 0.6001305935487422083, -46.60388846085731274, 11.94532529598298964 ) ) ;
#4250=FACE_OUTER_BOUND ( 'NONE', #32382, .T. ) ;
#4257=CARTESIAN_POINT ( 'NONE',  ( 0.3622758884714730732, 37.74294673546557988, 20.83792692158985460 ) ) ;
#4259=CARTESIAN_POINT ( 'NONE',  ( 0.1064266379913938326, 26.69589650908239165, 33.86837498006634206 ) ) ;
#4260=CARTESIAN_POINT ( 'NONE',  ( 0.6009452777970413218, 47.63713033690753917, -6.711700115493053787 ) ) ;
#4265=CARTESIAN_POINT ( 'NONE',  ( 4.691466044806103852, 37.25818859570272679, 24.49380602310827371 ) ) ;
#4269=CARTESIAN_POINT ( 'NONE',  ( 4.691466044806103852, 42.32811009116535672, 14.01607102724557841 ) ) ;
#4278=CARTESIAN_POINT ( 'NONE',  ( -5.995132425357893702, 18.19985213254578937, -4.885449473615140370 ) ) ;
#4280=CARTESIAN_POINT ( 'NONE',  ( 0.1103310638050662151, -5.710544932889240144, 42.74468893497607525 ) ) ;
#4281=EDGE_LOOP ( 'NONE', ( #39821, #12005, #60026, #17707 ) ) ;
#4284=LINE ( 'NONE', #51599, #32496 ) ;
#4285=CARTESIAN_POINT ( 'NONE',  ( 2.301430502907646947, -11.18388433759685441, -46.71331171933228887 ) ) ;
#4290=CARTESIAN_POINT ( 'NONE',  ( 0.3622758884714600280, -11.95365414648526148, 41.42293301073604539 ) ) ;
#4301=B_SPLINE_CURVE_WITH_KNOTS ( 'NONE', 3,
 ( #648, #10384, #28857, #19175, #10070, #48582 ),
 .UNSPECIFIED., .F., .F.,
 ( 4, 2, 4 ),
 ( 1.870559545977334001E-17, 0.0002293319059085093307, 0.0004586638118169999588 ),
 .UNSPECIFIED. ) ;
#4302=CARTESIAN_POINT ( 'NONE',  ( -6.016761891674565099, 17.41015286184812894, -7.207804629151121745 ) ) ;
#4305=CARTESIAN_POINT ( 'NONE',  ( 0.3622758884714730732, 42.84426538328725798, 4.808133778522027058 ) ) ;
#4306=CARTESIAN_POINT ( 'NONE',  ( 0.1098349054025746230, 26.08296594991493933, 34.34238705454311713 ) ) ;
#4311=VERTEX_POINT ( 'NONE', #25577 ) ;
#4312=CARTESIAN_POINT ( 'NONE',  ( 3.680974057930772592, 32.59081219553981867, 35.20670187740670798 ) ) ;
#4313=VERTEX_POINT ( 'NONE', #26816 ) ;
#4316=VERTEX_POINT ( 'NONE', #54992 ) ;
#4318=CARTESIAN_POINT ( 'NONE',  ( 0.5998501479064699549, -33.64490850298868452, 34.38546660123239462 ) ) ;
#4322=CARTESIAN_POINT ( 'NONE',  ( -6.010958268070873523, -7.197664668556314815, -17.41463273278786161 ) ) ;
#4326=ORIENTED_EDGE ( 'NONE', *, *, #19124, .T. ) ;
#4327=CARTESIAN_POINT ( 'NONE',  ( 0.6001305935487315502, 5.760103278697374485, 47.76436356026970032 ) ) ;
#4328=B_SPLINE_CURVE_WITH_KNOTS ( 'NONE', 3,
 ( #48007, #28884, #29809, #39868 ),
 .UNSPECIFIED., .F., .F.,
 ( 4, 4 ),
 ( 0.000000000000000000, 0.005014147105413702121 ),
 .UNSPECIFIED. ) ;
#4331=EDGE_CURVE ( 'NONE', #52228, #58926, #44223, .T. ) ;
#4339=AXIS2_PLACEMENT_3D ( 'NONE', #29402, #24400, #52273 ) ;
#4342=ORIENTED_EDGE ( 'NONE', *, *, #3878, .T. ) ;
#4351=EDGE_CURVE ( 'NONE', #52459, #58767, #50947, .T. ) ;
#4367=FACE_OUTER_BOUND ( 'NONE', #47776, .T. ) ;
#4374=CARTESIAN_POINT ( 'NONE',  ( 4.322998006666165516, -43.48102276965688873, -20.30542865297633881 ) ) ;
#4377=ADVANCED_FACE ( 'NONE', ( #16493 ), #40106, .F. ) ;
#4388=VERTEX_POINT ( 'NONE', #35622 ) ;
#4393=ORIENTED_EDGE ( 'NONE', *, *, #49227, .T. ) ;
#4402=CARTESIAN_POINT ( 'NONE',  ( 4.549368137175248350, -40.58005590356700765, 13.99871866169291579 ) ) ;
#4411=CARTESIAN_POINT ( 'NONE',  ( -6.016104459813374383, -16.32137543786089040, 9.416989654584247305 ) ) ;
#4412=CARTESIAN_POINT ( 'NONE',  ( -6.017396004339686577, 11.47192209077586789, 14.94857180791997209 ) ) ;
#4413=EDGE_CURVE ( 'NONE', #19627, #4009, #29196, .T. ) ;
#4414=CARTESIAN_POINT ( 'NONE',  ( 0.5980894510889457338, 6.974827154143460994, 47.60453381548694551 ) ) ;
#4416=LINE ( 'NONE', #8845, #31422 ) ;
#4423=CARTESIAN_POINT ( 'NONE',  ( -6.016104459813371719, 16.32137543786083000, 9.416989654584362768 ) ) ;
#4424=ADVANCED_FACE ( 'NONE', ( #8943 ), #31285, .F. ) ;
#4426=CARTESIAN_POINT ( 'NONE',  ( 4.975801465491695552, 26.14269827151680659, -40.15204426031507268 ) ) ;
#4431=CARTESIAN_POINT ( 'NONE',  ( 0.8751705887134423323, -33.37254303619531726, -34.63284514348573850 ) ) ;
#4432=EDGE_CURVE ( 'NONE', #31934, #41987, #29980, .T. ) ;
#4437=B_SPLINE_CURVE_WITH_KNOTS ( 'NONE', 3,
 ( #56026, #3394, #32243, #17521 ),
 .UNSPECIFIED., .F., .F.,
 ( 4, 4 ),
 ( 2.071251839531113129E-17, 0.004444306975806115029 ),
 .UNSPECIFIED. ) ;
#4438=EDGE_CURVE ( 'NONE', #52417, #21984, #50181, .T. ) ;
#4442=VERTEX_POINT ( 'NONE', #37165 ) ;
#4447=FACE_OUTER_BOUND ( 'NONE', #48206, .T. ) ;
#4452=CARTESIAN_POINT ( 'NONE',  ( 0.1092355843206037486, -30.28032287551058488, -30.70542469027314070 ) ) ;
#4455=( BOUNDED_SURFACE ( )  B_SPLINE_SURFACE ( 3, 1, ( 
 ( #43940, #18557 ),
 ( #61746, #33592 ),
 ( #4726, #52359 ),
 ( #14183, #9452 ) ),
 .UNSPECIFIED., .F., .F., .F. ) 
 B_SPLINE_SURFACE_WITH_KNOTS ( ( 4, 4 ),
 ( 2, 2 ),
 ( 0.000000000000000000, 1.000000000000000000 ),
 ( 0.000000000000000000, 1.000000000000000000 ),
 .UNSPECIFIED. ) 
 GEOMETRIC_REPRESENTATION_ITEM ( )  RATIONAL_B_SPLINE_SURFACE ( (
 ( 1.000000000000000000, 1.000000000000000000),
 ( 0.7223157951917480446, 0.9931996967497186413),
 ( 0.7223157951917480446, 0.9931996967497186413),
 ( 1.000000000000000000, 1.000000000000000000) ) ) 
 REPRESENTATION_ITEM ( '' )  SURFACE ( )  );
#4461=VERTEX_POINT ( 'NONE', #37793 ) ;
#4465=CARTESIAN_POINT ( 'NONE',  ( 0.1103310638050661874, 5.547176740492965052, 42.76619676553138305 ) ) ;
#4466=CARTESIAN_POINT ( 'NONE',  ( 5.880360259849752858, -9.312491912827802309, -47.05949693022704849 ) ) ;
#4469=FACE_OUTER_BOUND ( 'NONE', #58234, .T. ) ;
#4473=ORIENTED_EDGE ( 'NONE', *, *, #38138, .T. ) ;
#4475=CARTESIAN_POINT ( 'NONE',  ( 0.5980894510889448457, -46.65000524237095192, 11.77356634613236963 ) ) ;
#4481=CARTESIAN_POINT ( 'NONE',  ( 0.1100247026804066219, -42.77732815928603571, 5.460606496326182224 ) ) ;
#4482=EDGE_CURVE ( 'NONE', #45673, #59272, #23066, .T. ) ;
#4486=B_SPLINE_CURVE_WITH_KNOTS ( 'NONE', 3,
 ( #49126, #20028, #42913, #19100, #38214, #57260, #14396, #58198, #15321, #33504, #40076, #44463, #35051, #55348, #16865, #7421, #41001, #30622, #1490 ),
 .UNSPECIFIED., .F., .F.,
 ( 4, 3, 3, 3, 3, 3, 4 ),
 ( 1.153344816771540786E-16, 0.0002618519381806260794, 0.0003927759815485984689, 0.0005237000248299445142, 0.0006546240681324982588, 0.0007855481115631334681, 0.0009699050456655117008 ),
 .UNSPECIFIED. ) ;
#4499=ADVANCED_FACE ( 'NONE', ( #57445 ), #46484, .F. ) ;
#4511=CARTESIAN_POINT ( 'NONE',  ( 0.6001305935487422083, -11.94532529598347814, -46.60388846085719194 ) ) ;
#4516=CARTESIAN_POINT ( 'NONE',  ( 0.1100053167205930771, 39.91014771056754995, 16.33707796615720653 ) ) ;
#4517=CARTESIAN_POINT ( 'NONE',  ( -6.010958268070873523, -14.95835081545482304, 11.45964880703821187 ) ) ;
#4521=CARTESIAN_POINT ( 'NONE',  ( 0.1092565886968785288, 5.321013289171662386, -42.79503959566648064 ) ) ;
#4522=EDGE_LOOP ( 'NONE', ( #13999, #53612, #5981, #56012 ) ) ;
#4537=LINE ( 'NONE', #18998, #57830 ) ;
#4538=CARTESIAN_POINT ( 'NONE',  ( -6.015611763856276717, 13.31979030221817695, -13.32857883366819429 ) ) ;
#4543=CARTESIAN_POINT ( 'NONE',  ( 0.7246131072078556556, -7.091231226025147549, 47.57651137777902051 ) ) ;
#4544=VERTEX_POINT ( 'NONE', #50537 ) ;
#4560=EDGE_CURVE ( 'NONE', #1315, #37210, #36783, .T. ) ;
#4562=CARTESIAN_POINT ( 'NONE',  ( 0.3622758884714730732, -20.83792692158999316, 37.74294673546550172 ) ) ;
#4566=CARTESIAN_POINT ( 'NONE',  ( 0.1073791018717483448, 16.05399293000815675, -40.02496097243042072 ) ) ;
#4576=CARTESIAN_POINT ( 'NONE',  ( -6.001507490154111224, -11.48377994779711386, 14.94036486426009525 ) ) ;
#4578=CARTESIAN_POINT ( 'NONE',  ( 0.6041374136657475802, 38.05989626241390766, 29.42442150067210349 ) ) ;
#4581=CARTESIAN_POINT ( 'NONE',  ( -6.015611763856276717, 4.882992715191555533, -18.19956619163653500 ) ) ;
#4582=CARTESIAN_POINT ( 'NONE',  ( 0.6023143664670691511, 47.66103278671581478, 6.538774821499355738 ) ) ;
#4586=CARTESIAN_POINT ( 'NONE',  ( -6.015611763856276717, 0.006214430185405465240, -18.84324252354755203 ) ) ;
#4601=EDGE_CURVE ( 'NONE', #40739, #47659, #33783, .T. ) ;
#4608=VECTOR ( 'NONE', #1950, 1000.000000000000000 ) ;
#4628=B_SPLINE_CURVE_WITH_KNOTS ( 'NONE', 3,
 ( #40861, #41470, #12650, #7600 ),
 .UNSPECIFIED., .F., .F.,
 ( 4, 4 ),
 ( 0.000000000000000000, 0.005014147105413710795 ),
 .UNSPECIFIED. ) ;
#4630=( BOUNDED_SURFACE ( )  B_SPLINE_SURFACE ( 3, 1, ( 
 ( #13170, #56357 ),
 ( #56976, #32270 ),
 ( #31647, #50738 ),
 ( #51661, #60432 ) ),
 .UNSPECIFIED., .F., .F., .F. ) 
 B_SPLINE_SURFACE_WITH_KNOTS ( ( 4, 4 ),
 ( 2, 2 ),
 ( 0.000000000000000000, 1.000000000000000000 ),
 ( 0.000000000000000000, 1.000000000000000000 ),
 .UNSPECIFIED. ) 
 GEOMETRIC_REPRESENTATION_ITEM ( )  RATIONAL_B_SPLINE_SURFACE ( (
 ( 1.000000000000000000, 1.000000000000000000),
 ( 0.7223157951917476005, 0.9931996967497186413),
 ( 0.7223157951917476005, 0.9931996967497186413),
 ( 1.000000000000000000, 1.000000000000000000) ) ) 
 REPRESENTATION_ITEM ( '' )  SURFACE ( )  );
#4632=CARTESIAN_POINT ( 'NONE',  ( 0.1098349054025746230, -21.37724154645476204, -37.45309339978476970 ) ) ;
#4635=CARTESIAN_POINT ( 'NONE',  ( 0.3622758884714600280, -42.62881903538205108, -6.444611261694439541 ) ) ;
#4637=ORIENTED_EDGE ( 'NONE', *, *, #31836, .T. ) ;
#4645=CARTESIAN_POINT ( 'NONE',  ( 0.6031356755852232965, 4.336951783013129340E-16, 48.10744332413860747 ) ) ;
#4648=CARTESIAN_POINT ( 'NONE',  ( 4.549368137175248350, 0.000000000000000000, 0.000000000000000000 ) ) ;
#4654=VECTOR ( 'NONE', #43590, 1000.000000000000000 ) ;
#4657=LINE ( 'NONE', #28485, #50169 ) ;
#4659=CARTESIAN_POINT ( 'NONE',  ( -6.015611763856276717, 14.95313250337445332, -11.46610900684707701 ) ) ;
#4662=CARTESIAN_POINT ( 'NONE',  ( 0.1092565886968784733, 37.50119754628579472, 21.29292791075599567 ) ) ;
#4664=CARTESIAN_POINT ( 'NONE',  ( 3.680882792899935918, 39.15943299201950367, 27.71664061799161871 ) ) ;
#4665=CARTESIAN_POINT ( 'NONE',  ( 0.5980894510889457338, -41.31170365136905787, 24.66136644716748449 ) ) ;
#4672=CARTESIAN_POINT ( 'NONE',  ( 0.3622758884714600280, 36.91764744403290166, 22.26738722580180507 ) ) ;
#4678=ORIENTED_EDGE ( 'NONE', *, *, #51528, .F. ) ;
#4681=CARTESIAN_POINT ( 'NONE',  ( 0.5988103564986356764, 33.58571500783059349, -34.44345003622217405 ) ) ;
#4682=VERTEX_POINT ( 'NONE', #17653 ) ;
#4684=DIRECTION ( 'NONE',  ( -1.000000000000000000, 0.000000000000000000, 0.000000000000000000 ) ) ;
#4695=B_SPLINE_CURVE_WITH_KNOTS ( 'NONE', 3,
 ( #35484, #1306, #24837, #34549 ),
 .UNSPECIFIED., .F., .F.,
 ( 4, 4 ),
 ( 4.670885906470169154E-18, 0.004566006591234645501 ),
 .UNSPECIFIED. ) ;
#4696=CARTESIAN_POINT ( 'NONE',  ( 0.5988103622719990193, 5.677495780220407795, 47.77151394449999344 ) ) ;
#4697=AXIS2_PLACEMENT_3D ( 'NONE', #59102, #58786, #14995 ) ;
#4699=VERTEX_POINT ( 'NONE', #51448 ) ;
#4700=CARTESIAN_POINT ( 'NONE',  ( 0.09136607875274982415, 12.80000000000000071, 0.000000000000000000 ) ) ;
#4701=CARTESIAN_POINT ( 'NONE',  ( -6.010958268070873523, 16.31164801516955620, -9.434296419346035023 ) ) ;
#4713=CARTESIAN_POINT ( 'NONE',  ( 3.238741278300275805, -40.38334873621894161, 14.74792908357233401 ) ) ;
#4718=EDGE_CURVE ( 'NONE', #22109, #42733, #33093, .T. ) ;
#4725=CARTESIAN_POINT ( 'NONE',  ( 4.549368137175248350, -32.41327393324121431, -28.14399996863486209 ) ) ;
#4726=CARTESIAN_POINT ( 'NONE',  ( -6.001507490154110336, -16.31148204059953954, 9.435425682280760284 ) ) ;
#4734=CARTESIAN_POINT ( 'NONE',  ( 2.643462169533600914, 47.78621045426875469, -4.896978544601653383 ) ) ;
#4737=CARTESIAN_POINT ( 'NONE',  ( 3.238741278300274029, -1.828728677532126312, 42.95313747363660895 ) ) ;
#4745=ORIENTED_EDGE ( 'NONE', *, *, #37228, .T. ) ;
#4747=( BOUNDED_SURFACE ( )  B_SPLINE_SURFACE ( 3, 1, ( 
 ( #38068, #18947 ),
 ( #47749, #13944 ),
 ( #23938, #53346 ),
 ( #43062, #29548 ) ),
 .UNSPECIFIED., .F., .F., .F. ) 
 B_SPLINE_SURFACE_WITH_KNOTS ( ( 4, 4 ),
 ( 2, 2 ),
 ( 0.000000000000000000, 1.000000000000000000 ),
 ( 0.000000000000000000, 1.000000000000000000 ),
 .UNSPECIFIED. ) 
 GEOMETRIC_REPRESENTATION_ITEM ( )  RATIONAL_B_SPLINE_SURFACE ( (
 ( 1.000000000000000000, 1.000000000000000000),
 ( 0.9751682680413298332, 0.9999560080971552356),
 ( 0.9751682680413298332, 0.9999560080971552356),
 ( 1.000000000000000000, 1.000000000000000000) ) ) 
 REPRESENTATION_ITEM ( '' )  SURFACE ( )  );
#4751=CARTESIAN_POINT ( 'NONE',  ( 0.8760168074886965917, 24.81951362746078615, -41.20610493656884188 ) ) ;
#4764=CARTESIAN_POINT ( 'NONE',  ( 0.1073791018717483448, 0.4849339620927342054, 43.12183934961191767 ) ) ;
#4765=B_SPLINE_CURVE_WITH_KNOTS ( 'NONE', 3,
 ( #48497, #38207, #15316, #57255 ),
 .UNSPECIFIED., .F., .F.,
 ( 4, 4 ),
 ( 2.100108283942811974E-17, 0.004444306975806115896 ),
 .UNSPECIFIED. ) ;
#4776=CARTESIAN_POINT ( 'NONE',  ( 0.1103744047535531458, 5.590449877750019780, 42.76053735246613741 ) ) ;
#4792=CARTESIAN_POINT ( 'NONE',  ( -6.016761891674564211, 13.32172022638610365, -13.32657647165341253 ) ) ;
#4801=CARTESIAN_POINT ( 'NONE',  ( 0.3622758884714730732, -17.25816669464967035, -39.50828911766992491 ) ) ;
#4813=CARTESIAN_POINT ( 'NONE',  ( 0.6029303876144825880, -24.16699908817990661, 41.59667219751840861 ) ) ;
#4814=CARTESIAN_POINT ( 'NONE',  ( 0.1101816497532063371, 42.77304337559935732, 5.494186916735864123 ) ) ;
#4816=LINE ( 'NONE', #43083, #3831 ) ;
#4824=B_SPLINE_CURVE_WITH_KNOTS ( 'NONE', 3,
 ( #44811, #6522, #25667, #7784 ),
 .UNSPECIFIED., .F., .F.,
 ( 4, 4 ),
 ( 2.380212715961138075E-17, 0.004564976165746188579 ),
 .UNSPECIFIED. ) ;
#4825=CARTESIAN_POINT ( 'NONE',  ( 0.1095718737110177587, 39.74279513315650547, 16.74012863188518807 ) ) ;
#4826=CARTESIAN_POINT ( 'NONE',  ( 4.975801465491694664, 40.15204426031534268, -26.14269827151636605 ) ) ;
#4828=CARTESIAN_POINT ( 'NONE',  ( 4.833616638992205949, 35.06988470649569223, -30.15290813935864733 ) ) ;
#4830=CARTESIAN_POINT ( 'NONE',  ( 0.8760168074887076939, -44.77533136581870110, -17.58183840866384884 ) ) ;
#4832=( BOUNDED_SURFACE ( )  B_SPLINE_SURFACE ( 3, 1, ( 
 ( #41612, #60680 ),
 ( #17797, #25955 ),
 ( #41311, #17485 ),
 ( #2123, #31271 ) ),
 .UNSPECIFIED., .F., .F., .F. ) 
 B_SPLINE_SURFACE_WITH_KNOTS ( ( 4, 4 ),
 ( 2, 2 ),
 ( 0.000000000000000000, 1.000000000000000000 ),
 ( 0.000000000000000000, 1.000000000000000000 ),
 .UNSPECIFIED. ) 
 GEOMETRIC_REPRESENTATION_ITEM ( )  RATIONAL_B_SPLINE_SURFACE ( (
 ( 1.000000000000000000, 1.000000000000000000),
 ( 0.9751682680413298332, 0.9999560080971552356),
 ( 0.9751682680413298332, 0.9999560080971552356),
 ( 1.000000000000000000, 1.000000000000000000) ) ) 
 REPRESENTATION_ITEM ( '' )  SURFACE ( )  );
#4833=EDGE_LOOP ( 'NONE', ( #10139, #3603, #36909, #8122 ) ) ;
#4835=CARTESIAN_POINT ( 'NONE',  ( 3.238741278300273585, 36.28414388564863913, 23.06029422819016972 ) ) ;
#4842=FACE_OUTER_BOUND ( 'NONE', #42035, .T. ) ;
#4844=CARTESIAN_POINT ( 'NONE',  ( 0.6001305935487315502, 18.89378601236001387, 44.24520387813834787 ) ) ;
#4854=CARTESIAN_POINT ( 'NONE',  ( 2.301430502907645170, 17.18551536142187786, 44.85388302506913050 ) ) ;
#4856=CARTESIAN_POINT ( 'NONE',  ( 0.8760168074886965917, -23.27577685234568605, -42.09738177923946978 ) ) ;
#4857=CARTESIAN_POINT ( 'NONE',  ( 4.549368137175248350, 0.000000000000000000, 0.000000000000000000 ) ) ;
#4860=CARTESIAN_POINT ( 'NONE',  ( 0.8760168074887076939, 28.57146030081979760, -38.69913431881793997 ) ) ;
#4862=CARTESIAN_POINT ( 'NONE',  ( 0.1102144999581332746, -37.28370465375341780, -21.67128446981366707 ) ) ;
#4867=CARTESIAN_POINT ( 'NONE',  ( 0.6041374136657475802, -46.51335992032627331, 12.28249295041966782 ) ) ;
#4880=B_SPLINE_CURVE_WITH_KNOTS ( 'NONE', 3,
 ( #30902, #15896, #44123, #1152, #6445, #21201, #54689, #20288, #59396, #49090, #35316, #50016, #30281 ),
 .UNSPECIFIED., .F., .F.,
 ( 4, 3, 3, 3, 4 ),
 ( 0.0004849530346204834448, 0.0005237000248299427795, 0.0006546240681324977167, 0.0007855481115631319502, 0.0009699050456655105082 ),
 .UNSPECIFIED. ) ;
#4887=AXIS2_PLACEMENT_3D ( 'NONE', #34819, #1263, #29472 ) ;
#4888=CARTESIAN_POINT ( 'NONE',  ( 4.549368137175248350, 32.13400537129885493, 28.46244473166684941 ) ) ;
#4890=CARTESIAN_POINT ( 'NONE',  ( 1.827119703190779765, 4.394694966566483174, -42.82501615430326325 ) ) ;
#4891=DIRECTION ( 'NONE',  ( -0.1024043820194934645, 0.5950744814819184381, 0.7971196296869318410 ) ) ;
#4899=EDGE_CURVE ( 'NONE', #58253, #61214, #33657, .T. ) ;
#4900=CARTESIAN_POINT ( 'NONE',  ( 4.975801465491695552, 0.000000000000000000, 0.000000000000000000 ) ) ;
#4910=CARTESIAN_POINT ( 'NONE',  ( 0.1073791018717483448, 16.95003405440257893, 39.65380858626220828 ) ) ;
#4912=ORIENTED_EDGE ( 'NONE', *, *, #5318, .T. ) ;
#4918=EDGE_CURVE ( 'NONE', #27859, #32871, #61249, .T. ) ;
#4923=CIRCLE ( 'NONE', #56938, 42.92674063221959813 ) ;
#4931=VECTOR ( 'NONE', #6371, 1000.000000000000227 ) ;
#4946=CARTESIAN_POINT ( 'NONE',  ( 3.238931869106854489, 38.11291514434414296, 19.89273896137497033 ) ) ;
#4963=CARTESIAN_POINT ( 'NONE',  ( 0.6025881611877910160, 12.24025891548858347, 46.52425620537273687 ) ) ;
#4968=CARTESIAN_POINT ( 'NONE',  ( -2.708315649062910779, -5.356004933109375088, -13.61924161399631394 ) ) ;
#4984=VERTEX_POINT ( 'NONE', #37950 ) ;
#4989=CARTESIAN_POINT ( 'NONE',  ( 2.301529144917015657, 33.04216096093403365, -34.86298839095296387 ) ) ;
#4991=CARTESIAN_POINT ( 'NONE',  ( 0.5980894510889457338, 47.78766676462068119, 5.583794302585419977 ) ) ;
#4992=EDGE_CURVE ( 'NONE', #40811, #28532, #55252, .T. ) ;
#5000=ORIENTED_EDGE ( 'NONE', *, *, #30602, .T. ) ;
#5002=CARTESIAN_POINT ( 'NONE',  ( 50.00005079999999680, 12.80000000000000071, -3.000000000000000000 ) ) ;
#5004=CARTESIAN_POINT ( 'NONE',  ( 0.1073791018717483448, -37.10214135362904386, 21.98088480513601795 ) ) ;
#5010=ORIENTED_EDGE ( 'NONE', *, *, #1530, .T. ) ;
#5022=ORIENTED_EDGE ( 'NONE', *, *, #23207, .T. ) ;
#5031=CARTESIAN_POINT ( 'NONE',  ( 0.7246131072078558777, 13.24054562911126176, -46.24389631750676699 ) ) ;
#5034=CARTESIAN_POINT ( 'NONE',  ( 0.6001305935487315502, 47.62765676940934867, 6.798494447612393188 ) ) ;
#5035=FACE_OUTER_BOUND ( 'NONE', #16510, .T. ) ;
#5044=CARTESIAN_POINT ( 'NONE',  ( 0.2224561200757632085, -22.21411683958078243, 36.95704201588751658 ) ) ;
#5045=CARTESIAN_POINT ( 'NONE',  ( 0.6017666602106489515, 48.10631669010027878, -0.3491145841133775907 ) ) ;
#5046=CARTESIAN_POINT ( 'NONE',  ( 0.1095718737110179114, -21.78439022773181932, 37.21776476380618703 ) ) ;
#5056=CARTESIAN_POINT ( 'NONE',  ( -6.016489644550736315, 9.417787539062475233, -16.32089497094051467 ) ) ;
#5066=ORIENTED_EDGE ( 'NONE', *, *, #2082, .T. ) ;
#5072=ORIENTED_EDGE ( 'NONE', *, *, #58755, .F. ) ;
#5073=CARTESIAN_POINT ( 'NONE',  ( -2.708315649062910779, 1.648584381066855897, 14.54141329178162678 ) ) ;
#5076=EDGE_LOOP ( 'NONE', ( #54357, #40370, #27279, #42837 ) ) ;
#5077=CARTESIAN_POINT ( 'NONE',  ( 0.6254087463353942278, -44.70339519268203787, -17.77193046492936546 ) ) ;
#5079=EDGE_LOOP ( 'NONE', ( #60052, #47870, #27152, #38634 ) ) ;
#5087=CARTESIAN_POINT ( 'NONE',  ( 4.975801465491694664, 20.67815041659077835, 43.22084481528228395 ) ) ;
#5089=B_SPLINE_CURVE_WITH_KNOTS ( 'NONE', 3,
 ( #36926, #13411, #32516, #49285, #44318, #20484 ),
 .UNSPECIFIED., .F., .F.,
 ( 4, 2, 4 ),
 ( 1.283058336952897540E-16, 0.0002450741128632361911, 0.0004901482257263440126 ),
 .UNSPECIFIED. ) ;
#5090=VERTEX_POINT ( 'NONE', #11578 ) ;
#5091=CARTESIAN_POINT ( 'NONE',  ( 0.6029303876144825880, -12.57751758557302146, 46.43417959025969566 ) ) ;
#5105=CARTESIAN_POINT ( 'NONE',  ( -6.016489644550737204, 9.417787539062247859, 16.32089497094064967 ) ) ;
#5107=B_SPLINE_CURVE_WITH_KNOTS ( 'NONE', 3,
 ( #21751, #59639, #47335, #26441 ),
 .UNSPECIFIED., .F., .F.,
 ( 4, 4 ),
 ( 2.302551629917873038E-17, 0.004564976165746188579 ),
 .UNSPECIFIED. ) ;
#5114=CARTESIAN_POINT ( 'NONE',  ( -6.001507490154111224, -13.33564355450117844, 13.31361390284155277 ) ) ;
#5115=CARTESIAN_POINT ( 'NONE',  ( -6.016761891674564211, 17.41015286184802946, 7.207804629151374876 ) ) ;
#5116=ORIENTED_EDGE ( 'NONE', *, *, #43146, .F. ) ;
#5117=CARTESIAN_POINT ( 'NONE',  ( 0.7048096507298579061, 23.32077812596822852, 42.08020459959988813 ) ) ;
#5119=CARTESIAN_POINT ( 'NONE',  ( 4.691466044806102076, -39.84135254923121749, -20.01963481131645750 ) ) ;
#5121=CARTESIAN_POINT ( 'NONE',  ( 0.8751705887134553219, -46.67919521768879321, -11.58504748649183647 ) ) ;
#5123=EDGE_CURVE ( 'NONE', #19546, #50188, #43880, .T. ) ;
#5124=CARTESIAN_POINT ( 'NONE',  ( 4.549368137175248350, 0.000000000000000000, 0.000000000000000000 ) ) ;
#5127=( BOUNDED_SURFACE ( )  B_SPLINE_SURFACE ( 3, 1, ( 
 ( #28039, #51823 ),
 ( #23953, #4199 ),
 ( #18646, #23642 ),
 ( #14569, #38383 ) ),
 .UNSPECIFIED., .F., .F., .F. ) 
 B_SPLINE_SURFACE_WITH_KNOTS ( ( 4, 4 ),
 ( 2, 2 ),
 ( 0.000000000000000000, 1.000000000000000000 ),
 ( 0.000000000000000000, 1.000000000000000000 ),
 .UNSPECIFIED. ) 
 GEOMETRIC_REPRESENTATION_ITEM ( )  RATIONAL_B_SPLINE_SURFACE ( (
 ( 1.000000000000000000, 1.000000000000000000),
 ( 0.9953040768229013402, 0.8617119497784988535),
 ( 0.9953040768229013402, 0.8617119497784988535),
 ( 1.000000000000000000, 1.000000000000000000) ) ) 
 REPRESENTATION_ITEM ( '' )  SURFACE ( )  );
#5131=CARTESIAN_POINT ( 'NONE',  ( 1.827326673878743035, 42.50320212329570779, 6.839036141888717779 ) ) ;
#5133=ORIENTED_EDGE ( 'NONE', *, *, #18827, .T. ) ;
#5136=CARTESIAN_POINT ( 'NONE',  ( 0.1104177457020373149, -43.12445244485484608, 0.004894317366673364873 ) ) ;
#5137=CARTESIAN_POINT ( 'NONE',  ( 0.1073791018717483448, 40.02496097243036388, 16.05399293000829175 ) ) ;
#5145=CARTESIAN_POINT ( 'NONE',  ( -6.010958268070873523, 11.45964880703848543, -14.95835081545462053 ) ) ;
#5151=VECTOR ( 'NONE', #58495, 1000.000000000000114 ) ;
#5154=B_SPLINE_CURVE_WITH_KNOTS ( 'NONE', 3,
 ( #30183, #48992, #44323, #6045, #1353, #20488 ),
 .UNSPECIFIED., .F., .F.,
 ( 4, 2, 4 ),
 ( 1.271806119729192492E-16, 0.0002450741128632357032, 0.0004901482257263442294 ),
 .UNSPECIFIED. ) ;
#5158=ORIENTED_EDGE ( 'NONE', *, *, #4351, .F. ) ;
#5159=CARTESIAN_POINT ( 'NONE',  ( 4.975801465491695552, -47.76942479135487929, 3.702618843596635401 ) ) ;
#5164=CARTESIAN_POINT ( 'NONE',  ( 0.6001305935487315502, -23.60027211631799915, -41.92422178329161397 ) ) ;
#5168=VERTEX_POINT ( 'NONE', #59470 ) ;
#5180=CARTESIAN_POINT ( 'NONE',  ( 0.5998501479064699549, -47.62484632993692912, 6.798102206413326520 ) ) ;
#5182=B_SPLINE_CURVE_WITH_KNOTS ( 'NONE', 3,
 ( #19776, #29770, #36355, #21929, #46066, #2491 ),
 .UNSPECIFIED., .F., .F.,
 ( 4, 2, 4 ),
 ( 1.764953265579307567E-18, 0.0002450742804987332546, 0.0004901485609974646660 ),
 .UNSPECIFIED. ) ;
#5186=DIRECTION ( 'NONE',  ( 0.000000000000000000, 0.000000000000000000, -1.000000000000000000 ) ) ;
#5187=CARTESIAN_POINT ( 'NONE',  ( 0.1064266418746773885, 10.61815661559940338, 41.79703894102875239 ) ) ;
#5189=CARTESIAN_POINT ( 'NONE',  ( 0.8751705887134553219, 11.58504748649199811, -46.67919521768876479 ) ) ;
#5194=ORIENTED_EDGE ( 'NONE', *, *, #4482, .T. ) ;
#5200=CARTESIAN_POINT ( 'NONE',  ( 4.833616638992205949, 3.476827473557875692, -46.11947910922904725 ) ) ;
#5203=CARTESIAN_POINT ( 'NONE',  ( -6.016761891674565099, 4.880293656735219088, -18.20023637398594119 ) ) ;
#5207=( BOUNDED_SURFACE ( )  B_SPLINE_SURFACE ( 3, 1, ( 
 ( #60816, #22009 ),
 ( #31715, #41445 ),
 ( #27625, #2877 ),
 ( #55496, #45833 ) ),
 .UNSPECIFIED., .F., .F., .F. ) 
 B_SPLINE_SURFACE_WITH_KNOTS ( ( 4, 4 ),
 ( 2, 2 ),
 ( 0.000000000000000000, 1.000000000000000000 ),
 ( 0.000000000000000000, 1.000000000000000000 ),
 .UNSPECIFIED. ) 
 GEOMETRIC_REPRESENTATION_ITEM ( )  RATIONAL_B_SPLINE_SURFACE ( (
 ( 1.000000000000000000, 1.000000000000000000),
 ( 0.9953040768229013402, 0.8617119497784988535),
 ( 0.9953040768229013402, 0.8617119497784988535),
 ( 1.000000000000000000, 1.000000000000000000) ) ) 
 REPRESENTATION_ITEM ( '' )  SURFACE ( )  );
#5212=CARTESIAN_POINT ( 'NONE',  ( 2.643462169533600914, 19.65219740572190332, -43.83256147628713961 ) ) ;
#5214=ORIENTED_EDGE ( 'NONE', *, *, #34303, .F. ) ;
#5225=CARTESIAN_POINT ( 'NONE',  ( 4.975801465491694664, 46.87746200127440943, 9.906103548668390602 ) ) ;
#5233=CARTESIAN_POINT ( 'NONE',  ( 0.8751705887134553219, 46.21789262997757675, -13.30665218149314200 ) ) ;
#5235=CARTESIAN_POINT ( 'NONE',  ( 0.5988103564986360094, -13.03604522143325006, -46.30780741915661736 ) ) ;
#5236=CARTESIAN_POINT ( 'NONE',  ( 0.6031357023905875581, 33.98625823839253002, 34.04794059289660879 ) ) ;
#5237=VERTEX_POINT ( 'NONE', #26275 ) ;
#5242=EDGE_CURVE ( 'NONE', #26755, #55625, #4923, .T. ) ;
#5255=CARTESIAN_POINT ( 'NONE',  ( -6.015611763856276717, 11.46610900684722623, 14.95313250337433963 ) ) ;
#5260=CARTESIAN_POINT ( 'NONE',  ( 0.1100247026804066219, -21.41511734445772674, -37.43141430507365186 ) ) ;
#5263=AXIS2_PLACEMENT_3D ( 'NONE', #57004, #37312, #27586 ) ;
#5266=ORIENTED_EDGE ( 'NONE', *, *, #28630, .T. ) ;
#5269=CARTESIAN_POINT ( 'NONE',  ( 0.6031356219577718170, 12.53544563195234929, 46.44562759437258848 ) ) ;
#5273=CARTESIAN_POINT ( 'NONE',  ( 0.3622758884714730732, 33.69533458712344753, -26.89560658783350178 ) ) ;
#5282=EDGE_CURVE ( 'NONE', #33419, #26755, #2218, .T. ) ;
#5287=ADVANCED_FACE ( 'NONE', ( #42872 ), #6918, .F. ) ;
#5294=CARTESIAN_POINT ( 'NONE',  ( 0.7245667037590730608, -23.33692989609141222, 42.06183421678288425 ) ) ;
#5295=ORIENTED_EDGE ( 'NONE', *, *, #46659, .F. ) ;
#5299=CIRCLE ( 'NONE', #50346, 47.91270532121795611 ) ;
#5300=CARTESIAN_POINT ( 'NONE',  ( 4.975801465491694664, 32.01766832630313075, -35.64402118370923489 ) ) ;
#5302=CARTESIAN_POINT ( 'NONE',  ( 0.7246131072078586532, -44.74808308960866299, 17.64706930304217636 ) ) ;
#5304=CARTESIAN_POINT ( 'NONE',  ( 0.8751705887134423323, -0.8911681664091769539, 48.08707113907594533 ) ) ;
#5306=CARTESIAN_POINT ( 'NONE',  ( 0.7245667037590721726, 33.42814706018020843, -34.58857005974916632 ) ) ;
#5317=CARTESIAN_POINT ( 'NONE',  ( -2.569797478183790229, 13.34095667500596427, 6.011723966604196612 ) ) ;
#5318=EDGE_CURVE ( 'NONE', #46497, #23973, #10954, .T. ) ;
#5319=CARTESIAN_POINT ( 'NONE',  ( 0.6017667736363749853, -38.37782726569709268, 29.00830848931562400 ) ) ;
#5330=CARTESIAN_POINT ( 'NONE',  ( 4.975801465491695552, 39.51822597168496287, -27.09127437476339395 ) ) ;
#5336=CARTESIAN_POINT ( 'NONE',  ( 3.238931869106853600, 14.74782013370846734, -40.38337734129189016 ) ) ;
#5338=ORIENTED_EDGE ( 'NONE', *, *, #35086, .T. ) ;
#5344=B_SPLINE_CURVE_WITH_KNOTS ( 'NONE', 3,
 ( #8548, #28281, #32691, #18284 ),
 .UNSPECIFIED., .F., .F.,
 ( 4, 4 ),
 ( 0.000000000000000000, 0.005014147105413707325 ),
 .UNSPECIFIED. ) ;
#5345=CARTESIAN_POINT ( 'NONE',  ( -6.016489644550736315, 0.004404229197775727175, 18.84320342686341121 ) ) ;
#5346=CARTESIAN_POINT ( 'NONE',  ( 3.680974057930773480, 20.05478739720736314, -43.58300585207901889 ) ) ;
#5347=B_SPLINE_CURVE_WITH_KNOTS ( 'NONE', 3,
 ( #40785, #59848, #45781, #16965, #55136, #21959 ),
 .UNSPECIFIED., .F., .F.,
 ( 4, 2, 4 ),
 ( 0.000000000000000000, 0.0002450742804987332004, 0.0004901485609974664008 ),
 .UNSPECIFIED. ) ;
#5349=EDGE_CURVE ( 'NONE', #26311, #4316, #19590, .T. ) ;
#5354=CARTESIAN_POINT ( 'NONE',  ( 0.2230388203127562363, -36.95676097786397207, 22.21453373073326532 ) ) ;
#5358=CARTESIAN_POINT ( 'NONE',  ( 4.975801465491695552, 47.84403947906839960, 2.564218696447662982 ) ) ;
#5362=DIRECTION ( 'NONE',  ( 0.000000000000000000, 0.000000000000000000, 1.000000000000000000 ) ) ;
#5365=CARTESIAN_POINT ( 'NONE',  ( -6.017396004339687465, -9.422598049764740580, 16.31807101179367692 ) ) ;
#5372=ORIENTED_EDGE ( 'NONE', *, *, #23413, .T. ) ;
#5374=ORIENTED_EDGE ( 'NONE', *, *, #14351, .T. ) ;
#5377=B_SPLINE_CURVE_WITH_KNOTS ( 'NONE', 3,
 ( #20344, #39468, #34757, #35695, #54440, #53824 ),
 .UNSPECIFIED., .F., .F.,
 ( 4, 2, 4 ),
 ( 1.266823315017301927E-16, 0.0002450741128632351611, 0.0004901482257263435789 ),
 .UNSPECIFIED. ) ;
#5380=CARTESIAN_POINT ( 'NONE',  ( 0.1103878639767399694, 11.20830530106134759, 41.64243544356632754 ) ) ;
#5386=CARTESIAN_POINT ( 'NONE',  ( 0.3622758884714600280, 22.26738722580168073, -36.91764744403298693 ) ) ;
#5394=CARTESIAN_POINT ( 'NONE',  ( -6.016489644550736315, 11.46752133529406414, -14.95199950534935951 ) ) ;
#5396=CARTESIAN_POINT ( 'NONE',  ( 5.880360259849752858, 45.41096578730625311, 15.46489389606771780 ) ) ;
#5402=FACE_OUTER_BOUND ( 'NONE', #16126, .T. ) ;
#5408=CARTESIAN_POINT ( 'NONE',  ( 0.8760168074886965917, -46.68716261866184425, 11.58706983520244194 ) ) ;
#5415=ADVANCED_FACE ( 'NONE', ( #45265 ), #36608, .F. ) ;
#5416=CARTESIAN_POINT ( 'NONE',  ( 0.5980894510889457338, -24.66136644716792148, -41.31170365136879497 ) ) ;
#5419=DIRECTION ( 'NONE',  ( -1.000000000000000000, -0.000000000000000000, -0.000000000000000000 ) ) ;
#5420=CARTESIAN_POINT ( 'NONE',  ( 0.6254311100348625141, 19.04346769887692759, -44.17670535157489553 ) ) ;
#5422=CARTESIAN_POINT ( 'NONE',  ( 0.6017666602106490625, -18.73203020817331321, -44.31084100715245455 ) ) ;
#5424=ORIENTED_EDGE ( 'NONE', *, *, #30259, .T. ) ;
#5425=EDGE_CURVE ( 'NONE', #2500, #8307, #29213, .T. ) ;
#5427=CARTESIAN_POINT ( 'NONE',  ( 0.1101816497532062955, -34.29544870207495677, -26.14462713083283063 ) ) ;
#5431=CARTESIAN_POINT ( 'NONE',  ( 0.6254311100348654007, -34.49956326955439323, 33.52633430496167932 ) ) ;
#5432=CARTESIAN_POINT ( 'NONE',  ( 0.6023142530420679819, -46.39979989577489761, 12.70386526143691697 ) ) ;
#5439=DIRECTION ( 'NONE',  ( -1.000000000000000000, -0.000000000000000000, -0.000000000000000000 ) ) ;
#5442=ADVANCED_FACE ( 'NONE', ( #6678 ), #21122, .F. ) ;
#5447=ORIENTED_EDGE ( 'NONE', *, *, #31514, .T. ) ;
#5448=CARTESIAN_POINT ( 'NONE',  ( 0.1102144999581333162, -11.28312052188176473, 41.62223437741650400 ) ) ;
#5451=ORIENTED_EDGE ( 'NONE', *, *, #61228, .F. ) ;
#5460=B_SPLINE_CURVE_WITH_KNOTS ( 'NONE', 3,
 ( #43140, #19321, #57489, #56889 ),
 .UNSPECIFIED., .F., .F.,
 ( 4, 4 ),
 ( 0.000000000000000000, 0.005014147105413699519 ),
 .UNSPECIFIED. ) ;
#5462=AXIS2_PLACEMENT_3D ( 'NONE', #2727, #12165, #51268 ) ;
#5466=CARTESIAN_POINT ( 'NONE',  ( 0.8751705887134423323, 44.76769609654235893, -17.57879340691497561 ) ) ;
#5472=CARTESIAN_POINT ( 'NONE',  ( 4.549368137175248350, 18.79584381673534565, -38.59302160394733505 ) ) ;
#5473=CARTESIAN_POINT ( 'NONE',  ( 4.833616638992208614, 35.06988470649527301, 30.15290813935915537 ) ) ;
#5477=CARTESIAN_POINT ( 'NONE',  ( -6.016761891674565099, 17.40752468084782834, 7.214149619366422961 ) ) ;
#5479=LINE ( 'NONE', #39348, #8431 ) ;
#5482=ORIENTED_EDGE ( 'NONE', *, *, #21945, .T. ) ;
#5486=CARTESIAN_POINT ( 'NONE',  ( 3.238931869106852712, -24.69728751010312706, 35.19033040238025478 ) ) ;
#5487=CARTESIAN_POINT ( 'NONE',  ( 0.6009452777970413218, -47.63713033690757470, 6.711700115492742036 ) ) ;
#5491=CARTESIAN_POINT ( 'NONE',  ( 0.3622758884714600280, 10.35929834645864389, 41.85013935980105515 ) ) ;
#5492=CARTESIAN_POINT ( 'NONE',  ( 0.5998501479064699549, 28.86886762351124958, -38.48283596222000114 ) ) ;
#5493=( BOUNDED_SURFACE ( )  B_SPLINE_SURFACE ( 3, 1, ( 
 ( #6246, #58573 ),
 ( #29467, #25082 ),
 ( #38907, #44535 ),
 ( #44842, #57959 ) ),
 .UNSPECIFIED., .F., .F., .F. ) 
 B_SPLINE_SURFACE_WITH_KNOTS ( ( 4, 4 ),
 ( 2, 2 ),
 ( 0.000000000000000000, 1.000000000000000000 ),
 ( 0.000000000000000000, 1.000000000000000000 ),
 .UNSPECIFIED. ) 
 GEOMETRIC_REPRESENTATION_ITEM ( )  RATIONAL_B_SPLINE_SURFACE ( (
 ( 1.000000000000000000, 1.000000000000000000),
 ( 0.9953040768229013402, 0.8617119497784988535),
 ( 0.9953040768229013402, 0.8617119497784988535),
 ( 1.000000000000000000, 1.000000000000000000) ) ) 
 REPRESENTATION_ITEM ( '' )  SURFACE ( )  );
#5498=CARTESIAN_POINT ( 'NONE',  ( -6.016761891674565099, 2.456125503350710115, 18.68243340030203470 ) ) ;
#5503=FACE_OUTER_BOUND ( 'NONE', #35532, .T. ) ;
#5507=CARTESIAN_POINT ( 'NONE',  ( 0.6025881611877910160, 38.29866377863839944, -29.11258673756373483 ) ) ;
#5508=EDGE_CURVE ( 'NONE', #25496, #26613, #5344, .T. ) ;
#5516=EDGE_LOOP ( 'NONE', ( #27992, #47811, #4473, #16430 ) ) ;
#5524=DIRECTION ( 'NONE',  ( 0.1024043820194936449, -0.4859385467930519842, 0.8679729669084529364 ) ) ;
#5525=CARTESIAN_POINT ( 'NONE',  ( -5.995132425357893702, 18.68182899165014987, -2.468096378287932158 ) ) ;
#5526=ORIENTED_EDGE ( 'NONE', *, *, #25097, .F. ) ;
#5534=CARTESIAN_POINT ( 'NONE',  ( 4.975801465491694664, 45.55012473237754023, -14.85979367497125381 ) ) ;
#5535=ORIENTED_EDGE ( 'NONE', *, *, #2746, .T. ) ;
#5539=CARTESIAN_POINT ( 'NONE',  ( -6.010958268070873523, -16.32616437357118500, 9.409153349053527293 ) ) ;
#5541=CARTESIAN_POINT ( 'NONE',  ( 4.549368137175248350, 28.14399996863453168, 32.41327393324149853 ) ) ;
#5544=VERTEX_POINT ( 'NONE', #36789 ) ;
#5551=ORIENTED_EDGE ( 'NONE', *, *, #55572, .T. ) ;
#5563=VERTEX_POINT ( 'NONE', #7946 ) ;
#5577=FACE_OUTER_BOUND ( 'NONE', #18295, .T. ) ;
#5578=FACE_OUTER_BOUND ( 'NONE', #26849, .T. ) ;
#5585=ADVANCED_FACE ( 'NONE', ( #13585 ), #32209, .F. ) ;
#5594=DIRECTION ( 'NONE',  ( -1.000000000000000000, -0.000000000000000000, -0.000000000000000000 ) ) ;
#5599=CARTESIAN_POINT ( 'NONE',  ( 0.8751705887134423323, 5.393078191592057813, 47.79200036674281904 ) ) ;
#5604=FACE_OUTER_BOUND ( 'NONE', #18495, .T. ) ;
#5605=VERTEX_POINT ( 'NONE', #19214 ) ;
#5617=ORIENTED_EDGE ( 'NONE', *, *, #60792, .T. ) ;
#5621=CARTESIAN_POINT ( 'NONE',  ( 0.1103936448916694457, -6.269440624735986453E-17, 43.12443171339902648 ) ) ;
#5623=VERTEX_POINT ( 'NONE', #34233 ) ;
#5629=VERTEX_POINT ( 'NONE', #47707 ) ;
#5640=( BOUNDED_SURFACE ( )  B_SPLINE_SURFACE ( 3, 1, ( 
 ( #8997, #41925 ),
 ( #18100, #56292 ),
 ( #36919, #55985 ),
 ( #42536, #51907 ) ),
 .UNSPECIFIED., .F., .F., .F. ) 
 B_SPLINE_SURFACE_WITH_KNOTS ( ( 4, 4 ),
 ( 2, 2 ),
 ( 0.000000000000000000, 1.000000000000000000 ),
 ( 0.000000000000000000, 1.000000000000000000 ),
 .UNSPECIFIED. ) 
 GEOMETRIC_REPRESENTATION_ITEM ( )  RATIONAL_B_SPLINE_SURFACE ( (
 ( 1.000000000000000000, 1.000000000000000000),
 ( 0.7223157951917480446, 0.9931996967497186413),
 ( 0.7223157951917480446, 0.9931996967497186413),
 ( 1.000000000000000000, 1.000000000000000000) ) ) 
 REPRESENTATION_ITEM ( '' )  SURFACE ( )  );
#5642=CARTESIAN_POINT ( 'NONE',  ( 0.6009452777970410997, 18.00606236585372955, -44.61081509289886071 ) ) ;
#5655=DIRECTION ( 'NONE',  ( 0.000000000000000000, 0.000000000000000000, -1.000000000000000000 ) ) ;
#5656=CARTESIAN_POINT ( 'NONE',  ( 0.6041374136657476912, 44.51224464244974399, 18.24862627831550199 ) ) ;
#5663=CARTESIAN_POINT ( 'NONE',  ( 1.827326673878743923, -1.232746109312476301, 43.03225468313000590 ) ) ;
#5665=CARTESIAN_POINT ( 'NONE',  ( 0.6001305935487422083, 24.50730504006456556, -41.40054608060269459 ) ) ;
#5670=VERTEX_POINT ( 'NONE', #24822 ) ;
#5675=CIRCLE ( 'NONE', #20745, 43.12527911185304674 ) ;
#5676=VERTEX_POINT ( 'NONE', #43962 ) ;
#5680=CARTESIAN_POINT ( 'NONE',  ( 0.6027935024548037868, -29.42425667880464957, 38.05972402498726126 ) ) ;
#5681=CARTESIAN_POINT ( 'NONE',  ( 2.301430502907646503, 47.77346269870100315, -4.990893951996506317 ) ) ;
#5682=FACE_OUTER_BOUND ( 'NONE', #48485, .T. ) ;
#5689=AXIS2_PLACEMENT_3D ( 'NONE', #15663, #57917, #14732 ) ;
#5697=CARTESIAN_POINT ( 'NONE',  ( 0.1092565886968783623, 5.936467125236458031, 42.71401356099880786 ) ) ;
#5711=LINE ( 'NONE', #1329, #40712 ) ;
#5714=CARTESIAN_POINT ( 'NONE',  ( 0.1073791018717578927, 34.50606437925546999, -25.86618856530675714 ) ) ;
#5715=CARTESIAN_POINT ( 'NONE',  ( 0.1073791018717578927, -43.12183934961191056, -0.4849339620931655825 ) ) ;
#5720=CARTESIAN_POINT ( 'NONE',  ( 0.1102144999581332607, 30.58258619461921413, -30.40435207217196734 ) ) ;
#5721=CARTESIAN_POINT ( 'NONE',  ( 0.7246131072078552116, 38.65593150731050542, -28.62741613354252479 ) ) ;
#5724=VECTOR ( 'NONE', #56583, 1000.000000000000227 ) ;
#5728=CARTESIAN_POINT ( 'NONE',  ( 0.7048096507298579061, -0.8437160066910636136, 48.10291524268439645 ) ) ;
#5729=CARTESIAN_POINT ( 'NONE',  ( 0.8751705887134423323, -34.63284514348608667, 33.37254303619495488 ) ) ;
#5731=DIRECTION ( 'NONE',  ( 0.000000000000000000, 0.000000000000000000, -1.000000000000000000 ) ) ;
#5733=( BOUNDED_SURFACE ( )  B_SPLINE_SURFACE ( 3, 1, ( 
 ( #16778, #41519 ),
 ( #36506, #46217 ),
 ( #22388, #17088 ),
 ( #31165, #7651 ) ),
 .UNSPECIFIED., .F., .F., .F. ) 
 B_SPLINE_SURFACE_WITH_KNOTS ( ( 4, 4 ),
 ( 2, 2 ),
 ( 0.000000000000000000, 1.000000000000000000 ),
 ( 0.000000000000000000, 1.000000000000000000 ),
 .UNSPECIFIED. ) 
 GEOMETRIC_REPRESENTATION_ITEM ( )  RATIONAL_B_SPLINE_SURFACE ( (
 ( 1.000000000000000000, 1.000000000000000000),
 ( 0.9953040768229005630, 0.8617119497784937465),
 ( 0.9953040768229005630, 0.8617119497784937465),
 ( 1.000000000000000000, 1.000000000000000000) ) ) 
 REPRESENTATION_ITEM ( '' )  SURFACE ( )  );
#5735=FACE_OUTER_BOUND ( 'NONE', #38445, .T. ) ;
#5737=CARTESIAN_POINT ( 'NONE',  ( 0.6041374136657476912, -12.61972904329569012, -46.42299778158151469 ) ) ;
#5739=VERTEX_POINT ( 'NONE', #40189 ) ;
#5742=CARTESIAN_POINT ( 'NONE',  ( 0.1102847568649952675, -43.12433804869904463, 0.09217763870885797850 ) ) ;
#5750=VECTOR ( 'NONE', #23328, 1000.000000000000227 ) ;
#5760=FACE_OUTER_BOUND ( 'NONE', #47572, .T. ) ;
#5771=CARTESIAN_POINT ( 'NONE',  ( -6.015611763856276717, -13.31979030221808458, 13.32857883366828666 ) ) ;
#5773=ADVANCED_FACE ( 'NONE', ( #16047 ), #2543, .F. ) ;
#5781=VERTEX_POINT ( 'NONE', #18512 ) ;
#5790=FACE_OUTER_BOUND ( 'NONE', #16259, .T. ) ;
#5793=CARTESIAN_POINT ( 'NONE',  ( 0.3622758884714730732, -22.26738722580142138, -36.91764744403313614 ) ) ;
#5799=VERTEX_POINT ( 'NONE', #27288 ) ;
#5813=B_SPLINE_CURVE_WITH_KNOTS ( 'NONE', 3,
 ( #59306, #16412, #2288, #60537, #50840, #7931 ),
 .UNSPECIFIED., .F., .F.,
 ( 4, 2, 4 ),
 ( 1.964972962535902174E-17, 0.0002293319059085107401, 0.0004586638118170018020 ),
 .UNSPECIFIED. ) ;
#5816=CARTESIAN_POINT ( 'NONE',  ( 1.827119703190779321, -37.88337895042280934, -20.44859290426024145 ) ) ;
#5822=CARTESIAN_POINT ( 'NONE',  ( 0.1102847568649952675, 16.58813073670652116, 39.80641842112251538 ) ) ;
#5823=FACE_OUTER_BOUND ( 'NONE', #50170, .T. ) ;
#5825=CARTESIAN_POINT ( 'NONE',  ( -6.010958268070873523, 18.68034667844852237, -2.473955915502024983 ) ) ;
#5830=CARTESIAN_POINT ( 'NONE',  ( 0.8751705887134553219, 19.22545746485597817, 44.08562551107088723 ) ) ;
#5837=CARTESIAN_POINT ( 'NONE',  ( 2.301529144917015213, 46.04684498357980971, -13.67115311794016463 ) ) ;
#5839=ORIENTED_EDGE ( 'NONE', *, *, #7617, .F. ) ;
#5849=EDGE_LOOP ( 'NONE', ( #53246, #30508, #35852, #21741 ) ) ;
#5850=DIRECTION ( 'NONE',  ( 0.000000000000000000, 0.000000000000000000, 1.000000000000000000 ) ) ;
#5852=VERTEX_POINT ( 'NONE', #41723 ) ;
#5854=( BOUNDED_SURFACE ( )  B_SPLINE_SURFACE ( 3, 1, ( 
 ( #46587, #18074 ),
 ( #9906, #57175 ),
 ( #14930, #28384 ),
 ( #24618, #61571 ) ),
 .UNSPECIFIED., .F., .F., .F. ) 
 B_SPLINE_SURFACE_WITH_KNOTS ( ( 4, 4 ),
 ( 2, 2 ),
 ( 0.000000000000000000, 1.000000000000000000 ),
 ( 0.000000000000000000, 1.000000000000000000 ),
 .UNSPECIFIED. ) 
 GEOMETRIC_REPRESENTATION_ITEM ( )  RATIONAL_B_SPLINE_SURFACE ( (
 ( 1.000000000000000000, 1.000000000000000000),
 ( 0.9751682680413298332, 0.9999560080971552356),
 ( 0.9751682680413298332, 0.9999560080971552356),
 ( 1.000000000000000000, 1.000000000000000000) ) ) 
 REPRESENTATION_ITEM ( '' )  SURFACE ( )  );
#5856=ORIENTED_EDGE ( 'NONE', *, *, #7952, .T. ) ;
#5865=EDGE_CURVE ( 'NONE', #25265, #27177, #52396, .T. ) ;
#5867=VERTEX_POINT ( 'NONE', #32306 ) ;
#5868=ORIENTED_EDGE ( 'NONE', *, *, #44516, .T. ) ;
#5873=CARTESIAN_POINT ( 'NONE',  ( 0.8751705887134553219, -13.30665218149330364, -46.21789262997752701 ) ) ;
#5874=FACE_OUTER_BOUND ( 'NONE', #29230, .T. ) ;
#5875=ORIENTED_EDGE ( 'NONE', *, *, #46846, .F. ) ;
#5879=CARTESIAN_POINT ( 'NONE',  ( 0.6017666602106490625, 12.78804974226035540, 46.37677619531716999 ) ) ;
#5888=CARTESIAN_POINT ( 'NONE',  ( -6.015611763856276717, -18.20278301740940208, 4.870987357968111553 ) ) ;
#5891=EDGE_CURVE ( 'NONE', #6804, #39984, #36794, .T. ) ;
#5892=VECTOR ( 'NONE', #59160, 1000.000000000000000 ) ;
#5897=CARTESIAN_POINT ( 'NONE',  ( 0.1102144999581333301, 37.28370465375326859, 21.67128446981392997 ) ) ;
#5899=FACE_OUTER_BOUND ( 'NONE', #20816, .T. ) ;
#5900=CARTESIAN_POINT ( 'NONE',  ( 0.1073791018717483448, -16.05399293000841254, 40.02496097243031414 ) ) ;
#5908=VERTEX_POINT ( 'NONE', #55781 ) ;
#5909=CARTESIAN_POINT ( 'NONE',  ( 0.2230388203127608437, -31.02270543585807161, -29.94794547692434605 ) ) ;
#5913=CARTESIAN_POINT ( 'NONE',  ( 5.880360259849739535, -15.37531919565267735, 45.44137230084854906 ) ) ;
#5917=EDGE_CURVE ( 'NONE', #56955, #40637, #1451, .T. ) ;
#5920=CARTESIAN_POINT ( 'NONE',  ( -6.016761891674565099, -9.418621820384382559, -16.32039929810266798 ) ) ;
#5921=ORIENTED_EDGE ( 'NONE', *, *, #43939, .T. ) ;
#5923=ORIENTED_EDGE ( 'NONE', *, *, #42959, .T. ) ;
#5931=CARTESIAN_POINT ( 'NONE',  ( -2.569797478183790229, 8.547745408040636761, 11.87678401312197529 ) ) ;
#5932=CARTESIAN_POINT ( 'NONE',  ( -6.015611763856276717, -13.31979030221808458, 13.32857883366828666 ) ) ;
#5934=CARTESIAN_POINT ( 'NONE',  ( 0.6041374136657475802, -46.42299778158147205, -12.61972904329582867 ) ) ;
#5942=ORIENTED_EDGE ( 'NONE', *, *, #61314, .T. ) ;
#5948=VERTEX_POINT ( 'NONE', #5304 ) ;
#5949=CARTESIAN_POINT ( 'NONE',  ( 0.6029303876144825880, 18.53079182983344708, -44.39523326884619081 ) ) ;
#5951=DIRECTION ( 'NONE',  ( 0.1024043820194936311, -0.3684880688409263305, 0.9239750460186089143 ) ) ;
#5965=ADVANCED_FACE ( 'NONE', ( #47946 ), #13361, .F. ) ;
#5971=CARTESIAN_POINT ( 'NONE',  ( -6.016104459813371719, 9.416989654584535074, -16.32137543786072698 ) ) ;
#5972=ORIENTED_EDGE ( 'NONE', *, *, #55071, .T. ) ;
#5973=CARTESIAN_POINT ( 'NONE',  ( 0.3622758884714730732, -36.91764744403337062, 22.26738722580103413 ) ) ;
#5974=CARTESIAN_POINT ( 'NONE',  ( 0.1064266379913939020, -39.62374453032509081, 17.02047542254779700 ) ) ;
#5975=B_SPLINE_CURVE_WITH_KNOTS ( 'NONE', 3,
 ( #14426, #58532, #9704, #5294, #24421, #28814 ),
 .UNSPECIFIED., .F., .F.,
 ( 4, 2, 4 ),
 ( 0.000000000000000000, 0.0002450742804987318451, 0.0004901485609974636903 ),
 .UNSPECIFIED. ) ;
#5981=ORIENTED_EDGE ( 'NONE', *, *, #36796, .T. ) ;
#5986=CARTESIAN_POINT ( 'NONE',  ( 0.1087620492084205998, 10.81135549499722259, 41.74735017127134995 ) ) ;
#5988=CARTESIAN_POINT ( 'NONE',  ( 0.3622758884714730732, -33.69533458712361806, 26.89560658783328861 ) ) ;
#5992=CARTESIAN_POINT ( 'NONE',  ( 0.1092565886968784317, 0.3103822814773909977, 43.12345370280014833 ) ) ;
#5999=CARTESIAN_POINT ( 'NONE',  ( 0.6009453534118440743, -18.81239552213013511, 44.27682103112798728 ) ) ;
#6007=CARTESIAN_POINT ( 'NONE',  ( 0.6031356219577718170, -12.36679943215693456, 46.49081620741434051 ) ) ;
#6008=CARTESIAN_POINT ( 'NONE',  ( 4.975801465491694664, -3.702618843597810905, 47.76942479135478692 ) ) ;
#6010=CARTESIAN_POINT ( 'NONE',  ( 5.880360259849752858, 43.00389496650585386, 21.25991003419967740 ) ) ;
#6011=CARTESIAN_POINT ( 'NONE',  ( 3.238931869106853600, -31.66562935062918527, -29.07925862215120461 ) ) ;
#6017=EDGE_LOOP ( 'NONE', ( #27373, #8176, #15895, #881 ) ) ;
#6018=ORIENTED_EDGE ( 'NONE', *, *, #56776, .T. ) ;
#6021=CARTESIAN_POINT ( 'NONE',  ( 0.1100053167205930771, -39.77279469894225628, 16.66867746965576558 ) ) ;
#6024=CARTESIAN_POINT ( 'NONE',  ( 0.1101816497532063233, 34.13008584880293483, -26.36013219694235943 ) ) ;
#6025=CARTESIAN_POINT ( 'NONE',  ( -6.001507490154111224, -2.475062734132568831, 18.68062548815624879 ) ) ;
#6030=CARTESIAN_POINT ( 'NONE',  ( 0.1104177457020373010, 30.49013195371455609, -30.49705356371274334 ) ) ;
#6035=CARTESIAN_POINT ( 'NONE',  ( 0.1064266379913944016, -11.70292640078125324, -41.50637574965944054 ) ) ;
#6036=CARTESIAN_POINT ( 'NONE',  ( 0.6025881611877910160, -24.24244696985837066, 41.55278713510040234 ) ) ;
#6038=DIRECTION ( 'NONE',  ( 1.000000000000000000, 0.000000000000000000, 0.000000000000000000 ) ) ;
#6041=CONICAL_SURFACE ( 'NONE', #56099, 42.92674063221959813, 1.485477209440487556 ) ;
#6045=CARTESIAN_POINT ( 'NONE',  ( 0.6254311100348657337, -47.60023274471275556, -6.960804577576654495 ) ) ;
#6047=ADVANCED_FACE ( 'NONE', ( #30360 ), #10986, .F. ) ;
#6050=VERTEX_POINT ( 'NONE', #7153 ) ;
#6051=CARTESIAN_POINT ( 'NONE',  ( 0.1073791018717578927, -37.58707531572220262, 21.14095454447495115 ) ) ;
#6055=ORIENTED_EDGE ( 'NONE', *, *, #13563, .T. ) ;
#6063=CARTESIAN_POINT ( 'NONE',  ( 0.6009452777970413218, -24.43074291040877455, -41.44251326863921037 ) ) ;
#6070=CARTESIAN_POINT ( 'NONE',  ( 0.8760168074886965917, 19.22870327415304814, -44.09317760313732748 ) ) ;
#6074=CARTESIAN_POINT ( 'NONE',  ( 2.301529144917015213, 44.85388898587000028, 17.18548816179638905 ) ) ;
#6086=EDGE_CURVE ( 'NONE', #10506, #18533, #27848, .T. ) ;
#6090=VERTEX_POINT ( 'NONE', #59479 ) ;
#6091=CARTESIAN_POINT ( 'NONE',  ( 0.2230388203127621483, -26.84831060237819145, -33.74101226470655490 ) ) ;
#6092=DIRECTION ( 'NONE',  ( -0.1024043820194934645, -0.9946559125373959365, -0.01315135725336883353 ) ) ;
#6093=B_SPLINE_CURVE_WITH_KNOTS ( 'NONE', 3,
 ( #10318, #29413, #48522, #59143 ),
 .UNSPECIFIED., .F., .F.,
 ( 4, 4 ),
 ( 1.907487264466063683E-17, 0.004444306975806115029 ),
 .UNSPECIFIED. ) ;
#6095=CARTESIAN_POINT ( 'NONE',  ( 0.3622758884714600280, 39.50828911766974016, 17.25816669465007891 ) ) ;
#6096=LINE ( 'NONE', #30234, #57643 ) ;
#6100=CARTESIAN_POINT ( 'NONE',  ( -5.995132425357893702, 18.84415457712583475, 0.008513469642873375265 ) ) ;
#6113=LINE ( 'NONE', #15556, #14850 ) ;
#6118=CARTESIAN_POINT ( 'NONE',  ( 0.7246131072078504376, 17.64706930304232202, 44.74808308960857062 ) ) ;
#6120=CARTESIAN_POINT ( 'NONE',  ( 4.975801465491695552, 0.000000000000000000, 0.000000000000000000 ) ) ;
#6123=EDGE_CURVE ( 'NONE', #21383, #497, #50098, .T. ) ;
#6125=ORIENTED_EDGE ( 'NONE', *, *, #3367, .T. ) ;
#6129=ADVANCED_FACE ( 'NONE', ( #12517 ), #56146, .F. ) ;
#6130=CARTESIAN_POINT ( 'NONE',  ( 0.1103744047535531458, 16.46720136312925220, 39.85659247569267194 ) ) ;
#6133=CARTESIAN_POINT ( 'NONE',  ( 0.8760168074886960365, -47.80016357497252955, 5.394043284318696507 ) ) ;
#6146=CARTESIAN_POINT ( 'NONE',  ( 4.549368137175248350, 0.000000000000000000, 0.000000000000000000 ) ) ;
#6155=ORIENTED_EDGE ( 'NONE', *, *, #90, .F. ) ;
#6159=ORIENTED_EDGE ( 'NONE', *, *, #47421, .T. ) ;
#6164=ORIENTED_EDGE ( 'NONE', *, *, #24913, .F. ) ;
#6165=CARTESIAN_POINT ( 'NONE',  ( 4.549368137175248350, 38.40568845698250300, 19.17571786012337753 ) ) ;
#6171=CARTESIAN_POINT ( 'NONE',  ( -2.569797478183790229, -0.4487456364279838184, 14.62602397812940502 ) ) ;
#6176=CARTESIAN_POINT ( 'NONE',  ( 4.833616638992205949, 45.44786513329597710, -8.578242093415260783 ) ) ;
#6179=CARTESIAN_POINT ( 'NONE',  ( 0.1310142868023705109, 41.81449350725030456, -10.54463319394690224 ) ) ;
#6180=CARTESIAN_POINT ( 'NONE',  ( 0.2885697896453104927, 29.91358794843018742, 31.05173034173381907 ) ) ;
#6181=CARTESIAN_POINT ( 'NONE',  ( -6.010958268070873523, -2.473955915502089820, -18.68034667844851526 ) ) ;
#6184=ORIENTED_EDGE ( 'NONE', *, *, #56927, .T. ) ;
#6187=CARTESIAN_POINT ( 'NONE',  ( 4.833616638992208614, -20.86133030530261578, -41.27831852777636357 ) ) ;
#6188=CARTESIAN_POINT ( 'NONE',  ( 1.827119703190779321, 33.38937793923687991, -27.17434071502568216 ) ) ;
#6192=CARTESIAN_POINT ( 'NONE',  ( -6.016104459813374383, 18.20253432612973299, -4.871830707672867078 ) ) ;
#6205=CARTESIAN_POINT ( 'NONE',  ( 0.09136607875274982415, 0.000000000000000000, 0.000000000000000000 ) ) ;
#6206=CARTESIAN_POINT ( 'NONE',  ( -6.017396004339687465, -4.875835690939052114, -18.20140164570674202 ) ) ;
#6213=VECTOR ( 'NONE', #23881, 1000.000000000000114 ) ;
#6216=ORIENTED_EDGE ( 'NONE', *, *, #15658, .T. ) ;
#6222=CARTESIAN_POINT ( 'NONE',  ( 0.5988103622719990193, -46.62176011478430127, 11.86435782853352805 ) ) ;
#6231=ADVANCED_FACE ( 'NONE', ( #55091 ), #26155, .F. ) ;
#6232=ORIENTED_EDGE ( 'NONE', *, *, #4432, .T. ) ;
#6236=CARTESIAN_POINT ( 'NONE',  ( 0.6027935024548037868, 44.37842839362948411, 18.57106801640314586 ) ) ;
#6240=EDGE_LOOP ( 'NONE', ( #6155, #7105, #23019, #36101 ) ) ;
#6246=CARTESIAN_POINT ( 'NONE',  ( -6.016761891674564211, -4.873659902332494909, 18.20201388312094082 ) ) ;
#6250=VERTEX_POINT ( 'NONE', #26590 ) ;
#6251=CARTESIAN_POINT ( 'NONE',  ( 0.5998501479064699549, 17.92509395669108585, -44.64337787626229925 ) ) ;
#6263=CARTESIAN_POINT ( 'NONE',  ( 2.301430502907647391, -17.18551536142221181, -44.85388302506900260 ) ) ;
#6264=CARTESIAN_POINT ( 'NONE',  ( -6.015611763856276717, 9.427003116184401676, -16.31561949997065852 ) ) ;
#6267=DIRECTION ( 'NONE',  ( 0.09835009131224567436, 0.6981896185982624514, 0.7091251765524093642 ) ) ;
#6269=EDGE_CURVE ( 'NONE', #44917, #41784, #52278, .T. ) ;
#6270=( BOUNDED_SURFACE ( )  B_SPLINE_SURFACE ( 3, 1, ( 
 ( #15236, #58723 ),
 ( #53114, #52810 ),
 ( #15850, #10219 ),
 ( #54027, #20246 ) ),
 .UNSPECIFIED., .F., .F., .F. ) 
 B_SPLINE_SURFACE_WITH_KNOTS ( ( 4, 4 ),
 ( 2, 2 ),
 ( 0.000000000000000000, 1.000000000000000000 ),
 ( 0.000000000000000000, 1.000000000000000000 ),
 .UNSPECIFIED. ) 
 GEOMETRIC_REPRESENTATION_ITEM ( )  RATIONAL_B_SPLINE_SURFACE ( (
 ( 1.000000000000000000, 1.000000000000000000),
 ( 0.9953040768229013402, 0.8617119497784988535),
 ( 0.9953040768229013402, 0.8617119497784988535),
 ( 1.000000000000000000, 1.000000000000000000) ) ) 
 REPRESENTATION_ITEM ( '' )  SURFACE ( )  );
#6271=CIRCLE ( 'NONE', #5263, 47.91270532121795611 ) ;
#6275=EDGE_LOOP ( 'NONE', ( #27054, #24858, #45071, #19511 ) ) ;
#6281=ADVANCED_FACE ( 'NONE', ( #42565 ), #27806, .F. ) ;
#6282=CARTESIAN_POINT ( 'NONE',  ( 1.827326673878744145, 39.28486782721041237, 17.60663982372551217 ) ) ;
#6289=ORIENTED_EDGE ( 'NONE', *, *, #21493, .F. ) ;
#6294=ORIENTED_EDGE ( 'NONE', *, *, #58114, .T. ) ;
#6313=EDGE_CURVE ( 'NONE', #28193, #57844, #29365, .T. ) ;
#6314=CARTESIAN_POINT ( 'NONE',  ( 0.5998501479064699549, 5.759754759340783181, -47.76154736470751772 ) ) ;
#6315=ORIENTED_EDGE ( 'NONE', *, *, #24116, .T. ) ;
#6318=ADVANCED_FACE ( 'NONE', ( #52547 ), #43011, .F. ) ;
#6322=EDGE_LOOP ( 'NONE', ( #24751, #1008, #16187, #49375 ) ) ;
#6324=CARTESIAN_POINT ( 'NONE',  ( 0.1097557419366048670, 34.34829179474800043, 26.07515889977830170 ) ) ;
#6325=CARTESIAN_POINT ( 'NONE',  ( 0.7048096507298635682, -19.18768066167092456, -44.11842270945967215 ) ) ;
#6331=FACE_OUTER_BOUND ( 'NONE', #8732, .T. ) ;
#6333=EDGE_CURVE ( 'NONE', #2450, #30431, #28431, .T. ) ;
#6337=B_SPLINE_CURVE_WITH_KNOTS ( 'NONE', 3,
 ( #58639, #6011, #10132, #15452 ),
 .UNSPECIFIED., .F., .F.,
 ( 4, 4 ),
 ( 6.992893892674702526E-18, 0.004566006591234645501 ),
 .UNSPECIFIED. ) ;
#6343=CARTESIAN_POINT ( 'NONE',  ( 0.3622758884714600280, 10.35929834645864389, 41.85013935980105515 ) ) ;
#6345=B_SPLINE_CURVE_WITH_KNOTS ( 'NONE', 3,
 ( #56967, #47904, #42911, #18465 ),
 .UNSPECIFIED., .F., .F.,
 ( 4, 4 ),
 ( 2.033478910116247305E-17, 0.004444306975806115029 ),
 .UNSPECIFIED. ) ;
#6358=CARTESIAN_POINT ( 'NONE',  ( 0.1081432562775998113, -11.56998286599564807, 41.54352569227142311 ) ) ;
#6360=CARTESIAN_POINT ( 'NONE',  ( 0.5980894510889457338, -28.72954109785633037, 38.59343625445397663 ) ) ;
#6361=CARTESIAN_POINT ( 'NONE',  ( 0.1100053167205930632, -37.25683392728348053, 21.71746606919042932 ) ) ;
#6364=CARTESIAN_POINT ( 'NONE',  ( 0.5998501479064699549, -24.50586714782575726, -41.39809967730479201 ) ) ;
#6371=DIRECTION ( 'NONE',  ( -0.1024043820194934645, 0.3684880688409138960, 0.9239750460186137992 ) ) ;
#6374=CARTESIAN_POINT ( 'NONE',  ( 0.6254311100348631802, 44.70341307176154544, -17.77188277739572797 ) ) ;
#6383=CARTESIAN_POINT ( 'NONE',  ( 0.6017666602106489515, 18.73203020817298636, 44.31084100715259666 ) ) ;
#6385=CARTESIAN_POINT ( 'NONE',  ( 4.549368137175248350, -28.14399996863474129, -32.41327393324131378 ) ) ;
#6390=EDGE_CURVE ( 'NONE', #59975, #5739, #40343, .T. ) ;
#6392=CARTESIAN_POINT ( 'NONE',  ( 0.7954190325252773475, 42.08256085583540340, 23.29293489839749753 ) ) ;
#6401=LINE ( 'NONE', #48736, #37492 ) ;
#6404=CARTESIAN_POINT ( 'NONE',  ( 2.301529144917015213, -1.287519423136938679, -48.01619158420458433 ) ) ;
#6409=CARTESIAN_POINT ( 'NONE',  ( 3.238931869106854933, -40.38337734129193990, -14.74782013370832878 ) ) ;
#6413=FACE_OUTER_BOUND ( 'NONE', #59888, .T. ) ;
#6415=CARTESIAN_POINT ( 'NONE',  ( 1.827119703190779765, -39.28489939038900047, 17.60659059422107475 ) ) ;
#6417=DIRECTION ( 'NONE',  ( 0.09835009131224552170, -0.1375559175655225452, -0.9855991218957026456 ) ) ;
#6418=CARTESIAN_POINT ( 'NONE',  ( 0.2230388203127603441, -0.7599700551097323675, -43.11276071378621566 ) ) ;
#6422=CARTESIAN_POINT ( 'NONE',  ( 0.6009453534118438522, -0.4363813339961392646, 48.10564080474284054 ) ) ;
#6424=CARTESIAN_POINT ( 'NONE',  ( 4.691466044806103852, -36.88741755356086571, 25.04870410140726733 ) ) ;
#6427=CARTESIAN_POINT ( 'NONE',  ( 3.680974057930773924, 1.849713332883747841, -47.94008194857089222 ) ) ;
#6430=EDGE_CURVE ( 'NONE', #14715, #58555, #25436, .T. ) ;
#6431=CARTESIAN_POINT ( 'NONE',  ( -2.569797478183783568, -10.65947181927832865, -10.02484965418637586 ) ) ;
#6433=CARTESIAN_POINT ( 'NONE',  ( 0.1092565886968784455, 41.57372480460685438, -11.46097737058320298 ) ) ;
#6445=CARTESIAN_POINT ( 'NONE',  ( 0.1103310638050661735, -0.08238894504425745002, 43.12437788119554227 ) ) ;
#6456=CARTESIAN_POINT ( 'NONE',  ( 0.3622758884714600280, 43.10531414739104150, 0.8252992914329575491 ) ) ;
#6460=ADVANCED_FACE ( 'NONE', ( #60029 ), #23783, .F. ) ;
#6465=VERTEX_POINT ( 'NONE', #26518 ) ;
#6472=EDGE_LOOP ( 'NONE', ( #12224, #55308, #22603, #6736 ) ) ;
#6476=CARTESIAN_POINT ( 'NONE',  ( -5.995132425357893702, -14.94489030678143493, -11.47834865841111451 ) ) ;
#6481=CARTESIAN_POINT ( 'NONE',  ( 4.549368137175248350, 24.02461520945271900, -35.57418903283089406 ) ) ;
#6483=CARTESIAN_POINT ( 'NONE',  ( 0.1073791018717578927, 30.14884492832347718, 30.83464511437148659 ) ) ;
#6489=EDGE_LOOP ( 'NONE', ( #15221, #26737, #59392, #23914 ) ) ;
#6491=CARTESIAN_POINT ( 'NONE',  ( -6.016104459813371719, 11.47525878590916193, 14.94608397322088678 ) ) ;
#6499=CARTESIAN_POINT ( 'NONE',  ( -6.015611763856276717, 18.20278301740943405, -4.870987357967985432 ) ) ;
#6510=PLANE ( 'NONE',  #44955 ) ;
#6513=CARTESIAN_POINT ( 'NONE',  ( 0.1103744047535531458, -41.66501489234570954, 11.12399292196364442 ) ) ;
#6517=B_SPLINE_CURVE_WITH_KNOTS ( 'NONE', 3,
 ( #45244, #17032, #40243, #41463, #59296, #12645 ),
 .UNSPECIFIED., .F., .F.,
 ( 4, 2, 4 ),
 ( 3.511543213478341086E-18, 0.0002450742804987343930, 0.0004901485609974652081 ),
 .UNSPECIFIED. ) ;
#6522=CARTESIAN_POINT ( 'NONE',  ( 1.827326673878743923, 41.24690799101790617, 12.32830836993835177 ) ) ;
#6524=CARTESIAN_POINT ( 'NONE',  ( 0.8760168074886960365, -13.30888447662112561, 46.22580377597762435 ) ) ;
#6530=CARTESIAN_POINT ( 'NONE',  ( -2.569797478183783568, -10.02484965418648599, 10.65947181927822207 ) ) ;
#6534=B_SPLINE_CURVE_WITH_KNOTS ( 'NONE', 3,
 ( #48341, #14536, #29224, #58634 ),
 .UNSPECIFIED., .F., .F.,
 ( 4, 4 ),
 ( 2.318063799052743651E-17, 0.004564976165746187711 ),
 .UNSPECIFIED. ) ;
#6538=DIRECTION ( 'NONE',  ( 0.09835009131224552170, 0.5042575517176567379, 0.8579344853044360564 ) ) ;
#6544=CARTESIAN_POINT ( 'NONE',  ( 0.6031356219577718170, 24.12932366310808519, 41.61861914321219302 ) ) ;
#6553=VERTEX_POINT ( 'NONE', #38411 ) ;
#6554=CARTESIAN_POINT ( 'NONE',  ( -6.001507490154110336, 13.33564355450108430, 13.31361390284164692 ) ) ;
#6558=CARTESIAN_POINT ( 'NONE',  ( 3.680974057930773924, -45.82782223000864974, -14.19449211152921997 ) ) ;
#6560=CARTESIAN_POINT ( 'NONE',  ( 3.680882792899936362, -16.63701193714018700, 44.99870212802612457 ) ) ;
#6562=ORIENTED_EDGE ( 'NONE', *, *, #36899, .F. ) ;
#6563=CARTESIAN_POINT ( 'NONE',  ( 4.322998006666179727, -32.40067585697823205, 35.39923696758956595 ) ) ;
#6575=CIRCLE ( 'NONE', #54567, 47.91270532121795611 ) ;
#6577=CARTESIAN_POINT ( 'NONE',  ( -6.016104459813371719, -11.47525878590906423, -14.94608397322096138 ) ) ;
#6578=EDGE_CURVE ( 'NONE', #50243, #226, #4537, .T. ) ;
#6581=CIRCLE ( 'NONE', #60618, 47.91270532121795611 ) ;
#6584=CARTESIAN_POINT ( 'NONE',  ( 0.7048096507298635682, -47.58126109679107429, 7.115188260603041215 ) ) ;
#6603=CARTESIAN_POINT ( 'NONE',  ( -6.016761891674565099, 16.31696541414272161, 9.424569481870310739 ) ) ;
#6610=CARTESIAN_POINT ( 'NONE',  ( 0.6030672727741701600, -18.49051564326162023, 44.41203814406376438 ) ) ;
#6615=CARTESIAN_POINT ( 'NONE',  ( 0.8751705887134553219, 13.30665218149297857, 46.21789262997761938 ) ) ;
#6623=CARTESIAN_POINT ( 'NONE',  ( -4.908599999999998964, 12.80000000000000071, 3.000000000000000000 ) ) ;
#6630=CARTESIAN_POINT ( 'NONE',  ( 0.1100247026804066219, 34.10937070541709204, 26.38690693952968758 ) ) ;
#6640=CARTESIAN_POINT ( 'NONE',  ( 5.880360259849752858, 47.04104239318753855, 9.405269135695407456 ) ) ;
#6641=CARTESIAN_POINT ( 'NONE',  ( 0.6023143664670691511, -6.538774821499543144, 47.66103278671578636 ) ) ;
#6649=CARTESIAN_POINT ( 'NONE',  ( 0.6023142530420679819, -6.538792732869529445, -47.66103033449096671 ) ) ;
#6653=VECTOR ( 'NONE', #61284, 1000.000000000000000 ) ;
#6660=CARTESIAN_POINT ( 'NONE',  ( -6.015611763856276717, -18.19956619163654565, -4.882992715191491584 ) ) ;
#6661=CARTESIAN_POINT ( 'NONE',  ( 0.3622758884714600280, 11.95365414648497193, -41.42293301073613776 ) ) ;
#6664=EDGE_CURVE ( 'NONE', #23991, #14306, #24553, .T. ) ;
#6665=ORIENTED_EDGE ( 'NONE', *, *, #57751, .T. ) ;
#6668=CARTESIAN_POINT ( 'NONE',  ( 0.6028618097248864549, 6.452328974162978348, 47.67286800277445735 ) ) ;
#6670=EDGE_CURVE ( 'NONE', #31157, #2500, #39553, .T. ) ;
#6671=VERTEX_POINT ( 'NONE', #24290 ) ;
#6675=AXIS2_PLACEMENT_3D ( 'NONE', #41405, #55456, #40477 ) ;
#6678=FACE_OUTER_BOUND ( 'NONE', #18161, .T. ) ;
#6680=B_SPLINE_CURVE_WITH_KNOTS ( 'NONE', 3,
 ( #18376, #37490, #56567, #13681 ),
 .UNSPECIFIED., .F., .F.,
 ( 4, 4 ),
 ( 0.000000000000000000, 0.005014147105413704723 ),
 .UNSPECIFIED. ) ;
#6682=CARTESIAN_POINT ( 'NONE',  ( -6.016761891674565099, 18.84319130225482297, 0.003433883959850178927 ) ) ;
#6684=ORIENTED_EDGE ( 'NONE', *, *, #11551, .T. ) ;
#6687=CARTESIAN_POINT ( 'NONE',  ( 0.5998501479064708430, 44.64337787626247689, -17.92509395669061689 ) ) ;
#6688=CARTESIAN_POINT ( 'NONE',  ( -5.995132425357893702, 9.429450169548182714, -16.31525984181023148 ) ) ;
#6689=ORIENTED_EDGE ( 'NONE', *, *, #17053, .T. ) ;
#6690=CARTESIAN_POINT ( 'NONE',  ( -5.995132425357893702, -18.20425902871271262, 4.869002713216508127 ) ) ;
#6694=ADVANCED_FACE ( 'NONE', ( #14914 ), #30168, .F. ) ;
#6696=CARTESIAN_POINT ( 'NONE',  ( 0.6009453534118438522, 18.00606795643212621, 44.61081284455538309 ) ) ;
#6703=EDGE_LOOP ( 'NONE', ( #32876, #36871, #29626, #13580 ) ) ;
#6707=CARTESIAN_POINT ( 'NONE',  ( 0.1073791018717578927, 39.65380858626191696, 16.95003405440326816 ) ) ;
#6713=DIRECTION ( 'NONE',  ( 0.09835009131224550782, 0.1375559175655161059, 0.9855991218957035338 ) ) ;
#6720=ORIENTED_EDGE ( 'NONE', *, *, #42025, .F. ) ;
#6722=DIRECTION ( 'NONE',  ( 1.000000000000000000, 0.000000000000000000, 0.000000000000000000 ) ) ;
#6725=CARTESIAN_POINT ( 'NONE',  ( 3.238741278300274917, -31.66556122967977771, 29.07934833201312941 ) ) ;
#6729=CARTESIAN_POINT ( 'NONE',  ( 4.975801465491695552, -32.01766832630288206, -35.64402118370946937 ) ) ;
#6736=ORIENTED_EDGE ( 'NONE', *, *, #53649, .F. ) ;
#6737=CARTESIAN_POINT ( 'NONE',  ( 0.1073791018717578927, -34.50606437925563341, 25.86618856530653687 ) ) ;
#6739=CARTESIAN_POINT ( 'NONE',  ( 0.1087620492084205998, 16.16798550313366434, 39.97903073778071814 ) ) ;
#6741=VERTEX_POINT ( 'NONE', #20221 ) ;
#6743=CARTESIAN_POINT ( 'NONE',  ( 0.8751705887134553219, 0.8911681664081729792, 48.08707113907595243 ) ) ;
#6744=CARTESIAN_POINT ( 'NONE',  ( -6.016761891674564211, -14.94721834528423088, 11.47373234755497862 ) ) ;
#6745=B_SPLINE_CURVE_WITH_KNOTS ( 'NONE', 3,
 ( #18332, #52124, #42758, #3574, #37763, #51501 ),
 .UNSPECIFIED., .F., .F.,
 ( 4, 2, 4 ),
 ( 0.000000000000000000, 0.0002450742804987321162, 0.0004901485609974642324 ),
 .UNSPECIFIED. ) ;
#6750=EDGE_CURVE ( 'NONE', #59272, #4442, #14146, .T. ) ;
#6757=CARTESIAN_POINT ( 'NONE',  ( 0.3622758884714730732, -10.35929834645951964, 41.85013935980084199 ) ) ;
#6762=CARTESIAN_POINT ( 'NONE',  ( 4.549368137175248350, -35.80950303116117794, 23.67244292351576718 ) ) ;
#6765=CARTESIAN_POINT ( 'NONE',  ( 0.2885697896453111033, -36.93108635218683844, -22.25146201964130555 ) ) ;
#6771=CARTESIAN_POINT ( 'NONE',  ( -6.015611763856276717, 16.32183393015609951, -9.416239407363130809 ) ) ;
#6777=EDGE_CURVE ( 'NONE', #14733, #33003, #19354, .T. ) ;
#6783=CARTESIAN_POINT ( 'NONE',  ( 0.2885697896453112699, 41.43179225254749554, 11.93479333319038993 ) ) ;
#6789=FACE_OUTER_BOUND ( 'NONE', #55397, .T. ) ;
#6790=EDGE_CURVE ( 'NONE', #11251, #13823, #49287, .T. ) ;
#6791=ORIENTED_EDGE ( 'NONE', *, *, #55460, .T. ) ;
#6794=CARTESIAN_POINT ( 'NONE',  ( -2.708315649062910779, 2.171184472130682774, -14.47261168455367653 ) ) ;
#6797=CARTESIAN_POINT ( 'NONE',  ( 0.1100247026804066219, -5.460606496326611214, -42.77732815928598598 ) ) ;
#6799=CARTESIAN_POINT ( 'NONE',  ( 0.8760168074886960365, 5.394043284318862597, 47.80016357497251533 ) ) ;
#6800=ORIENTED_EDGE ( 'NONE', *, *, #46870, .F. ) ;
#6804=VERTEX_POINT ( 'NONE', #40277 ) ;
#6806=B_SPLINE_CURVE_WITH_KNOTS ( 'NONE', 3,
 ( #35492, #39582, #16684, #30765, #1944, #31087, #54243, #44907, #15764, #21380, #58635, #40511, #34558, #45513, #20764, #34871, #2565, #16369, #25767 ),
 .UNSPECIFIED., .F., .F.,
 ( 4, 3, 3, 3, 3, 3, 4 ),
 ( 1.161276725443423652E-16, 0.0002618519381806260794, 0.0003927759815485985773, 0.0005237000248299448395, 0.0006546240681325003188, 0.0007855481115631321671, 0.0009699050456655092071 ),
 .UNSPECIFIED. ) ;
#6808=B_SPLINE_CURVE_WITH_KNOTS ( 'NONE', 3,
 ( #30063, #44204, #49172, #15680 ),
 .UNSPECIFIED., .F., .F.,
 ( 4, 4 ),
 ( 0.000000000000000000, 0.005014147105413699519 ),
 .UNSPECIFIED. ) ;
#6814=CARTESIAN_POINT ( 'NONE',  ( 0.6001305935487315502, 44.64600790884055215, -17.92615948558493599 ) ) ;
#6820=EDGE_CURVE ( 'NONE', #4388, #2051, #24604, .T. ) ;
#6824=EDGE_CURVE ( 'NONE', #27931, #16986, #5107, .T. ) ;
#6825=VERTEX_POINT ( 'NONE', #8480 ) ;
#6831=FACE_OUTER_BOUND ( 'NONE', #12213, .T. ) ;
#6834=CARTESIAN_POINT ( 'NONE',  ( 0.1098349054025745952, -41.70974743324821787, 10.95525583467203745 ) ) ;
#6837=CARTESIAN_POINT ( 'NONE',  ( 4.975801465491695552, 31.15993731089124097, -36.39623109580435312 ) ) ;
#6842=EDGE_CURVE ( 'NONE', #22443, #10591, #50723, .T. ) ;
#6843=CARTESIAN_POINT ( 'NONE',  ( 4.549368137175248350, 18.79584381673477012, 38.59302160394760506 ) ) ;
#6851=ORIENTED_EDGE ( 'NONE', *, *, #50571, .T. ) ;
#6854=ORIENTED_EDGE ( 'NONE', *, *, #6578, .F. ) ;
#6856=B_SPLINE_CURVE_WITH_KNOTS ( 'NONE', 3,
 ( #39896, #1017, #29527, #39578, #53622, #58955 ),
 .UNSPECIFIED., .F., .F.,
 ( 4, 2, 4 ),
 ( 1.807478856737577690E-17, 0.0002293319059085094391, 0.0004586638118170007720 ),
 .UNSPECIFIED. ) ;
#6858=ORIENTED_EDGE ( 'NONE', *, *, #11690, .T. ) ;
#6869=EDGE_LOOP ( 'NONE', ( #39580, #48031, #41890, #43013 ) ) ;
#6878=CARTESIAN_POINT ( 'NONE',  ( 0.1104177457020373010, -42.75615561261997755, -5.624018123398488278 ) ) ;
#6888=SURFACE_STYLE_FILL_AREA ( #2510 ) ;
#6903=LINE ( 'NONE', #20725, #29183 ) ;
#6907=CARTESIAN_POINT ( 'NONE',  ( 3.238741278300272697, -41.01623499586005295, -12.88350628398725917 ) ) ;
#6917=CARTESIAN_POINT ( 'NONE',  ( -2.569797478183783568, -14.44232325624828306, 2.353985772484507244 ) ) ;
#6918=( BOUNDED_SURFACE ( )  B_SPLINE_SURFACE ( 3, 1, ( 
 ( #58691, #18747 ),
 ( #23130, #19917 ),
 ( #39028, #58083 ),
 ( #61319, #15818 ) ),
 .UNSPECIFIED., .F., .F., .F. ) 
 B_SPLINE_SURFACE_WITH_KNOTS ( ( 4, 4 ),
 ( 2, 2 ),
 ( 0.000000000000000000, 1.000000000000000000 ),
 ( 0.000000000000000000, 1.000000000000000000 ),
 .UNSPECIFIED. ) 
 GEOMETRIC_REPRESENTATION_ITEM ( )  RATIONAL_B_SPLINE_SURFACE ( (
 ( 1.000000000000000000, 1.000000000000000000),
 ( 0.7223157951917476005, 0.9931996967497186413),
 ( 0.7223157951917476005, 0.9931996967497186413),
 ( 1.000000000000000000, 1.000000000000000000) ) ) 
 REPRESENTATION_ITEM ( '' )  SURFACE ( )  );
#6922=B_SPLINE_CURVE_WITH_KNOTS ( 'NONE', 3,
 ( #17600, #7241, #41123, #18222 ),
 .UNSPECIFIED., .F., .F.,
 ( 4, 4 ),
 ( 2.122407100861210359E-17, 0.004444306975806114161 ),
 .UNSPECIFIED. ) ;
#6927=ORIENTED_EDGE ( 'NONE', *, *, #38793, .F. ) ;
#6931=CARTESIAN_POINT ( 'NONE',  ( 0.1100053167205930910, 0.1794603581038460294, 43.12409768020066281 ) ) ;
#6934=EDGE_LOOP ( 'NONE', ( #37729, #6720, #9035, #33413 ) ) ;
#6936=VECTOR ( 'NONE', #18674, 999.9999999999998863 ) ;
#6938=CARTESIAN_POINT ( 'NONE',  ( 0.1103878639767399694, -30.45925431905134317, 30.52789484587400892 ) ) ;
#6943=CARTESIAN_POINT ( 'NONE',  ( -6.010958268070873523, -16.31164801516935370, -9.434296419346379636 ) ) ;
#6945=CARTESIAN_POINT ( 'NONE',  ( 0.8751705887134553219, 0.8911681664081729792, 48.08707113907595243 ) ) ;
#6954=CARTESIAN_POINT ( 'NONE',  ( 4.975801465491694664, 26.14269827151623105, 40.15204426031542795 ) ) ;
#6956=CARTESIAN_POINT ( 'NONE',  ( 0.1081432562775997558, -40.00205417854824219, 16.11101151263754616 ) ) ;
#6964=CARTESIAN_POINT ( 'NONE',  ( 4.549368137175248350, -42.06008734272402450, 8.582197505783685898 ) ) ;
#6965=CARTESIAN_POINT ( 'NONE',  ( 0.1073791018717483448, -11.62916352156123168, -41.52698815987163528 ) ) ;
#6968=DIRECTION ( 'NONE',  ( 0.09835009131224552170, 0.9876177374393958486, 0.1222230102475044128 ) ) ;
#6969=CARTESIAN_POINT ( 'NONE',  ( 0.6017666602106490625, -6.625262199740747704, -47.64919188470826583 ) ) ;
#6970=B_SPLINE_CURVE_WITH_KNOTS ( 'NONE', 3,
 ( #36634, #61629, #41643, #8106, #56325, #4003, #51628, #47257, #23141, #60708, #32237, #60396, #42270, #4306, #12835, #23444, #61028, #8720, #27524 ),
 .UNSPECIFIED., .F., .F.,
 ( 4, 3, 3, 3, 3, 3, 4 ),
 ( 1.165802754517233128E-16, 0.0002618519381806274889, 0.0003927759815485978726, 0.0005237000248299410448, 0.0006546240681324946810, 0.0007855481115631296734, 0.0009699050456655074724 ),
 .UNSPECIFIED. ) ;
#6972=ADVANCED_FACE ( 'NONE', ( #34174 ), #38614, .F. ) ;
#6975=CARTESIAN_POINT ( 'NONE',  ( 0.3622758884714730732, 43.10531414739106282, -0.8252992914323589169 ) ) ;
#6976=VERTEX_POINT ( 'NONE', #48265 ) ;
#6980=CARTESIAN_POINT ( 'NONE',  ( 5.880360259849752858, 36.03610316515339917, 31.66572319753574405 ) ) ;
#6982=ORIENTED_EDGE ( 'NONE', *, *, #21171, .T. ) ;
#6988=VERTEX_POINT ( 'NONE', #52321 ) ;
#6994=CARTESIAN_POINT ( 'NONE',  ( -6.016761891674565099, 2.456125503350710115, 18.68243340030203470 ) ) ;
#6998=B_SPLINE_CURVE_WITH_KNOTS ( 'NONE', 3,
 ( #43788, #19965, #6118, #34365, #53135, #34991 ),
 .UNSPECIFIED., .F., .F.,
 ( 4, 2, 4 ),
 ( 1.272149902321906704E-16, 0.0002450741128632372211, 0.0004901482257263471568 ),
 .UNSPECIFIED. ) ;
#6999=CARTESIAN_POINT ( 'NONE',  ( -6.016489644550737204, 18.84320342686341121, 0.004404229197842324944 ) ) ;
#7004=CARTESIAN_POINT ( 'NONE',  ( -2.708315649062910779, -14.06540004355479923, -4.041664582652747306 ) ) ;
#7005=ORIENTED_EDGE ( 'NONE', *, *, #15232, .F. ) ;
#7018=EDGE_CURVE ( 'NONE', #25568, #20738, #34214, .T. ) ;
#7020=FACE_OUTER_BOUND ( 'NONE', #56354, .T. ) ;
#7021=CARTESIAN_POINT ( 'NONE',  ( 4.975801465491695552, 47.84403947906839960, 2.564218696447662982 ) ) ;
#7023=CARTESIAN_POINT ( 'NONE',  ( -6.015611763856276717, -4.882992715191428523, 18.19956619163656697 ) ) ;
#7027=CARTESIAN_POINT ( 'NONE',  ( 0.1100053167205930910, -42.73174076921948483, 5.806749312984397449 ) ) ;
#7028=CARTESIAN_POINT ( 'NONE',  ( 0.1064266379913941657, -22.04679939086809171, -37.06314005629904784 ) ) ;
#7030=CARTESIAN_POINT ( 'NONE',  ( 0.6023142530420679819, -41.53076277789759274, 24.28014345169096799 ) ) ;
#7037=EDGE_CURVE ( 'NONE', #32714, #17539, #42433, .T. ) ;
#7038=CARTESIAN_POINT ( 'NONE',  ( 0.1073791018717483448, 21.98088480513615295, 37.10214135362896570 ) ) ;
#7039=CARTESIAN_POINT ( 'NONE',  ( -2.569797478183783568, 7.701637110048508816, 12.44213550320655948 ) ) ;
#7046=B_SPLINE_CURVE_WITH_KNOTS ( 'NONE', 3,
 ( #59499, #60123, #36653, #8417 ),
 .UNSPECIFIED., .F., .F.,
 ( 4, 4 ),
 ( 0.000000000000000000, 0.005014147105413698652 ),
 .UNSPECIFIED. ) ;
#7049=LINE ( 'NONE', #32128, #11900 ) ;
#7052=CARTESIAN_POINT ( 'NONE',  ( 0.3622758884714600280, -6.444611261694905835, 42.62881903538198713 ) ) ;
#7055=ORIENTED_EDGE ( 'NONE', *, *, #24347, .F. ) ;
#7056=CARTESIAN_POINT ( 'NONE',  ( 0.2885697896453132127, -34.69058521462552847, 25.60460893337419108 ) ) ;
#7066=CARTESIAN_POINT ( 'NONE',  ( 0.1073791018717578927, -25.86618856530687793, -34.50606437925538472 ) ) ;
#7074=CARTESIAN_POINT ( 'NONE',  ( 0.8751705887134423323, 0.8911681664088411114, -48.08707113907595243 ) ) ;
#7079=ORIENTED_EDGE ( 'NONE', *, *, #52702, .T. ) ;
#7090=CARTESIAN_POINT ( 'NONE',  ( 0.2885697896453108813, -31.05173034173391855, 29.91358794843008440 ) ) ;
#7102=CARTESIAN_POINT ( 'NONE',  ( -6.015611763856276717, -14.94556629257417590, -11.47596948473826650 ) ) ;
#7105=ORIENTED_EDGE ( 'NONE', *, *, #29261, .F. ) ;
#7109=CARTESIAN_POINT ( 'NONE',  ( 0.2224561200757624035, 41.84032767736802327, -10.42482236669260054 ) ) ;
#7112=EDGE_LOOP ( 'NONE', ( #37948, #58035, #21921, #45166 ) ) ;
#7113=ADVANCED_FACE ( 'NONE', ( #32845 ), #45032, .F. ) ;
#7124=CARTESIAN_POINT ( 'NONE',  ( 0.6027935024548037868, 38.05972402498736784, 29.42425667880449325 ) ) ;
#7130=CARTESIAN_POINT ( 'NONE',  ( 0.8751705887134553219, 11.58504748649199811, -46.67919521768876479 ) ) ;
#7132=EDGE_CURVE ( 'NONE', #15054, #28479, #15578, .T. ) ;
#7133=CARTESIAN_POINT ( 'NONE',  ( 4.833616638992205949, 43.64812679991096900, 15.29495699393742036 ) ) ;
#7134=B_SPLINE_CURVE_WITH_KNOTS ( 'NONE', 3,
 ( #16688, #31090, #50192, #7255, #31399, #26384 ),
 .UNSPECIFIED., .F., .F.,
 ( 4, 2, 4 ),
 ( 1.269611854458016711E-16, 0.0002450741128632349442, 0.0004901482257263429284 ),
 .UNSPECIFIED. ) ;
#7138=( BOUNDED_SURFACE ( )  B_SPLINE_SURFACE ( 3, 1, ( 
 ( #24818, #55466 ),
 ( #60469, #21355 ),
 ( #45488, #54528 ),
 ( #2221, #31683 ) ),
 .UNSPECIFIED., .F., .F., .F. ) 
 B_SPLINE_SURFACE_WITH_KNOTS ( ( 4, 4 ),
 ( 2, 2 ),
 ( 0.000000000000000000, 1.000000000000000000 ),
 ( 0.000000000000000000, 1.000000000000000000 ),
 .UNSPECIFIED. ) 
 GEOMETRIC_REPRESENTATION_ITEM ( )  RATIONAL_B_SPLINE_SURFACE ( (
 ( 1.000000000000000000, 1.000000000000000000),
 ( 0.9953040768229005630, 0.8617119497784937465),
 ( 0.9953040768229005630, 0.8617119497784937465),
 ( 1.000000000000000000, 1.000000000000000000) ) ) 
 REPRESENTATION_ITEM ( '' )  SURFACE ( )  );
#7140=CARTESIAN_POINT ( 'NONE',  ( 0.1081432562775998946, 37.13343246403895392, 21.92800090985282679 ) ) ;
#7145=CARTESIAN_POINT ( 'NONE',  ( 4.549368137175248350, 13.59764261105751793, -40.71620287708331176 ) ) ;
#7153=CARTESIAN_POINT ( 'NONE',  ( 0.8751705887134423323, -24.81530984069236823, 41.19904111682465242 ) ) ;
#7154=CARTESIAN_POINT ( 'NONE',  ( 0.6041374136657475802, 33.89363087703001298, 34.14050483116148627 ) ) ;
#7159=CARTESIAN_POINT ( 'NONE',  ( 0.1104177457020373010, -26.25638621857967792, -34.20994892372200979 ) ) ;
#7160=EDGE_LOOP ( 'NONE', ( #28295, #38709, #37095, #61409 ) ) ;
#7163=CARTESIAN_POINT ( 'NONE',  ( -6.010958268070873523, 9.409153349053815063, -16.32616437357102157 ) ) ;
#7164=ORIENTED_EDGE ( 'NONE', *, *, #480, .F. ) ;
#7165=CARTESIAN_POINT ( 'NONE',  ( -6.010958268070873523, -0.01451635840176482631, 18.84344976839986785 ) ) ;
#7173=CARTESIAN_POINT ( 'NONE',  ( 0.5980894510889448457, 41.31170365136853917, 24.66136644716835491 ) ) ;
#7182=FACE_OUTER_BOUND ( 'NONE', #39196, .T. ) ;
#7184=VERTEX_POINT ( 'NONE', #14518 ) ;
#7185=CARTESIAN_POINT ( 'NONE',  ( 0.1081432562775997003, -42.69830087850308331, -6.048481838665884958 ) ) ;
#7188=CARTESIAN_POINT ( 'NONE',  ( 4.549368137175248350, 0.000000000000000000, 0.000000000000000000 ) ) ;
#7191=B_SPLINE_CURVE_WITH_KNOTS ( 'NONE', 3,
 ( #5715, #1335, #33970, #39600, #11081, #39291 ),
 .UNSPECIFIED., .F., .F.,
 ( 4, 2, 4 ),
 ( 1.807478856737577690E-17, 0.0002293319059085093307, 0.0004586638118170005551 ),
 .UNSPECIFIED. ) ;
#7200=CARTESIAN_POINT ( 'NONE',  ( 0.5998501479064708430, -5.759754759340450114, -47.76154736470756745 ) ) ;
#7205=CARTESIAN_POINT ( 'NONE',  ( 4.975801465491695552, -3.702618843597113685, -47.76942479135485087 ) ) ;
#7224=EDGE_CURVE ( 'NONE', #17384, #40739, #27986, .T. ) ;
#7227=CARTESIAN_POINT ( 'NONE',  ( 3.238741278300274029, 38.11287256318061623, -19.89284324544654226 ) ) ;
#7241=CARTESIAN_POINT ( 'NONE',  ( 2.301529144917015213, 17.18548816179623628, -44.85388898587007134 ) ) ;
#7250=CARTESIAN_POINT ( 'NONE',  ( 4.691466044806102076, -3.249105306918757652, 44.46979273209129246 ) ) ;
#7255=CARTESIAN_POINT ( 'NONE',  ( 0.6254311100348668440, -47.77988293940239117, 5.596225872411223712 ) ) ;
#7256=ORIENTED_EDGE ( 'NONE', *, *, #942, .F. ) ;
#7263=ORIENTED_EDGE ( 'NONE', *, *, #56554, .T. ) ;
#7265=EDGE_CURVE ( 'NONE', #42991, #51963, #14797, .T. ) ;
#7272=CARTESIAN_POINT ( 'NONE',  ( 4.322998006666179727, 46.85697641700694049, 10.36018990813329310 ) ) ;
#7274=CARTESIAN_POINT ( 'NONE',  ( 0.1064266379913944155, -15.98292486309362737, 40.05351204369879525 ) ) ;
#7279=CARTESIAN_POINT ( 'NONE',  ( 4.975801465491695552, 0.000000000000000000, 0.000000000000000000 ) ) ;
#7282=CARTESIAN_POINT ( 'NONE',  ( -6.010958268070873523, -4.891065400978257038, -18.19761767765835359 ) ) ;
#7285=CARTESIAN_POINT ( 'NONE',  ( 3.238931869106854489, 42.95312220797017488, -1.828840280768938120 ) ) ;
#7286=ORIENTED_EDGE ( 'NONE', *, *, #36924, .F. ) ;
#7290=CARTESIAN_POINT ( 'NONE',  ( 4.322998006666179727, 35.39923696758967964, 32.40067585697811126 ) ) ;
#7292=ORIENTED_EDGE ( 'NONE', *, *, #12343, .F. ) ;
#7294=CARTESIAN_POINT ( 'NONE',  ( 0.1073791018717578927, -37.58707531572220262, 21.14095454447495115 ) ) ;
#7297=ORIENTED_EDGE ( 'NONE', *, *, #1057, .T. ) ;
#7299=ADVANCED_FACE ( 'NONE', ( #48022 ), #47755, .F. ) ;
#7305=ORIENTED_EDGE ( 'NONE', *, *, #43973, .T. ) ;
#7327=CARTESIAN_POINT ( 'NONE',  ( 4.975801465491695552, 0.000000000000000000, 0.000000000000000000 ) ) ;
#7329=CARTESIAN_POINT ( 'NONE',  ( 0.1073791018717483448, -5.147744207007177053, 42.81622261970985477 ) ) ;
#7331=CARTESIAN_POINT ( 'NONE',  ( 0.7954196712028466232, 7.138712347928183988, -47.56618050291067590 ) ) ;
#7344=CARTESIAN_POINT ( 'NONE',  ( 0.6041374136657476912, -6.452348380035592967, -47.67304777898696955 ) ) ;
#7345=LINE ( 'NONE', #7039, #27821 ) ;
#7351=CARTESIAN_POINT ( 'NONE',  ( 3.680882792899937250, 1.849662971457552540, 47.94008871805920080 ) ) ;
#7352=EDGE_CURVE ( 'NONE', #41987, #41115, #50606, .T. ) ;
#7358=CARTESIAN_POINT ( 'NONE',  ( 0.6030672727741701600, -44.47882233696937249, 18.32928433899675014 ) ) ;
#7360=CARTESIAN_POINT ( 'NONE',  ( 0.7954190325252783467, -29.96539637359188646, -37.62416463577099535 ) ) ;
#7363=ORIENTED_EDGE ( 'NONE', *, *, #38549, .T. ) ;
#7367=VERTEX_POINT ( 'NONE', #26283 ) ;
#7370=CARTESIAN_POINT ( 'NONE',  ( 0.5998501479064708430, 41.39809967730453621, 24.50586714782619424 ) ) ;
#7371=VERTEX_POINT ( 'NONE', #15434 ) ;
#7372=ORIENTED_EDGE ( 'NONE', *, *, #61197, .T. ) ;
#7375=CARTESIAN_POINT ( 'NONE',  ( 0.7048096507298579061, -17.62869676200378066, -44.76417498422306807 ) ) ;
#7378=CARTESIAN_POINT ( 'NONE',  ( 1.827326673878743923, -4.394636550976340317, -42.82501343454093501 ) ) ;
#7381=ORIENTED_EDGE ( 'NONE', *, *, #56045, .T. ) ;
#7392=VERTEX_POINT ( 'NONE', #36029 ) ;
#7393=CARTESIAN_POINT ( 'NONE',  ( 0.6017666602106489515, -47.74032907933394654, -5.933006478840522568 ) ) ;
#7398=ORIENTED_EDGE ( 'NONE', *, *, #11110, .T. ) ;
#7399=CARTESIAN_POINT ( 'NONE',  ( 0.09136607875274982415, 0.000000000000000000, 0.000000000000000000 ) ) ;
#7400=CARTESIAN_POINT ( 'NONE',  ( 0.2224561200757621260, -42.84309024201780147, 4.874377913225771408 ) ) ;
#7407=CARTESIAN_POINT ( 'NONE',  ( -6.017396004339687465, 0.001173774849245718494, -18.84316306185412415 ) ) ;
#7408=CARTESIAN_POINT ( 'NONE',  ( 0.7245667037590747261, 44.12005358974304414, -19.16327388244015495 ) ) ;
#7410=ORIENTED_EDGE ( 'NONE', *, *, #49220, .F. ) ;
#7413=CARTESIAN_POINT ( 'NONE',  ( 4.975801465491695552, 0.000000000000000000, 0.000000000000000000 ) ) ;
#7416=EDGE_CURVE ( 'NONE', #49781, #10248, #29757, .T. ) ;
#7421=CARTESIAN_POINT ( 'NONE',  ( 0.1092355843206037486, 30.28032287551036816, 30.70542469027335031 ) ) ;
#7423=CARTESIAN_POINT ( 'NONE',  ( 4.549368137175248350, 35.80950303116100741, -23.67244292351601942 ) ) ;
#7426=CARTESIAN_POINT ( 'NONE',  ( 0.5998501479064708430, 6.798102206414135651, -47.62484632993681544 ) ) ;
#7427=ORIENTED_EDGE ( 'NONE', *, *, #23305, .F. ) ;
#7431=EDGE_CURVE ( 'NONE', #29097, #56408, #49563, .T. ) ;
#7432=CARTESIAN_POINT ( 'NONE',  ( -6.017396004339687465, -14.94857180791985130, -11.47192209077602776 ) ) ;
#7447=ORIENTED_EDGE ( 'NONE', *, *, #56084, .F. ) ;
#7449=CARTESIAN_POINT ( 'NONE',  ( 0.1101816497532063094, 43.12424935764384060, -0.1358190954551057039 ) ) ;
#7458=LINE ( 'NONE', #10967, #8517 ) ;
#7461=EDGE_CURVE ( 'NONE', #11438, #18533, #46989, .T. ) ;
#7465=CARTESIAN_POINT ( 'NONE',  ( 0.6009452777970409887, -28.93864923253926946, 38.43042656245023636 ) ) ;
#7469=ORIENTED_EDGE ( 'NONE', *, *, #60436, .F. ) ;
#7473=ORIENTED_EDGE ( 'NONE', *, *, #23305, .T. ) ;
#7475=ORIENTED_EDGE ( 'NONE', *, *, #37879, .T. ) ;
#7479=EDGE_CURVE ( 'NONE', #11294, #2547, #61025, .T. ) ;
#7481=CARTESIAN_POINT ( 'NONE',  ( -6.016761891674564211, -9.424569481870138432, -16.31696541414282109 ) ) ;
#7486=CARTESIAN_POINT ( 'NONE',  ( 0.6031356219577718170, 44.47888959008672316, 18.32926896140846296 ) ) ;
#7496=CARTESIAN_POINT ( 'NONE',  ( 0.1073791018717483448, -21.98088480513640874, -37.10214135362880228 ) ) ;
#7499=CARTESIAN_POINT ( 'NONE',  ( 0.1102847568649952675, -42.76743495471826151, -5.537466591275519434 ) ) ;
#7503=CARTESIAN_POINT ( 'NONE',  ( -6.015611763856276717, 13.32857883366851937, -13.31979030221785365 ) ) ;
#7510=CARTESIAN_POINT ( 'NONE',  ( 0.8751705887134423323, -5.393078191592370452, -47.79200036674278351 ) ) ;
#7514=DIRECTION ( 'NONE',  ( -1.000000000000000000, -0.000000000000000000, -0.000000000000000000 ) ) ;
#7516=CARTESIAN_POINT ( 'NONE',  ( 0.1100053167205930632, 21.40663161100993506, -37.43629428538741877 ) ) ;
#7521=B_SPLINE_CURVE_WITH_KNOTS ( 'NONE', 3,
 ( #55346, #17464, #8056, #32185, #27170, #32495 ),
 .UNSPECIFIED., .F., .F.,
 ( 4, 2, 4 ),
 ( 1.275615807185303638E-16, 0.0002450741128632383595, 0.0004901482257263492168 ),
 .UNSPECIFIED. ) ;
#7522=CARTESIAN_POINT ( 'NONE',  ( 0.3622758884714600280, -0.8252992914331080954, 43.10531414739104150 ) ) ;
#7523=VECTOR ( 'NONE', #54936, 1000.000000000000227 ) ;
#7529=FACE_OUTER_BOUND ( 'NONE', #1003, .T. ) ;
#7533=CARTESIAN_POINT ( 'NONE',  ( 0.8751705887134553219, 47.79200036674271956, 5.393078191592866055 ) ) ;
#7541=ADVANCED_FACE ( 'NONE', ( #12832 ), #2908, .F. ) ;
#7543=ORIENTED_EDGE ( 'NONE', *, *, #38102, .T. ) ;
#7545=EDGE_CURVE ( 'NONE', #14372, #5781, #39585, .T. ) ;
#7546=ORIENTED_EDGE ( 'NONE', *, *, #25338, .F. ) ;
#7556=CARTESIAN_POINT ( 'NONE',  ( 4.975801465491695552, -35.64402118370979622, 32.01766832630250548 ) ) ;
#7567=( BOUNDED_SURFACE ( )  B_SPLINE_SURFACE ( 3, 1, ( 
 ( #9750, #28856 ),
 ( #57641, #14776 ),
 ( #33889, #52965 ),
 ( #29166, #39524 ) ),
 .UNSPECIFIED., .F., .F., .F. ) 
 B_SPLINE_SURFACE_WITH_KNOTS ( ( 4, 4 ),
 ( 2, 2 ),
 ( 0.000000000000000000, 1.000000000000000000 ),
 ( 0.000000000000000000, 1.000000000000000000 ),
 .UNSPECIFIED. ) 
 GEOMETRIC_REPRESENTATION_ITEM ( )  RATIONAL_B_SPLINE_SURFACE ( (
 ( 1.000000000000000000, 1.000000000000000000),
 ( 0.9751682680413298332, 0.9999560080971552356),
 ( 0.9751682680413298332, 0.9999560080971552356),
 ( 1.000000000000000000, 1.000000000000000000) ) ) 
 REPRESENTATION_ITEM ( '' )  SURFACE ( )  );
#7570=CARTESIAN_POINT ( 'NONE',  ( 0.3622758884714600280, 17.25816669464994746, -39.50828911766980411 ) ) ;
#7575=CARTESIAN_POINT ( 'NONE',  ( 0.6017667736363749853, -41.48674115080387281, -24.35549005323402127 ) ) ;
#7583=CARTESIAN_POINT ( 'NONE',  ( 0.6017667736363752073, 6.625250263233628978, -47.64919355032682091 ) ) ;
#7584=ADVANCED_FACE ( 'NONE', ( #43818 ), #15740, .F. ) ;
#7585=( BOUNDED_SURFACE ( )  B_SPLINE_SURFACE ( 3, 1, ( 
 ( #1212, #44182 ),
 ( #16567, #35381 ),
 ( #39789, #52675 ),
 ( #40101, #20958 ) ),
 .UNSPECIFIED., .F., .F., .F. ) 
 B_SPLINE_SURFACE_WITH_KNOTS ( ( 4, 4 ),
 ( 2, 2 ),
 ( 0.000000000000000000, 1.000000000000000000 ),
 ( 0.000000000000000000, 1.000000000000000000 ),
 .UNSPECIFIED. ) 
 GEOMETRIC_REPRESENTATION_ITEM ( )  RATIONAL_B_SPLINE_SURFACE ( (
 ( 1.000000000000000000, 1.000000000000000000),
 ( 0.9953040768229013402, 0.8617119497784988535),
 ( 0.9953040768229013402, 0.8617119497784988535),
 ( 1.000000000000000000, 1.000000000000000000) ) ) 
 REPRESENTATION_ITEM ( '' )  SURFACE ( )  );
#7587=CARTESIAN_POINT ( 'NONE',  ( -6.016489644550737204, -14.95199950534956201, 11.46752133529379414 ) ) ;
#7595=CARTESIAN_POINT ( 'NONE',  ( 0.1073791018717578927, -16.95003405440338895, 39.65380858626186722 ) ) ;
#7597=CARTESIAN_POINT ( 'NONE',  ( 0.6029303876144825880, -6.149480157546260983, -47.71279573267356966 ) ) ;
#7598=CARTESIAN_POINT ( 'NONE',  ( 0.3622758884714730732, -40.13994584881772454, -15.73321244754840720 ) ) ;
#7600=CARTESIAN_POINT ( 'NONE',  ( 4.975801465491695552, -26.14269827151708370, 40.15204426031488794 ) ) ;
#7601=FACE_OUTER_BOUND ( 'NONE', #19359, .T. ) ;
#7602=VERTEX_POINT ( 'NONE', #33474 ) ;
#7603=ORIENTED_EDGE ( 'NONE', *, *, #45100, .F. ) ;
#7607=VERTEX_POINT ( 'NONE', #19998 ) ;
#7609=DIRECTION ( 'NONE',  ( -1.000000000000000000, -0.000000000000000000, -0.000000000000000000 ) ) ;
#7617=EDGE_CURVE ( 'NONE', #9846, #40367, #11811, .T. ) ;
#7619=CARTESIAN_POINT ( 'NONE',  ( -6.016489644550737204, 13.32727118274456579, -13.32104266208085619 ) ) ;
#7624=VERTEX_POINT ( 'NONE', #30288 ) ;
#7628=DIRECTION ( 'NONE',  ( -1.000000000000000000, 0.000000000000000000, 0.000000000000000000 ) ) ;
#7638=VERTEX_POINT ( 'NONE', #58776 ) ;
#7641=B_SPLINE_CURVE_WITH_KNOTS ( 'NONE', 3,
 ( #24294, #43428, #19610, #57785, #44357, #35566 ),
 .UNSPECIFIED., .F., .F.,
 ( 4, 2, 4 ),
 ( 8.492412771929966223E-17, 0.0002293366620881466381, 0.0004586733241762083833 ),
 .UNSPECIFIED. ) ;
#7644=CARTESIAN_POINT ( 'NONE',  ( 0.1073791018717483448, 42.68962945260953035, -6.109314776652274404 ) ) ;
#7648=ORIENTED_EDGE ( 'NONE', *, *, #42294, .F. ) ;
#7650=CARTESIAN_POINT ( 'NONE',  ( 0.3622758884714600280, 34.70015533914828865, -25.58609868863731407 ) ) ;
#7651=CARTESIAN_POINT ( 'NONE',  ( 0.6001305935487315502, -0.5236757026886070809, -48.10757715638248300 ) ) ;
#7653=CARTESIAN_POINT ( 'NONE',  ( -6.015611763856276717, -16.32183393015590056, -9.416239407363475422 ) ) ;
#7655=EDGE_CURVE ( 'NONE', #4461, #11343, #11542, .T. ) ;
#7670=CARTESIAN_POINT ( 'NONE',  ( 0.6254087463353884546, -28.73645667569980233, 38.58044986685640509 ) ) ;
#7673=CARTESIAN_POINT ( 'NONE',  ( 0.6023143664670691511, -44.54505257464873580, 18.16777128831313348 ) ) ;
#7675=CARTESIAN_POINT ( 'NONE',  ( 0.6031356219577718170, 41.61861914321211486, -24.12932366310823440 ) ) ;
#7678=CARTESIAN_POINT ( 'NONE',  ( 0.5998501479064699549, 41.92175333043586960, 23.59887241503369282 ) ) ;
#7680=ORIENTED_EDGE ( 'NONE', *, *, #61314, .F. ) ;
#7695=FACE_OUTER_BOUND ( 'NONE', #23082, .T. ) ;
#7696=EDGE_CURVE ( 'NONE', #34095, #11994, #2391, .T. ) ;
#7697=CARTESIAN_POINT ( 'NONE',  ( 0.1073791018717578927, -10.69234304550026593, -41.77800844988510676 ) ) ;
#7703=CARTESIAN_POINT ( 'NONE',  ( 4.833616638992205949, -9.466882727842460099, 45.27110352095230184 ) ) ;
#7714=CARTESIAN_POINT ( 'NONE',  ( 0.2885700199627498352, 34.69058524452978531, 25.60460887553389853 ) ) ;
#7720=CARTESIAN_POINT ( 'NONE',  ( 4.975801465491695552, 0.000000000000000000, 0.000000000000000000 ) ) ;
#7721=CARTESIAN_POINT ( 'NONE',  ( 0.6031356219577719280, 44.41207482560206188, -18.49057407199411074 ) ) ;
#7725=CARTESIAN_POINT ( 'NONE',  ( -6.016761891674564211, 7.214149619366359900, 17.40752468084784965 ) ) ;
#7730=EDGE_LOOP ( 'NONE', ( #48614, #32134, #34996, #379 ) ) ;
#7737=CARTESIAN_POINT ( 'NONE',  ( 0.5998501479064708430, -18.89267974119696447, 44.24259072156053918 ) ) ;
#7741=CARTESIAN_POINT ( 'NONE',  ( 0.3622758884714730732, 36.91764744403321430, -22.26738722580129348 ) ) ;
#7746=EDGE_LOOP ( 'NONE', ( #3545, #35986, #21379, #59545 ) ) ;
#7752=CARTESIAN_POINT ( 'NONE',  ( 4.833616638992205949, -34.47248434257890182, -30.83411269743551841 ) ) ;
#7759=CARTESIAN_POINT ( 'NONE',  ( 4.549368137175248350, 19.17571786012324608, -38.40568845698256695 ) ) ;
#7760=AXIS2_PLACEMENT_3D ( 'NONE', #13943, #26089, #29547 ) ;
#7763=CARTESIAN_POINT ( 'NONE',  ( -6.001507490154110336, -14.94036486426021249, 11.48377994779695754 ) ) ;
#7768=( BOUNDED_SURFACE ( )  B_SPLINE_SURFACE ( 3, 1, ( 
 ( #20404, #33896 ),
 ( #5345, #15094 ),
 ( #9757, #34203 ),
 ( #53278, #15403 ) ),
 .UNSPECIFIED., .F., .F., .F. ) 
 B_SPLINE_SURFACE_WITH_KNOTS ( ( 4, 4 ),
 ( 2, 2 ),
 ( 0.000000000000000000, 1.000000000000000000 ),
 ( 0.000000000000000000, 1.000000000000000000 ),
 .UNSPECIFIED. ) 
 GEOMETRIC_REPRESENTATION_ITEM ( )  RATIONAL_B_SPLINE_SURFACE ( (
 ( 1.000000000000000000, 1.000000000000000000),
 ( 0.9953040768229013402, 0.8617119497784988535),
 ( 0.9953040768229013402, 0.8617119497784988535),
 ( 1.000000000000000000, 1.000000000000000000) ) ) 
 REPRESENTATION_ITEM ( '' )  SURFACE ( )  );
#7771=ADVANCED_FACE ( 'NONE', ( #50933 ), #17744, .F. ) ;
#7781=AXIS2_PLACEMENT_3D ( 'NONE', #58344, #5419, #16088 ) ;
#7784=CARTESIAN_POINT ( 'NONE',  ( 4.549368137175248350, 40.71620287708324781, 13.59764261105765826 ) ) ;
#7795=B_SPLINE_CURVE_WITH_KNOTS ( 'NONE', 3,
 ( #60219, #11714, #46162, #49915, #59298, #40857, #7597, #26719, #2903, #17332, #27035, #55212, #6649, #6969, #3208, #25796 ),
 .UNSPECIFIED., .F., .F.,
 ( 4, 3, 3, 3, 3, 4 ),
 ( 2.168512762477887481E-17, 0.0002618515315864423021, 0.0003927756766341991296, 0.0005236998216950568058, 0.0007855159896329902240, 0.001047349442285927437 ),
 .UNSPECIFIED. ) ;
#7796=ORIENTED_EDGE ( 'NONE', *, *, #42115, .F. ) ;
#7801=ORIENTED_EDGE ( 'NONE', *, *, #2451, .T. ) ;
#7802=CARTESIAN_POINT ( 'NONE',  ( 0.6001305935487422083, 24.50730504006400423, 41.40054608060301433 ) ) ;
#7804=AXIS2_PLACEMENT_3D ( 'NONE', #16277, #45419, #58546 ) ;
#7809=ORIENTED_EDGE ( 'NONE', *, *, #36316, .T. ) ;
#7820=ORIENTED_EDGE ( 'NONE', *, *, #35961, .F. ) ;
#7821=CARTESIAN_POINT ( 'NONE',  ( 4.549368137175248350, -13.59764261105780214, 40.71620287708320518 ) ) ;
#7824=ORIENTED_EDGE ( 'NONE', *, *, #36380, .F. ) ;
#7825=CARTESIAN_POINT ( 'NONE',  ( 0.7048096507298579061, 47.58126109679093219, 7.115188260604007553 ) ) ;
#7838=CARTESIAN_POINT ( 'NONE',  ( 0.5988103564986356764, 46.30780741915666709, -13.03604522143308664 ) ) ;
#7850=VECTOR ( 'NONE', #33605, 1000.000000000000114 ) ;
#7853=CARTESIAN_POINT ( 'NONE',  ( 4.549368137175248350, -28.46244473166695954, 32.13400537129875545 ) ) ;
#7859=CARTESIAN_POINT ( 'NONE',  ( 0.5998501479064699549, 47.76154736470750350, 5.759754759340949271 ) ) ;
#7867=CARTESIAN_POINT ( 'NONE',  ( 0.6028618097248863439, 29.42431480658679988, 38.05975027458347171 ) ) ;
#7874=EDGE_CURVE ( 'NONE', #13235, #28616, #34020, .T. ) ;
#7892=( BOUNDED_SURFACE ( )  B_SPLINE_SURFACE ( 3, 1, ( 
 ( #41812, #59642 ),
 ( #45895, #2941 ),
 ( #56181, #36802 ),
 ( #60562, #16754 ) ),
 .UNSPECIFIED., .F., .F., .F. ) 
 B_SPLINE_SURFACE_WITH_KNOTS ( ( 4, 4 ),
 ( 2, 2 ),
 ( 0.000000000000000000, 1.000000000000000000 ),
 ( 0.000000000000000000, 1.000000000000000000 ),
 .UNSPECIFIED. ) 
 GEOMETRIC_REPRESENTATION_ITEM ( )  RATIONAL_B_SPLINE_SURFACE ( (
 ( 1.000000000000000000, 1.000000000000000000),
 ( 0.9751682680413298332, 0.9999560080971552356),
 ( 0.9751682680413298332, 0.9999560080971552356),
 ( 1.000000000000000000, 1.000000000000000000) ) ) 
 REPRESENTATION_ITEM ( '' )  SURFACE ( )  );
#7895=LINE ( 'NONE', #16690, #2536 ) ;
#7896=CARTESIAN_POINT ( 'NONE',  ( 2.301529144917016101, 48.01619158420459144, -1.287519423136770813 ) ) ;
#7900=CIRCLE ( 'NONE', #12936, 42.92674063221959813 ) ;
#7907=B_SPLINE_CURVE_WITH_KNOTS ( 'NONE', 3,
 ( #16622, #35125, #20096, #26017, #39214, #29782 ),
 .UNSPECIFIED., .F., .F.,
 ( 4, 2, 4 ),
 ( 0.000000000000000000, 0.0002450742804987355856, 0.0004901485609974711713 ),
 .UNSPECIFIED. ) ;
#7909=ADVANCED_FACE ( 'NONE', ( #4234 ), #30533, .F. ) ;
#7912=EDGE_CURVE ( 'NONE', #23651, #51385, #33443, .T. ) ;
#7913=CARTESIAN_POINT ( 'NONE',  ( 0.3622758884714730732, -39.50828911767010965, 17.25816669464924047 ) ) ;
#7920=CARTESIAN_POINT ( 'NONE',  ( 0.6023143664670691511, -33.83148565876907554, -34.20175727332116367 ) ) ;
#7923=CARTESIAN_POINT ( 'NONE',  ( 0.1073791018717483448, 43.12183934961191056, -0.4849339620928847516 ) ) ;
#7924=ADVANCED_FACE ( 'NONE', ( #58394 ), #36987, .F. ) ;
#7927=CARTESIAN_POINT ( 'NONE',  ( -6.016761891674564211, -18.68153697670643609, 2.462934516563739518 ) ) ;
#7931=CARTESIAN_POINT ( 'NONE',  ( 0.3622758884714600280, 31.06363466427727360, -29.89648521331598729 ) ) ;
#7932=CARTESIAN_POINT ( 'NONE',  ( 0.7048096507298579061, -47.58126109679096771, -7.115188260603675374 ) ) ;
#7933=ADVANCED_FACE ( 'NONE', ( #11130 ), #43380, .F. ) ;
#7942=ORIENTED_EDGE ( 'NONE', *, *, #24819, .T. ) ;
#7946=CARTESIAN_POINT ( 'NONE',  ( 0.1073791018717578927, -34.50606437925563341, 25.86618856530653687 ) ) ;
#7947=ORIENTED_EDGE ( 'NONE', *, *, #25114, .F. ) ;
#7952=EDGE_CURVE ( 'NONE', #16902, #52610, #39650, .T. ) ;
#7953=CARTESIAN_POINT ( 'NONE',  ( 0.1103744047535531458, 0.03874731383731806061, -43.12441516302519773 ) ) ;
#7955=ORIENTED_EDGE ( 'NONE', *, *, #39147, .T. ) ;
#7967=( BOUNDED_SURFACE ( )  B_SPLINE_SURFACE ( 3, 1, ( 
 ( #18499, #51069 ),
 ( #61382, #56078 ),
 ( #55766, #4665 ),
 ( #13191, #32292 ) ),
 .UNSPECIFIED., .F., .F., .F. ) 
 B_SPLINE_SURFACE_WITH_KNOTS ( ( 4, 4 ),
 ( 2, 2 ),
 ( 0.000000000000000000, 1.000000000000000000 ),
 ( 0.000000000000000000, 1.000000000000000000 ),
 .UNSPECIFIED. ) 
 GEOMETRIC_REPRESENTATION_ITEM ( )  RATIONAL_B_SPLINE_SURFACE ( (
 ( 1.000000000000000000, 1.000000000000000000),
 ( 0.9953040768229005630, 0.8617119497784937465),
 ( 0.9953040768229005630, 0.8617119497784937465),
 ( 1.000000000000000000, 1.000000000000000000) ) ) 
 REPRESENTATION_ITEM ( '' )  SURFACE ( )  );
#7968=CARTESIAN_POINT ( 'NONE',  ( 0.1103310638050661735, 39.87325896099741840, -16.42686748615365389 ) ) ;
#7983=DIRECTION ( 'NONE',  ( 0.000000000000000000, 0.000000000000000000, -1.000000000000000000 ) ) ;
#7985=EDGE_CURVE ( 'NONE', #6050, #43089, #20830, .T. ) ;
#7989=B_SPLINE_CURVE_WITH_KNOTS ( 'NONE', 3,
 ( #60201, #17313, #7575, #12626, #55499, #1635, #44914, #1951, #31717, #49568, #50808, #59271, #59897, #17012, #25453, #58967 ),
 .UNSPECIFIED., .F., .F.,
 ( 4, 3, 3, 3, 3, 4 ),
 ( 1.868480190406682863E-17, 0.0002618515315864444705, 0.0003927756766342024365, 0.0005236998216950591910, 0.0007855159896329946692, 0.001047349442285930039 ),
 .UNSPECIFIED. ) ;
#7995=DIRECTION ( 'NONE',  ( -1.000000000000000000, -0.000000000000000000, -0.000000000000000000 ) ) ;
#8007=CARTESIAN_POINT ( 'NONE',  ( -2.569797478183783568, 14.01151037928423015, -4.218948559326104686 ) ) ;
#8011=CARTESIAN_POINT ( 'NONE',  ( 0.8751705887134553219, -38.69254731947813752, -28.56654290188640033 ) ) ;
#8012=CARTESIAN_POINT ( 'NONE',  ( 0.8751705887134553219, 47.79200036674271956, 5.393078191592866055 ) ) ;
#8014=CARTESIAN_POINT ( 'NONE',  ( 0.1084644655670281149, 5.234391617063994140, -42.80575641816242438 ) ) ;
#8019=CARTESIAN_POINT ( 'NONE',  ( 4.975801465491695552, 3.702618843596801934, 47.76942479135487218 ) ) ;
#8023=CARTESIAN_POINT ( 'NONE',  ( 0.5988103622719990193, -23.52668907282314947, -41.96244039798782666 ) ) ;
#8026=CARTESIAN_POINT ( 'NONE',  ( -6.016489644550737204, -7.215050741358165709, 17.40716454747926889 ) ) ;
#8035=EDGE_LOOP ( 'NONE', ( #17970, #6289, #55736, #47709, #8344, #44742 ) ) ;
#8040=CARTESIAN_POINT ( 'NONE',  ( 0.3622758884714730732, 42.84426538328725798, 4.808133778522027058 ) ) ;
#8046=CARTESIAN_POINT ( 'NONE',  ( 0.8751705887134553219, 44.08562551107081617, -19.22545746485614870 ) ) ;
#8048=CARTESIAN_POINT ( 'NONE',  ( 0.1103310638050662151, -26.31782144882266294, 34.16271402810823332 ) ) ;
#8056=CARTESIAN_POINT ( 'NONE',  ( 0.7246131072078539903, -24.75818606403478483, 41.24126838495057967 ) ) ;
#8058=CARTESIAN_POINT ( 'NONE',  ( 0.5988103622719986863, -11.86435782853401300, -46.62176011478417337 ) ) ;
#8059=VERTEX_POINT ( 'NONE', #17366 ) ;
#8061=B_SPLINE_CURVE_WITH_KNOTS ( 'NONE', 3,
 ( #58369, #53669, #10797, #41168, #36464, #35845 ),
 .UNSPECIFIED., .F., .F.,
 ( 4, 2, 4 ),
 ( 1.426045310262811165E-18, 0.0002450742804987333088, 0.0004901485609974652081 ),
 .UNSPECIFIED. ) ;
#8062=CARTESIAN_POINT ( 'NONE',  ( 0.8751705887134423323, 46.67919521768887847, -11.58504748649151317 ) ) ;
#8068=FACE_OUTER_BOUND ( 'NONE', #58232, .T. ) ;
#8071=DIRECTION ( 'NONE',  ( 0.000000000000000000, 0.000000000000000000, 1.000000000000000000 ) ) ;
#8082=CARTESIAN_POINT ( 'NONE',  ( 0.1073791018717483448, 30.83464511437097499, 30.14884492832400298 ) ) ;
#8092=CARTESIAN_POINT ( 'NONE',  ( -6.010958268070873523, -11.45964880703837174, 14.95835081545469869 ) ) ;
#8102=CARTESIAN_POINT ( 'NONE',  ( 0.5980894510889457338, 29.84264441023728054, 37.73932204245528510 ) ) ;
#8106=CARTESIAN_POINT ( 'NONE',  ( 0.1097557419366048670, 26.42915440612286204, 34.07666148910654158 ) ) ;
#8109=CARTESIAN_POINT ( 'NONE',  ( 0.1064266418746777493, -15.98292515284435744, -40.05351192729354892 ) ) ;
#8122=ORIENTED_EDGE ( 'NONE', *, *, #15658, .F. ) ;
#8127=B_SPLINE_CURVE_WITH_KNOTS ( 'NONE', 3,
 ( #53698, #49330, #24299, #25524, #48413, #24612 ),
 .UNSPECIFIED., .F., .F.,
 ( 4, 2, 4 ),
 ( 1.736958732247374613E-17, 0.0002293319059085094391, 0.0004586638118170014767 ),
 .UNSPECIFIED. ) ;
#8130=CARTESIAN_POINT ( 'NONE',  ( 0.6041374136657476912, -48.10739871142803992, 0.1745662470643146724 ) ) ;
#8134=ORIENTED_EDGE ( 'NONE', *, *, #5282, .T. ) ;
#8140=ADVANCED_FACE ( 'NONE', ( #47414 ), #8957, .F. ) ;
#8145=CARTESIAN_POINT ( 'NONE',  ( 0.7954196712028471783, -5.415566793625004927, -47.79303691884129535 ) ) ;
#8151=CARTESIAN_POINT ( 'NONE',  ( 0.1092565886968784594, -16.78938711553603014, -39.72209809039391359 ) ) ;
#8152=EDGE_CURVE ( 'NONE', #15900, #24850, #14529, .T. ) ;
#8154=ADVANCED_FACE ( 'NONE', ( #52093 ), #15377, .F. ) ;
#8157=CARTESIAN_POINT ( 'NONE',  ( 0.2885697896453121580, 33.71073718007502151, 26.88157175352899486 ) ) ;
#8158=CARTESIAN_POINT ( 'NONE',  ( 0.5998501479064708430, 33.64490850298796687, 34.38546660123309096 ) ) ;
#8166=B_SPLINE_CURVE_WITH_KNOTS ( 'NONE', 3,
 ( #31562, #26551, #45678, #60062 ),
 .UNSPECIFIED., .F., .F.,
 ( 4, 4 ),
 ( 2.216451077356609476E-17, 0.004564976165746189446 ),
 .UNSPECIFIED. ) ;
#8167=AXIS2_PLACEMENT_3D ( 'NONE', #17572, #26969, #45475 ) ;
#8168=ORIENTED_EDGE ( 'NONE', *, *, #50405, .T. ) ;
#8172=CARTESIAN_POINT ( 'NONE',  ( 0.5980894510889448457, -5.583794302584927038, -47.78766676462073804 ) ) ;
#8176=ORIENTED_EDGE ( 'NONE', *, *, #8686, .F. ) ;
#8194=CARTESIAN_POINT ( 'NONE',  ( 0.6041374136657476912, -29.14743607025112482, 38.27243465845292292 ) ) ;
#8206=CARTESIAN_POINT ( 'NONE',  ( 0.5998501479064708430, 6.798102206414135651, -47.62484632993681544 ) ) ;
#8218=FACE_OUTER_BOUND ( 'NONE', #28377, .T. ) ;
#8219=CARTESIAN_POINT ( 'NONE',  ( 4.975801465491695552, -26.14269827151708370, 40.15204426031488794 ) ) ;
#8223=CARTESIAN_POINT ( 'NONE',  ( -5.995132425357893702, -4.885449473615202542, -18.19985213254577161 ) ) ;
#8236=ORIENTED_EDGE ( 'NONE', *, *, #49791, .T. ) ;
#8241=ORIENTED_EDGE ( 'NONE', *, *, #20312, .F. ) ;
#8242=CARTESIAN_POINT ( 'NONE',  ( 4.975801465491694664, 26.14269827151623105, 40.15204426031542795 ) ) ;
#8247=CARTESIAN_POINT ( 'NONE',  ( 0.1103310638050662290, 21.49083802119848841, 37.38800124003719105 ) ) ;
#8249=EDGE_CURVE ( 'NONE', #34923, #24850, #21435, .T. ) ;
#8256=CARTESIAN_POINT ( 'NONE',  ( 0.6023143664670691511, 34.20175727332128446, -33.83148565876894764 ) ) ;
#8260=CARTESIAN_POINT ( 'NONE',  ( 0.3622758884714730732, -41.85013935980095567, -10.35929834645908265 ) ) ;
#8266=CARTESIAN_POINT ( 'NONE',  ( 5.880360259849752858, -36.03610316515361234, -31.66572319753549536 ) ) ;
#8272=CARTESIAN_POINT ( 'NONE',  ( 4.549368137175248350, 8.166781970325150297, 42.14271863032836762 ) ) ;
#8276=LINE ( 'NONE', #18330, #24019 ) ;
#8284=CARTESIAN_POINT ( 'NONE',  ( 2.643462169533613793, 47.78621045426868363, 4.896978544602314187 ) ) ;
#8290=CARTESIAN_POINT ( 'NONE',  ( 0.1098349054025746507, 42.72717686504321932, 5.840292671757814524 ) ) ;
#8294=CARTESIAN_POINT ( 'NONE',  ( 0.1310142868023690677, 6.259743112235529594, -42.66681113736512287 ) ) ;
#8306=( BOUNDED_SURFACE ( )  B_SPLINE_SURFACE ( 3, 1, ( 
 ( #61808, #37434 ),
 ( #56198, #37754 ),
 ( #28017, #33352 ),
 ( #33043, #60580 ) ),
 .UNSPECIFIED., .F., .F., .F. ) 
 B_SPLINE_SURFACE_WITH_KNOTS ( ( 4, 4 ),
 ( 2, 2 ),
 ( 0.000000000000000000, 1.000000000000000000 ),
 ( 0.000000000000000000, 1.000000000000000000 ),
 .UNSPECIFIED. ) 
 GEOMETRIC_REPRESENTATION_ITEM ( )  RATIONAL_B_SPLINE_SURFACE ( (
 ( 1.000000000000000000, 1.000000000000000000),
 ( 0.9953040768229005630, 0.8617119497784937465),
 ( 0.9953040768229005630, 0.8617119497784937465),
 ( 1.000000000000000000, 1.000000000000000000) ) ) 
 REPRESENTATION_ITEM ( '' )  SURFACE ( )  );
#8307=VERTEX_POINT ( 'NONE', #49554 ) ;
#8308=ORIENTED_EDGE ( 'NONE', *, *, #46271, .F. ) ;
#8324=CARTESIAN_POINT ( 'NONE',  ( 0.5998501479064708430, -47.62484632993683675, -6.798102206413969562 ) ) ;
#8344=ORIENTED_EDGE ( 'NONE', *, *, #2713, .F. ) ;
#8349=B_SPLINE_CURVE_WITH_KNOTS ( 'NONE', 3,
 ( #35632, #44723, #10892, #11824, #59088, #50018 ),
 .UNSPECIFIED., .F., .F.,
 ( 4, 2, 4 ),
 ( 0.000000000000000000, 0.0002450742804987326583, 0.0004901485609974653166 ),
 .UNSPECIFIED. ) ;
#8354=CARTESIAN_POINT ( 'NONE',  ( 0.6009453534118440743, 47.75104957283898699, -5.846398087358881668 ) ) ;
#8356=ORIENTED_EDGE ( 'NONE', *, *, #2471, .T. ) ;
#8357=CARTESIAN_POINT ( 'NONE',  ( 0.1081432562775997974, 37.55692207416026918, -21.19449538864519056 ) ) ;
#8359=ORIENTED_EDGE ( 'NONE', *, *, #53462, .T. ) ;
#8365=CARTESIAN_POINT ( 'NONE',  ( 0.8751705887134423323, -38.69254731947852832, 28.56654290188588163 ) ) ;
#8366=CARTESIAN_POINT ( 'NONE',  ( -2.569797478183783568, -2.353985772484652017, -14.44232325624825819 ) ) ;
#8370=CARTESIAN_POINT ( 'NONE',  ( 0.8751705887134553219, -11.58504748649232496, 46.67919521768867241 ) ) ;
#8384=CARTESIAN_POINT ( 'NONE',  ( 5.880360259849739535, 47.05949693022694191, 9.312491912828287255 ) ) ;
#8387=ORIENTED_EDGE ( 'NONE', *, *, #17072, .T. ) ;
#8392=DIRECTION ( 'NONE',  ( 0.000000000000000000, 0.000000000000000000, 1.000000000000000000 ) ) ;
#8399=CARTESIAN_POINT ( 'NONE',  ( -2.569797478183783568, 10.02484965418641316, -10.65947181927829135 ) ) ;
#8408=CARTESIAN_POINT ( 'NONE',  ( 5.880360259849739535, -26.61251048557276633, 39.91356965504101595 ) ) ;
#8409=ORIENTED_EDGE ( 'NONE', *, *, #16969, .F. ) ;
#8410=CARTESIAN_POINT ( 'NONE',  ( 0.5998501479064708430, 29.69975237324613460, -37.84527566984826308 ) ) ;
#8417=CARTESIAN_POINT ( 'NONE',  ( 4.549368137175248350, -42.84816078363928682, 2.596185425821780246 ) ) ;
#8424=ORIENTED_EDGE ( 'NONE', *, *, #6313, .T. ) ;
#8429=CARTESIAN_POINT ( 'NONE',  ( 0.1073791018717578927, -34.50606437925563341, 25.86618856530653687 ) ) ;
#8431=VECTOR ( 'NONE', #46665, 1000.000000000000227 ) ;
#8434=CARTESIAN_POINT ( 'NONE',  ( 4.549368137175248350, -8.582197505784725067, 42.06008734272381133 ) ) ;
#8439=CARTESIAN_POINT ( 'NONE',  ( 0.2885700199627511120, 39.51953436244172480, -17.24062365614554437 ) ) ;
#8445=CARTESIAN_POINT ( 'NONE',  ( 0.1095718737110178420, 21.78439022773156353, -37.21776476380635046 ) ) ;
#8451=DIRECTION ( 'NONE',  ( -0.1024043820194934645, -0.9239750460186150205, 0.3684880688409106209 ) ) ;
#8463=ORIENTED_EDGE ( 'NONE', *, *, #13128, .F. ) ;
#8465=CARTESIAN_POINT ( 'NONE',  ( 0.8760168074887076939, -47.80016357497245849, -5.394043284319333331 ) ) ;
#8468=ORIENTED_EDGE ( 'NONE', *, *, #35586, .T. ) ;
#8479=LINE ( 'NONE', #55790, #8753 ) ;
#8480=CARTESIAN_POINT ( 'NONE',  ( -4.908599999999998964, 9.539392014169456147, -3.000000000000000000 ) ) ;
#8486=CARTESIAN_POINT ( 'NONE',  ( 4.549368137175248350, -28.14399996863522446, 32.41327393324091588 ) ) ;
#8499=CARTESIAN_POINT ( 'NONE',  ( 0.3622758884714730732, 11.95365414648439462, 41.42293301073630118 ) ) ;
#8516=CARTESIAN_POINT ( 'NONE',  ( -6.010958268070873523, 2.473955915502211944, 18.68034667844849750 ) ) ;
#8517=VECTOR ( 'NONE', #44495, 1000.000000000000114 ) ;
#8527=DIRECTION ( 'NONE',  ( 0.000000000000000000, 0.000000000000000000, -1.000000000000000000 ) ) ;
#8530=CARTESIAN_POINT ( 'NONE',  ( 0.6023143664670691511, 46.53533348214991605, -12.19804739160213281 ) ) ;
#8531=CARTESIAN_POINT ( 'NONE',  ( -6.015611763856276717, -9.416239407363189429, -16.32183393015606754 ) ) ;
#8547=DIRECTION ( 'NONE',  ( 0.000000000000000000, 0.000000000000000000, -1.000000000000000000 ) ) ;
#8548=CARTESIAN_POINT ( 'NONE',  ( 4.549368137175248350, -8.166781970326043805, 42.14271863032818999 ) ) ;
#8554=CARTESIAN_POINT ( 'NONE',  ( 1.827119703190779321, -33.38937793923705755, 27.17434071502546189 ) ) ;
#8555=CARTESIAN_POINT ( 'NONE',  ( -2.569797478183783568, -14.62602397812941035, 0.4487456364278328835 ) ) ;
#8558=CARTESIAN_POINT ( 'NONE',  ( 0.1100247026804066219, 0.1696715072117343237, -43.12411436000287779 ) ) ;
#8565=CARTESIAN_POINT ( 'NONE',  ( 4.549368137175248350, 13.99871866169365653, -40.58005590356676606 ) ) ;
#8571=CARTESIAN_POINT ( 'NONE',  ( 0.6041374136657475802, -24.20487816031549855, 41.57494627055102399 ) ) ;
#8572=CARTESIAN_POINT ( 'NONE',  ( 0.2224561200757618484, -10.42482236669274620, -41.84032767736798775 ) ) ;
#8573=CARTESIAN_POINT ( 'NONE',  ( 0.1073791018717578927, 40.02496097243057704, -16.05399293000775529 ) ) ;
#8575=CARTESIAN_POINT ( 'NONE',  ( 0.1101816497532062400, 42.73758747687830351, -5.763501205266673644 ) ) ;
#8576=CARTESIAN_POINT ( 'NONE',  ( 4.322998006666179727, -35.39923696758989990, -32.40067585697786967 ) ) ;
#8578=CARTESIAN_POINT ( 'NONE',  ( 0.5998501479064699549, 38.48283596221989455, 28.86886762351138103 ) ) ;
#8582=FACE_OUTER_BOUND ( 'NONE', #13735, .T. ) ;
#8593=EDGE_LOOP ( 'NONE', ( #22108, #12281, #47397, #27989 ) ) ;
#8595=CARTESIAN_POINT ( 'NONE',  ( -6.015611763856276717, -9.427003116184058840, -16.31561949997086103 ) ) ;
#8604=EDGE_CURVE ( 'NONE', #28634, #6825, #30687, .T. ) ;
#8607=ORIENTED_EDGE ( 'NONE', *, *, #34255, .F. ) ;
#8611=CARTESIAN_POINT ( 'NONE',  ( 0.1073791018717578927, 39.65380858626191696, 16.95003405440326816 ) ) ;
#8618=B_SPLINE_CURVE_WITH_KNOTS ( 'NONE', 3,
 ( #55259, #21766, #31159, #2643, #45289, #7329 ),
 .UNSPECIFIED., .F., .F.,
 ( 4, 2, 4 ),
 ( 8.559238840292260229E-17, 0.0002293366620881447137, 0.0004586733241762038296 ),
 .UNSPECIFIED. ) ;
#8621=B_SPLINE_CURVE_WITH_KNOTS ( 'NONE', 3,
 ( #34457, #10027, #15968, #53831, #29426, #30046 ),
 .UNSPECIFIED., .F., .F.,
 ( 4, 2, 4 ),
 ( 8.672106141451628927E-17, 0.0002293366620881453371, 0.0004586733241762039922 ),
 .UNSPECIFIED. ) ;
#8626=CARTESIAN_POINT ( 'NONE',  ( 0.6009453534118440743, 41.44251633523857947, 24.43073772334932769 ) ) ;
#8637=CARTESIAN_POINT ( 'NONE',  ( 0.6028618097248863439, -47.71844004092984903, -6.106174977918878533 ) ) ;
#8654=CARTESIAN_POINT ( 'NONE',  ( 0.1310142868023688456, 42.66681113736508024, 6.259743112235677920 ) ) ;
#8655=EDGE_LOOP ( 'NONE', ( #44041, #48943, #43033, #36071 ) ) ;
#8657=AXIS2_PLACEMENT_3D ( 'NONE', #25610, #22154, #21846 ) ;
#8662=LINE ( 'NONE', #51889, #426 ) ;
#8664=CARTESIAN_POINT ( 'NONE',  ( 0.1073791018717578927, 26.63563652260167203, -33.91564619577780348 ) ) ;
#8682=CARTESIAN_POINT ( 'NONE',  ( 0.6017666602106490625, 47.74032907933390391, 5.933006478840855635 ) ) ;
#8683=( BOUNDED_SURFACE ( )  B_SPLINE_SURFACE ( 3, 1, ( 
 ( #56282, #3959 ),
 ( #32817, #28400 ),
 ( #33744, #14635 ),
 ( #41916, #46923 ) ),
 .UNSPECIFIED., .F., .F., .F. ) 
 B_SPLINE_SURFACE_WITH_KNOTS ( ( 4, 4 ),
 ( 2, 2 ),
 ( 0.000000000000000000, 1.000000000000000000 ),
 ( 0.000000000000000000, 1.000000000000000000 ),
 .UNSPECIFIED. ) 
 GEOMETRIC_REPRESENTATION_ITEM ( )  RATIONAL_B_SPLINE_SURFACE ( (
 ( 1.000000000000000000, 1.000000000000000000),
 ( 0.7223157951917480446, 0.9931996967497186413),
 ( 0.7223157951917480446, 0.9931996967497186413),
 ( 1.000000000000000000, 1.000000000000000000) ) ) 
 REPRESENTATION_ITEM ( '' )  SURFACE ( )  );
#8684=DIRECTION ( 'NONE',  ( 0.000000000000000000, 0.000000000000000000, -1.000000000000000000 ) ) ;
#8686=EDGE_CURVE ( 'NONE', #57080, #6050, #60917, .T. ) ;
#8687=EDGE_CURVE ( 'NONE', #23902, #42831, #24316, .T. ) ;
#8688=CARTESIAN_POINT ( 'NONE',  ( 0.1103744047535531458, -5.667281528142711799, 42.75042227379817916 ) ) ;
#8690=LINE ( 'NONE', #24345, #39546 ) ;
#8695=CARTESIAN_POINT ( 'NONE',  ( 0.6031357023905875581, -38.19275261685294964, 29.25135304925216673 ) ) ;
#8697=ORIENTED_EDGE ( 'NONE', *, *, #25324, .T. ) ;
#8698=VECTOR ( 'NONE', #6538, 1000.000000000000114 ) ;
#8702=COLOUR_RGB ( '', 0.31764706, 0.68627451, 0.89019608) ;
#8704=DIRECTION ( 'NONE',  ( 0.000000000000000000, 0.000000000000000000, 1.000000000000000000 ) ) ;
#8720=CARTESIAN_POINT ( 'NONE',  ( 0.1081432562775997974, 25.91533557232844487, 34.46918062033758900 ) ) ;
#8732=EDGE_LOOP ( 'NONE', ( #11599, #57179, #8828, #6689 ) ) ;
#8739=CARTESIAN_POINT ( 'NONE',  ( 0.8760168074887090262, -29.98565522133319661, -37.61398439004523198 ) ) ;
#8751=VECTOR ( 'NONE', #46827, 1000.000000000000000 ) ;
#8753=VECTOR ( 'NONE', #12913, 1000.000000000000114 ) ;
#8803=SHAPE_REPRESENTATION ( 'straight bevel gear(wobble out)_iso_ISO - Straight bevel gear 2M 48GT 47PT 20PA 5FW ---48O1H50MD20.0S1', ( #14677 ), #46738 ) ;
#8804=EDGE_CURVE ( 'NONE', #21034, #50035, #5479, .T. ) ;
#8824=DIRECTION ( 'NONE',  ( -1.000000000000000000, -0.000000000000000000, -0.000000000000000000 ) ) ;
#8828=ORIENTED_EDGE ( 'NONE', *, *, #47468, .T. ) ;
#8832=CARTESIAN_POINT ( 'NONE',  ( 0.7048096507298579061, 48.10291524268439645, 0.8437160066908956368 ) ) ;
#8845=CARTESIAN_POINT ( 'NONE',  ( -2.708315649062916552, 10.53288422393042190, 10.16016146078292337 ) ) ;
#8852=FACE_OUTER_BOUND ( 'NONE', #10553, .T. ) ;
#8854=ORIENTED_EDGE ( 'NONE', *, *, #26219, .T. ) ;
#8862=EDGE_LOOP ( 'NONE', ( #56115, #11543, #2675, #57158 ) ) ;
#8871=CIRCLE ( 'NONE', #51883, 47.91270532121795611 ) ;
#8876=CARTESIAN_POINT ( 'NONE',  ( 0.1313383488274124933, 15.91164383651745950, -40.08066228784247897 ) ) ;
#8877=CARTESIAN_POINT ( 'NONE',  ( -2.569797478183783568, -4.218948559326153536, -14.01151037928421417 ) ) ;
#8878=CARTESIAN_POINT ( 'NONE',  ( 2.643462169533600914, -46.02269433264222442, -13.76277278785544844 ) ) ;
#8880=( BOUNDED_SURFACE ( )  B_SPLINE_SURFACE ( 3, 1, ( 
 ( #17028, #30172 ),
 ( #40239, #44930 ),
 ( #59603, #54268 ),
 ( #53653, #25473 ) ),
 .UNSPECIFIED., .F., .F., .F. ) 
 B_SPLINE_SURFACE_WITH_KNOTS ( ( 4, 4 ),
 ( 2, 2 ),
 ( 0.000000000000000000, 1.000000000000000000 ),
 ( 0.000000000000000000, 1.000000000000000000 ),
 .UNSPECIFIED. ) 
 GEOMETRIC_REPRESENTATION_ITEM ( )  RATIONAL_B_SPLINE_SURFACE ( (
 ( 1.000000000000000000, 1.000000000000000000),
 ( 0.9953040768229005630, 0.8617119497784937465),
 ( 0.9953040768229005630, 0.8617119497784937465),
 ( 1.000000000000000000, 1.000000000000000000) ) ) 
 REPRESENTATION_ITEM ( '' )  SURFACE ( )  );
#8884=CIRCLE ( 'NONE', #22888, 42.92674063221959813 ) ;
#8894=ORIENTED_EDGE ( 'NONE', *, *, #17678, .F. ) ;
#8896=CARTESIAN_POINT ( 'NONE',  ( 4.975801465491695552, 27.09127437476327671, 39.51822597168504814 ) ) ;
#8899=ORIENTED_EDGE ( 'NONE', *, *, #52265, .T. ) ;
#8914=DIRECTION ( 'NONE',  ( 0.09835009131224552170, 0.6119264800004677873, 0.7847759187265561653 ) ) ;
#8915=CARTESIAN_POINT ( 'NONE',  ( 0.1064266418746777493, 42.82540703015432371, -5.071708474752798956 ) ) ;
#8920=ORIENTED_EDGE ( 'NONE', *, *, #6670, .T. ) ;
#8923=CARTESIAN_POINT ( 'NONE',  ( 0.1100247026804066219, -34.10937070541727678, -26.38690693952944955 ) ) ;
#8924=CARTESIAN_POINT ( 'NONE',  ( -6.016761891674564211, -11.46828378093569789, 14.95139917749700587 ) ) ;
#8925=CARTESIAN_POINT ( 'NONE',  ( 0.6001305935487315502, -37.84751346122835969, -29.70149728382423504 ) ) ;
#8929=CARTESIAN_POINT ( 'NONE',  ( 0.8751705887134553219, 17.57879340691544101, -44.76769609654218129 ) ) ;
#8934=ORIENTED_EDGE ( 'NONE', *, *, #17619, .F. ) ;
#8937=CARTESIAN_POINT ( 'NONE',  ( 0.1073791018717483448, 42.81622261970987608, 5.147744207007008299 ) ) ;
#8940=ORIENTED_EDGE ( 'NONE', *, *, #56776, .F. ) ;
#8943=FACE_OUTER_BOUND ( 'NONE', #6934, .T. ) ;
#8947=VECTOR ( 'NONE', #29702, 1000.000000000000114 ) ;
#8953=CARTESIAN_POINT ( 'NONE',  ( 0.8760168074887076939, 19.22870327415240865, 44.09317760313759749 ) ) ;
#8957=( BOUNDED_SURFACE ( )  B_SPLINE_SURFACE ( 3, 1, ( 
 ( #61481, #48333 ),
 ( #38646, #47116 ),
 ( #24518, #57701 ),
 ( #53019, #33331 ) ),
 .UNSPECIFIED., .F., .F., .F. ) 
 B_SPLINE_SURFACE_WITH_KNOTS ( ( 4, 4 ),
 ( 2, 2 ),
 ( 0.000000000000000000, 1.000000000000000000 ),
 ( 0.000000000000000000, 1.000000000000000000 ),
 .UNSPECIFIED. ) 
 GEOMETRIC_REPRESENTATION_ITEM ( )  RATIONAL_B_SPLINE_SURFACE ( (
 ( 1.000000000000000000, 1.000000000000000000),
 ( 0.9953040768229013402, 0.8617119497784988535),
 ( 0.9953040768229013402, 0.8617119497784988535),
 ( 1.000000000000000000, 1.000000000000000000) ) ) 
 REPRESENTATION_ITEM ( '' )  SURFACE ( )  );
#8966=ORIENTED_EDGE ( 'NONE', *, *, #42743, .F. ) ;
#8969=CARTESIAN_POINT ( 'NONE',  ( 3.680974057930774812, -39.15945827951728830, 27.71659654258229821 ) ) ;
#8974=ORIENTED_EDGE ( 'NONE', *, *, #34006, .T. ) ;
#8986=CARTESIAN_POINT ( 'NONE',  ( 0.1100053167205930771, 26.10991185395887371, -34.32189548568256754 ) ) ;
#8992=ADVANCED_FACE ( 'NONE', ( #36811 ), #19890, .F. ) ;
#8993=CARTESIAN_POINT ( 'NONE',  ( 0.3622758884714730732, 33.69533458712344753, -26.89560658783350178 ) ) ;
#8997=CARTESIAN_POINT ( 'NONE',  ( -6.015611763856276717, -18.84324252354755203, 0.006214430185075541652 ) ) ;
#8999=EDGE_CURVE ( 'NONE', #43474, #32408, #26529, .T. ) ;
#9006=ORIENTED_EDGE ( 'NONE', *, *, #23413, .F. ) ;
#9010=B_SPLINE_CURVE_WITH_KNOTS ( 'NONE', 3,
 ( #61082, #22586, #56688, #13817 ),
 .UNSPECIFIED., .F., .F.,
 ( 4, 4 ),
 ( 0.000000000000000000, 0.004445488388166994251 ),
 .UNSPECIFIED. ) ;
#9028=CARTESIAN_POINT ( 'NONE',  ( 0.3622758884714600280, -43.10531414739104861, -0.8252992914326565677 ) ) ;
#9029=ORIENTED_EDGE ( 'NONE', *, *, #27026, .T. ) ;
#9034=EDGE_CURVE ( 'NONE', #19218, #60297, #31757, .T. ) ;
#9035=ORIENTED_EDGE ( 'NONE', *, *, #42959, .F. ) ;
#9043=CARTESIAN_POINT ( 'NONE',  ( -6.016761891674564211, 13.32657647165355286, 13.32172022638596509 ) ) ;
#9044=CARTESIAN_POINT ( 'NONE',  ( 0.6030672727741701600, -34.07876014368883943, 33.95535904584727405 ) ) ;
#9053=ORIENTED_EDGE ( 'NONE', *, *, #53430, .F. ) ;
#9056=CARTESIAN_POINT ( 'NONE',  ( 0.1102144999581333301, -21.45299314243968070, -37.40973521037455640 ) ) ;
#9071=ORIENTED_EDGE ( 'NONE', *, *, #35173, .T. ) ;
#9079=CARTESIAN_POINT ( 'NONE',  ( 4.549368137175248350, -35.57418903283098643, -24.02461520945259466 ) ) ;
#9105=VERTEX_POINT ( 'NONE', #14841 ) ;
#9116=DIRECTION ( 'NONE',  ( -0.9990097760809876215, 0.000000000000000000, 0.04449120468828354769 ) ) ;
#9126=CARTESIAN_POINT ( 'NONE',  ( 4.549368137175248350, 8.582197505783829783, 42.06008734272398897 ) ) ;
#9127=ADVANCED_FACE ( 'NONE', ( #39583 ), #21510, .F. ) ;
#9130=CARTESIAN_POINT ( 'NONE',  ( 0.1313383488274124933, -37.66088038379825775, -21.00709374781526861 ) ) ;
#9140=B_SPLINE_CURVE_WITH_KNOTS ( 'NONE', 3,
 ( #4645, #23796, #28176, #42608, #56981, #42922, #19115, #38227, #14409, #33516 ),
 .UNSPECIFIED., .F., .F.,
 ( 4, 3, 3, 4 ),
 ( 0.0005236741812378729226, 0.0005236998216949948978, 0.0007855159896329592158, 0.001047349442285928304 ),
 .UNSPECIFIED. ) ;
#9141=CARTESIAN_POINT ( 'NONE',  ( 0.3622758884714600280, -6.444611261694905835, 42.62881903538198713 ) ) ;
#9144=DIRECTION ( 'NONE',  ( -0.1024043820194934507, -0.7811075516170038480, -0.6159418278945628655 ) ) ;
#9148=EDGE_CURVE ( 'NONE', #45060, #25025, #40513, .T. ) ;
#9152=CARTESIAN_POINT ( 'NONE',  ( 0.7048096507298635682, -38.67623024744029436, -28.61383451045685078 ) ) ;
#9161=CARTESIAN_POINT ( 'NONE',  ( 0.8760168074887090262, -46.22580377597795120, 13.30888447661999940 ) ) ;
#9167=ORIENTED_EDGE ( 'NONE', *, *, #7224, .T. ) ;
#9175=ORIENTED_EDGE ( 'NONE', *, *, #40466, .F. ) ;
#9179=CARTESIAN_POINT ( 'NONE',  ( 2.643462169533600914, -28.13401304854693663, -38.93558293168531037 ) ) ;
#9180=CARTESIAN_POINT ( 'NONE',  ( 0.1100247026804066219, -30.37337782329870350, -30.61332956994571575 ) ) ;
#9181=ORIENTED_EDGE ( 'NONE', *, *, #235, .F. ) ;
#9187=ORIENTED_EDGE ( 'NONE', *, *, #32181, .F. ) ;
#9193=CARTESIAN_POINT ( 'NONE',  ( -6.015611763856276717, -2.465697960551179513, 18.68122482568278997 ) ) ;
#9194=LINE ( 'NONE', #14226, #10642 ) ;
#9199=CARTESIAN_POINT ( 'NONE',  ( -5.995132425357893702, -4.869002713216700862, 18.20425902871266288 ) ) ;
#9200=VECTOR ( 'NONE', #57976, 999.9999999999998863 ) ;
#9201=DIRECTION ( 'NONE',  ( 0.000000000000000000, 0.000000000000000000, -1.000000000000000000 ) ) ;
#9204=ORIENTED_EDGE ( 'NONE', *, *, #2279, .F. ) ;
#9208=VERTEX_POINT ( 'NONE', #60196 ) ;
#9209=EDGE_LOOP ( 'NONE', ( #30149, #13529, #33866, #6800 ) ) ;
#9211=CARTESIAN_POINT ( 'NONE',  ( 0.1095718737110178836, -42.78833451865671123, 5.374020908746216740 ) ) ;
#9214=DIRECTION ( 'NONE',  ( 0.09835009131224552170, -0.7941905447268777785, -0.5996571005210378225 ) ) ;
#9215=CARTESIAN_POINT ( 'NONE',  ( -6.001507490154111224, -4.892199142591432626, 18.19774963328906736 ) ) ;
#9218=DIRECTION ( 'NONE',  ( 0.000000000000000000, 0.000000000000000000, 1.000000000000000000 ) ) ;
#9220=CARTESIAN_POINT ( 'NONE',  ( 4.322998006666179727, -4.155494336619063311, 47.80838462754057616 ) ) ;
#9224=CARTESIAN_POINT ( 'NONE',  ( 0.1073791018717483448, -34.50606437925530656, -25.86618856530698451 ) ) ;
#9233=CARTESIAN_POINT ( 'NONE',  ( 3.680974057930773924, -43.58300585207908995, -20.05478739720721038 ) ) ;
#9234=CARTESIAN_POINT ( 'NONE',  ( 2.301430502907645170, 4.990893951996359768, 47.77346269870101736 ) ) ;
#9236=ORIENTED_EDGE ( 'NONE', *, *, #4093, .T. ) ;
#9242=CARTESIAN_POINT ( 'NONE',  ( 1.827119703190779765, -4.394694966566802030, 42.82501615430323483 ) ) ;
#9243=CARTESIAN_POINT ( 'NONE',  ( 0.6017667736363749853, -44.31084570541189294, -18.73201910948646542 ) ) ;
#9246=VERTEX_POINT ( 'NONE', #3482 ) ;
#9249=CARTESIAN_POINT ( 'NONE',  ( 4.549368137175248350, -40.58005590356681580, -13.99871866169351442 ) ) ;
#9256=CARTESIAN_POINT ( 'NONE',  ( 0.09136607875274982415, 0.000000000000000000, 10.00000000000000000 ) ) ;
#9260=CARTESIAN_POINT ( 'NONE',  ( 2.643462169533600914, -34.93025802711748895, 32.97543604874614687 ) ) ;
#9267=ORIENTED_EDGE ( 'NONE', *, *, #38028, .F. ) ;
#9272=VERTEX_POINT ( 'NONE', #32641 ) ;
#9277=EDGE_CURVE ( 'NONE', #5799, #50136, #36966, .T. ) ;
#9291=CARTESIAN_POINT ( 'NONE',  ( 0.1102847568649952675, 16.41780866919043191, -39.87696813145912245 ) ) ;
#9296=LINE ( 'NONE', #28101, #23884 ) ;
#9300=CARTESIAN_POINT ( 'NONE',  ( 2.643462169533613793, -25.20536747735751604, -40.89244134039102363 ) ) ;
#9301=DIRECTION ( 'NONE',  ( 0.000000000000000000, 0.000000000000000000, 1.000000000000000000 ) ) ;
#9305=CARTESIAN_POINT ( 'NONE',  ( 0.5998501479064699549, 47.76154736470750350, 5.759754759340949271 ) ) ;
#9307=ADVANCED_FACE ( 'NONE', ( #37662 ), #47030, .F. ) ;
#9308=DIRECTION ( 'NONE',  ( -1.000000000000000000, -0.000000000000000000, -0.000000000000000000 ) ) ;
#9309=B_SPLINE_CURVE_WITH_KNOTS ( 'NONE', 3,
 ( #60999, #18418, #38161, #28114, #37857, #51592, #37538, #47853, #18106, #8688, #4280, #56917, #37229, #56299, #43163, #42543, #57207, #13412, #56610 ),
 .UNSPECIFIED., .F., .F.,
 ( 4, 3, 3, 3, 3, 3, 4 ),
 ( 1.161956753697875813E-16, 0.0002618519381806255915, 0.0003927759815485971679, 0.0005237000248299424543, 0.0006546240681324976083, 0.0007855481115631327092, 0.0009699050456655109419 ),
 .UNSPECIFIED. ) ;
#9311=CARTESIAN_POINT ( 'NONE',  ( 0.1310142868023669860, 22.11113027429286504, -37.02349354742221266 ) ) ;
#9323=ORIENTED_EDGE ( 'NONE', *, *, #44485, .F. ) ;
#9329=ORIENTED_EDGE ( 'NONE', *, *, #24824, .T. ) ;
#9331=EDGE_CURVE ( 'NONE', #58675, #43360, #47350, .T. ) ;
#9333=( BOUNDED_SURFACE ( )  B_SPLINE_SURFACE ( 3, 1, ( 
 ( #35813, #54880 ),
 ( #12016, #45520 ),
 ( #21693, #56736 ),
 ( #3801, #27018 ) ),
 .UNSPECIFIED., .F., .F., .F. ) 
 B_SPLINE_SURFACE_WITH_KNOTS ( ( 4, 4 ),
 ( 2, 2 ),
 ( 0.000000000000000000, 1.000000000000000000 ),
 ( 0.000000000000000000, 1.000000000000000000 ),
 .UNSPECIFIED. ) 
 GEOMETRIC_REPRESENTATION_ITEM ( )  RATIONAL_B_SPLINE_SURFACE ( (
 ( 1.000000000000000000, 1.000000000000000000),
 ( 0.7223157951917480446, 0.9931996967497186413),
 ( 0.7223157951917480446, 0.9931996967497186413),
 ( 1.000000000000000000, 1.000000000000000000) ) ) 
 REPRESENTATION_ITEM ( '' )  SURFACE ( )  );
#9342=( BOUNDED_SURFACE ( )  B_SPLINE_SURFACE ( 3, 1, ( 
 ( #31954, #27247 ),
 ( #26314, #55118 ),
 ( #41073, #45449 ),
 ( #2498, #21621 ) ),
 .UNSPECIFIED., .F., .F., .F. ) 
 B_SPLINE_SURFACE_WITH_KNOTS ( ( 4, 4 ),
 ( 2, 2 ),
 ( 0.000000000000000000, 1.000000000000000000 ),
 ( 0.000000000000000000, 1.000000000000000000 ),
 .UNSPECIFIED. ) 
 GEOMETRIC_REPRESENTATION_ITEM ( )  RATIONAL_B_SPLINE_SURFACE ( (
 ( 1.000000000000000000, 1.000000000000000000),
 ( 0.7223157951917480446, 0.9931996967497186413),
 ( 0.7223157951917480446, 0.9931996967497186413),
 ( 1.000000000000000000, 1.000000000000000000) ) ) 
 REPRESENTATION_ITEM ( '' )  SURFACE ( )  );
#9350=EDGE_LOOP ( 'NONE', ( #4071, #29435, #9361, #39183 ) ) ;
#9352=CARTESIAN_POINT ( 'NONE',  ( 0.5998501479064708430, -34.38546660123321175, 33.64490850298784608 ) ) ;
#9361=ORIENTED_EDGE ( 'NONE', *, *, #37068, .F. ) ;
#9362=CARTESIAN_POINT ( 'NONE',  ( 4.975801465491694664, -2.564218696447152279, -47.84403947906842092 ) ) ;
#9365=CARTESIAN_POINT ( 'NONE',  ( 0.5980894510889457338, 42.01322166096886690, 23.44630161211600949 ) ) ;
#9369=CARTESIAN_POINT ( 'NONE',  ( 0.5980894510889448457, 37.73932204245478772, 29.84264441023791292 ) ) ;
#9371=AXIS2_PLACEMENT_3D ( 'NONE', #24169, #14791, #38606 ) ;
#9375=ORIENTED_EDGE ( 'NONE', *, *, #22140, .T. ) ;
#9387=CARTESIAN_POINT ( 'NONE',  ( -5.995132425357893702, 14.95525565067290508, -11.46484027925352578 ) ) ;
#9389=CARTESIAN_POINT ( 'NONE',  ( 0.1100053167205930632, 37.43629428538733350, 21.40663161101006295 ) ) ;
#9399=CARTESIAN_POINT ( 'NONE',  ( -6.016489644550736315, 2.463898142942760661, 18.68142234211825325 ) ) ;
#9403=VERTEX_POINT ( 'NONE', #33883 ) ;
#9408=FACE_OUTER_BOUND ( 'NONE', #13827, .T. ) ;
#9409=VERTEX_POINT ( 'NONE', #9126 ) ;
#9412=EDGE_LOOP ( 'NONE', ( #57442, #10733, #57075, #39051 ) ) ;
#9416=CARTESIAN_POINT ( 'NONE',  ( -6.017396004339687465, -18.20079405513546433, -4.878103249821258203 ) ) ;
#9426=CARTESIAN_POINT ( 'NONE',  ( 0.7954196712028465122, -13.28627209367609474, 46.22745629466049877 ) ) ;
#9432=CARTESIAN_POINT ( 'NONE',  ( 0.2885697896453109368, -41.43179225254756659, -11.93479333319010216 ) ) ;
#9440=CARTESIAN_POINT ( 'NONE',  ( 4.975801465491695552, 3.702618843596801934, 47.76942479135487218 ) ) ;
#9446=AXIS2_PLACEMENT_3D ( 'NONE', #1058, #9860, #53659 ) ;
#9448=CARTESIAN_POINT ( 'NONE',  ( 0.3622758884714600280, 42.84426538328730771, -4.808133778521432866 ) ) ;
#9451=EDGE_CURVE ( 'NONE', #9272, #43892, #42251, .T. ) ;
#9452=CARTESIAN_POINT ( 'NONE',  ( 5.880360259849739535, 43.00389496650614518, -21.25991003419908054 ) ) ;
#9461=CARTESIAN_POINT ( 'NONE',  ( -2.708315649062916552, 14.20182604343555255, 3.532515819624394204 ) ) ;
#9462=CARTESIAN_POINT ( 'NONE',  ( -6.010958268070873523, -18.68034667844850460, 2.473955915502147107 ) ) ;
#9463=ADVANCED_FACE ( 'NONE', ( #24777 ), #51873, .F. ) ;
#9474=EDGE_CURVE ( 'NONE', #2450, #29811, #44838, .T. ) ;
#9480=VERTEX_POINT ( 'NONE', #35121 ) ;
#9481=ORIENTED_EDGE ( 'NONE', *, *, #55351, .T. ) ;
#9488=CARTESIAN_POINT ( 'NONE',  ( -2.569797478183790229, 11.87678401312194865, -8.547745408040670512 ) ) ;
#9490=B_SPLINE_CURVE_WITH_KNOTS ( 'NONE', 3,
 ( #9141, #61739, #27951, #3498 ),
 .UNSPECIFIED., .F., .F.,
 ( 4, 4 ),
 ( 2.292215966409847588E-17, 0.004564976165746187711 ),
 .UNSPECIFIED. ) ;
#9497=CARTESIAN_POINT ( 'NONE',  ( -6.016761891674565099, -2.462934516563935805, 18.68153697670640767 ) ) ;
#9502=CARTESIAN_POINT ( 'NONE',  ( 4.975801465491695552, 0.000000000000000000, 0.000000000000000000 ) ) ;
#9503=FACE_OUTER_BOUND ( 'NONE', #46168, .T. ) ;
#9507=ORIENTED_EDGE ( 'NONE', *, *, #12614, .F. ) ;
#9508=CARTESIAN_POINT ( 'NONE',  ( 0.3622758884714730732, -29.89648521331652731, 31.06363466427676201 ) ) ;
#9514=CARTESIAN_POINT ( 'NONE',  ( 0.1103744047535531458, -42.76053735246615872, 5.590449877749870566 ) ) ;
#9515=CARTESIAN_POINT ( 'NONE',  ( 0.1092565886968784594, -39.72209809039409834, 16.78938711553560026 ) ) ;
#9519=CARTESIAN_POINT ( 'NONE',  ( 0.1064266418746774995, 40.05351192729361287, -15.98292515284421533 ) ) ;
#9522=CARTESIAN_POINT ( 'NONE',  ( 4.975801465491695552, -45.55012473237743365, -14.85979367497158599 ) ) ;
#9524=CARTESIAN_POINT ( 'NONE',  ( 0.7048096507298579061, -44.11842270945960109, -19.18768066167107023 ) ) ;
#9531=CARTESIAN_POINT ( 'NONE',  ( 0.1095718737110178281, 42.72125633542926693, 5.883530294870284116 ) ) ;
#9536=( BOUNDED_SURFACE ( )  B_SPLINE_SURFACE ( 3, 1, ( 
 ( #49153, #30045 ),
 ( #6206, #53527 ),
 ( #58530, #10643 ),
 ( #43554, #44489 ) ),
 .UNSPECIFIED., .F., .F., .F. ) 
 B_SPLINE_SURFACE_WITH_KNOTS ( ( 4, 4 ),
 ( 2, 2 ),
 ( 0.000000000000000000, 1.000000000000000000 ),
 ( 0.000000000000000000, 1.000000000000000000 ),
 .UNSPECIFIED. ) 
 GEOMETRIC_REPRESENTATION_ITEM ( )  RATIONAL_B_SPLINE_SURFACE ( (
 ( 1.000000000000000000, 1.000000000000000000),
 ( 0.9751682680413298332, 0.9999560080971552356),
 ( 0.9751682680413298332, 0.9999560080971552356),
 ( 1.000000000000000000, 1.000000000000000000) ) ) 
 REPRESENTATION_ITEM ( '' )  SURFACE ( )  );
#9538=EDGE_CURVE ( 'NONE', #6553, #22299, #49501, .T. ) ;
#9541=CARTESIAN_POINT ( 'NONE',  ( 0.5998501479064708430, -46.33007877220729398, -12.95623334615486222 ) ) ;
#9544=ORIENTED_EDGE ( 'NONE', *, *, #25506, .T. ) ;
#9546=CARTESIAN_POINT ( 'NONE',  ( 0.1100247026804066219, 39.77655614012830654, 16.65964013375399588 ) ) ;
#9552=CARTESIAN_POINT ( 'NONE',  ( -6.015611763856276717, 17.40650793417844255, 7.216738110653344584 ) ) ;
#9553=ORIENTED_EDGE ( 'NONE', *, *, #50497, .F. ) ;
#9557=CARTESIAN_POINT ( 'NONE',  ( 2.643462169533600914, -30.32726672320828243, 37.25264019563361018 ) ) ;
#9558=CARTESIAN_POINT ( 'NONE',  ( 0.8751705887134553219, 13.30665218149297857, 46.21789262997761938 ) ) ;
#9562=CARTESIAN_POINT ( 'NONE',  ( 0.7245667037590739490, -17.64710816761290957, 44.74806999162959187 ) ) ;
#9563=CARTESIAN_POINT ( 'NONE',  ( 0.2885700199627514451, 10.38006184593202263, -41.84838128711413674 ) ) ;
#9566=CARTESIAN_POINT ( 'NONE',  ( -5.995132425357893702, -9.429450169548070804, 16.31525984181029898 ) ) ;
#9571=CARTESIAN_POINT ( 'NONE',  ( 0.6009453534118441853, 46.35353704332094082, 12.87216801774561326 ) ) ;
#9574=VERTEX_POINT ( 'NONE', #54807 ) ;
#9575=CARTESIAN_POINT ( 'NONE',  ( 1.827326673878743923, 34.89023127623421061, -25.21837361081552586 ) ) ;
#9577=CARTESIAN_POINT ( 'NONE',  ( 0.1102847568649952675, -37.39286109091562338, -21.48234084756682805 ) ) ;
#9578=ADVANCED_FACE ( 'NONE', ( #13163 ), #32315, .F. ) ;
#9580=CARTESIAN_POINT ( 'NONE',  ( -6.017396004339687465, 18.20140164570675978, -4.875835690938989053 ) ) ;
#9582=CARTESIAN_POINT ( 'NONE',  ( 0.1073791018717483448, -26.63563652260144821, -33.91564619577798823 ) ) ;
#9584=VERTEX_POINT ( 'NONE', #2802 ) ;
#9588=CARTESIAN_POINT ( 'NONE',  ( 0.5998501479064699549, -46.33007877220747872, 12.95623334615421740 ) ) ;
#9589=ORIENTED_EDGE ( 'NONE', *, *, #23311, .T. ) ;
#9595=CARTESIAN_POINT ( 'NONE',  ( 0.1092355843206037486, 16.78033551728664108, -39.72582785521899496 ) ) ;
#9597=CARTESIAN_POINT ( 'NONE',  ( 5.880360259849739535, -36.09847387447837974, -31.59460303415970017 ) ) ;
#9614=CARTESIAN_POINT ( 'NONE',  ( 2.301529144917014769, -11.18385659262710696, 46.71331407887419118 ) ) ;
#9615=EDGE_CURVE ( 'NONE', #31234, #33708, #30222, .T. ) ;
#9620=CARTESIAN_POINT ( 'NONE',  ( 0.3622758884714730732, 20.83792692158972670, -37.74294673546565804 ) ) ;
#9631=EDGE_CURVE ( 'NONE', #32619, #12277, #11611, .T. ) ;
#9641=AXIS2_PLACEMENT_3D ( 'NONE', #7413, #2097, #36898 ) ;
#9652=ORIENTED_EDGE ( 'NONE', *, *, #29175, .T. ) ;
#9654=ORIENTED_EDGE ( 'NONE', *, *, #59977, .F. ) ;
#9672=CARTESIAN_POINT ( 'NONE',  ( 0.1081432562775998946, -21.19449538864532556, -37.55692207416018391 ) ) ;
#9673=CARTESIAN_POINT ( 'NONE',  ( 0.6254311100348648456, 47.60023274471269872, 6.960804577576987562 ) ) ;
#9674=CARTESIAN_POINT ( 'NONE',  ( 3.680974057930773924, -42.44218549341225355, 22.36814223828894299 ) ) ;
#9675=CARTESIAN_POINT ( 'NONE',  ( 0.1098349054025746230, -34.34238705454320240, 26.08296594991481854 ) ) ;
#9677=EDGE_LOOP ( 'NONE', ( #19779, #12136, #50628, #42564 ) ) ;
#9688=EDGE_CURVE ( 'NONE', #40342, #50920, #6345, .T. ) ;
#9695=FACE_OUTER_BOUND ( 'NONE', #29934, .T. ) ;
#9704=CARTESIAN_POINT ( 'NONE',  ( 0.6254087463353908971, -23.45485308995630191, 42.00124903776029583 ) ) ;
#9706=( BOUNDED_SURFACE ( )  B_SPLINE_SURFACE ( 3, 1, ( 
 ( #26629, #12554 ),
 ( #2187, #6563 ),
 ( #50437, #40768 ),
 ( #7503, #16310 ) ),
 .UNSPECIFIED., .F., .F., .F. ) 
 B_SPLINE_SURFACE_WITH_KNOTS ( ( 4, 4 ),
 ( 2, 2 ),
 ( 0.000000000000000000, 1.000000000000000000 ),
 ( 0.000000000000000000, 1.000000000000000000 ),
 .UNSPECIFIED. ) 
 GEOMETRIC_REPRESENTATION_ITEM ( )  RATIONAL_B_SPLINE_SURFACE ( (
 ( 1.000000000000000000, 1.000000000000000000),
 ( 0.7223157951917476005, 0.9931996967497186413),
 ( 0.7223157951917476005, 0.9931996967497186413),
 ( 1.000000000000000000, 1.000000000000000000) ) ) 
 REPRESENTATION_ITEM ( '' )  SURFACE ( )  );
#9711=CARTESIAN_POINT ( 'NONE',  ( 2.301430502907644726, -44.85388302506918734, 17.18551536142172154 ) ) ;
#9712=CIRCLE ( 'NONE', #52672, 47.91270532121795611 ) ;
#9715=CARTESIAN_POINT ( 'NONE',  ( 4.975801465491694664, -45.55012473237763260, 14.85979367497093762 ) ) ;
#9716=CARTESIAN_POINT ( 'NONE',  ( 0.5998501479064699549, -12.95623334615470057, -46.33007877220734372 ) ) ;
#9719=ORIENTED_EDGE ( 'NONE', *, *, #25063, .T. ) ;
#9726=VERTEX_POINT ( 'NONE', #9362 ) ;
#9728=CARTESIAN_POINT ( 'NONE',  ( -6.017396004339686577, -18.20140164570665675, -4.875835690939370970 ) ) ;
#9729=ADVANCED_FACE ( 'NONE', ( #13465 ), #38739, .F. ) ;
#9750=CARTESIAN_POINT ( 'NONE',  ( -6.016761891674565099, -18.68153697670640057, -2.462934516564000198 ) ) ;
#9753=CARTESIAN_POINT ( 'NONE',  ( 0.6023143664670691511, 18.65155446683251839, -44.34466302085804301 ) ) ;
#9754=CARTESIAN_POINT ( 'NONE',  ( -2.708315649062916552, -14.20182604343557742, -3.532515819624296061 ) ) ;
#9756=B_SPLINE_CURVE_WITH_KNOTS ( 'NONE', 3,
 ( #47834, #28708, #33429, #57490 ),
 .UNSPECIFIED., .F., .F.,
 ( 4, 4 ),
 ( 7.046480070129584215E-18, 0.005014147105413696917 ),
 .UNSPECIFIED. ) ;
#9757=CARTESIAN_POINT ( 'NONE',  ( -6.016104459813371719, 0.005335450885065978234, 18.84322058118302579 ) ) ;
#9760=EDGE_CURVE ( 'NONE', #45826, #6741, #22690, .T. ) ;
#9766=CARTESIAN_POINT ( 'NONE',  ( 0.6028618097248863439, 48.10721794025128162, -0.1745704727160814207 ) ) ;
#9770=CARTESIAN_POINT ( 'NONE',  ( 0.6001305935487315502, -11.94532529598346038, -46.60388846085719194 ) ) ;
#9777=B_SPLINE_CURVE_WITH_KNOTS ( 'NONE', 3,
 ( #57324, #9426, #42976, #24772, #43915, #20086 ),
 .UNSPECIFIED., .F., .F.,
 ( 4, 2, 4 ),
 ( 1.266794085606387986E-16, 0.0002450741128632346190, 0.0004901482257263424947 ),
 .UNSPECIFIED. ) ;
#9792=VERTEX_POINT ( 'NONE', #19704 ) ;
#9799=CARTESIAN_POINT ( 'NONE',  ( 5.880360259849739535, -26.69116321728542829, -39.86101557989661615 ) ) ;
#9817=VERTEX_POINT ( 'NONE', #54728 ) ;
#9818=CARTESIAN_POINT ( 'NONE',  ( 0.5998501479064708430, -12.95623334615534716, 46.33007877220716608 ) ) ;
#9825=CARTESIAN_POINT ( 'NONE',  ( 0.7048096507298579061, -46.68221792389248037, 11.63498350884255750 ) ) ;
#9828=CONICAL_SURFACE ( 'NONE', #44869, 42.92674063221959813, 1.485477209440487556 ) ;
#9832=CARTESIAN_POINT ( 'NONE',  ( 4.549368137175248350, 0.000000000000000000, 0.000000000000000000 ) ) ;
#9835=CARTESIAN_POINT ( 'NONE',  ( 0.6001305935487315502, -24.50730504006429200, -41.40054608060284380 ) ) ;
#9837=FACE_OUTER_BOUND ( 'NONE', #31442, .T. ) ;
#9838=CARTESIAN_POINT ( 'NONE',  ( -5.995132425357893702, -2.468096378288251458, 18.68182899165010724 ) ) ;
#9844=CARTESIAN_POINT ( 'NONE',  ( 0.6030672727741701600, -18.32928433899722975, -44.47882233696916643 ) ) ;
#9846=VERTEX_POINT ( 'NONE', #31558 ) ;
#9849=CARTESIAN_POINT ( 'NONE',  ( -6.016761891674564211, 2.456125503350979677, -18.68243340030200272 ) ) ;
#9850=CARTESIAN_POINT ( 'NONE',  ( 0.1100053167205930771, -34.32189548568265991, -26.10991185395875291 ) ) ;
#9853=CARTESIAN_POINT ( 'NONE',  ( -6.015611763856276717, 7.216738110653516891, -17.40650793417836439 ) ) ;
#9854=CARTESIAN_POINT ( 'NONE',  ( 0.5998501479064708430, -46.60114184914326074, 11.94461217097388328 ) ) ;
#9860=DIRECTION ( 'NONE',  ( 1.000000000000000000, 0.000000000000000000, 0.000000000000000000 ) ) ;
#9864=ORIENTED_EDGE ( 'NONE', *, *, #36688, .F. ) ;
#9865=ORIENTED_EDGE ( 'NONE', *, *, #10807, .F. ) ;
#9871=VERTEX_POINT ( 'NONE', #45675 ) ;
#9874=DIRECTION ( 'NONE',  ( 0.000000000000000000, 0.000000000000000000, 1.000000000000000000 ) ) ;
#9876=EDGE_CURVE ( 'NONE', #20738, #20913, #246, .T. ) ;
#9878=CARTESIAN_POINT ( 'NONE',  ( 0.1310142868023669305, 17.08943085418587415, -39.59283406808313543 ) ) ;
#9884=CARTESIAN_POINT ( 'NONE',  ( 0.09136607875274982415, 9.539392014169456147, -3.000000000000000000 ) ) ;
#9886=ORIENTED_EDGE ( 'NONE', *, *, #46634, .F. ) ;
#9888=CARTESIAN_POINT ( 'NONE',  ( 3.680882792899937250, 22.36818923730770337, -42.44216617524794799 ) ) ;
#9890=VECTOR ( 'NONE', #28402, 999.9999999999998863 ) ;
#9893=CARTESIAN_POINT ( 'NONE',  ( -2.708315649062916552, 8.698422600177121211, -11.76894112707803863 ) ) ;
#9902=CARTESIAN_POINT ( 'NONE',  ( 0.1084644655670284202, -37.54424727804286022, -21.21700107124035029 ) ) ;
#9905=ORIENTED_EDGE ( 'NONE', *, *, #22654, .F. ) ;
#9906=CARTESIAN_POINT ( 'NONE',  ( -6.017396004339687465, 13.32495836419643176, -13.32329839588541098 ) ) ;
#9910=CARTESIAN_POINT ( 'NONE',  ( 0.5980894510889457338, -42.01322166096903743, -23.44630161211571462 ) ) ;
#9914=ADVANCED_FACE ( 'NONE', ( #45998 ), #22491, .F. ) ;
#9916=CARTESIAN_POINT ( 'NONE',  ( 4.975801465491695552, -27.09127437476353251, -39.51822597168487050 ) ) ;
#9934=CARTESIAN_POINT ( 'NONE',  ( 0.8751705887134423323, -28.56654290188627243, -38.69254731947824411 ) ) ;
#9940=CARTESIAN_POINT ( 'NONE',  ( 0.6030672727741701600, 47.68443224372862943, 6.365785297724940506 ) ) ;
#9951=CARTESIAN_POINT ( 'NONE',  ( 4.833616638992205949, 26.07076047129135787, -38.20222678111910852 ) ) ;
#9957=CARTESIAN_POINT ( 'NONE',  ( 4.322998006666179727, -27.50295597456480934, 39.32552843303803058 ) ) ;
#9968=CARTESIAN_POINT ( 'NONE',  ( 0.6027935024548037868, 33.89348162668930087, 34.14031893787236527 ) ) ;
#9974=CARTESIAN_POINT ( 'NONE',  ( 0.1310142868023697060, 43.11885108606329453, 0.6370537502137997299 ) ) ;
#9984=CARTESIAN_POINT ( 'NONE',  ( 1.827119703190779321, 37.88337895042268144, 20.44859290426050791 ) ) ;
#9985=CARTESIAN_POINT ( 'NONE',  ( 4.549368137175248350, -38.59302160394740611, -18.79584381673521065 ) ) ;
#9989=CARTESIAN_POINT ( 'NONE',  ( 0.2885697896453110478, 20.85752796052960889, 37.73587455644754840 ) ) ;
#9999=DIRECTION ( 'NONE',  ( -1.000000000000000000, -0.000000000000000000, -0.000000000000000000 ) ) ;
#10004=ORIENTED_EDGE ( 'NONE', *, *, #47299, .F. ) ;
#10005=EDGE_CURVE ( 'NONE', #14306, #23536, #5460, .T. ) ;
#10008=CARTESIAN_POINT ( 'NONE',  ( 3.238931869106854489, -12.88361013339135219, -41.01619136531521548 ) ) ;
#10013=DIRECTION ( 'NONE',  ( 0.000000000000000000, 0.000000000000000000, -1.000000000000000000 ) ) ;
#10017=DIRECTION ( 'NONE',  ( 0.000000000000000000, 0.000000000000000000, 1.000000000000000000 ) ) ;
#10019=CARTESIAN_POINT ( 'NONE',  ( -2.708315649062910779, -11.76894112707817897, 8.698422600176929365 ) ) ;
#10027=CARTESIAN_POINT ( 'NONE',  ( 0.2885700199627511675, -29.91358789498803361, 31.05173037893190013 ) ) ;
#10030=CARTESIAN_POINT ( 'NONE',  ( 0.8751705887134553219, -33.37254303619578621, 34.63284514348527665 ) ) ;
#10033=ORIENTED_EDGE ( 'NONE', *, *, #53974, .F. ) ;
#10034=FACE_OUTER_BOUND ( 'NONE', #6322, .T. ) ;
#10037=CARTESIAN_POINT ( 'NONE',  ( 0.6001305935487422083, -37.84751346122836679, -29.70149728382421728 ) ) ;
#10042=CARTESIAN_POINT ( 'NONE',  ( 0.1073791018717483448, 40.02496097243036388, 16.05399293000829175 ) ) ;
#10049=CARTESIAN_POINT ( 'NONE',  ( 0.6041374136657476912, 46.51335992032601752, 12.28249295042061817 ) ) ;
#10064=CARTESIAN_POINT ( 'NONE',  ( -2.708315649062910779, 10.53288422393055690, -10.16016146078278481 ) ) ;
#10070=CARTESIAN_POINT ( 'NONE',  ( 0.2885697896453107703, -40.13549262224790226, 15.75356890148085398 ) ) ;
#10080=CARTESIAN_POINT ( 'NONE',  ( -6.016489644550737204, -2.455165042129613617, -18.68257207665199005 ) ) ;
#10087=CARTESIAN_POINT ( 'NONE',  ( 4.691466044806103852, -39.84135254923150882, 20.01963481131589617 ) ) ;
#10094=DIRECTION ( 'NONE',  ( -1.000000000000000000, -0.000000000000000000, -0.000000000000000000 ) ) ;
#10100=AXIS2_PLACEMENT_3D ( 'NONE', #28562, #38305, #5655 ) ;
#10102=ORIENTED_EDGE ( 'NONE', *, *, #45014, .F. ) ;
#10103=CARTESIAN_POINT ( 'NONE',  ( 5.880360259849752858, -15.37531919565204852, -45.44137230084876933 ) ) ;
#10107=ORIENTED_EDGE ( 'NONE', *, *, #13247, .T. ) ;
#10113=CARTESIAN_POINT ( 'NONE',  ( -5.995132425357893702, 18.20425902871267354, 4.869002713216636913 ) ) ;
#10132=CARTESIAN_POINT ( 'NONE',  ( 1.827119703190777988, -31.30004882613822303, -29.55676396270173711 ) ) ;
#10139=ORIENTED_EDGE ( 'NONE', *, *, #5282, .F. ) ;
#10140=DIRECTION ( 'NONE',  ( 1.000000000000000000, 0.000000000000000000, 0.000000000000000000 ) ) ;
#10141=LINE ( 'NONE', #724, #12709 ) ;
#10142=CARTESIAN_POINT ( 'NONE',  ( 0.1073791018717578927, 33.91564619577771111, 26.63563652260178927 ) ) ;
#10143=ADVANCED_FACE ( 'NONE', ( #48133 ), #53827, .F. ) ;
#10152=CARTESIAN_POINT ( 'NONE',  ( 4.322998006666179727, 32.40067585697798336, -35.39923696758977911 ) ) ;
#10159=B_SPLINE_CURVE_WITH_KNOTS ( 'NONE', 3,
 ( #25569, #6427, #30265, #44706 ),
 .UNSPECIFIED., .F., .F.,
 ( 4, 4 ),
 ( 0.000000000000000000, 0.004445488388166993383 ),
 .UNSPECIFIED. ) ;
#10160=CARTESIAN_POINT ( 'NONE',  ( 0.5998501479064708430, -24.50586714782633280, 41.39809967730445095 ) ) ;
#10162=CARTESIAN_POINT ( 'NONE',  ( 0.5988103564986357874, 23.52668867203648517, -41.96244062389627061 ) ) ;
#10163=CARTESIAN_POINT ( 'NONE',  ( 0.3622758884714730732, 31.06363466427686504, 29.89648521331642428 ) ) ;
#10164=( BOUNDED_SURFACE ( )  B_SPLINE_SURFACE ( 3, 1, ( 
 ( #5115, #33662 ),
 ( #42456, #52743 ),
 ( #53353, #9524 ),
 ( #24244, #23634 ) ),
 .UNSPECIFIED., .F., .F., .F. ) 
 B_SPLINE_SURFACE_WITH_KNOTS ( ( 4, 4 ),
 ( 2, 2 ),
 ( 0.000000000000000000, 1.000000000000000000 ),
 ( 0.000000000000000000, 1.000000000000000000 ),
 .UNSPECIFIED. ) 
 GEOMETRIC_REPRESENTATION_ITEM ( )  RATIONAL_B_SPLINE_SURFACE ( (
 ( 1.000000000000000000, 1.000000000000000000),
 ( 0.9953040768229013402, 0.8617119497784988535),
 ( 0.9953040768229013402, 0.8617119497784988535),
 ( 1.000000000000000000, 1.000000000000000000) ) ) 
 REPRESENTATION_ITEM ( '' )  SURFACE ( )  );
#10171=ORIENTED_EDGE ( 'NONE', *, *, #27355, .T. ) ;
#10178=CARTESIAN_POINT ( 'NONE',  ( 0.1073791018717578927, -11.62916352156179123, 41.52698815987148606 ) ) ;
#10183=EDGE_LOOP ( 'NONE', ( #31528, #45968, #2037, #2732 ) ) ;
#10194=ORIENTED_EDGE ( 'NONE', *, *, #24626, .F. ) ;
#10198=CARTESIAN_POINT ( 'NONE',  ( 0.8760168074886960365, -34.63873394077511136, 33.37827814204065646 ) ) ;
#10200=CARTESIAN_POINT ( 'NONE',  ( 4.975801465491695552, -47.10002938642136883, -8.787181743659990829 ) ) ;
#10204=VERTEX_POINT ( 'NONE', #13242 ) ;
#10215=CARTESIAN_POINT ( 'NONE',  ( 4.975801465491694664, -40.15204426031552032, 26.14269827151608894 ) ) ;
#10216=CARTESIAN_POINT ( 'NONE',  ( -2.569797478183790229, 14.62602397812940680, 0.4487456364279327481 ) ) ;
#10219=CARTESIAN_POINT ( 'NONE',  ( 0.7048096507298579061, -42.08020459959998050, 23.32077812596807576 ) ) ;
#10220=CARTESIAN_POINT ( 'NONE',  ( 4.691466044806102076, -24.49380602310786870, -37.25818859570297548 ) ) ;
#10233=DIRECTION ( 'NONE',  ( 0.000000000000000000, 0.000000000000000000, 1.000000000000000000 ) ) ;
#10234=CARTESIAN_POINT ( 'NONE',  ( 4.322998006666179727, 27.50295597456451802, -39.32552843303822243 ) ) ;
#10248=VERTEX_POINT ( 'NONE', #7038 ) ;
#10249=ORIENTED_EDGE ( 'NONE', *, *, #36588, .T. ) ;
#10252=CARTESIAN_POINT ( 'NONE',  ( 0.1098349054025746230, 16.30574661324314079, 39.92296693299713439 ) ) ;
#10256=CARTESIAN_POINT ( 'NONE',  ( -6.001507490154110336, 18.68062548815628787, -2.475062734132249975 ) ) ;
#10261=EDGE_CURVE ( 'NONE', #7367, #49767, #50809, .T. ) ;
#10265=LINE ( 'NONE', #28745, #21770 ) ;
#10275=ORIENTED_EDGE ( 'NONE', *, *, #36168, .F. ) ;
#10277=CARTESIAN_POINT ( 'NONE',  ( 4.975801465491694664, -27.09127437476410805, 39.51822597168447260 ) ) ;
#10280=B_SPLINE_CURVE_WITH_KNOTS ( 'NONE', 3,
 ( #15638, #10008, #52903, #24715 ),
 .UNSPECIFIED., .F., .F.,
 ( 4, 4 ),
 ( 6.254634441385501517E-18, 0.004566006591234645501 ),
 .UNSPECIFIED. ) ;
#10286=( BOUNDED_SURFACE ( )  B_SPLINE_SURFACE ( 3, 1, ( 
 ( #18328, #56511 ),
 ( #9215, #37759 ),
 ( #32731, #61813 ),
 ( #18948, #409 ) ),
 .UNSPECIFIED., .F., .F., .F. ) 
 B_SPLINE_SURFACE_WITH_KNOTS ( ( 4, 4 ),
 ( 2, 2 ),
 ( 0.000000000000000000, 1.000000000000000000 ),
 ( 0.000000000000000000, 1.000000000000000000 ),
 .UNSPECIFIED. ) 
 GEOMETRIC_REPRESENTATION_ITEM ( )  RATIONAL_B_SPLINE_SURFACE ( (
 ( 1.000000000000000000, 1.000000000000000000),
 ( 0.7223157951917476005, 0.9931996967497186413),
 ( 0.7223157951917476005, 0.9931996967497186413),
 ( 1.000000000000000000, 1.000000000000000000) ) ) 
 REPRESENTATION_ITEM ( '' )  SURFACE ( )  );
#10289=CARTESIAN_POINT ( 'NONE',  ( 0.1073791018717578927, 41.52698815987152159, 11.62916352156164557 ) ) ;
#10304=CARTESIAN_POINT ( 'NONE',  ( 4.549368137175248350, -28.14399996863522446, 32.41327393324091588 ) ) ;
#10308=ORIENTED_EDGE ( 'NONE', *, *, #42331, .F. ) ;
#10309=CARTESIAN_POINT ( 'NONE',  ( 0.6023142530420679819, 12.70386526143707684, 46.39979989577485497 ) ) ;
#10314=CARTESIAN_POINT ( 'NONE',  ( -6.016761891674565099, 16.32039929810269996, -9.418621820384323939 ) ) ;
#10318=CARTESIAN_POINT ( 'NONE',  ( 0.8751705887134553219, 19.22545746485597817, 44.08562551107088723 ) ) ;
#10320=CARTESIAN_POINT ( 'NONE',  ( 1.827119703190780653, 34.89020442382223308, 25.21842556008197533 ) ) ;
#10321=ADVANCED_FACE ( 'NONE', ( #57651 ), #57900, .F. ) ;
#10322=CARTESIAN_POINT ( 'NONE',  ( -5.995132425357893702, -7.219211173946362692, -17.40647075750124273 ) ) ;
#10326=ORIENTED_EDGE ( 'NONE', *, *, #37473, .F. ) ;
#10330=B_SPLINE_CURVE_WITH_KNOTS ( 'NONE', 3,
 ( #10839, #29932, #49039, #59656 ),
 .UNSPECIFIED., .F., .F.,
 ( 4, 4 ),
 ( 0.000000000000000000, 0.005014147105413700387 ),
 .UNSPECIFIED. ) ;
#10336=VERTEX_POINT ( 'NONE', #24477 ) ;
#10361=( BOUNDED_SURFACE ( )  B_SPLINE_SURFACE ( 3, 1, ( 
 ( #43304, #15716 ),
 ( #33585, #10393 ),
 ( #972, #1270 ),
 ( #15096, #58275 ) ),
 .UNSPECIFIED., .F., .F., .F. ) 
 B_SPLINE_SURFACE_WITH_KNOTS ( ( 4, 4 ),
 ( 2, 2 ),
 ( 0.000000000000000000, 1.000000000000000000 ),
 ( 0.000000000000000000, 1.000000000000000000 ),
 .UNSPECIFIED. ) 
 GEOMETRIC_REPRESENTATION_ITEM ( )  RATIONAL_B_SPLINE_SURFACE ( (
 ( 1.000000000000000000, 1.000000000000000000),
 ( 0.7223157951917476005, 0.9931996967497186413),
 ( 0.7223157951917476005, 0.9931996967497186413),
 ( 1.000000000000000000, 1.000000000000000000) ) ) 
 REPRESENTATION_ITEM ( '' )  SURFACE ( )  );
#10363=CARTESIAN_POINT ( 'NONE',  ( 0.6001305935487422083, 46.60388846085706405, 11.94532529598394177 ) ) ;
#10374=LINE ( 'NONE', #47970, #35785 ) ;
#10376=CARTESIAN_POINT ( 'NONE',  ( 2.301529144917015213, -7.543875168382815133, -47.43735140118861437 ) ) ;
#10380=ORIENTED_EDGE ( 'NONE', *, *, #43275, .F. ) ;
#10384=CARTESIAN_POINT ( 'NONE',  ( 0.1064266418746776244, -40.05351192729372656, 15.98292515284391335 ) ) ;
#10393=CARTESIAN_POINT ( 'NONE',  ( 4.322998006666179727, -39.32552843303831480, -27.50295597456437591 ) ) ;
#10396=CARTESIAN_POINT ( 'NONE',  ( 0.3622758884714600280, -33.69533458712325569, -26.89560658783373626 ) ) ;
#10399=CARTESIAN_POINT ( 'NONE',  ( 4.549368137175248350, -38.40568845698290801, 19.17571786012255686 ) ) ;
#10403=CARTESIAN_POINT ( 'NONE',  ( 0.8751705887134423323, 48.08707113907594533, 0.8911681664090089772 ) ) ;
#10408=CARTESIAN_POINT ( 'NONE',  ( -6.016761891674564211, 9.418621820384725396, -16.32039929810246903 ) ) ;
#10409=EDGE_CURVE ( 'NONE', #43794, #30127, #51738, .T. ) ;
#10417=ORIENTED_EDGE ( 'NONE', *, *, #34037, .T. ) ;
#10419=CARTESIAN_POINT ( 'NONE',  ( 0.5980894510889448457, 24.66136644716821280, -41.31170365136863154 ) ) ;
#10420=VERTEX_POINT ( 'NONE', #21329 ) ;
#10429=EDGE_LOOP ( 'NONE', ( #5535, #31289, #21635, #60056 ) ) ;
#10435=CARTESIAN_POINT ( 'NONE',  ( -5.995132425357893702, -17.40647075750111483, -7.219211173946675331 ) ) ;
#10436=CARTESIAN_POINT ( 'NONE',  ( 0.8760168074887076939, 5.394043284319499421, -47.80016357497244428 ) ) ;
#10444=LINE ( 'NONE', #12309, #31039 ) ;
#10445=ORIENTED_EDGE ( 'NONE', *, *, #18274, .T. ) ;
#10451=ORIENTED_EDGE ( 'NONE', *, *, #1057, .F. ) ;
#10462=CARTESIAN_POINT ( 'NONE',  ( 0.1101816497532063233, 30.39741055095859323, -30.58948775778055662 ) ) ;
#10478=FACE_OUTER_BOUND ( 'NONE', #42129, .T. ) ;
#10497=DIRECTION ( 'NONE',  ( 0.09835009131224552170, 0.007732607185417008852, 0.9951218349151971232 ) ) ;
#10506=VERTEX_POINT ( 'NONE', #31033 ) ;
#10515=CARTESIAN_POINT ( 'NONE',  ( 0.1100053167205930632, -37.43629428538748272, -21.40663161100980005 ) ) ;
#10523=CARTESIAN_POINT ( 'NONE',  ( 0.2224561200757607382, 39.54039348282956468, 17.20021002050938463 ) ) ;
#10540=MANIFOLD_SOLID_BREP ( 'Move Face1', #53014 ) ;
#10541=CARTESIAN_POINT ( 'NONE',  ( -6.010958268070873523, -11.48268200989207877, 14.94067681728545871 ) ) ;
#10542=CARTESIAN_POINT ( 'NONE',  ( 0.1073791018717578927, -26.63563652260192427, 33.91564619577761874 ) ) ;
#10546=CARTESIAN_POINT ( 'NONE',  ( 0.6031356755773454870, 38.16618524502122511, -29.28597628606506831 ) ) ;
#10548=CARTESIAN_POINT ( 'NONE',  ( 0.6027935024548037868, -0.1745403365874843293, 48.10716172909472022 ) ) ;
#10553=EDGE_LOOP ( 'NONE', ( #61787, #10451, #682, #20587 ) ) ;
#10556=AXIS2_PLACEMENT_3D ( 'NONE', #46956, #47247, #8392 ) ;
#10559=EDGE_CURVE ( 'NONE', #5852, #43474, #35354, .T. ) ;
#10563=CARTESIAN_POINT ( 'NONE',  ( 0.5988103564986357874, 11.86435738293443087, -46.62176022926374941 ) ) ;
#10572=EDGE_LOOP ( 'NONE', ( #49952, #19279, #17902, #12243 ) ) ;
#10583=CARTESIAN_POINT ( 'NONE',  ( 0.5988103622719989083, 23.52668907282285460, 41.96244039798798298 ) ) ;
#10591=VERTEX_POINT ( 'NONE', #56363 ) ;
#10593=B_SPLINE_CURVE_WITH_KNOTS ( 'NONE', 3,
 ( #44701, #11173, #49678, #34993 ),
 .UNSPECIFIED., .F., .F.,
 ( 4, 4 ),
 ( 0.000000000000000000, 0.004445488388166993383 ),
 .UNSPECIFIED. ) ;
#10599=EDGE_CURVE ( 'NONE', #19445, #28616, #53942, .T. ) ;
#10603=CARTESIAN_POINT ( 'NONE',  ( 4.549368137175248350, -19.17571786012351254, 38.40568845698243194 ) ) ;
#10612=CARTESIAN_POINT ( 'NONE',  ( 3.238931869106854045, 9.350562014686129686, -41.96286875554259410 ) ) ;
#10616=EDGE_LOOP ( 'NONE', ( #45754, #33500, #2973, #32182 ) ) ;
#10621=B_SPLINE_CURVE_WITH_KNOTS ( 'NONE', 3,
 ( #4245, #8969, #41576, #47197 ),
 .UNSPECIFIED., .F., .F.,
 ( 4, 4 ),
 ( 0.000000000000000000, 0.004445488388166991649 ),
 .UNSPECIFIED. ) ;
#10624=DIRECTION ( 'NONE',  ( -1.000000000000000000, -0.000000000000000000, -0.000000000000000000 ) ) ;
#10625=CARTESIAN_POINT ( 'NONE',  ( 0.5998501479064699549, -47.62484632993692912, 6.798102206413326520 ) ) ;
#10632=CARTESIAN_POINT ( 'NONE',  ( 0.3622758884714600280, 20.83792692158919735, 37.74294673546592804 ) ) ;
#10636=CARTESIAN_POINT ( 'NONE',  ( 0.8751705887134553219, 41.19904111682508585, -24.81530984069164703 ) ) ;
#10638=ADVANCED_FACE ( 'NONE', ( #55438 ), #28809, .F. ) ;
#10641=CARTESIAN_POINT ( 'NONE',  ( 0.1101816497532062955, 37.41460501058185883, 21.44450189183881861 ) ) ;
#10642=VECTOR ( 'NONE', #38344, 1000.000000000000114 ) ;
#10643=CARTESIAN_POINT ( 'NONE',  ( 0.6041374136657475802, 12.28249295041982947, 46.51335992032623068 ) ) ;
#10647=VERTEX_POINT ( 'NONE', #29105 ) ;
#10652=ORIENTED_EDGE ( 'NONE', *, *, #50482, .T. ) ;
#10656=ORIENTED_EDGE ( 'NONE', *, *, #38755, .F. ) ;
#10657=AXIS2_PLACEMENT_3D ( 'NONE', #7279, #60525, #17638 ) ;
#10658=CARTESIAN_POINT ( 'NONE',  ( 4.322998006666165516, -14.45630056002971742, 45.75942687572273826 ) ) ;
#10660=CARTESIAN_POINT ( 'NONE',  ( -6.010958268070873523, 17.41463273278788648, -7.197664668556254419 ) ) ;
#10666=ORIENTED_EDGE ( 'NONE', *, *, #42115, .T. ) ;
#10675=EDGE_CURVE ( 'NONE', #47799, #37650, #43229, .T. ) ;
#10676=CARTESIAN_POINT ( 'NONE',  ( 4.975801465491695552, -14.85979367497206205, 45.55012473237727733 ) ) ;
#10677=CARTESIAN_POINT ( 'NONE',  ( -5.995132425357893702, 16.31525984181046240, -9.429450169547783034 ) ) ;
#10681=ORIENTED_EDGE ( 'NONE', *, *, #6750, .F. ) ;
#10687=CARTESIAN_POINT ( 'NONE',  ( 0.6254087463353913412, -0.6881259009464468779, -48.10157520235525652 ) ) ;
#10688=CARTESIAN_POINT ( 'NONE',  ( 0.7954196712028467342, 13.28627209367577677, -46.22745629466059825 ) ) ;
#10701=FACE_OUTER_BOUND ( 'NONE', #46080, .T. ) ;
#10703=CARTESIAN_POINT ( 'NONE',  ( 0.3622758884714730732, 6.444611261694017657, 42.62881903538212924 ) ) ;
#10706=CARTESIAN_POINT ( 'NONE',  ( -6.016104459813374383, 9.426230926598869075, -16.31603998697559987 ) ) ;
#10707=CARTESIAN_POINT ( 'NONE',  ( 0.8751705887134423323, -42.09020928323391075, 23.27176129838352736 ) ) ;
#10712=( BOUNDED_SURFACE ( )  B_SPLINE_SURFACE ( 3, 1, ( 
 ( #5498, #31174 ),
 ( #22093, #7344 ),
 ( #21787, #26473 ),
 ( #45000, #2347 ) ),
 .UNSPECIFIED., .F., .F., .F. ) 
 B_SPLINE_SURFACE_WITH_KNOTS ( ( 4, 4 ),
 ( 2, 2 ),
 ( 0.000000000000000000, 1.000000000000000000 ),
 ( 0.000000000000000000, 1.000000000000000000 ),
 .UNSPECIFIED. ) 
 GEOMETRIC_REPRESENTATION_ITEM ( )  RATIONAL_B_SPLINE_SURFACE ( (
 ( 1.000000000000000000, 1.000000000000000000),
 ( 0.9751682680413298332, 0.9999560080971552356),
 ( 0.9751682680413298332, 0.9999560080971552356),
 ( 1.000000000000000000, 1.000000000000000000) ) ) 
 REPRESENTATION_ITEM ( '' )  SURFACE ( )  );
#10713=B_SPLINE_CURVE_WITH_KNOTS ( 'NONE', 3,
 ( #664, #20718, #16026, #30405, #57978, #29796 ),
 .UNSPECIFIED., .F., .F.,
 ( 4, 2, 4 ),
 ( 1.258037581941437391E-16, 0.0002450741128632354863, 0.0004901482257263450968 ),
 .UNSPECIFIED. ) ;
#10725=ORIENTED_EDGE ( 'NONE', *, *, #46027, .T. ) ;
#10726=EDGE_CURVE ( 'NONE', #39562, #20774, #13722, .T. ) ;
#10730=MECHANICAL_DESIGN_GEOMETRIC_PRESENTATION_REPRESENTATION('',(#21724),#35749);
#10732=VECTOR ( 'NONE', #1467, 1000.000000000000000 ) ;
#10733=ORIENTED_EDGE ( 'NONE', *, *, #14261, .F. ) ;
#10734=EDGE_LOOP ( 'NONE', ( #5374, #25052, #14817, #8940 ) ) ;
#10735=CARTESIAN_POINT ( 'NONE',  ( 0.1102144999581332746, 11.03964818279716020, 41.68747259405353844 ) ) ;
#10738=CARTESIAN_POINT ( 'NONE',  ( 0.8751705887134553219, -23.27176129838455054, 42.09020928323333521 ) ) ;
#10739=VERTEX_POINT ( 'NONE', #51666 ) ;
#10741=CARTESIAN_POINT ( 'NONE',  ( -6.016489644550737204, 2.463898142943031555, -18.68142234211821773 ) ) ;
#10744=ORIENTED_EDGE ( 'NONE', *, *, #1898, .T. ) ;
#10745=CARTESIAN_POINT ( 'NONE',  ( 0.6009452777970412107, -18.00606236585402087, 44.61081509289873281 ) ) ;
#10747=CARTESIAN_POINT ( 'NONE',  ( 0.1064266379913940963, 41.50637574965949028, -11.70292640078110935 ) ) ;
#10748=CARTESIAN_POINT ( 'NONE',  ( 0.1073791018717578927, -30.83464511437158961, 30.14884492832337060 ) ) ;
#10764=EDGE_CURVE ( 'NONE', #17692, #21442, #9140, .T. ) ;
#10769=CARTESIAN_POINT ( 'NONE',  ( -6.016489644550736315, 13.32104266208117771, -13.32727118274423894 ) ) ;
#10770=CARTESIAN_POINT ( 'NONE',  ( 0.1102144999581332746, -39.88986724628646385, 16.38650952318839060 ) ) ;
#10772=CARTESIAN_POINT ( 'NONE',  ( 0.1100247026804066219, 34.31594964380183654, -26.11768802553209312 ) ) ;
#10775=CARTESIAN_POINT ( 'NONE',  ( 3.680974057930773924, 27.71659654258243322, 39.15945827951719593 ) ) ;
#10777=CARTESIAN_POINT ( 'NONE',  ( 0.1097557419366048670, 30.33543403792237925, -30.65094619415035737 ) ) ;
#10778=CARTESIAN_POINT ( 'NONE',  ( 0.6017667736363750963, -6.625250263233982473, 47.64919355032676407 ) ) ;
#10779=EDGE_CURVE ( 'NONE', #24396, #46146, #1819, .T. ) ;
#10786=CARTESIAN_POINT ( 'NONE',  ( 0.6023142530420679819, -23.82662387835896212, 41.79260242564358663 ) ) ;
#10789=CARTESIAN_POINT ( 'NONE',  ( 4.691466044806102076, -43.66525414675636085, -9.025781474741316757 ) ) ;
#10797=CARTESIAN_POINT ( 'NONE',  ( 0.6254087463353920073, -48.10157520235525652, 0.6881259009466142995 ) ) ;
#10799=ORIENTED_EDGE ( 'NONE', *, *, #42104, .F. ) ;
#10800=ORIENTED_EDGE ( 'NONE', *, *, #25666, .T. ) ;
#10804=VECTOR ( 'NONE', #14706, 1000.000000000000114 ) ;
#10807=EDGE_CURVE ( 'NONE', #940, #19546, #39135, .T. ) ;
#10809=CONICAL_SURFACE ( 'NONE', #13811, 42.92674063221959813, 1.485477209440487556 ) ;
#10816=CARTESIAN_POINT ( 'NONE',  ( -6.016761891674564211, -7.207804629151436160, 17.41015286184800459 ) ) ;
#10818=EDGE_LOOP ( 'NONE', ( #51112, #40632, #61833, #58866 ) ) ;
#10820=CARTESIAN_POINT ( 'NONE',  ( -6.001507490154111224, 9.435425682281048054, -16.31148204059937257 ) ) ;
#10830=CARTESIAN_POINT ( 'NONE',  ( 0.1104177457020372732, -37.34931850022154975, -21.55798761925374407 ) ) ;
#10833=ORIENTED_EDGE ( 'NONE', *, *, #6750, .T. ) ;
#10839=CARTESIAN_POINT ( 'NONE',  ( 4.549368137175248350, 13.99871866169305434, 40.58005590356696501 ) ) ;
#10842=CARTESIAN_POINT ( 'NONE',  ( 0.7954190325252784577, -5.415566973723597854, 47.79303692714232454 ) ) ;
#10854=( GEOMETRIC_REPRESENTATION_CONTEXT ( 3 ) GLOBAL_UNCERTAINTY_ASSIGNED_CONTEXT ( ( #41794 ) ) GLOBAL_UNIT_ASSIGNED_CONTEXT ( ( #42001, #22870, #60438 ) ) REPRESENTATION_CONTEXT ( 'NONE', 'WORKASPACE' ) );
#10863=FACE_OUTER_BOUND ( 'NONE', #54293, .T. ) ;
#10870=CARTESIAN_POINT ( 'NONE',  ( 0.2885697896453108813, -6.424755442172918940, 42.63514065501003358 ) ) ;
#10874=CARTESIAN_POINT ( 'NONE',  ( 0.8751705887134553219, -44.08562551107095828, 19.22545746485582185 ) ) ;
#10886=B_SPLINE_CURVE_WITH_KNOTS ( 'NONE', 3,
 ( #49633, #1088, #20833, #43743 ),
 .UNSPECIFIED., .F., .F.,
 ( 4, 4 ),
 ( 0.000000000000000000, 0.005014147105413700387 ),
 .UNSPECIFIED. ) ;
#10889=CARTESIAN_POINT ( 'NONE',  ( 4.549368137175248350, -8.582197505784725067, 42.06008734272381133 ) ) ;
#10892=CARTESIAN_POINT ( 'NONE',  ( 0.6254087463353908971, -11.78492518233843001, 46.64065386173393790 ) ) ;
#10899=VERTEX_POINT ( 'NONE', #46018 ) ;
#10921=CARTESIAN_POINT ( 'NONE',  ( -6.017396004339686577, 7.209881890566790297, -17.40926186480771776 ) ) ;
#10922=EDGE_CURVE ( 'NONE', #36895, #40762, #43561, .T. ) ;
#10925=ORIENTED_EDGE ( 'NONE', *, *, #3684, .F. ) ;
#10930=CARTESIAN_POINT ( 'NONE',  ( 4.975801465491694664, 40.15204426031534268, -26.14269827151636605 ) ) ;
#10932=CARTESIAN_POINT ( 'NONE',  ( 0.1310142868023667639, 30.03916697317172790, 30.94009702668483186 ) ) ;
#10933=AXIS2_PLACEMENT_3D ( 'NONE', #15620, #39438, #58490 ) ;
#10936=CIRCLE ( 'NONE', #12905, 47.91270532121795611 ) ;
#10945=CARTESIAN_POINT ( 'NONE',  ( 4.549368137175248350, -18.79584381673505789, -38.59302160394747006 ) ) ;
#10947=CARTESIAN_POINT ( 'NONE',  ( 0.8760168074886965917, 44.77533136581881479, -17.58183840866353265 ) ) ;
#10949=CARTESIAN_POINT ( 'NONE',  ( -6.016489644550737204, -18.20227673842147809, 4.872725758886126357 ) ) ;
#10954=CIRCLE ( 'NONE', #25966, 42.92674063221959813 ) ;
#10955=ORIENTED_EDGE ( 'NONE', *, *, #29340, .T. ) ;
#10957=CIRCLE ( 'NONE', #4887, 42.92674063221959813 ) ;
#10958=CARTESIAN_POINT ( 'NONE',  ( 0.1102847568649952675, 43.12433804869904463, -0.09217763870855683050 ) ) ;
#10961=CARTESIAN_POINT ( 'NONE',  ( -2.569797478183783568, 0.4487456364276796728, 14.62602397812941568 ) ) ;
#10967=CARTESIAN_POINT ( 'NONE',  ( -2.569797478183790229, -14.55946937464484847, 1.464172661883917703 ) ) ;
#10969=CARTESIAN_POINT ( 'NONE',  ( -6.016489644550737204, -18.68142234211822839, -2.463898142942957836 ) ) ;
#10970=EDGE_CURVE ( 'NONE', #46146, #17208, #29338, .T. ) ;
#10973=CARTESIAN_POINT ( 'NONE',  ( -5.995132425357893702, 4.869002713216827871, -18.20425902871262736 ) ) ;
#10986=( BOUNDED_SURFACE ( )  B_SPLINE_SURFACE ( 3, 1, ( 
 ( #59800, #6524 ),
 ( #36027, #11586 ),
 ( #39490, #10658 ),
 ( #10973, #5913 ) ),
 .UNSPECIFIED., .F., .F., .F. ) 
 B_SPLINE_SURFACE_WITH_KNOTS ( ( 4, 4 ),
 ( 2, 2 ),
 ( 0.000000000000000000, 1.000000000000000000 ),
 ( 0.000000000000000000, 1.000000000000000000 ),
 .UNSPECIFIED. ) 
 GEOMETRIC_REPRESENTATION_ITEM ( )  RATIONAL_B_SPLINE_SURFACE ( (
 ( 1.000000000000000000, 1.000000000000000000),
 ( 0.7223157951917480446, 0.9931996967497186413),
 ( 0.7223157951917480446, 0.9931996967497186413),
 ( 1.000000000000000000, 1.000000000000000000) ) ) 
 REPRESENTATION_ITEM ( '' )  SURFACE ( )  );
#10990=CARTESIAN_POINT ( 'NONE',  ( 0.6017666602106489515, 24.35550044372386580, 41.48673504406954038 ) ) ;
#10991=CARTESIAN_POINT ( 'NONE',  ( 0.6025881611877910160, 44.36157157392728578, 18.61132239451801595 ) ) ;
#10992=ORIENTED_EDGE ( 'NONE', *, *, #20312, .T. ) ;
#11003=FACE_OUTER_BOUND ( 'NONE', #35337, .T. ) ;
#11004=CARTESIAN_POINT ( 'NONE',  ( 0.8751705887134423323, -46.21789262997747727, -13.30665218149346529 ) ) ;
#11006=FACE_OUTER_BOUND ( 'NONE', #30682, .T. ) ;
#11007=CIRCLE ( 'NONE', #58952, 42.92674063221959813 ) ;
#11009=CARTESIAN_POINT ( 'NONE',  ( 0.6027935024548037868, 18.57106801640299309, -44.37842839362955516 ) ) ;
#11018=VECTOR ( 'NONE', #58343, 1000.000000000000114 ) ;
#11021=CARTESIAN_POINT ( 'NONE',  ( 4.691466044806103852, 33.30232861642433306, -29.64918311951093699 ) ) ;
#11026=DIRECTION ( 'NONE',  ( 0.09835009131224567436, 0.2500873580884576119, 0.9632152266566431642 ) ) ;
#11035=B_SPLINE_CURVE_WITH_KNOTS ( 'NONE', 3,
 ( #21064, #40208, #44280, #59258, #16363, #11675, #49879, #6938, #40506, #59572, #16677, #35801, #54866, #58317, #12003, #39267, #20150, #34554, #10748 ),
 .UNSPECIFIED., .F., .F.,
 ( 4, 3, 3, 3, 3, 3, 4 ),
 ( 1.153344816771540786E-16, 0.0002618519381806261336, 0.0003927759815485985231, 0.0005237000248299446227, 0.0006546240681324982588, 0.0007855481115631335765, 0.0009699050456655117008 ),
 .UNSPECIFIED. ) ;
#11047=ORIENTED_EDGE ( 'NONE', *, *, #9760, .T. ) ;
#11055=EDGE_CURVE ( 'NONE', #37013, #56393, #19041, .T. ) ;
#11057=EDGE_CURVE ( 'NONE', #42620, #28210, #55609, .T. ) ;
#11066=CARTESIAN_POINT ( 'NONE',  ( 0.6001305935487422083, 5.760103278698015750, -47.76436356026962216 ) ) ;
#11077=CARTESIAN_POINT ( 'NONE',  ( 0.1073791018717578927, -40.02496097243069784, 16.05399293000745686 ) ) ;
#11080=CARTESIAN_POINT ( 'NONE',  ( 4.975801465491695552, 0.000000000000000000, 0.000000000000000000 ) ) ;
#11081=CARTESIAN_POINT ( 'NONE',  ( 0.2885697896453111588, -43.10898998017122352, -0.8047882042605032371 ) ) ;
#11087=CARTESIAN_POINT ( 'NONE',  ( 0.1073791018717578927, 30.83464511437137645, -30.14884492832358731 ) ) ;
#11090=CARTESIAN_POINT ( 'NONE',  ( 4.549368137175248350, 40.71620287708344677, -13.59764261105707739 ) ) ;
#11091=CARTESIAN_POINT ( 'NONE',  ( -2.569797478183790229, -1.464172661884063587, -14.55946937464483248 ) ) ;
#11092=B_SPLINE_CURVE_WITH_KNOTS ( 'NONE', 3,
 ( #18158, #4021, #33809, #52887 ),
 .UNSPECIFIED., .F., .F.,
 ( 4, 4 ),
 ( 0.000000000000000000, 0.005014147105413695182 ),
 .UNSPECIFIED. ) ;
#11101=CARTESIAN_POINT ( 'NONE',  ( 1.827119703190778877, -22.58367210012866266, -36.65069040194700989 ) ) ;
#11105=ORIENTED_EDGE ( 'NONE', *, *, #12614, .T. ) ;
#11106=CARTESIAN_POINT ( 'NONE',  ( 0.2885700199627509455, -33.71073713194540034, 26.88157179738447056 ) ) ;
#11109=VERTEX_POINT ( 'NONE', #58136 ) ;
#11110=EDGE_CURVE ( 'NONE', #38885, #17061, #6998, .T. ) ;
#11112=CARTESIAN_POINT ( 'NONE',  ( 0.1104177457020373010, -11.15670205480033594, 41.65628910360720027 ) ) ;
#11113=CARTESIAN_POINT ( 'NONE',  ( 0.8760168074887076939, -28.57146030082009247, 38.69913431881774102 ) ) ;
#11116=ORIENTED_EDGE ( 'NONE', *, *, #7479, .T. ) ;
#11118=CARTESIAN_POINT ( 'NONE',  ( 0.6017666602106488405, -24.35550044372416068, -41.48673504406937695 ) ) ;
#11125=FACE_OUTER_BOUND ( 'NONE', #53623, .T. ) ;
#11129=CARTESIAN_POINT ( 'NONE',  ( 0.5988103622719986863, 44.67429504351059677, -17.84821742497949515 ) ) ;
#11130=FACE_OUTER_BOUND ( 'NONE', #38113, .T. ) ;
#11131=ORIENTED_EDGE ( 'NONE', *, *, #44743, .T. ) ;
#11132=CARTESIAN_POINT ( 'NONE',  ( -6.010958268070873523, -18.20513189769812357, 4.863021950010583794 ) ) ;
#11134=DIRECTION ( 'NONE',  ( 0.000000000000000000, 0.000000000000000000, 1.000000000000000000 ) ) ;
#11138=CARTESIAN_POINT ( 'NONE',  ( 0.6017667736363749853, 18.08696174077326901, 44.57803721604157943 ) ) ;
#11146=CARTESIAN_POINT ( 'NONE',  ( 0.5998501479064699549, 41.92175333043586960, 23.59887241503369282 ) ) ;
#11147=CARTESIAN_POINT ( 'NONE',  ( -6.015611763856276717, 16.31561949997075445, 9.427003116184231146 ) ) ;
#11150=CARTESIAN_POINT ( 'NONE',  ( 0.6031357023905874470, -47.70157053127533686, 6.236038527293246148 ) ) ;
#11151=CARTESIAN_POINT ( 'NONE',  ( 0.3622758884714730732, 0.8252992914322084816, 43.10531414739106282 ) ) ;
#11152=B_SPLINE_CURVE_WITH_KNOTS ( 'NONE', 3,
 ( #34224, #6282, #44563, #53597 ),
 .UNSPECIFIED., .F., .F.,
 ( 4, 4 ),
 ( 2.504207788927570074E-17, 0.004564976165746191181 ),
 .UNSPECIFIED. ) ;
#11156=CARTESIAN_POINT ( 'NONE',  ( 4.322998006666179727, -46.85697641700701155, -10.36018990813296448 ) ) ;
#11158=CARTESIAN_POINT ( 'NONE',  ( 4.549368137175248350, 18.79584381673534565, -38.59302160394733505 ) ) ;
#11165=FACE_OUTER_BOUND ( 'NONE', #59413, .T. ) ;
#11166=CARTESIAN_POINT ( 'NONE',  ( 4.975801465491695552, -27.09127437476353251, -39.51822597168487050 ) ) ;
#11169=CARTESIAN_POINT ( 'NONE',  ( 0.3622758884714600280, 41.42293301073608802, 11.95365414648511582 ) ) ;
#11172=CARTESIAN_POINT ( 'NONE',  ( 0.6031356755852238516, -0.04363310494625852187, 48.10744332413860747 ) ) ;
#11173=CARTESIAN_POINT ( 'NONE',  ( 3.680974057930773036, -30.65154904503207689, 36.90739001595120072 ) ) ;
#11179=CARTESIAN_POINT ( 'NONE',  ( -6.015611763856276717, -16.31561949997082905, 9.427003116184113907 ) ) ;
#11187=EDGE_CURVE ( 'NONE', #55039, #48869, #45885, .T. ) ;
#11189=CARTESIAN_POINT ( 'NONE',  ( 0.1084644655670283370, -39.99242539812104980, -16.13497904887289636 ) ) ;
#11206=CARTESIAN_POINT ( 'NONE',  ( 0.2224561200757619039, 43.11279565427785343, 0.7594684977686744221 ) ) ;
#11208=EDGE_LOOP ( 'NONE', ( #38329, #3191, #58633, #31795 ) ) ;
#11210=CARTESIAN_POINT ( 'NONE',  ( 0.6017666602106489515, 44.31084100715252561, -18.73203020817316045 ) ) ;
#11212=CARTESIAN_POINT ( 'NONE',  ( 2.301529144917016101, 47.77346141661144685, 4.990866136406802767 ) ) ;
#11221=CARTESIAN_POINT ( 'NONE',  ( 2.643462169533613793, -44.89050350746140339, -17.09809940585645904 ) ) ;
#11223=ORIENTED_EDGE ( 'NONE', *, *, #7874, .F. ) ;
#11229=CARTESIAN_POINT ( 'NONE',  ( 0.1101816497532063510, -5.763501205266821081, -42.73758747687828219 ) ) ;
#11230=EDGE_CURVE ( 'NONE', #26300, #55548, #7049, .T. ) ;
#11247=CARTESIAN_POINT ( 'NONE',  ( 4.691466044806102076, 42.11359095667468466, 14.64802401911244445 ) ) ;
#11251=VERTEX_POINT ( 'NONE', #31820 ) ;
#11252=EDGE_CURVE ( 'NONE', #9246, #59097, #38454, .T. ) ;
#11258=EDGE_LOOP ( 'NONE', ( #39402, #41273, #50705, #26215 ) ) ;
#11262=EDGE_CURVE ( 'NONE', #49895, #52432, #45011, .T. ) ;
#11266=VERTEX_POINT ( 'NONE', #40932 ) ;
#11277=ORIENTED_EDGE ( 'NONE', *, *, #22140, .F. ) ;
#11278=B_SPLINE_CURVE_WITH_KNOTS ( 'NONE', 3,
 ( #1855, #25060, #53545, #58868, #35098, #15060 ),
 .UNSPECIFIED., .F., .F.,
 ( 4, 2, 4 ),
 ( 3.496446946337351263E-18, 0.0002450742804987318451, 0.0004901485609974602208 ),
 .UNSPECIFIED. ) ;
#11282=CARTESIAN_POINT ( 'NONE',  ( 0.09136607875274982415, 0.000000000000000000, 0.000000000000000000 ) ) ;
#11287=CARTESIAN_POINT ( 'NONE',  ( 0.6017667736363749853, 23.75082673020805402, 41.83584368312199331 ) ) ;
#11293=FACE_OUTER_BOUND ( 'NONE', #17447, .T. ) ;
#11294=VERTEX_POINT ( 'NONE', #57132 ) ;
#11304=EDGE_LOOP ( 'NONE', ( #35503, #30359, #33177, #61699 ) ) ;
#11307=EDGE_CURVE ( 'NONE', #34476, #50243, #54047, .T. ) ;
#11318=CARTESIAN_POINT ( 'NONE',  ( 0.8760168074887076939, -23.27577685234627225, 42.09738177923915003 ) ) ;
#11323=ADVANCED_FACE ( 'NONE', ( #38084 ), #16901, .F. ) ;
#11326=ORIENTED_EDGE ( 'NONE', *, *, #20245, .F. ) ;
#11333=CARTESIAN_POINT ( 'NONE',  ( 0.1073791018717483448, -39.65380858626227223, 16.95003405440244038 ) ) ;
#11335=ADVANCED_FACE ( 'NONE', ( #43081 ), #60642, .F. ) ;
#11336=CARTESIAN_POINT ( 'NONE',  ( 0.6017667736363749853, -12.11362382130104187, -46.55748817282771057 ) ) ;
#11342=CARTESIAN_POINT ( 'NONE',  ( -6.010958268070873523, 14.94067681728565589, -11.48268200989181942 ) ) ;
#11343=VERTEX_POINT ( 'NONE', #23955 ) ;
#11351=VERTEX_POINT ( 'NONE', #8929 ) ;
#11358=CARTESIAN_POINT ( 'NONE',  ( -2.708315649062910779, 9.116606751444328083, -11.44805714186562895 ) ) ;
#11359=CARTESIAN_POINT ( 'NONE',  ( 4.549368137175248350, 13.59764261105693350, 40.71620287708348940 ) ) ;
#11360=EDGE_LOOP ( 'NONE', ( #21861, #38864, #16290, #39729 ) ) ;
#11366=CARTESIAN_POINT ( 'NONE',  ( 0.8751705887134553219, 29.98056538504910051, 37.60752970653838645 ) ) ;
#11371=CARTESIAN_POINT ( 'NONE',  ( 0.8751705887134423323, 41.19904111682474479, 24.81530984069222256 ) ) ;
#11373=VERTEX_POINT ( 'NONE', #23340 ) ;
#11374=ORIENTED_EDGE ( 'NONE', *, *, #41591, .F. ) ;
#11384=CARTESIAN_POINT ( 'NONE',  ( 0.6001305935487422083, -29.70149728382410714, -37.84751346122845206 ) ) ;
#11386=CARTESIAN_POINT ( 'NONE',  ( 0.3622758884714730732, -6.444611261694294768, -42.62881903538208661 ) ) ;
#11392=CARTESIAN_POINT ( 'NONE',  ( -5.995132425357893702, -14.95525565067266882, -11.46484027925383309 ) ) ;
#11398=CARTESIAN_POINT ( 'NONE',  ( 4.549368137175248350, 8.166781970325150297, 42.14271863032836762 ) ) ;
#11412=CARTESIAN_POINT ( 'NONE',  ( 0.3622758884714730732, -15.73321244754880688, 40.13994584881756111 ) ) ;
#11415=EDGE_CURVE ( 'NONE', #31002, #49359, #34665, .T. ) ;
#11417=VERTEX_POINT ( 'NONE', #431 ) ;
#11424=EDGE_CURVE ( 'NONE', #6671, #9409, #51842, .T. ) ;
#11425=CARTESIAN_POINT ( 'NONE',  ( -6.016104459813374383, 18.84322058118302223, 0.005335450885132661872 ) ) ;
#11437=AXIS2_PLACEMENT_3D ( 'NONE', #28649, #19579, #121 ) ;
#11438=VERTEX_POINT ( 'NONE', #44619 ) ;
#11449=VERTEX_POINT ( 'NONE', #10163 ) ;
#11451=LINE ( 'NONE', #2962, #15706 ) ;
#11456=CARTESIAN_POINT ( 'NONE',  ( 0.6029303876144825880, -41.72757124235838688, 23.94027529185480319 ) ) ;
#11459=CARTESIAN_POINT ( 'NONE',  ( 4.975801465491694664, -2.564218696447152279, -47.84403947906842092 ) ) ;
#11461=CARTESIAN_POINT ( 'NONE',  ( 0.1073791018717578927, -41.52698815987159264, -11.62916352156135780 ) ) ;
#11465=ADVANCED_FACE ( 'NONE', ( #28958 ), #38773, .F. ) ;
#11470=CARTESIAN_POINT ( 'NONE',  ( -2.708315649062916552, -13.61924161399630329, -5.356004933109414168 ) ) ;
#11471=CARTESIAN_POINT ( 'NONE',  ( 4.833616638992208614, 2.572717262757989509, -46.17873762321151077 ) ) ;
#11477=CARTESIAN_POINT ( 'NONE',  ( 0.6017667736363749853, 41.83584368312190804, -23.75082673020819968 ) ) ;
#11484=CARTESIAN_POINT ( 'NONE',  ( 0.1095718737110178281, 16.26534146842150719, 39.93945841550381459 ) ) ;
#11488=CARTESIAN_POINT ( 'NONE',  ( 0.1081432562775997280, 41.76274004527633110, -10.75186376283298806 ) ) ;
#11489=B_SPLINE_CURVE_WITH_KNOTS ( 'NONE', 3,
 ( #48420, #38429, #6091, #57177, #43131, #9582 ),
 .UNSPECIFIED., .F., .F.,
 ( 4, 2, 4 ),
 ( 8.699011523299069796E-17, 0.0002293366620881468008, 0.0004586733241762066485 ),
 .UNSPECIFIED. ) ;
#11491=ORIENTED_EDGE ( 'NONE', *, *, #33294, .F. ) ;
#11498=VECTOR ( 'NONE', #40289, 1000.000000000000114 ) ;
#11499=ORIENTED_EDGE ( 'NONE', *, *, #38028, .T. ) ;
#11508=B_SPLINE_CURVE_WITH_KNOTS ( 'NONE', 3,
 ( #46887, #26829, #36556, #13057, #17741, #46568 ),
 .UNSPECIFIED., .F., .F.,
 ( 4, 2, 4 ),
 ( 1.870559545977334001E-17, 0.0002293319059085090867, 0.0004586638118169994709 ),
 .UNSPECIFIED. ) ;
#11510=CARTESIAN_POINT ( 'NONE',  ( 0.7246131072078538793, 23.33689307364193866, 42.06185227555123873 ) ) ;
#11513=FACE_OUTER_BOUND ( 'NONE', #36912, .T. ) ;
#11516=CARTESIAN_POINT ( 'NONE',  ( -2.569797478183790229, 7.701637110048681123, -12.44213550320645645 ) ) ;
#11520=ORIENTED_EDGE ( 'NONE', *, *, #32118, .T. ) ;
#11528=CARTESIAN_POINT ( 'NONE',  ( 4.975801465491695552, 32.01766832630263337, 35.64402118370968964 ) ) ;
#11531=ORIENTED_EDGE ( 'NONE', *, *, #12516, .F. ) ;
#11532=B_SPLINE_CURVE_WITH_KNOTS ( 'NONE', 3,
 ( #29170, #40082, #59130, #57967 ),
 .UNSPECIFIED., .F., .F.,
 ( 4, 4 ),
 ( 2.061695315165020171E-17, 0.004444306975806115029 ),
 .UNSPECIFIED. ) ;
#11538=CARTESIAN_POINT ( 'NONE',  ( 0.1100053167205930216, -5.806749312984825551, -42.73174076921942799 ) ) ;
#11542=CIRCLE ( 'NONE', #2526, 47.91270532121795611 ) ;
#11543=ORIENTED_EDGE ( 'NONE', *, *, #53350, .T. ) ;
#11544=EDGE_CURVE ( 'NONE', #28616, #55958, #7795, .T. ) ;
#11549=ORIENTED_EDGE ( 'NONE', *, *, #38288, .F. ) ;
#11551=EDGE_CURVE ( 'NONE', #36543, #12367, #35332, .T. ) ;
#11552=LINE ( 'NONE', #49746, #32374 ) ;
#11561=CARTESIAN_POINT ( 'NONE',  ( 0.1073791018717578927, -41.77800844988522755, 10.69234304549982895 ) ) ;
#11568=CARTESIAN_POINT ( 'NONE',  ( 0.3622758884714730732, -42.62881903538215056, 6.444611261693867554 ) ) ;
#11575=CARTESIAN_POINT ( 'NONE',  ( 0.1100247026804066219, -41.69861001364780861, 10.99745200874623130 ) ) ;
#11578=CARTESIAN_POINT ( 'NONE',  ( 0.1073791018717578927, 41.52698815987152159, 11.62916352156164557 ) ) ;
#11579=B_SPLINE_CURVE_WITH_KNOTS ( 'NONE', 3,
 ( #25546, #44387, #1413, #57811 ),
 .UNSPECIFIED., .F., .F.,
 ( 4, 4 ),
 ( 2.276721302528256512E-17, 0.004564976165746189446 ),
 .UNSPECIFIED. ) ;
#11586=CARTESIAN_POINT ( 'NONE',  ( 2.643462169533600914, -13.76277278785592806, 46.02269433264208232 ) ) ;
#11587=CARTESIAN_POINT ( 'NONE',  ( 0.6031356219577718170, -29.21669799774991461, 38.21934428970563147 ) ) ;
#11594=ORIENTED_EDGE ( 'NONE', *, *, #32630, .F. ) ;
#11598=CARTESIAN_POINT ( 'NONE',  ( 0.1073791018717483448, 11.62916352156094035, 41.52698815987171344 ) ) ;
#11599=ORIENTED_EDGE ( 'NONE', *, *, #29132, .F. ) ;
#11602=DIRECTION ( 'NONE',  ( 0.000000000000000000, 0.000000000000000000, -1.000000000000000000 ) ) ;
#11605=CARTESIAN_POINT ( 'NONE',  ( -6.016761891674564211, -13.32172022638601128, 13.32657647165350490 ) ) ;
#11610=DIRECTION ( 'NONE',  ( 0.000000000000000000, 0.000000000000000000, 1.000000000000000000 ) ) ;
#11611=B_SPLINE_CURVE_WITH_KNOTS ( 'NONE', 3,
 ( #7496, #41072, #17238, #36360, #31638, #61053, #28464, #42594, #37592, #51964, #37280, #9056, #5260, #4632, #24392, #32574, #47591, #9672, #32890 ),
 .UNSPECIFIED., .F., .F.,
 ( 4, 3, 3, 3, 3, 3, 4 ),
 ( 1.184243374405472686E-16, 0.0002618519381806228268, 0.0003927759815485937526, 0.0005237000248299437553, 0.0006546240681324990178, 0.0007855481115631294566, 0.0009699050456655100745 ),
 .UNSPECIFIED. ) ;
#11618=CARTESIAN_POINT ( 'NONE',  ( 0.8751705887134553219, -0.8911681664085087107, -48.08707113907594533 ) ) ;
#11619=CARTESIAN_POINT ( 'NONE',  ( 0.6009453534118439633, -28.93865405070921426, -38.43042294376904522 ) ) ;
#11636=EDGE_CURVE ( 'NONE', #57072, #61620, #8871, .T. ) ;
#11639=B_SPLINE_CURVE_WITH_KNOTS ( 'NONE', 3,
 ( #35154, #12280, #11336, #54214, #31368, #11651, #31060, #49534, #25735, #50167, #1917, #40183, #21043, #59232, #59550, #35467 ),
 .UNSPECIFIED., .F., .F.,
 ( 4, 3, 3, 3, 3, 4 ),
 ( 2.030557555191247372E-17, 0.0002618515315864420852, 0.0003927756766341980454, 0.0005236998216950584321, 0.0007855159896329918503, 0.001047349442285929605 ),
 .UNSPECIFIED. ) ;
#11649=CARTESIAN_POINT ( 'NONE',  ( 2.301529144917016101, -22.89307126380016300, 42.22700141647002425 ) ) ;
#11651=CARTESIAN_POINT ( 'NONE',  ( 0.6027935024548037868, -12.28245664247814162, -46.51312430684501464 ) ) ;
#11656=ORIENTED_EDGE ( 'NONE', *, *, #27048, .F. ) ;
#11657=B_SPLINE_CURVE_WITH_KNOTS ( 'NONE', 3,
 ( #23752, #23443, #52241, #4305 ),
 .UNSPECIFIED., .F., .F.,
 ( 4, 4 ),
 ( 5.818439421673296370E-18, 0.004566006591234647236 ),
 .UNSPECIFIED. ) ;
#11661=CARTESIAN_POINT ( 'NONE',  ( 0.8751705887134423323, 42.09020928323375443, -23.27176129838382224 ) ) ;
#11667=DIRECTION ( 'NONE',  ( 0.09835009131224567436, -0.9223318362920814861, 0.3736726418952155404 ) ) ;
#11669=ADVANCED_FACE ( 'NONE', ( #61141 ), #32908, .F. ) ;
#11675=CARTESIAN_POINT ( 'NONE',  ( 0.1101816497532062955, -30.39741055095880284, 30.58948775778034346 ) ) ;
#11683=CARTESIAN_POINT ( 'NONE',  ( -6.001507490154111224, -16.31148204059940809, -9.435425682280991211 ) ) ;
#11685=ORIENTED_EDGE ( 'NONE', *, *, #47655, .F. ) ;
#11688=CARTESIAN_POINT ( 'NONE',  ( -2.569797478183790229, -10.65947181927846543, 10.02484965418622842 ) ) ;
#11690=EDGE_CURVE ( 'NONE', #32619, #49021, #32670, .T. ) ;
#11692=ORIENTED_EDGE ( 'NONE', *, *, #32047, .F. ) ;
#11695=CARTESIAN_POINT ( 'NONE',  ( 0.7245667037590752813, 28.62745028382816415, -38.65590879674357438 ) ) ;
#11697=CARTESIAN_POINT ( 'NONE',  ( 0.1095718737110178420, -39.93945841550387854, 16.26534146842136508 ) ) ;
#11701=CARTESIAN_POINT ( 'NONE',  ( 0.1092565886968784594, 34.02318727879963944, -26.49813811968549615 ) ) ;
#11706=CARTESIAN_POINT ( 'NONE',  ( 0.5998501479064708430, 12.95623334615502387, -46.33007877220726556 ) ) ;
#11707=CARTESIAN_POINT ( 'NONE',  ( 0.8751705887134423323, 38.69254731947834358, -28.56654290188613032 ) ) ;
#11709=CARTESIAN_POINT ( 'NONE',  ( 0.1313383488274124100, -11.77600546273740534, -41.48452234694092056 ) ) ;
#11710=EDGE_CURVE ( 'NONE', #51385, #45191, #32326, .T. ) ;
#11712=CARTESIAN_POINT ( 'NONE',  ( 0.6031356755773454870, -34.01711753073234945, -34.01708126935030663 ) ) ;
#11714=CARTESIAN_POINT ( 'NONE',  ( 0.6009453534118438522, -5.846398087359047757, -47.75104957283896567 ) ) ;
#11720=CARTESIAN_POINT ( 'NONE',  ( 0.6001305935487422083, 47.62765676940944104, -6.798494447611732383 ) ) ;
#11721=ORIENTED_EDGE ( 'NONE', *, *, #34182, .F. ) ;
#11724=CARTESIAN_POINT ( 'NONE',  ( -6.016489644550737204, -18.19999694163060511, -4.881234076340565942 ) ) ;
#11727=CARTESIAN_POINT ( 'NONE',  ( -6.015611763856276717, 18.68284711750058591, 2.453375430804133117 ) ) ;
#11731=CARTESIAN_POINT ( 'NONE',  ( 0.7048096507298635682, 33.41730025321754027, -34.61049487267025171 ) ) ;
#11732=CARTESIAN_POINT ( 'NONE',  ( 0.6025881611877911270, 6.062907795288723811, 47.72390913208167262 ) ) ;
#11737=CARTESIAN_POINT ( 'NONE',  ( 2.301529144917016101, -38.87759814529798774, -28.20894756932127478 ) ) ;
#11740=( BOUNDED_SURFACE ( )  B_SPLINE_SURFACE ( 3, 1, ( 
 ( #18778, #19697 ),
 ( #13777, #47586 ),
 ( #52260, #48202 ),
 ( #5255, #8739 ) ),
 .UNSPECIFIED., .F., .F., .F. ) 
 B_SPLINE_SURFACE_WITH_KNOTS ( ( 4, 4 ),
 ( 2, 2 ),
 ( 0.000000000000000000, 1.000000000000000000 ),
 ( 0.000000000000000000, 1.000000000000000000 ),
 .UNSPECIFIED. ) 
 GEOMETRIC_REPRESENTATION_ITEM ( )  RATIONAL_B_SPLINE_SURFACE ( (
 ( 1.000000000000000000, 1.000000000000000000),
 ( 0.7223157951917476005, 0.9931996967497186413),
 ( 0.7223157951917476005, 0.9931996967497186413),
 ( 1.000000000000000000, 1.000000000000000000) ) ) 
 REPRESENTATION_ITEM ( '' )  SURFACE ( )  );
#11741=ORIENTED_EDGE ( 'NONE', *, *, #2878, .T. ) ;
#11760=CARTESIAN_POINT ( 'NONE',  ( 0.5998501479064708430, 17.92509395669044636, 44.64337787626254794 ) ) ;
#11765=CARTESIAN_POINT ( 'NONE',  ( 0.7954190325252781246, -47.79303692714238139, -5.415566973723075606 ) ) ;
#11766=CARTESIAN_POINT ( 'NONE',  ( 4.975801465491694664, -47.76942479135482955, -3.702618843597289544 ) ) ;
#11769=ORIENTED_EDGE ( 'NONE', *, *, #46640, .F. ) ;
#11773=CARTESIAN_POINT ( 'NONE',  ( 0.1092565886968784317, -42.71401356099882918, 5.936467125236308817 ) ) ;
#11781=CARTESIAN_POINT ( 'NONE',  ( 4.975801465491695552, -40.15204426031515794, -26.14269827151666092 ) ) ;
#11788=CARTESIAN_POINT ( 'NONE',  ( 4.975801465491695552, 2.564218696447496004, -47.84403947906841381 ) ) ;
#11797=CARTESIAN_POINT ( 'NONE',  ( 0.6017666602106488405, 41.48673504406946932, -24.35550044372401501 ) ) ;
#11801=ORIENTED_EDGE ( 'NONE', *, *, #60378, .T. ) ;
#11804=CARTESIAN_POINT ( 'NONE',  ( 3.680974057930773480, -8.091325130366769258, 47.28851186370993531 ) ) ;
#11809=B_SPLINE_CURVE_WITH_KNOTS ( 'NONE', 3,
 ( #6707, #39358, #34341, #10523, #16156, #6095 ),
 .UNSPECIFIED., .F., .F.,
 ( 4, 2, 4 ),
 ( 2.196750944941757354E-17, 0.0002293319059085104420, 0.0004586638118169989288 ),
 .UNSPECIFIED. ) ;
#11811=B_SPLINE_CURVE_WITH_KNOTS ( 'NONE', 3,
 ( #39110, #43188, #24993, #218, #44131, #9968, #48184, #19677, #5236, #14988, #56943, #1159, #34097, #20293, #14064, #52239 ),
 .UNSPECIFIED., .F., .F.,
 ( 4, 3, 3, 3, 3, 4 ),
 ( 1.962735358247464152E-17, 0.0002618515315864398084, 0.0003927756766341925702, 0.0005236998216950552879, 0.0007855159896329908745, 0.001047349442285923317 ),
 .UNSPECIFIED. ) ;
#11814=ORIENTED_EDGE ( 'NONE', *, *, #6333, .F. ) ;
#11817=CARTESIAN_POINT ( 'NONE',  ( 0.1073791018717483448, -40.02496097243048467, -16.05399293000801819 ) ) ;
#11821=ORIENTED_EDGE ( 'NONE', *, *, #30827, .F. ) ;
#11824=CARTESIAN_POINT ( 'NONE',  ( 0.7245667037590747261, -11.65533952568384990, 46.66865388241065915 ) ) ;
#11834=B_SPLINE_CURVE_WITH_KNOTS ( 'NONE', 3,
 ( #55357, #26561, #26246, #60070 ),
 .UNSPECIFIED., .F., .F.,
 ( 4, 4 ),
 ( 2.204559228842524708E-17, 0.004564976165746186844 ),
 .UNSPECIFIED. ) ;
#11836=ORIENTED_EDGE ( 'NONE', *, *, #11636, .T. ) ;
#11844=DIRECTION ( 'NONE',  ( -0.1024043820194934368, -0.5087173657443582186, 0.8548216096550944609 ) ) ;
#11845=VERTEX_POINT ( 'NONE', #61609 ) ;
#11853=CARTESIAN_POINT ( 'NONE',  ( -6.016761891674564211, -0.003433883959652091721, -18.84319130225482297 ) ) ;
#11855=DIRECTION ( 'NONE',  ( -1.000000000000000000, -0.000000000000000000, -0.000000000000000000 ) ) ;
#11860=ORIENTED_EDGE ( 'NONE', *, *, #21864, .F. ) ;
#11865=CARTESIAN_POINT ( 'NONE',  ( 0.1103878639767399139, -5.676988162228372659, -42.74915604780179024 ) ) ;
#11869=CARTESIAN_POINT ( 'NONE',  ( 0.5998501479064699549, 17.92509395669108585, -44.64337787626229925 ) ) ;
#11874=FACE_OUTER_BOUND ( 'NONE', #58721, .T. ) ;
#11875=CARTESIAN_POINT ( 'NONE',  ( -2.708315649062910779, -4.041664582652894744, 14.06540004355475837 ) ) ;
#11886=CARTESIAN_POINT ( 'NONE',  ( 0.2230388203127590674, -40.12182516270790700, -15.79641846944905481 ) ) ;
#11896=CARTESIAN_POINT ( 'NONE',  ( 0.1097557419366048670, 43.12388302211984126, -0.2231007852155202087 ) ) ;
#11900=VECTOR ( 'NONE', #31185, 1000.000000000000000 ) ;
#11913=CARTESIAN_POINT ( 'NONE',  ( 0.5998501479064708430, -29.69975237324642237, 37.84527566984805702 ) ) ;
#11917=ORIENTED_EDGE ( 'NONE', *, *, #35439, .T. ) ;
#11919=CARTESIAN_POINT ( 'NONE',  ( 0.1103310638050662013, -26.18709435931501872, -34.26302445194738766 ) ) ;
#11920=ORIENTED_EDGE ( 'NONE', *, *, #23341, .T. ) ;
#11925=CARTESIAN_POINT ( 'NONE',  ( 0.1100053167205930632, 11.33468317718497964, 41.60823192620011923 ) ) ;
#11926=ORIENTED_EDGE ( 'NONE', *, *, #50151, .T. ) ;
#11943=CARTESIAN_POINT ( 'NONE',  ( 4.549368137175248350, -23.67244292351665536, 35.80950303116058819 ) ) ;
#11948=DIRECTION ( 'NONE',  ( 0.000000000000000000, 0.000000000000000000, -1.000000000000000000 ) ) ;
#11952=CARTESIAN_POINT ( 'NONE',  ( 0.7954196712028469562, 44.09776749253654060, 19.20650004025017665 ) ) ;
#11954=B_SPLINE_CURVE_WITH_KNOTS ( 'NONE', 3,
 ( #49532, #11649, #16336, #58927 ),
 .UNSPECIFIED., .F., .F.,
 ( 4, 4 ),
 ( 2.071251839531113129E-17, 0.004444306975806116763 ),
 .UNSPECIFIED. ) ;
#11959=ORIENTED_EDGE ( 'NONE', *, *, #56272, .T. ) ;
#11965=CARTESIAN_POINT ( 'NONE',  ( 4.975801465491695552, 2.564218696447496004, -47.84403947906841381 ) ) ;
#11970=ORIENTED_EDGE ( 'NONE', *, *, #49580, .F. ) ;
#11981=CARTESIAN_POINT ( 'NONE',  ( 4.549368137175248350, 38.40568845698277300, -19.17571786012283042 ) ) ;
#11983=CARTESIAN_POINT ( 'NONE',  ( 0.5980894510889448457, -33.52121017007803516, -34.51330645350390824 ) ) ;
#11984=EDGE_CURVE ( 'NONE', #18536, #34317, #45113, .T. ) ;
#11985=ORIENTED_EDGE ( 'NONE', *, *, #24358, .T. ) ;
#11986=B_SPLINE_CURVE_WITH_KNOTS ( 'NONE', 3,
 ( #13408, #52210, #61901, #32829 ),
 .UNSPECIFIED., .F., .F.,
 ( 4, 4 ),
 ( 2.261237429940862397E-17, 0.004564976165746191181 ),
 .UNSPECIFIED. ) ;
#11991=CARTESIAN_POINT ( 'NONE',  ( 2.301430502907646058, 42.22699195640107206, -22.89309745268846186 ) ) ;
#11994=VERTEX_POINT ( 'NONE', #25885 ) ;
#12003=CARTESIAN_POINT ( 'NONE',  ( 0.1095718737110178559, -30.67477146794393761, 30.31138510522940877 ) ) ;
#12005=ORIENTED_EDGE ( 'NONE', *, *, #7912, .F. ) ;
#12006=EDGE_CURVE ( 'NONE', #25025, #37013, #53276, .T. ) ;
#12016=CARTESIAN_POINT ( 'NONE',  ( -6.010958268070873523, -11.48268200989187271, -14.94067681728561681 ) ) ;
#12022=CARTESIAN_POINT ( 'NONE',  ( -6.016761891674565099, -16.31696541414265766, -9.424569481870424426 ) ) ;
#12023=CARTESIAN_POINT ( 'NONE',  ( 0.6023142530420679819, 6.019593586345300729, -47.72938419887613293 ) ) ;
#12029=CARTESIAN_POINT ( 'NONE',  ( 0.6017666602106490625, 12.11361215600179975, -46.55749120190034773 ) ) ;
#12048=CARTESIAN_POINT ( 'NONE',  ( 4.833616638992208614, 41.67905425467677816, 20.04871863793823650 ) ) ;
#12049=EDGE_LOOP ( 'NONE', ( #45558, #43277, #15693, #7256 ) ) ;
#12054=ORIENTED_EDGE ( 'NONE', *, *, #2082, .F. ) ;
#12060=EDGE_CURVE ( 'NONE', #9726, #34790, #37556, .T. ) ;
#12079=CARTESIAN_POINT ( 'NONE',  ( 0.6030672727741701600, 18.32928433899690290, 44.47882233696930854 ) ) ;
#12080=CARTESIAN_POINT ( 'NONE',  ( 4.833616638992208614, -34.47248434257934235, 30.83411269743503880 ) ) ;
#12082=ORIENTED_EDGE ( 'NONE', *, *, #51837, .F. ) ;
#12097=CARTESIAN_POINT ( 'NONE',  ( 0.1104177457020373149, -41.65628910360730686, -11.15670205479989896 ) ) ;
#12104=CARTESIAN_POINT ( 'NONE',  ( -6.010958268070873523, 4.891065400978640731, -18.19761767765824700 ) ) ;
#12109=EDGE_CURVE ( 'NONE', #6804, #56628, #41547, .T. ) ;
#12112=CARTESIAN_POINT ( 'NONE',  ( 0.6025881611877910160, 41.77096849334450468, -23.86454577211521411 ) ) ;
#12114=CARTESIAN_POINT ( 'NONE',  ( 0.1310142868023695673, -6.259743112235846674, 42.66681113736507314 ) ) ;
#12117=CARTESIAN_POINT ( 'NONE',  ( 4.322998006666165516, -16.38761975793177683, -45.10383234877027547 ) ) ;
#12123=CARTESIAN_POINT ( 'NONE',  ( 0.1103310638050662013, 41.67627416617914093, -11.08182869403250947 ) ) ;
#12125=ORIENTED_EDGE ( 'NONE', *, *, #25159, .F. ) ;
#12127=EDGE_CURVE ( 'NONE', #59574, #33107, #17414, .T. ) ;
#12134=EDGE_CURVE ( 'NONE', #53679, #60046, #47791, .T. ) ;
#12136=ORIENTED_EDGE ( 'NONE', *, *, #53041, .F. ) ;
#12151=CARTESIAN_POINT ( 'NONE',  ( 0.1073791018717578927, -42.81622261970997556, 5.147744207006151207 ) ) ;
#12153=ORIENTED_EDGE ( 'NONE', *, *, #30185, .F. ) ;
#12156=DIRECTION ( 'NONE',  ( 0.09835009131224566048, 0.4908642831975245091, 0.8656670924898630659 ) ) ;
#12157=CARTESIAN_POINT ( 'NONE',  ( 0.5998501479064708430, -17.92509395669076966, -44.64337787626241294 ) ) ;
#12159=VERTEX_POINT ( 'NONE', #46550 ) ;
#12163=ORIENTED_EDGE ( 'NONE', *, *, #22100, .F. ) ;
#12165=DIRECTION ( 'NONE',  ( 1.000000000000000000, 0.000000000000000000, 0.000000000000000000 ) ) ;
#12168=CARTESIAN_POINT ( 'NONE',  ( 0.1097557419366048670, -5.849988371690785449, -42.72583172879051716 ) ) ;
#12170=CARTESIAN_POINT ( 'NONE',  ( 0.1313383488274126321, 41.81465294768271690, 10.54394128763572702 ) ) ;
#12176=CYLINDRICAL_SURFACE ( 'NONE', #18940, 10.00000000000000000 ) ;
#12179=CARTESIAN_POINT ( 'NONE',  ( 4.975801465491695552, -31.15993731089151808, 36.39623109580413285 ) ) ;
#12180=FACE_OUTER_BOUND ( 'NONE', #43213, .T. ) ;
#12185=CARTESIAN_POINT ( 'NONE',  ( 0.6017666602106490625, 38.37783452831165931, 29.00829887116083583 ) ) ;
#12188=CARTESIAN_POINT ( 'NONE',  ( 0.7048096507298635682, -46.24547838151377732, 13.26491767067435390 ) ) ;
#12191=DIRECTION ( 'NONE',  ( 1.000000000000000000, 0.000000000000000000, 0.000000000000000000 ) ) ;
#12202=CARTESIAN_POINT ( 'NONE',  ( 0.1095718737110177865, 43.12372487139541732, 0.2569529612659335327 ) ) ;
#12204=CARTESIAN_POINT ( 'NONE',  ( 0.5998501479064708430, 18.89267974119668025, -44.24259072156067418 ) ) ;
#12206=CARTESIAN_POINT ( 'NONE',  ( 4.975801465491695552, 14.85979367497174408, -45.55012473237738391 ) ) ;
#12210=EDGE_LOOP ( 'NONE', ( #13364, #61000, #45200, #41573 ) ) ;
#12211=B_SPLINE_CURVE_WITH_KNOTS ( 'NONE', 3,
 ( #32561, #22840, #18773, #13449 ),
 .UNSPECIFIED., .F., .F.,
 ( 4, 4 ),
 ( 0.000000000000000000, 0.005014147105413704723 ),
 .UNSPECIFIED. ) ;
#12212=CARTESIAN_POINT ( 'NONE',  ( 4.549368137175248350, 8.166781970325150297, 42.14271863032836762 ) ) ;
#12213=EDGE_LOOP ( 'NONE', ( #28458, #2286 ) ) ;
#12214=CARTESIAN_POINT ( 'NONE',  ( 0.6001305935487315502, 29.70149728382386201, 37.84751346122865101 ) ) ;
#12215=CARTESIAN_POINT ( 'NONE',  ( 0.6041374136657476912, 34.14050483116091783, 33.89363087703058852 ) ) ;
#12221=ADVANCED_FACE ( 'NONE', ( #38096 ), #15487, .F. ) ;
#12224=ORIENTED_EDGE ( 'NONE', *, *, #35105, .F. ) ;
#12238=EDGE_LOOP ( 'NONE', ( #42457, #52541, #7305, #39555 ) ) ;
#12239=EDGE_LOOP ( 'NONE', ( #34703, #37985, #42407, #50597 ) ) ;
#12243=ORIENTED_EDGE ( 'NONE', *, *, #50824, .F. ) ;
#12246=ORIENTED_EDGE ( 'NONE', *, *, #14261, .T. ) ;
#12260=CARTESIAN_POINT ( 'NONE',  ( 0.1103878639767399417, -16.54784522866442842, -39.82320122342697744 ) ) ;
#12270=ADVANCED_FACE ( 'NONE', ( #18355 ), #10809, .F. ) ;
#12273=VERTEX_POINT ( 'NONE', #4826 ) ;
#12277=VERTEX_POINT ( 'NONE', #52766 ) ;
#12280=CARTESIAN_POINT ( 'NONE',  ( 0.6009453534118439633, -12.02914401651140786, -46.57942464365170565 ) ) ;
#12281=ORIENTED_EDGE ( 'NONE', *, *, #60017, .F. ) ;
#12288=VERTEX_POINT ( 'NONE', #28970 ) ;
#12294=DIRECTION ( 'NONE',  ( 0.1024043820194936033, -0.9239750460186124670, -0.3684880688409171157 ) ) ;
#12308=( BOUNDED_SURFACE ( )  B_SPLINE_SURFACE ( 3, 1, ( 
 ( #6690, #44970 ),
 ( #59332, #30834 ),
 ( #11132, #15520 ),
 ( #39652, #25215 ) ),
 .UNSPECIFIED., .F., .F., .F. ) 
 B_SPLINE_SURFACE_WITH_KNOTS ( ( 4, 4 ),
 ( 2, 2 ),
 ( 0.000000000000000000, 1.000000000000000000 ),
 ( 0.000000000000000000, 1.000000000000000000 ),
 .UNSPECIFIED. ) 
 GEOMETRIC_REPRESENTATION_ITEM ( )  RATIONAL_B_SPLINE_SURFACE ( (
 ( 1.000000000000000000, 1.000000000000000000),
 ( 0.7223157951917476005, 0.9931996967497186413),
 ( 0.7223157951917476005, 0.9931996967497186413),
 ( 1.000000000000000000, 1.000000000000000000) ) ) 
 REPRESENTATION_ITEM ( '' )  SURFACE ( )  );
#12309=CARTESIAN_POINT ( 'NONE',  ( -2.708315649062910779, -10.53288422393062795, 10.16016146078271198 ) ) ;
#12310=ORIENTED_EDGE ( 'NONE', *, *, #37099, .F. ) ;
#12317=CARTESIAN_POINT ( 'NONE',  ( 0.1103878639767399139, 34.24245495762985314, 26.21398130517529168 ) ) ;
#12323=B_SPLINE_CURVE_WITH_KNOTS ( 'NONE', 3,
 ( #30262, #58139, #5816, #49373 ),
 .UNSPECIFIED., .F., .F.,
 ( 4, 4 ),
 ( 6.254634441385501517E-18, 0.004566006591234645501 ),
 .UNSPECIFIED. ) ;
#12326=CARTESIAN_POINT ( 'NONE',  ( 0.6025881611877910160, 12.66175293297402504, -46.41131722377296853 ) ) ;
#12339=CARTESIAN_POINT ( 'NONE',  ( 0.6028618097248863439, 46.42282207635403068, -12.61968633793867411 ) ) ;
#12343=EDGE_CURVE ( 'NONE', #23714, #25486, #21000, .T. ) ;
#12346=CARTESIAN_POINT ( 'NONE',  ( 0.6254311100348668440, 34.49956326955417296, -33.52633430496194933 ) ) ;
#12347=ORIENTED_EDGE ( 'NONE', *, *, #18676, .F. ) ;
#12348=EDGE_CURVE ( 'NONE', #41175, #1146, #38999, .T. ) ;
#12349=ORIENTED_EDGE ( 'NONE', *, *, #47053, .F. ) ;
#12351=B_SPLINE_CURVE_WITH_KNOTS ( 'NONE', 3,
 ( #20101, #48897, #19479, #9753, #15400, #11009, #5949, #44233, #25087, #30090, #43609, #43295, #20399, #28860, #5642, #6251 ),
 .UNSPECIFIED., .F., .F.,
 ( 4, 3, 3, 3, 3, 4 ),
 ( 2.194378057379452319E-17, 0.0002618515315864391037, 0.0003927756766341967986, 0.0005236998216950561552, 0.0007855159896329881640, 0.001047349442285927653 ),
 .UNSPECIFIED. ) ;
#12361=CARTESIAN_POINT ( 'NONE',  ( 4.975801465491694664, -32.01766832630337944, 35.64402118370901462 ) ) ;
#12363=CARTESIAN_POINT ( 'NONE',  ( -6.015611763856276717, 18.20278301740936655, 4.870987357968240339 ) ) ;
#12367=VERTEX_POINT ( 'NONE', #58071 ) ;
#12373=CARTESIAN_POINT ( 'NONE',  ( 0.6028618097248862329, 33.89350006451827824, -34.14037999462335193 ) ) ;
#12376=ORIENTED_EDGE ( 'NONE', *, *, #34050, .T. ) ;
#12378=CARTESIAN_POINT ( 'NONE',  ( 0.6027935024548038978, 18.24855952726166564, 44.51201578381234469 ) ) ;
#12379=( BOUNDED_SURFACE ( )  B_SPLINE_SURFACE ( 3, 1, ( 
 ( #15811, #11113 ),
 ( #30196, #1990 ),
 ( #36699, #6360 ),
 ( #46102, #25494 ) ),
 .UNSPECIFIED., .F., .F., .F. ) 
 B_SPLINE_SURFACE_WITH_KNOTS ( ( 4, 4 ),
 ( 2, 2 ),
 ( 0.000000000000000000, 1.000000000000000000 ),
 ( 0.000000000000000000, 1.000000000000000000 ),
 .UNSPECIFIED. ) 
 GEOMETRIC_REPRESENTATION_ITEM ( )  RATIONAL_B_SPLINE_SURFACE ( (
 ( 1.000000000000000000, 1.000000000000000000),
 ( 0.9953040768229005630, 0.8617119497784937465),
 ( 0.9953040768229005630, 0.8617119497784937465),
 ( 1.000000000000000000, 1.000000000000000000) ) ) 
 REPRESENTATION_ITEM ( '' )  SURFACE ( )  );
#12380=CARTESIAN_POINT ( 'NONE',  ( 0.1092355843206037486, 39.95589129953367546, -16.22491322981586492 ) ) ;
#12405=VECTOR ( 'NONE', #30373, 1000.000000000000227 ) ;
#12413=ORIENTED_EDGE ( 'NONE', *, *, #37228, .F. ) ;
#12421=CARTESIAN_POINT ( 'NONE',  ( 0.1073791018717578927, 41.77800844988514939, -10.69234304550012027 ) ) ;
#12424=DIRECTION ( 'NONE',  ( 0.000000000000000000, 0.000000000000000000, -1.000000000000000000 ) ) ;
#12425=CARTESIAN_POINT ( 'NONE',  ( 0.1098349054025746230, -39.75970464594254139, -16.69989664087441028 ) ) ;
#12426=CARTESIAN_POINT ( 'NONE',  ( 0.6029303876144825880, 41.59667219751848677, 24.16699908817976450 ) ) ;
#12433=CARTESIAN_POINT ( 'NONE',  ( 4.975801465491694664, -9.906103548668557579, 46.87746200127438101 ) ) ;
#12438=ORIENTED_EDGE ( 'NONE', *, *, #12348, .T. ) ;
#12442=CARTESIAN_POINT ( 'NONE',  ( -5.995132425357893702, 16.32377331145333699, -9.414704407577630718 ) ) ;
#12443=B_SPLINE_CURVE_WITH_KNOTS ( 'NONE', 3,
 ( #47861, #29349, #53450, #14348, #34080, #4910 ),
 .UNSPECIFIED., .F., .F.,
 ( 4, 2, 4 ),
 ( 8.558167549966216424E-17, 0.0002293366620881469092, 0.0004586733241762082748 ),
 .UNSPECIFIED. ) ;
#12445=ORIENTED_EDGE ( 'NONE', *, *, #34037, .F. ) ;
#12446=ORIENTED_EDGE ( 'NONE', *, *, #28361, .F. ) ;
#12447=EDGE_CURVE ( 'NONE', #11449, #45029, #25490, .T. ) ;
#12449=CARTESIAN_POINT ( 'NONE',  ( 0.6009453534118439633, 44.61081284455531204, -18.00606795643230029 ) ) ;
#12458=CARTESIAN_POINT ( 'NONE',  ( 0.1092565886968785566, -26.00565248013079156, 34.40108480122206203 ) ) ;
#12460=CARTESIAN_POINT ( 'NONE',  ( -6.016489644550737204, 17.41053539857209742, -7.206912786933101778 ) ) ;
#12470=CARTESIAN_POINT ( 'NONE',  ( 0.1098349054025746369, -5.417317591399518406, -42.78286259078961962 ) ) ;
#12471=CARTESIAN_POINT ( 'NONE',  ( 0.6254311100348641794, -11.78487556908975264, -46.64066536338336988 ) ) ;
#12474=CARTESIAN_POINT ( 'NONE',  ( 0.1103878639767399694, 37.32258098927768231, -21.60424693647518168 ) ) ;
#12477=ADVANCED_FACE ( 'NONE', ( #16727 ), #28273, .F. ) ;
#12492=DIRECTION ( 'NONE',  ( 0.09835009131224567436, 0.7847759187265459513, 0.6119264800004807769 ) ) ;
#12498=AXIS2_PLACEMENT_3D ( 'NONE', #22776, #35746, #11948 ) ;
#12503=CARTESIAN_POINT ( 'NONE',  ( 4.322998006666165516, 30.86725474310359729, -36.74401119231377777 ) ) ;
#12516=EDGE_CURVE ( 'NONE', #41236, #22780, #14356, .T. ) ;
#12517=FACE_OUTER_BOUND ( 'NONE', #56422, .T. ) ;
#12518=DIRECTION ( 'NONE',  ( -1.000000000000000000, -0.000000000000000000, -0.000000000000000000 ) ) ;
#12524=ADVANCED_FACE ( 'NONE', ( #50232 ), #41121, .F. ) ;
#12527=CARTESIAN_POINT ( 'NONE',  ( 2.643462169533600914, -25.20536747735808447, 40.89244134039068257 ) ) ;
#12532=EDGE_CURVE ( 'NONE', #40338, #32714, #31434, .T. ) ;
#12534=CARTESIAN_POINT ( 'NONE',  ( 0.7954190325252802340, 34.61997719899436987, 33.39101560460813545 ) ) ;
#12536=CARTESIAN_POINT ( 'NONE',  ( 2.301529144917015213, -4.990866136406990172, 47.77346141661142553 ) ) ;
#12538=DIRECTION ( 'NONE',  ( 0.09835009131224552170, -0.7847759187265582748, 0.6119264800004649008 ) ) ;
#12539=VERTEX_POINT ( 'NONE', #55846 ) ;
#12543=VECTOR ( 'NONE', #2016, 1000.000000000000000 ) ;
#12546=CARTESIAN_POINT ( 'NONE',  ( 0.3622758884714600280, -33.69533458712325569, -26.89560658783373626 ) ) ;
#12549=EDGE_LOOP ( 'NONE', ( #12555, #47018, #38484, #13893 ) ) ;
#12550=CARTESIAN_POINT ( 'NONE',  ( 0.1073791018717483448, -42.81622261970991161, -5.147744207006710759 ) ) ;
#12551=FACE_OUTER_BOUND ( 'NONE', #23797, .T. ) ;
#12552=EDGE_CURVE ( 'NONE', #6090, #43360, #46421, .T. ) ;
#12553=VERTEX_POINT ( 'NONE', #32066 ) ;
#12554=CARTESIAN_POINT ( 'NONE',  ( 5.880360259849752858, -31.66572319753586839, 36.03610316515328549 ) ) ;
#12555=ORIENTED_EDGE ( 'NONE', *, *, #49779, .F. ) ;
#12563=EDGE_LOOP ( 'NONE', ( #40733, #47878, #24085, #56657 ) ) ;
#12564=CARTESIAN_POINT ( 'NONE',  ( 0.7246131072078569879, 37.65685186358352610, 29.92944207473665585 ) ) ;
#12592=CARTESIAN_POINT ( 'NONE',  ( 0.1073791018717578927, 41.77800844988514939, -10.69234304550012027 ) ) ;
#12602=ORIENTED_EDGE ( 'NONE', *, *, #48182, .T. ) ;
#12614=EDGE_CURVE ( 'NONE', #56393, #45060, #13577, .T. ) ;
#12622=ORIENTED_EDGE ( 'NONE', *, *, #4226, .F. ) ;
#12626=CARTESIAN_POINT ( 'NONE',  ( 0.6023143664670691511, -41.53077189784247736, -24.28012784216863551 ) ) ;
#12628=ORIENTED_EDGE ( 'NONE', *, *, #1987, .F. ) ;
#12629=EDGE_LOOP ( 'NONE', ( #45549, #49163, #10666, #27346 ) ) ;
#12634=CARTESIAN_POINT ( 'NONE',  ( 0.6009452777970409887, 5.846392105360529001, -47.75105029762386266 ) ) ;
#12638=B_SPLINE_CURVE_WITH_KNOTS ( 'NONE', 3,
 ( #10399, #10087, #39233, #30104 ),
 .UNSPECIFIED., .F., .F.,
 ( 4, 4 ),
 ( 0.000000000000000000, 0.005014147105413701254 ),
 .UNSPECIFIED. ) ;
#12640=CARTESIAN_POINT ( 'NONE',  ( 2.643462169533600914, -4.896978544601818584, -47.78621045426874048 ) ) ;
#12645=CARTESIAN_POINT ( 'NONE',  ( 0.8751705887134553219, -19.22545746485630502, -44.08562551107074512 ) ) ;
#12650=CARTESIAN_POINT ( 'NONE',  ( 4.833616638992208614, -25.31740731790925025, 38.70560126501819553 ) ) ;
#12656=CARTESIAN_POINT ( 'NONE',  ( -6.001507490154111224, -13.31361390284150659, -13.33564355450122285 ) ) ;
#12663=VERTEX_POINT ( 'NONE', #56154 ) ;
#12666=CARTESIAN_POINT ( 'NONE',  ( -6.016761891674565099, 13.32657647165373760, -13.32172022638577680 ) ) ;
#12674=EDGE_CURVE ( 'NONE', #36543, #46057, #17720, .T. ) ;
#12675=CARTESIAN_POINT ( 'NONE',  ( 0.1103936448916685020, 0.01291577404961429323, -43.12443171339901227 ) ) ;
#12678=AXIS2_PLACEMENT_3D ( 'NONE', #5124, #6038, #5731 ) ;
#12684=FACE_OUTER_BOUND ( 'NONE', #51273, .T. ) ;
#12686=ADVANCED_FACE ( 'NONE', ( #28885 ), #23892, .F. ) ;
#12687=CARTESIAN_POINT ( 'NONE',  ( -6.015611763856276717, 11.46610900684722623, 14.95313250337433963 ) ) ;
#12691=CARTESIAN_POINT ( 'NONE',  ( 0.7246131072078536572, 24.75818606403450417, -41.24126838495074310 ) ) ;
#12697=EDGE_CURVE ( 'NONE', #57388, #25265, #41213, .T. ) ;
#12698=ORIENTED_EDGE ( 'NONE', *, *, #52702, .F. ) ;
#12701=ADVANCED_FACE ( 'NONE', ( #20122 ), #40388, .F. ) ;
#12705=FACE_OUTER_BOUND ( 'NONE', #31364, .T. ) ;
#12709=VECTOR ( 'NONE', #19865, 1000.000000000000114 ) ;
#12715=CARTESIAN_POINT ( 'NONE',  ( 0.6041374136657475802, -6.452348380036255548, 47.67304777898688428 ) ) ;
#12720=CARTESIAN_POINT ( 'NONE',  ( 4.322998006666179727, 2.120302895115615538, 47.94177812210865142 ) ) ;
#12723=CARTESIAN_POINT ( 'NONE',  ( 0.5998501479064699549, -44.24259072156099393, 18.89267974119588445 ) ) ;
#12727=CARTESIAN_POINT ( 'NONE',  ( 0.3622758884714600280, 6.444611261694588755, -42.62881903538203687 ) ) ;
#12729=ORIENTED_EDGE ( 'NONE', *, *, #24867, .T. ) ;
#12730=VERTEX_POINT ( 'NONE', #987 ) ;
#12733=CARTESIAN_POINT ( 'NONE',  ( 2.643462169533600914, -17.09809940585630272, -44.89050350746145313 ) ) ;
#12739=AXIS2_PLACEMENT_3D ( 'NONE', #56297, #61905, #8684 ) ;
#12746=ORIENTED_EDGE ( 'NONE', *, *, #25395, .T. ) ;
#12751=CARTESIAN_POINT ( 'NONE',  ( 0.6001305935487315502, 17.92615948558540850, -44.64600790884038162 ) ) ;
#12758=AXIS2_PLACEMENT_3D ( 'NONE', #18311, #48342, #52103 ) ;
#12765=VERTEX_POINT ( 'NONE', #52993 ) ;
#12766=EDGE_LOOP ( 'NONE', ( #45213, #10326, #60421, #22581 ) ) ;
#12770=CARTESIAN_POINT ( 'NONE',  ( 0.1064266379913941518, 42.82540706760016747, 5.071708164747208869 ) ) ;
#12772=CARTESIAN_POINT ( 'NONE',  ( 0.6041374136657476912, -18.57118264377508865, -44.37863742124660149 ) ) ;
#12783=B_SPLINE_CURVE_WITH_KNOTS ( 'NONE', 3,
 ( #54090, #11212, #30299, #49410 ),
 .UNSPECIFIED., .F., .F.,
 ( 4, 4 ),
 ( 1.992131139712224140E-17, 0.004444306975806115896 ),
 .UNSPECIFIED. ) ;
#12789=CARTESIAN_POINT ( 'NONE',  ( 0.7246131072078533242, -11.65529928397605808, -46.66866179549012372 ) ) ;
#12792=CARTESIAN_POINT ( 'NONE',  ( 0.1102847568649952675, 37.30068345220691839, -21.64199720113203895 ) ) ;
#12799=CARTESIAN_POINT ( 'NONE',  ( 0.8760168074886965917, -47.80016357497253665, 5.394043284318689402 ) ) ;
#12800=CARTESIAN_POINT ( 'NONE',  ( 4.975801465491695552, 0.000000000000000000, 0.000000000000000000 ) ) ;
#12809=CIRCLE ( 'NONE', #28647, 47.91270532121795611 ) ;
#12810=CARTESIAN_POINT ( 'NONE',  ( 0.6254087463353906751, -46.64065386173405869, -11.78492518233793795 ) ) ;
#12824=CARTESIAN_POINT ( 'NONE',  ( 0.6030672727741701600, 24.12926094633986196, -41.61859040196959114 ) ) ;
#12825=ORIENTED_EDGE ( 'NONE', *, *, #11424, .T. ) ;
#12831=CARTESIAN_POINT ( 'NONE',  ( -5.995132425357893702, -18.84415457712583475, -0.008513469643004962714 ) ) ;
#12832=FACE_OUTER_BOUND ( 'NONE', #39808, .T. ) ;
#12833=ORIENTED_EDGE ( 'NONE', *, *, #31635, .T. ) ;
#12835=CARTESIAN_POINT ( 'NONE',  ( 0.1095718737110178836, 26.04820588677147697, 34.36877422441008179 ) ) ;
#12838=CARTESIAN_POINT ( 'NONE',  ( 4.549368137175248350, -40.58005590356700765, 13.99871866169291579 ) ) ;
#12841=CARTESIAN_POINT ( 'NONE',  ( 0.5998501479064708430, -29.69975237324642237, 37.84527566984805702 ) ) ;
#12845=ORIENTED_EDGE ( 'NONE', *, *, #46455, .F. ) ;
#12853=CARTESIAN_POINT ( 'NONE',  ( -6.016104459813371719, -16.32137543786076250, -9.416989654584476455 ) ) ;
#12854=ORIENTED_EDGE ( 'NONE', *, *, #10764, .F. ) ;
#12859=ORIENTED_EDGE ( 'NONE', *, *, #4413, .T. ) ;
#12863=CARTESIAN_POINT ( 'NONE',  ( 0.2885700199627513340, -42.63514063525633446, 6.424755504217515067 ) ) ;
#12874=DIRECTION ( 'NONE',  ( -0.9990097760809875105, 5.448601141172015318E-18, -0.04449120468828680897 ) ) ;
#12877=CARTESIAN_POINT ( 'NONE',  ( 4.975801465491694664, -21.70134120755230711, 42.71626295676225027 ) ) ;
#12879=EDGE_CURVE ( 'NONE', #22472, #57080, #27733, .T. ) ;
#12889=AXIS2_PLACEMENT_3D ( 'NONE', #49266, #43999, #19554 ) ;
#12892=CARTESIAN_POINT ( 'NONE',  ( -6.016104459813374383, -13.32794178585006861, 13.32039631884679842 ) ) ;
#12898=ORIENTED_EDGE ( 'NONE', *, *, #17816, .F. ) ;
#12905=AXIS2_PLACEMENT_3D ( 'NONE', #47524, #48145, #10233 ) ;
#12912=EDGE_LOOP ( 'NONE', ( #47118, #692, #21016, #27741 ) ) ;
#12913=DIRECTION ( 'NONE',  ( 0.1024043820194936311, 0.9239750460186099135, 0.3684880688409236105 ) ) ;
#12916=CARTESIAN_POINT ( 'NONE',  ( 4.833616638992205949, 46.17873762321152498, -2.572717262757493906 ) ) ;
#12917=ORIENTED_EDGE ( 'NONE', *, *, #25997, .T. ) ;
#12919=B_SPLINE_CURVE_WITH_KNOTS ( 'NONE', 3,
 ( #10703, #49835, #57974, #44549, #20716, #48906 ),
 .UNSPECIFIED., .F., .F.,
 ( 4, 2, 4 ),
 ( 8.594572927133164801E-17, 0.0002293366620881456082, 0.0004586733241762052391 ),
 .UNSPECIFIED. ) ;
#12922=DIRECTION ( 'NONE',  ( 0.09835009131224552170, 0.9223318362920736035, 0.3736726418952349693 ) ) ;
#12929=EDGE_LOOP ( 'NONE', ( #34777, #1456, #44769, #9187 ) ) ;
#12934=CARTESIAN_POINT ( 'NONE',  ( 0.3622758884714600280, -17.25816669465019615, 39.50828911766968332 ) ) ;
#12936=AXIS2_PLACEMENT_3D ( 'NONE', #35312, #50612, #2690 ) ;
#12939=CARTESIAN_POINT ( 'NONE',  ( 1.827119703190777988, -27.17434071502579229, -33.38937793923678043 ) ) ;
#12940=CARTESIAN_POINT ( 'NONE',  ( 0.3622758884714730732, -37.74294673546571488, -20.83792692158958815 ) ) ;
#12947=CIRCLE ( 'NONE', #37954, 42.92674063221959813 ) ;
#12949=CARTESIAN_POINT ( 'NONE',  ( 4.975801465491694664, -45.18341283946446651, -15.94009207553035523 ) ) ;
#12953=ADVANCED_FACE ( 'NONE', ( #30732 ), #7967, .F. ) ;
#12955=CARTESIAN_POINT ( 'NONE',  ( -5.995132425357893702, -7.219211173946615823, 17.40647075750114325 ) ) ;
#12960=FACE_OUTER_BOUND ( 'NONE', #31283, .T. ) ;
#12962=CARTESIAN_POINT ( 'NONE',  ( 2.643462169533600914, 11.09243630552468218, 46.73820883660209802 ) ) ;
#12963=CARTESIAN_POINT ( 'NONE',  ( 0.6031356219577718170, 46.44562759437254584, -12.53544563195251271 ) ) ;
#12971=CARTESIAN_POINT ( 'NONE',  ( 0.7954196712028447358, 34.61997730204581813, -33.39101545667300286 ) ) ;
#12974=CARTESIAN_POINT ( 'NONE',  ( 0.3622758884714730732, -31.06363466427707820, -29.89648521331620756 ) ) ;
#12986=EDGE_LOOP ( 'NONE', ( #52, #25000, #55850, #16081 ) ) ;
#12987=CARTESIAN_POINT ( 'NONE',  ( 3.680882792899936806, 25.57189948075129848, 40.59250320379022270 ) ) ;
#12989=LINE ( 'NONE', #8555, #40627 ) ;
#12991=CARTESIAN_POINT ( 'NONE',  ( 0.1095718737110178281, 0.2569529612657829865, -43.12372487139541732 ) ) ;
#12992=ORIENTED_EDGE ( 'NONE', *, *, #27825, .T. ) ;
#12993=ORIENTED_EDGE ( 'NONE', *, *, #23451, .T. ) ;
#12996=ORIENTED_EDGE ( 'NONE', *, *, #15986, .T. ) ;
#12999=CARTESIAN_POINT ( 'NONE',  ( 0.6009453534118438522, 34.32439302680967330, -33.70725662590621852 ) ) ;
#13002=EDGE_CURVE ( 'NONE', #22082, #57516, #9010, .T. ) ;
#13005=CARTESIAN_POINT ( 'NONE',  ( 0.7954196712028464011, 24.79809944608775396, -41.21355366240439366 ) ) ;
#13017=CARTESIAN_POINT ( 'NONE',  ( 4.833616638992208614, -45.44786513329592736, -8.578242093415591185 ) ) ;
#13024=CARTESIAN_POINT ( 'NONE',  ( 4.691466044806103852, -44.51344083442437238, -2.583163953528327283 ) ) ;
#13048=CARTESIAN_POINT ( 'NONE',  ( 0.5998501479064699549, -38.48283596222010061, -28.86886762351111457 ) ) ;
#13050=CARTESIAN_POINT ( 'NONE',  ( 0.5998501479064708430, -44.24259072156073813, -18.89267974119652749 ) ) ;
#13055=LINE ( 'NONE', #37170, #49937 ) ;
#13057=CARTESIAN_POINT ( 'NONE',  ( 0.2224561200757611545, 11.89200283918790646, -41.44719785461218464 ) ) ;
#13058=ORIENTED_EDGE ( 'NONE', *, *, #13701, .T. ) ;
#13077=CARTESIAN_POINT ( 'NONE',  ( -6.010958268070873523, -18.20513189769804896, -4.863021950010837813 ) ) ;
#13078=CARTESIAN_POINT ( 'NONE',  ( 0.7954196712028472893, -17.60078400783993047, -44.76287685048079368 ) ) ;
#13080=CARTESIAN_POINT ( 'NONE',  ( 0.1095718737110177865, -26.45591486700782369, 34.05592812063336083 ) ) ;
#13101=CARTESIAN_POINT ( 'NONE',  ( 0.1073791018717483448, -41.52698815987176317, 11.62916352156079824 ) ) ;
#13103=B_SPLINE_CURVE_WITH_KNOTS ( 'NONE', 3,
 ( #5793, #21461, #20247, #30853, #7028, #29938 ),
 .UNSPECIFIED., .F., .F.,
 ( 4, 2, 4 ),
 ( 8.541065402288461036E-17, 0.0002293366620881459063, 0.0004586733241762064317 ),
 .UNSPECIFIED. ) ;
#13113=CARTESIAN_POINT ( 'NONE',  ( 0.1313383488274142974, 30.94058105930520952, 30.03864748494556736 ) ) ;
#13115=EDGE_CURVE ( 'NONE', #11251, #26923, #28713, .T. ) ;
#13119=CARTESIAN_POINT ( 'NONE',  ( 0.7954190325252780136, -42.08256085583556683, -23.29293489839720976 ) ) ;
#13121=ORIENTED_EDGE ( 'NONE', *, *, #12060, .T. ) ;
#13124=FACE_OUTER_BOUND ( 'NONE', #53760, .T. ) ;
#13128=EDGE_CURVE ( 'NONE', #9574, #60249, #5975, .T. ) ;
#13135=CARTESIAN_POINT ( 'NONE',  ( -6.016489644550737204, 18.19999694163064063, 4.881234076340438932 ) ) ;
#13143=EDGE_LOOP ( 'NONE', ( #42590, #35543, #60478, #36483 ) ) ;
#13147=EDGE_CURVE ( 'NONE', #5867, #25607, #43556, .T. ) ;
#13151=LINE ( 'NONE', #32250, #57381 ) ;
#13153=CARTESIAN_POINT ( 'NONE',  ( 0.1092565886968784594, -16.21587544131350000, 39.95965440403619340 ) ) ;
#13154=CARTESIAN_POINT ( 'NONE',  ( 0.6031356755773454870, 44.44549206087155824, 18.40989784469875801 ) ) ;
#13162=VECTOR ( 'NONE', #35140, 1000.000000000000114 ) ;
#13163=FACE_OUTER_BOUND ( 'NONE', #35100, .T. ) ;
#13170=CARTESIAN_POINT ( 'NONE',  ( -5.995132425357893702, -11.46484027925357729, -14.95525565067286600 ) ) ;
#13172=B_SPLINE_CURVE_WITH_KNOTS ( 'NONE', 3,
 ( #55187, #31712, #60496, #1946, #25769, #59266 ),
 .UNSPECIFIED., .F., .F.,
 ( 4, 2, 4 ),
 ( 1.710438460654249876E-17, 0.0002293319059085093036, 0.0004586638118170015309 ),
 .UNSPECIFIED. ) ;
#13181=CARTESIAN_POINT ( 'NONE',  ( 0.1103744047535531458, 21.59576373962417151, -37.32746539760798754 ) ) ;
#13191=CARTESIAN_POINT ( 'NONE',  ( -6.016761891674565099, 16.32039929810269996, -9.418621820384323939 ) ) ;
#13196=VECTOR ( 'NONE', #35649, 1000.000000000000000 ) ;
#13204=CARTESIAN_POINT ( 'NONE',  ( 0.5998501479064699549, 29.69975237324562656, 37.84527566984866809 ) ) ;
#13209=CARTESIAN_POINT ( 'NONE',  ( -6.016489644550737204, 4.872725758886191194, 18.20227673842146032 ) ) ;
#13218=CARTESIAN_POINT ( 'NONE',  ( 0.7954196712028465122, -41.21355366240445761, -24.79809944608760475 ) ) ;
#13222=CARTESIAN_POINT ( 'NONE',  ( 4.549368137175248350, -32.13400537129945178, 28.46244473166616729 ) ) ;
#13229=ORIENTED_EDGE ( 'NONE', *, *, #53017, .T. ) ;
#13234=DIRECTION ( 'NONE',  ( -1.000000000000000000, -0.000000000000000000, -0.000000000000000000 ) ) ;
#13235=VERTEX_POINT ( 'NONE', #20967 ) ;
#13239=CARTESIAN_POINT ( 'NONE',  ( -6.017396004339687465, 18.68211039806567086, -2.458362590802601222 ) ) ;
#13240=AXIS2_PLACEMENT_3D ( 'NONE', #39465, #58519, #10017 ) ;
#13242=CARTESIAN_POINT ( 'NONE',  ( -4.908599999999998964, 0.000000000000000000, 48.35291015139245019 ) ) ;
#13244=B_SPLINE_CURVE_WITH_KNOTS ( 'NONE', 3,
 ( #25663, #15668, #25357, #34771 ),
 .UNSPECIFIED., .F., .F.,
 ( 4, 4 ),
 ( 0.000000000000000000, 0.005014147105413706458 ),
 .UNSPECIFIED. ) ;
#13245=CARTESIAN_POINT ( 'NONE',  ( 0.5998501479064699549, 28.86886762351124958, -38.48283596222000114 ) ) ;
#13246=CARTESIAN_POINT ( 'NONE',  ( -6.016761891674564211, 11.47373234755503013, 14.94721834528419002 ) ) ;
#13247=EDGE_CURVE ( 'NONE', #2081, #13939, #42643, .T. ) ;
#13248=CARTESIAN_POINT ( 'NONE',  ( 4.322998006666165516, -4.155494336618380302, -47.80838462754064011 ) ) ;
#13252=CARTESIAN_POINT ( 'NONE',  ( -2.708315649062910779, -7.544341609840062191, 12.54007339125002041 ) ) ;
#13254=DIRECTION ( 'NONE',  ( 0.000000000000000000, 0.000000000000000000, 1.000000000000000000 ) ) ;
#13258=CARTESIAN_POINT ( 'NONE',  ( 2.301529144917015213, 46.71331407887422671, 11.18385659262694531 ) ) ;
#13260=CARTESIAN_POINT ( 'NONE',  ( 0.6009453534118438522, 46.57942464365174118, -12.02914401651124443 ) ) ;
#13265=CARTESIAN_POINT ( 'NONE',  ( -6.001507490154111224, 18.20581304543304668, -4.862106078787734376 ) ) ;
#13266=DIRECTION ( 'NONE',  ( 0.000000000000000000, 0.000000000000000000, 1.000000000000000000 ) ) ;
#13269=VERTEX_POINT ( 'NONE', #20552 ) ;
#13285=CARTESIAN_POINT ( 'NONE',  ( 0.1092355843206037486, 21.30139719602319559, 37.49628696754466262 ) ) ;
#13292=CARTESIAN_POINT ( 'NONE',  ( 4.975801465491694664, 15.94009207553051510, -45.18341283946441678 ) ) ;
#13297=ORIENTED_EDGE ( 'NONE', *, *, #30939, .T. ) ;
#13298=CARTESIAN_POINT ( 'NONE',  ( -6.010958268070873523, -4.863021950010776528, 18.20513189769807028 ) ) ;
#13299=CARTESIAN_POINT ( 'NONE',  ( 0.1310142868023689011, -10.54463319394704435, -41.81449350725025482 ) ) ;
#13318=CARTESIAN_POINT ( 'NONE',  ( 0.3622758884714730732, 42.62881903538210793, -6.444611261694146442 ) ) ;
#13324=ORIENTED_EDGE ( 'NONE', *, *, #15910, .T. ) ;
#13328=FACE_OUTER_BOUND ( 'NONE', #31328, .T. ) ;
#13329=B_SPLINE_CURVE_WITH_KNOTS ( 'NONE', 3,
 ( #50468, #59235, #40483, #26982 ),
 .UNSPECIFIED., .F., .F.,
 ( 4, 4 ),
 ( 0.000000000000000000, 0.005014147105413696917 ),
 .UNSPECIFIED. ) ;
#13339=ORIENTED_EDGE ( 'NONE', *, *, #24913, .T. ) ;
#13349=CARTESIAN_POINT ( 'NONE',  ( 2.643462169533600914, 32.97543604874627476, 34.93025802711738237 ) ) ;
#13361=( BOUNDED_SURFACE ( )  B_SPLINE_SURFACE ( 3, 1, ( 
 ( #42955, #37957 ),
 ( #24748, #19752 ),
 ( #3, #18832 ),
 ( #14137, #10037 ) ),
 .UNSPECIFIED., .F., .F., .F. ) 
 B_SPLINE_SURFACE_WITH_KNOTS ( ( 4, 4 ),
 ( 2, 2 ),
 ( 0.000000000000000000, 1.000000000000000000 ),
 ( 0.000000000000000000, 1.000000000000000000 ),
 .UNSPECIFIED. ) 
 GEOMETRIC_REPRESENTATION_ITEM ( )  RATIONAL_B_SPLINE_SURFACE ( (
 ( 1.000000000000000000, 1.000000000000000000),
 ( 0.9751682680413298332, 0.9999560080971552356),
 ( 0.9751682680413298332, 0.9999560080971552356),
 ( 1.000000000000000000, 1.000000000000000000) ) ) 
 REPRESENTATION_ITEM ( '' )  SURFACE ( )  );
#13364=ORIENTED_EDGE ( 'NONE', *, *, #9538, .T. ) ;
#13367=CARTESIAN_POINT ( 'NONE',  ( 0.8751705887134423323, -7.160166390004656378, 47.55935879196458416 ) ) ;
#13369=B_SPLINE_CURVE_WITH_KNOTS ( 'NONE', 3,
 ( #25810, #45555, #55533, #50236 ),
 .UNSPECIFIED., .F., .F.,
 ( 4, 4 ),
 ( 6.254634441385501517E-18, 0.004566006591234647236 ),
 .UNSPECIFIED. ) ;
#13380=ORIENTED_EDGE ( 'NONE', *, *, #46624, .F. ) ;
#13383=ADVANCED_FACE ( 'NONE', ( #10701 ), #10361, .F. ) ;
#13386=CARTESIAN_POINT ( 'NONE',  ( 0.5988103564986355654, -33.58571500783082797, 34.44345003622193246 ) ) ;
#13391=ORIENTED_EDGE ( 'NONE', *, *, #18274, .F. ) ;
#13395=EDGE_CURVE ( 'NONE', #52432, #34503, #18014, .T. ) ;
#13406=CARTESIAN_POINT ( 'NONE',  ( -6.015611763856276717, 18.68122482568283260, -2.465697960550860657 ) ) ;
#13408=CARTESIAN_POINT ( 'NONE',  ( 0.3622758884714600280, -25.58609868863743841, -34.70015533914819628 ) ) ;
#13411=CARTESIAN_POINT ( 'NONE',  ( 0.7954196712028467342, -44.09776749253668271, -19.20650004024986401 ) ) ;
#13412=CARTESIAN_POINT ( 'NONE',  ( 0.1081432562775997835, -6.048481838666351251, 42.69830087850301226 ) ) ;
#13416=VECTOR ( 'NONE', #28559, 1000.000000000000227 ) ;
#13429=CARTESIAN_POINT ( 'NONE',  ( 0.6009452777970410997, 23.67489783211094334, -41.87890062806012281 ) ) ;
#13437=CARTESIAN_POINT ( 'NONE',  ( 0.8751705887134423323, 44.08562551107055327, 19.22545746485676688 ) ) ;
#13445=CARTESIAN_POINT ( 'NONE',  ( 0.8751705887134553219, 24.81530984069150136, 41.19904111682516401 ) ) ;
#13446=EDGE_LOOP ( 'NONE', ( #57143, #49411, #13831, #9865 ) ) ;
#13449=CARTESIAN_POINT ( 'NONE',  ( 4.549368137175248350, 42.06008734272383975, 8.582197505784577629 ) ) ;
#13453=CARTESIAN_POINT ( 'NONE',  ( 0.1073791018717578927, -16.95003405440338895, 39.65380858626186722 ) ) ;
#13465=FACE_OUTER_BOUND ( 'NONE', #38244, .T. ) ;
#13468=CARTESIAN_POINT ( 'NONE',  ( 0.1102144999581333162, -34.28951223307547025, 26.15241010112966435 ) ) ;
#13474=EDGE_CURVE ( 'NONE', #940, #3592, #40640, .T. ) ;
#13480=CARTESIAN_POINT ( 'NONE',  ( 0.6254311100348660668, -5.596225872411697111, -47.77988293940227749 ) ) ;
#13490=CARTESIAN_POINT ( 'NONE',  ( 4.975801465491694664, 40.15204426031534268, -26.14269827151636605 ) ) ;
#13491=VECTOR ( 'NONE', #23263, 999.9999999999998863 ) ;
#13496=B_SPLINE_CURVE_WITH_KNOTS ( 'NONE', 3,
 ( #2803, #35741, #16940, #11943 ),
 .UNSPECIFIED., .F., .F.,
 ( 4, 4 ),
 ( 2.414736334504793811E-17, 0.004564976165746186844 ),
 .UNSPECIFIED. ) ;
#13501=CARTESIAN_POINT ( 'NONE',  ( 4.691466044806103852, 9.025781474740853128, 43.66525414675645322 ) ) ;
#13505=CARTESIAN_POINT ( 'NONE',  ( -6.016489644550737204, 18.68142234211824260, 2.463898142942827274 ) ) ;
#13507=CARTESIAN_POINT ( 'NONE',  ( 0.5998501479064699549, 24.50586714782546593, 41.39809967730496254 ) ) ;
#13509=CARTESIAN_POINT ( 'NONE',  ( -6.001507490154110336, 14.94036486426028887, -11.48377994779686162 ) ) ;
#13512=EDGE_LOOP ( 'NONE', ( #52297, #40279, #11223, #59376 ) ) ;
#13514=DIRECTION ( 'NONE',  ( -1.000000000000000000, -0.000000000000000000, -0.000000000000000000 ) ) ;
#13520=CARTESIAN_POINT ( 'NONE',  ( 0.7246131072078544344, 48.09507913767660625, 0.8205838906004792044 ) ) ;
#13521=CARTESIAN_POINT ( 'NONE',  ( 0.5998501479064708430, 47.62484632993678701, 6.798102206414301740 ) ) ;
#13529=ORIENTED_EDGE ( 'NONE', *, *, #39220, .F. ) ;
#13538=ORIENTED_EDGE ( 'NONE', *, *, #12879, .F. ) ;
#13540=CARTESIAN_POINT ( 'NONE',  ( 0.7048096507298579061, 46.68221792389239511, -11.63498350884287724 ) ) ;
#13546=CARTESIAN_POINT ( 'NONE',  ( 4.322998006666179727, 43.48102276965701662, -20.30542865297603683 ) ) ;
#13547=EDGE_CURVE ( 'NONE', #1398, #40637, #26638, .T. ) ;
#13555=CARTESIAN_POINT ( 'NONE',  ( 0.1064266418746774162, -22.04679912212855442, 37.06314021531073877 ) ) ;
#13556=AXIS2_PLACEMENT_3D ( 'NONE', #28939, #43371, #38673 ) ;
#13558=B_SPLINE_CURVE_WITH_KNOTS ( 'NONE', 3,
 ( #34581, #19873, #52429, #5420, #48361, #38679 ),
 .UNSPECIFIED., .F., .F.,
 ( 4, 2, 4 ),
 ( 1.271362391926013986E-16, 0.0002450741128632365163, 0.0004901482257263459642 ),
 .UNSPECIFIED. ) ;
#13559=CARTESIAN_POINT ( 'NONE',  ( 4.549368137175248350, 0.000000000000000000, 0.000000000000000000 ) ) ;
#13563=EDGE_CURVE ( 'NONE', #199, #4129, #47730, .T. ) ;
#13566=CARTESIAN_POINT ( 'NONE',  ( 0.5980894510889457338, 24.66136644716763371, 41.31170365136896550 ) ) ;
#13577=B_SPLINE_CURVE_WITH_KNOTS ( 'NONE', 3,
 ( #18574, #42397, #33302, #4431 ),
 .UNSPECIFIED., .F., .F.,
 ( 4, 4 ),
 ( 0.000000000000000000, 0.004445488388166994251 ),
 .UNSPECIFIED. ) ;
#13580=ORIENTED_EDGE ( 'NONE', *, *, #7461, .F. ) ;
#13582=CARTESIAN_POINT ( 'NONE',  ( 0.6030672727741701600, -38.11303703924448172, -29.35514790473137481 ) ) ;
#13583=EDGE_CURVE ( 'NONE', #19448, #56393, #6581, .T. ) ;
#13584=DIRECTION ( 'NONE',  ( 1.000000000000000000, 0.000000000000000000, 0.000000000000000000 ) ) ;
#13585=FACE_OUTER_BOUND ( 'NONE', #56180, .T. ) ;
#13592=CARTESIAN_POINT ( 'NONE',  ( 0.1103744047535531458, -30.46616790811201625, -30.52096488484616899 ) ) ;
#13593=ORIENTED_EDGE ( 'NONE', *, *, #59184, .T. ) ;
#13595=FACE_OUTER_BOUND ( 'NONE', #23572, .T. ) ;
#13597=EDGE_CURVE ( 'NONE', #30061, #34292, #14129, .T. ) ;
#13598=EDGE_LOOP ( 'NONE', ( #33540, #9864, #50110, #6562 ) ) ;
#13600=AXIS2_PLACEMENT_3D ( 'NONE', #1686, #20824, #39962 ) ;
#13604=CARTESIAN_POINT ( 'NONE',  ( 0.8751705887134553219, -24.81530984069179269, -41.19904111682499348 ) ) ;
#13613=CARTESIAN_POINT ( 'NONE',  ( 2.301430502907645170, -48.01619648598872203, -1.287492012859226875 ) ) ;
#13618=EDGE_LOOP ( 'NONE', ( #17157, #55219, #41197, #16753 ) ) ;
#13631=CARTESIAN_POINT ( 'NONE',  ( 0.8760168074887090262, -5.394043284319860021, 47.80016357497240165 ) ) ;
#13636=CARTESIAN_POINT ( 'NONE',  ( -6.001507490154111224, -18.68062548815624169, -2.475062734132633224 ) ) ;
#13640=FACE_OUTER_BOUND ( 'NONE', #5516, .T. ) ;
#13647=CARTESIAN_POINT ( 'NONE',  ( 0.6017667736363749853, -46.37677940471289162, -12.78803812527872097 ) ) ;
#13656=VERTEX_POINT ( 'NONE', #56061 ) ;
#13659=CARTESIAN_POINT ( 'NONE',  ( 0.6031356219577718170, -44.47888959008686527, -18.32926896140815387 ) ) ;
#13669=CARTESIAN_POINT ( 'NONE',  ( 0.6030672727741701600, 41.61859040196950588, 24.12926094634001117 ) ) ;
#13674=CARTESIAN_POINT ( 'NONE',  ( 2.301529144917015213, 22.89307126379987167, -42.22700141647020189 ) ) ;
#13676=ORIENTED_EDGE ( 'NONE', *, *, #1401, .F. ) ;
#13681=CARTESIAN_POINT ( 'NONE',  ( 4.975801465491695552, 47.10002938642130488, 8.787181743660319455 ) ) ;
#13691=ORIENTED_EDGE ( 'NONE', *, *, #55583, .T. ) ;
#13692=CARTESIAN_POINT ( 'NONE',  ( -6.016761891674565099, -0.003433883959915969616, 18.84319130225482297 ) ) ;
#13701=EDGE_CURVE ( 'NONE', #44114, #19627, #20112, .T. ) ;
#13703=DIRECTION ( 'NONE',  ( -0.1024043820194934229, -0.3927886084231700936, 0.9139094329506590730 ) ) ;
#13706=CARTESIAN_POINT ( 'NONE',  ( 0.1101816497532063233, 26.14462713083295498, -34.29544870207487151 ) ) ;
#13707=CARTESIAN_POINT ( 'NONE',  ( 2.643462169533613793, 7.637863311826968093, 47.42536612906431515 ) ) ;
#13710=FACE_OUTER_BOUND ( 'NONE', #11258, .T. ) ;
#13716=CARTESIAN_POINT ( 'NONE',  ( 0.2224561200757616264, -11.89200283918819423, 41.44719785461210648 ) ) ;
#13721=CARTESIAN_POINT ( 'NONE',  ( 0.6023142530420679819, 47.72938419887611161, 6.019593586345465930 ) ) ;
#13722=B_SPLINE_CURVE_WITH_KNOTS ( 'NONE', 3,
 ( #18479, #15027, #57275, #18799 ),
 .UNSPECIFIED., .F., .F.,
 ( 4, 4 ),
 ( 4.670885906470169154E-18, 0.004566006591234648103 ),
 .UNSPECIFIED. ) ;
#13726=CARTESIAN_POINT ( 'NONE',  ( 0.1064266418746777354, 22.04679912212828796, -37.06314021531088088 ) ) ;
#13735=EDGE_LOOP ( 'NONE', ( #47330, #57531, #30351, #37655 ) ) ;
#13747=CARTESIAN_POINT ( 'NONE',  ( 0.6254087463353924514, -46.28445368454761422, 13.11428234126282888 ) ) ;
#13749=ORIENTED_EDGE ( 'NONE', *, *, #53854, .F. ) ;
#13751=B_SPLINE_CURVE_WITH_KNOTS ( 'NONE', 3,
 ( #11817, #11189, #44421, #40032, #59083, #20585, #60014, #2377, #2689, #17126, #54685, #55306, #50611, #12425, #35311, #36239, #30898, #31518, #54372 ),
 .UNSPECIFIED., .F., .F.,
 ( 4, 3, 3, 3, 3, 3, 4 ),
 ( 1.121058697680834634E-16, 0.0002618519381806306873, 0.0003927759815485986315, 0.0005237000248299465742, 0.0006546240681325006441, 0.0007855481115631358533, 0.0009699050456655141945 ),
 .UNSPECIFIED. ) ;
#13753=ORIENTED_EDGE ( 'NONE', *, *, #15780, .T. ) ;
#13755=( BOUNDED_SURFACE ( )  B_SPLINE_SURFACE ( 3, 1, ( 
 ( #12442, #45352 ),
 ( #3016, #40972 ),
 ( #50326, #60036 ),
 ( #6771, #40658 ) ),
 .UNSPECIFIED., .F., .F., .F. ) 
 B_SPLINE_SURFACE_WITH_KNOTS ( ( 4, 4 ),
 ( 2, 2 ),
 ( 0.000000000000000000, 1.000000000000000000 ),
 ( 0.000000000000000000, 1.000000000000000000 ),
 .UNSPECIFIED. ) 
 GEOMETRIC_REPRESENTATION_ITEM ( )  RATIONAL_B_SPLINE_SURFACE ( (
 ( 1.000000000000000000, 1.000000000000000000),
 ( 0.7223157951917476005, 0.9931996967497186413),
 ( 0.7223157951917476005, 0.9931996967497186413),
 ( 1.000000000000000000, 1.000000000000000000) ) ) 
 REPRESENTATION_ITEM ( '' )  SURFACE ( )  );
#13758=B_SPLINE_CURVE_WITH_KNOTS ( 'NONE', 3,
 ( #51814, #8915, #14559, #28027, #42757, #23027 ),
 .UNSPECIFIED., .F., .F.,
 ( 4, 2, 4 ),
 ( 1.823789517034659149E-17, 0.0002293319059085091138, 0.0004586638118169999588 ),
 .UNSPECIFIED. ) ;
#13772=CARTESIAN_POINT ( 'NONE',  ( 0.6001305935487422083, -33.64689939321919354, -34.38748867424700961 ) ) ;
#13776=VERTEX_POINT ( 'NONE', #28481 ) ;
#13777=CARTESIAN_POINT ( 'NONE',  ( -6.001507490154111224, 11.45906331631431030, 14.95933060264877845 ) ) ;
#13786=CARTESIAN_POINT ( 'NONE',  ( 0.1092565886968784178, -34.02318727879980997, 26.49813811968527588 ) ) ;
#13792=CARTESIAN_POINT ( 'NONE',  ( 4.549368137175248350, 0.000000000000000000, 0.000000000000000000 ) ) ;
#13804=CARTESIAN_POINT ( 'NONE',  ( 2.301529144917013436, -34.86298839095307756, -33.04216096093391997 ) ) ;
#13805=CARTESIAN_POINT ( 'NONE',  ( 0.8760168074886960365, 17.58183840866336212, 44.77533136581888584 ) ) ;
#13811=AXIS2_PLACEMENT_3D ( 'NONE', #13974, #23353, #42477 ) ;
#13812=CARTESIAN_POINT ( 'NONE',  ( 4.975801465491694664, -46.87746200127448049, -9.906103548668065528 ) ) ;
#13814=EDGE_CURVE ( 'NONE', #53679, #49781, #23107, .T. ) ;
#13817=CARTESIAN_POINT ( 'NONE',  ( 0.8751705887134423323, 47.55935879196461968, 7.160166390004468973 ) ) ;
#13822=DIRECTION ( 'NONE',  ( 1.000000000000000000, 0.000000000000000000, 0.000000000000000000 ) ) ;
#13823=VERTEX_POINT ( 'NONE', #19721 ) ;
#13827=EDGE_LOOP ( 'NONE', ( #34460, #5214, #57167, #32767 ) ) ;
#13830=ORIENTED_EDGE ( 'NONE', *, *, #5349, .F. ) ;
#13831=ORIENTED_EDGE ( 'NONE', *, *, #5123, .F. ) ;
#13838=( BOUNDED_SURFACE ( )  B_SPLINE_SURFACE ( 3, 1, ( 
 ( #30555, #35903 ),
 ( #39377, #54971 ),
 ( #12104, #31179 ),
 ( #25553, #44691 ) ),
 .UNSPECIFIED., .F., .F., .F. ) 
 B_SPLINE_SURFACE_WITH_KNOTS ( ( 4, 4 ),
 ( 2, 2 ),
 ( 0.000000000000000000, 1.000000000000000000 ),
 ( 0.000000000000000000, 1.000000000000000000 ),
 .UNSPECIFIED. ) 
 GEOMETRIC_REPRESENTATION_ITEM ( )  RATIONAL_B_SPLINE_SURFACE ( (
 ( 1.000000000000000000, 1.000000000000000000),
 ( 0.7223157951917476005, 0.9931996967497186413),
 ( 0.7223157951917476005, 0.9931996967497186413),
 ( 1.000000000000000000, 1.000000000000000000) ) ) 
 REPRESENTATION_ITEM ( '' )  SURFACE ( )  );
#13840=CARTESIAN_POINT ( 'NONE',  ( 0.6009452777970410997, -0.4363873594209082829, -48.10564074251961131 ) ) ;
#13842=( BOUNDED_SURFACE ( )  B_SPLINE_SURFACE ( 3, 1, ( 
 ( #41962, #55398 ),
 ( #17516, #41344 ),
 ( #56638, #60395 ),
 ( #18136, #22524 ) ),
 .UNSPECIFIED., .F., .F., .F. ) 
 B_SPLINE_SURFACE_WITH_KNOTS ( ( 4, 4 ),
 ( 2, 2 ),
 ( 0.000000000000000000, 1.000000000000000000 ),
 ( 0.000000000000000000, 1.000000000000000000 ),
 .UNSPECIFIED. ) 
 GEOMETRIC_REPRESENTATION_ITEM ( )  RATIONAL_B_SPLINE_SURFACE ( (
 ( 1.000000000000000000, 1.000000000000000000),
 ( 0.9751682680413298332, 0.9999560080971552356),
 ( 0.9751682680413298332, 0.9999560080971552356),
 ( 1.000000000000000000, 1.000000000000000000) ) ) 
 REPRESENTATION_ITEM ( '' )  SURFACE ( )  );
#13866=CARTESIAN_POINT ( 'NONE',  ( -6.016104459813371719, -18.84322058118302579, 0.005335450885000186244 ) ) ;
#13876=CARTESIAN_POINT ( 'NONE',  ( 0.1073791018717483448, -21.14095454447585709, 37.58707531572169813 ) ) ;
#13893=ORIENTED_EDGE ( 'NONE', *, *, #12516, .T. ) ;
#13896=B_SPLINE_CURVE_WITH_KNOTS ( 'NONE', 3,
 ( #5121, #53359, #43388, #38382 ),
 .UNSPECIFIED., .F., .F.,
 ( 4, 4 ),
 ( 1.998817200139820460E-17, 0.004444306975806115029 ),
 .UNSPECIFIED. ) ;
#13899=CARTESIAN_POINT ( 'NONE',  ( 0.5998501479064708430, 41.39809967730453621, 24.50586714782619424 ) ) ;
#13906=ORIENTED_EDGE ( 'NONE', *, *, #51619, .F. ) ;
#13908=ADVANCED_FACE ( 'NONE', ( #25335 ), #25528, .F. ) ;
#13909=ORIENTED_EDGE ( 'NONE', *, *, #54547, .T. ) ;
#13911=CARTESIAN_POINT ( 'NONE',  ( 4.975801465491695552, 47.84403947906839960, 2.564218696447662982 ) ) ;
#13920=CARTESIAN_POINT ( 'NONE',  ( -6.016761891674564211, 11.46828378093580980, -14.95139917749692415 ) ) ;
#13922=ORIENTED_EDGE ( 'NONE', *, *, #29760, .T. ) ;
#13926=CARTESIAN_POINT ( 'NONE',  ( 0.1103878639767399694, 5.676988162228092882, 42.74915604780181866 ) ) ;
#13927=FACE_OUTER_BOUND ( 'NONE', #38554, .T. ) ;
#13928=ORIENTED_EDGE ( 'NONE', *, *, #17619, .T. ) ;
#13930=CARTESIAN_POINT ( 'NONE',  ( 0.1073791018717578927, -10.69234304550026593, -41.77800844988510676 ) ) ;
#13932=ADVANCED_FACE ( 'NONE', ( #30031 ), #46782, .F. ) ;
#13939=VERTEX_POINT ( 'NONE', #11561 ) ;
#13941=CARTESIAN_POINT ( 'NONE',  ( 0.1081432562775999084, -42.80885385101085916, 5.208748643065970185 ) ) ;
#13942=CARTESIAN_POINT ( 'NONE',  ( 4.975801465491695552, -8.787181743660504196, 47.10002938642126935 ) ) ;
#13943=CARTESIAN_POINT ( 'NONE',  ( 4.975801465491695552, 0.000000000000000000, 0.000000000000000000 ) ) ;
#13944=CARTESIAN_POINT ( 'NONE',  ( 0.6041374136657476912, 29.14743607025083350, -38.27243465845312187 ) ) ;
#13945=CARTESIAN_POINT ( 'NONE',  ( -2.569797478183783568, 5.182550149005303197, -13.68441171582010973 ) ) ;
#13947=CARTESIAN_POINT ( 'NONE',  ( 0.2224561200757667057, 40.12166550582812619, -15.79689521915824280 ) ) ;
#13956=CARTESIAN_POINT ( 'NONE',  ( -6.015611763856276717, -11.46610900684733281, 14.95313250337425970 ) ) ;
#13960=CARTESIAN_POINT ( 'NONE',  ( 4.322998006666165516, -47.94177812210863010, -2.120302895116112030 ) ) ;
#13974=CARTESIAN_POINT ( 'NONE',  ( 4.549368137175248350, 0.000000000000000000, 0.000000000000000000 ) ) ;
#13979=CARTESIAN_POINT ( 'NONE',  ( 0.6025881611877910160, -44.36157157392742079, -18.61132239451771042 ) ) ;
#13983=DIRECTION ( 'NONE',  ( 0.1024043820194936311, 0.2701391291102721026, 0.9573600124648768972 ) ) ;
#13987=CARTESIAN_POINT ( 'NONE',  ( 0.5998501479064699549, -17.92509395669137362, 44.64337787626217846 ) ) ;
#13994=CARTESIAN_POINT ( 'NONE',  ( 2.301430502907646058, -47.43735983879647478, -7.543848632415047106 ) ) ;
#13999=ORIENTED_EDGE ( 'NONE', *, *, #39888, .T. ) ;
#14002=CARTESIAN_POINT ( 'NONE',  ( -6.016761891674564211, -2.462934516563682230, -18.68153697670644320 ) ) ;
#14005=ORIENTED_EDGE ( 'NONE', *, *, #13583, .T. ) ;
#14006=CARTESIAN_POINT ( 'NONE',  ( -6.017396004339687465, -0.001173774849114137117, 18.84316306185412415 ) ) ;
#14017=CARTESIAN_POINT ( 'NONE',  ( 0.5998501479064708430, 47.76154736470757456, -5.759754759340284913 ) ) ;
#14021=CARTESIAN_POINT ( 'NONE',  ( 4.322998006666179727, 8.359821156455842228, 47.25487450103538833 ) ) ;
#14022=ORIENTED_EDGE ( 'NONE', *, *, #942, .T. ) ;
#14032=CARTESIAN_POINT ( 'NONE',  ( -5.995132425357893702, 9.414704407577803025, 16.32377331145323751 ) ) ;
#14034=CARTESIAN_POINT ( 'NONE',  ( 0.8760168074887076939, -11.58706983520358236, 46.68716261866156003 ) ) ;
#14051=CARTESIAN_POINT ( 'NONE',  ( 1.827326673878744812, -12.32830836993849566, 41.24690799101787064 ) ) ;
#14063=AXIS2_PLACEMENT_3D ( 'NONE', #52437, #61824, #33668 ) ;
#14064=CARTESIAN_POINT ( 'NONE',  ( 0.6009452777970410997, 34.32439724342992093, 33.70725232128904736 ) ) ;
#14066=CARTESIAN_POINT ( 'NONE',  ( 4.549368137175248350, 0.000000000000000000, 0.000000000000000000 ) ) ;
#14067=CARTESIAN_POINT ( 'NONE',  ( 0.8751705887134423323, 34.63284514348585930, -33.37254303619518225 ) ) ;
#14080=CARTESIAN_POINT ( 'NONE',  ( 0.1081432562775998807, -16.89351827868247824, 39.67792926340371906 ) ) ;
#14085=CARTESIAN_POINT ( 'NONE',  ( 4.549368137175248350, 0.000000000000000000, 0.000000000000000000 ) ) ;
#14089=EDGE_LOOP ( 'NONE', ( #9204, #40679, #27923, #27243 ) ) ;
#14092=CARTESIAN_POINT ( 'NONE',  ( 0.1100053167205930910, -34.10339839758302816, 26.39466280306210777 ) ) ;
#14093=LINE ( 'NONE', #24395, #10804 ) ;
#14097=EDGE_CURVE ( 'NONE', #46978, #42733, #37314, .T. ) ;
#14099=EDGE_CURVE ( 'NONE', #9817, #52417, #5089, .T. ) ;
#14104=CARTESIAN_POINT ( 'NONE',  ( 4.975801465491694664, 27.09127437476381317, -39.51822597168466444 ) ) ;
#14109=ORIENTED_EDGE ( 'NONE', *, *, #40281, .F. ) ;
#14116=CARTESIAN_POINT ( 'NONE',  ( 5.880360259849739535, 15.46489389606690779, 45.41096578730653022 ) ) ;
#14118=LINE ( 'NONE', #42016, #22268 ) ;
#14127=CARTESIAN_POINT ( 'NONE',  ( 4.975801465491694664, -47.10002938642148251, 8.787181743659342459 ) ) ;
#14128=CARTESIAN_POINT ( 'NONE',  ( 4.975801465491695552, -45.18341283946470099, 15.94009207552969620 ) ) ;
#14129=B_SPLINE_CURVE_WITH_KNOTS ( 'NONE', 3,
 ( #40461, #20714, #59526, #16634 ),
 .UNSPECIFIED., .F., .F.,
 ( 4, 4 ),
 ( 0.000000000000000000, 0.005014147105413706458 ),
 .UNSPECIFIED. ) ;
#14130=ADVANCED_FACE ( 'NONE', ( #44020 ), #51682, .F. ) ;
#14134=EDGE_CURVE ( 'NONE', #6976, #20061, #20190, .T. ) ;
#14137=CARTESIAN_POINT ( 'NONE',  ( -6.016761891674564211, 14.95139917749704495, 11.46828378093564460 ) ) ;
#14145=DIRECTION ( 'NONE',  ( 0.09835009131224564660, 0.3879606369183636883, -0.9164135549743742670 ) ) ;
#14146=B_SPLINE_CURVE_WITH_KNOTS ( 'NONE', 3,
 ( #54617, #39037, #34941, #49321 ),
 .UNSPECIFIED., .F., .F.,
 ( 4, 4 ),
 ( 0.000000000000000000, 0.005014147105413704723 ),
 .UNSPECIFIED. ) ;
#14148=CARTESIAN_POINT ( 'NONE',  ( 0.5998501479064708430, -38.48283596222049141, 28.86886762351059588 ) ) ;
#14149=CARTESIAN_POINT ( 'NONE',  ( 0.6023142530420679819, -0.2618396477464183247, -48.10676733004997629 ) ) ;
#14155=ORIENTED_EDGE ( 'NONE', *, *, #16280, .F. ) ;
#14157=CARTESIAN_POINT ( 'NONE',  ( -4.908599999999998964, 12.80000000000000071, -3.000000000000000000 ) ) ;
#14162=DIRECTION ( 'NONE',  ( 0.09835009131224567436, 0.7091251765524070327, -0.6981896185982648939 ) ) ;
#14163=CARTESIAN_POINT ( 'NONE',  ( 0.1064266379913938465, 11.70292640078096369, 41.50637574965952581 ) ) ;
#14169=EDGE_CURVE ( 'NONE', #8059, #23991, #29088, .T. ) ;
#14175=CARTESIAN_POINT ( 'NONE',  ( 2.301529144917014325, -19.56451384729014364, -43.86846428170453294 ) ) ;
#14177=CARTESIAN_POINT ( 'NONE',  ( -6.016761891674565099, -16.32039929810263601, 9.418621820384437626 ) ) ;
#14183=CARTESIAN_POINT ( 'NONE',  ( -5.995132425357893702, -16.31525984181039846, 9.429450169547896721 ) ) ;
#14184=DIRECTION ( 'NONE',  ( 0.000000000000000000, 0.000000000000000000, 1.000000000000000000 ) ) ;
#14193=B_SPLINE_CURVE_WITH_KNOTS ( 'NONE', 3,
 ( #54049, #45314, #2357, #17716, #50902, #21477 ),
 .UNSPECIFIED., .F., .F.,
 ( 4, 2, 4 ),
 ( 3.496446946337351263E-18, 0.0002450742804987356398, 0.0004901485609974678102 ),
 .UNSPECIFIED. ) ;
#14196=CARTESIAN_POINT ( 'NONE',  ( 5.880360259849752858, -45.44137230084892565, 15.37531919565157246 ) ) ;
#14197=CARTESIAN_POINT ( 'NONE',  ( 4.975801465491695552, 0.000000000000000000, 0.000000000000000000 ) ) ;
#14206=CARTESIAN_POINT ( 'NONE',  ( 0.6023143664670691511, -38.00627775314942625, -29.49326149840218747 ) ) ;
#14220=ORIENTED_EDGE ( 'NONE', *, *, #31851, .F. ) ;
#14226=CARTESIAN_POINT ( 'NONE',  ( -2.708315649062916552, -3.532515819624444831, 14.20182604343554189 ) ) ;
#14228=B_SPLINE_CURVE_WITH_KNOTS ( 'NONE', 3,
 ( #34135, #53811, #6188, #5273 ),
 .UNSPECIFIED., .F., .F.,
 ( 4, 4 ),
 ( 4.336808689942017736E-18, 0.004566006591234648970 ),
 .UNSPECIFIED. ) ;
#14230=AXIS2_PLACEMENT_3D ( 'NONE', #30337, #2444, #21570 ) ;
#14231=CARTESIAN_POINT ( 'NONE',  ( -6.010958268070873523, 0.01451635840163226568, 18.84344976839986785 ) ) ;
#14239=CARTESIAN_POINT ( 'NONE',  ( 0.7245667037590747261, 38.65590879674347491, 28.62745028382829560 ) ) ;
#14245=CARTESIAN_POINT ( 'NONE',  ( 4.691466044806102076, 8.371234562541253865, 43.79545162262311919 ) ) ;
#14250=CARTESIAN_POINT ( 'NONE',  ( 0.1310142868023724816, 40.08041389954882305, -15.91230901232182759 ) ) ;
#14251=CARTESIAN_POINT ( 'NONE',  ( 4.975801465491694664, -35.64402118370934147, -32.01766832630300286 ) ) ;
#14257=ORIENTED_EDGE ( 'NONE', *, *, #35105, .T. ) ;
#14261=EDGE_CURVE ( 'NONE', #42525, #50188, #6517, .T. ) ;
#14266=CARTESIAN_POINT ( 'NONE',  ( 5.880360259849739535, -47.87242051977163726, -3.090325311464695801 ) ) ;
#14270=CARTESIAN_POINT ( 'NONE',  ( 0.6025881611877910160, -46.41131722377301116, -12.66175293297386162 ) ) ;
#14274=CARTESIAN_POINT ( 'NONE',  ( 0.1101816497532063510, 39.89358705406962002, 16.37745527993603289 ) ) ;
#14276=VERTEX_POINT ( 'NONE', #2902 ) ;
#14278=CARTESIAN_POINT ( 'NONE',  ( 0.3622758884714600280, -29.89648521331609743, -31.06363466427717412 ) ) ;
#14285=CARTESIAN_POINT ( 'NONE',  ( 4.322998006666165516, -30.86725474310387085, 36.74401119231355750 ) ) ;
#14288=B_SPLINE_CURVE_WITH_KNOTS ( 'NONE', 3,
 ( #4426, #36769, #51139, #3828 ),
 .UNSPECIFIED., .F., .F.,
 ( 4, 4 ),
 ( 0.000000000000000000, 0.004445488388166995986 ),
 .UNSPECIFIED. ) ;
#14299=CARTESIAN_POINT ( 'NONE',  ( 0.5998501479064708430, -6.798102206414489146, 47.62484632993676570 ) ) ;
#14305=CARTESIAN_POINT ( 'NONE',  ( 0.2224561200757640689, 25.64288022150836355, 34.66601556960360142 ) ) ;
#14306=VERTEX_POINT ( 'NONE', #16399 ) ;
#14322=CARTESIAN_POINT ( 'NONE',  ( 0.6027935024548037868, 29.42425667880436180, -38.05972402498746732 ) ) ;
#14323=( BOUNDED_SURFACE ( )  B_SPLINE_SURFACE ( 3, 1, ( 
 ( #9838, #14860 ),
 ( #6025, #25160 ),
 ( #53046, #53347 ),
 ( #15165, #15779 ) ),
 .UNSPECIFIED., .F., .F., .F. ) 
 B_SPLINE_SURFACE_WITH_KNOTS ( ( 4, 4 ),
 ( 2, 2 ),
 ( 0.000000000000000000, 1.000000000000000000 ),
 ( 0.000000000000000000, 1.000000000000000000 ),
 .UNSPECIFIED. ) 
 GEOMETRIC_REPRESENTATION_ITEM ( )  RATIONAL_B_SPLINE_SURFACE ( (
 ( 1.000000000000000000, 1.000000000000000000),
 ( 0.7223157951917476005, 0.9931996967497186413),
 ( 0.7223157951917476005, 0.9931996967497186413),
 ( 1.000000000000000000, 1.000000000000000000) ) ) 
 REPRESENTATION_ITEM ( '' )  SURFACE ( )  );
#14324=CARTESIAN_POINT ( 'NONE',  ( 0.1102144999581333162, 16.61938362665549818, -39.79340763430492700 ) ) ;
#14326=LINE ( 'NONE', #42838, #6653 ) ;
#14332=EDGE_CURVE ( 'NONE', #42831, #58372, #52665, .T. ) ;
#14340=CARTESIAN_POINT ( 'NONE',  ( 4.975801465491694664, -9.906103548668557579, 46.87746200127438101 ) ) ;
#14342=CARTESIAN_POINT ( 'NONE',  ( 1.827119703190777988, 20.44859290426037646, -37.88337895042275250 ) ) ;
#14344=EDGE_LOOP ( 'NONE', ( #23068, #20968, #37167, #30496 ) ) ;
#14347=CARTESIAN_POINT ( 'NONE',  ( 0.7954196712028469562, -48.09103417491925114, -0.8690072546823950361 ) ) ;
#14348=CARTESIAN_POINT ( 'NONE',  ( 0.1313383488274136590, 17.09007684155447748, 39.59253935480806064 ) ) ;
#14349=CARTESIAN_POINT ( 'NONE',  ( 0.5998501479064699549, -41.92175333043603302, -23.59887241503339439 ) ) ;
#14350=ORIENTED_EDGE ( 'NONE', *, *, #47556, .T. ) ;
#14351=EDGE_CURVE ( 'NONE', #57783, #17208, #30793, .T. ) ;
#14356=B_SPLINE_CURVE_WITH_KNOTS ( 'NONE', 3,
 ( #49925, #54596, #12048, #30804 ),
 .UNSPECIFIED., .F., .F.,
 ( 4, 4 ),
 ( 0.000000000000000000, 0.005014147105413707325 ),
 .UNSPECIFIED. ) ;
#14365=CARTESIAN_POINT ( 'NONE',  ( -6.015611763856276717, -13.32857883366824048, -13.31979030221813254 ) ) ;
#14370=DIRECTION ( 'NONE',  ( 0.1024043820194936311, -0.9878630899050863112, -0.1167898032637303823 ) ) ;
#14372=VERTEX_POINT ( 'NONE', #26718 ) ;
#14378=ORIENTED_EDGE ( 'NONE', *, *, #53926, .F. ) ;
#14379=ADVANCED_FACE ( 'NONE', ( #46161 ), #48767, .F. ) ;
#14383=CARTESIAN_POINT ( 'NONE',  ( 0.2224561200757590174, 20.89867881469716338, 37.71651051365635254 ) ) ;
#14385=ORIENTED_EDGE ( 'NONE', *, *, #26487, .F. ) ;
#14388=DIRECTION ( 'NONE',  ( 0.000000000000000000, 0.000000000000000000, -1.000000000000000000 ) ) ;
#14396=CARTESIAN_POINT ( 'NONE',  ( 0.1102847568649952675, 30.55869130182067295, 30.42833243501160823 ) ) ;
#14409=CARTESIAN_POINT ( 'NONE',  ( 0.6009452777970413218, 0.4363873594205723294, 48.10564074251961841 ) ) ;
#14411=CARTESIAN_POINT ( 'NONE',  ( 0.2885697896453118805, 34.69058521462536504, -25.60460893337440780 ) ) ;
#14425=CARTESIAN_POINT ( 'NONE',  ( 0.5980894510889457338, 13.12879507229223819, 46.28687279963696710 ) ) ;
#14426=CARTESIAN_POINT ( 'NONE',  ( 0.5998501479064699549, -23.59887241503383493, 41.92175333043579144 ) ) ;
#14429=CARTESIAN_POINT ( 'NONE',  ( -2.708315649062910779, 14.20182604343559873, -3.532515819624206799 ) ) ;
#14450=CARTESIAN_POINT ( 'NONE',  ( 0.6041374136657475802, 46.42299778158138679, 12.61972904329615197 ) ) ;
#14458=CARTESIAN_POINT ( 'NONE',  ( 0.6041374136657476912, -24.20487816031493367, -41.57494627055135794 ) ) ;
#14463=EDGE_CURVE ( 'NONE', #58483, #9846, #14795, .T. ) ;
#14465=CARTESIAN_POINT ( 'NONE',  ( 0.8760168074886965917, -46.22580377597776646, -13.30888447662064777 ) ) ;
#14473=CARTESIAN_POINT ( 'NONE',  ( -6.016761891674564211, -18.68243340030201338, -2.456125503350905959 ) ) ;
#14477=CARTESIAN_POINT ( 'NONE',  ( 4.975801465491694664, -21.70134120755230711, 42.71626295676225027 ) ) ;
#14484=CARTESIAN_POINT ( 'NONE',  ( 0.3622758884714600280, -22.26738722580193652, 36.91764744403282350 ) ) ;
#14486=CARTESIAN_POINT ( 'NONE',  ( 0.6031357023905875581, 48.10744334619843698, 0.04361601114929824358 ) ) ;
#14503=CIRCLE ( 'NONE', #22498, 42.92674063221959813 ) ;
#14505=ADVANCED_FACE ( 'NONE', ( #44554 ), #23518, .F. ) ;
#14510=EDGE_LOOP ( 'NONE', ( #35956, #30927, #48126, #41007 ) ) ;
#14518=CARTESIAN_POINT ( 'NONE',  ( 4.975801465491694664, -20.67815041659109809, -43.22084481528213473 ) ) ;
#14519=CARTESIAN_POINT ( 'NONE',  ( -6.010958268070873523, 11.48268200989196863, 14.94067681728554042 ) ) ;
#14520=CARTESIAN_POINT ( 'NONE',  ( 0.1084644655670282398, -30.77359411724706106, -30.21121552070987448 ) ) ;
#14521=ORIENTED_EDGE ( 'NONE', *, *, #7461, .T. ) ;
#14529=LINE ( 'NONE', #28913, #19593 ) ;
#14532=CARTESIAN_POINT ( 'NONE',  ( -6.016104459813374383, -2.464823636987575117, 18.68131780085930771 ) ) ;
#14534=CARTESIAN_POINT ( 'NONE',  ( 0.1087620492084205304, 5.269740196867345183, 42.80136086877935497 ) ) ;
#14536=CARTESIAN_POINT ( 'NONE',  ( 1.827326673878744367, 20.44853789448401216, 37.88339879236866636 ) ) ;
#14538=B_SPLINE_CURVE_WITH_KNOTS ( 'NONE', 3,
 ( #23022, #36824, #13017, #3568 ),
 .UNSPECIFIED., .F., .F.,
 ( 4, 4 ),
 ( 0.000000000000000000, 0.005014147105413707325 ),
 .UNSPECIFIED. ) ;
#14545=CARTESIAN_POINT ( 'NONE',  ( 0.5998501479064708430, -44.24259072156073813, -18.89267974119652749 ) ) ;
#14549=CARTESIAN_POINT ( 'NONE',  ( 0.2885697896453121580, 37.73587455644747735, -20.85752796052974389 ) ) ;
#14556=CARTESIAN_POINT ( 'NONE',  ( 0.3622758884714600280, -33.69533458712325569, -26.89560658783373626 ) ) ;
#14559=CARTESIAN_POINT ( 'NONE',  ( 0.1310142868023716767, 42.83311553787493864, -4.996535778098907699 ) ) ;
#14561=CARTESIAN_POINT ( 'NONE',  ( 0.5998501479064708430, -17.92509395669076966, -44.64337787626241294 ) ) ;
#14563=ORIENTED_EDGE ( 'NONE', *, *, #2332, .T. ) ;
#14564=CARTESIAN_POINT ( 'NONE',  ( -6.016761891674564211, -9.424569481870138432, -16.31696541414282109 ) ) ;
#14569=CARTESIAN_POINT ( 'NONE',  ( -6.015611763856276717, -17.41126425312532433, -7.205255340944797027 ) ) ;
#14571=( BOUNDED_SURFACE ( )  B_SPLINE_SURFACE ( 3, 1, ( 
 ( #42612, #18805 ),
 ( #22876, #56369 ),
 ( #57279, #33520 ),
 ( #33213, #37929 ) ),
 .UNSPECIFIED., .F., .F., .F. ) 
 B_SPLINE_SURFACE_WITH_KNOTS ( ( 4, 4 ),
 ( 2, 2 ),
 ( 0.000000000000000000, 1.000000000000000000 ),
 ( 0.000000000000000000, 1.000000000000000000 ),
 .UNSPECIFIED. ) 
 GEOMETRIC_REPRESENTATION_ITEM ( )  RATIONAL_B_SPLINE_SURFACE ( (
 ( 1.000000000000000000, 1.000000000000000000),
 ( 0.7223157951917480446, 0.9931996967497186413),
 ( 0.7223157951917480446, 0.9931996967497186413),
 ( 1.000000000000000000, 1.000000000000000000) ) ) 
 REPRESENTATION_ITEM ( '' )  SURFACE ( )  );
#14574=CARTESIAN_POINT ( 'NONE',  ( -2.708315649062916552, -0.2635547933242615160, -14.63219292706383001 ) ) ;
#14578=ORIENTED_EDGE ( 'NONE', *, *, #13115, .T. ) ;
#14580=CARTESIAN_POINT ( 'NONE',  ( 0.1104177457020372732, 39.84367193872654411, 16.49849172082177162 ) ) ;
#14598=CARTESIAN_POINT ( 'NONE',  ( 0.3622758884714730732, 10.35929834645922831, -41.85013935980092015 ) ) ;
#14615=CARTESIAN_POINT ( 'NONE',  ( 0.1100247026804066219, -37.26174279786198440, -21.70899701554510841 ) ) ;
#14625=CARTESIAN_POINT ( 'NONE',  ( 5.880360259849739535, -39.91356965504129306, -26.61251048557234711 ) ) ;
#14630=DIRECTION ( 'NONE',  ( 0.000000000000000000, 0.000000000000000000, 1.000000000000000000 ) ) ;
#14631=EDGE_CURVE ( 'NONE', #12553, #1788, #37203, .T. ) ;
#14632=CARTESIAN_POINT ( 'NONE',  ( -5.995132425357893702, -2.451215106828221302, -18.68405145320026506 ) ) ;
#14635=CARTESIAN_POINT ( 'NONE',  ( 4.322998006666165516, 22.13465289016567894, 42.57894920390135240 ) ) ;
#14641=CARTESIAN_POINT ( 'NONE',  ( 2.301430502907645170, -28.20897229937376594, -38.87758534782497577 ) ) ;
#14644=CARTESIAN_POINT ( 'NONE',  ( 4.322998006666179727, -25.80712523194247510, -40.45864630878510582 ) ) ;
#14646=CARTESIAN_POINT ( 'NONE',  ( -6.016104459813374383, 4.882138007283004733, -18.19977249352305648 ) ) ;
#14667=ADVANCED_FACE ( 'NONE', ( #26649 ), #33971, .F. ) ;
#14668=B_SPLINE_CURVE_WITH_KNOTS ( 'NONE', 3,
 ( #30270, #20577, #40634, #21189, #49687, #6743 ),
 .UNSPECIFIED., .F., .F.,
 ( 4, 2, 4 ),
 ( 1.426045310262811165E-18, 0.0002450742804987334714, 0.0004901485609974655334 ),
 .UNSPECIFIED. ) ;
#14673=ORIENTED_EDGE ( 'NONE', *, *, #60171, .F. ) ;
#14676=CARTESIAN_POINT ( 'NONE',  ( -6.016104459813371719, 7.206059014950318087, -17.41090761020828737 ) ) ;
#14677=AXIS2_PLACEMENT_3D ( 'NONE', #3759, #61387, #13822 ) ;
#14678=ORIENTED_EDGE ( 'NONE', *, *, #48749, .T. ) ;
#14683=EDGE_CURVE ( 'NONE', #12273, #60753, #28971, .T. ) ;
#14685=ORIENTED_EDGE ( 'NONE', *, *, #11252, .F. ) ;
#14692=CARTESIAN_POINT ( 'NONE',  ( 0.6009452777970410997, -33.70725232128916815, 34.32439724342980014 ) ) ;
#14700=CIRCLE ( 'NONE', #39755, 47.91270532121795611 ) ;
#14702=CARTESIAN_POINT ( 'NONE',  ( 0.8751705887134553219, 41.19904111682508585, -24.81530984069164703 ) ) ;
#14706=DIRECTION ( 'NONE',  ( -0.1024043820194934368, -0.2447326578667193553, -0.9641676559171111771 ) ) ;
#14711=DIRECTION ( 'NONE',  ( 0.000000000000000000, 0.000000000000000000, 1.000000000000000000 ) ) ;
#14715=VERTEX_POINT ( 'NONE', #61074 ) ;
#14716=CARTESIAN_POINT ( 'NONE',  ( 4.975801465491694664, -42.71626295676247764, -21.70134120755185947 ) ) ;
#14721=VECTOR ( 'NONE', #11667, 1000.000000000000114 ) ;
#14732=DIRECTION ( 'NONE',  ( 0.000000000000000000, 0.000000000000000000, 1.000000000000000000 ) ) ;
#14733=VERTEX_POINT ( 'NONE', #4048 ) ;
#14737=VECTOR ( 'NONE', #51040, 1000.000000000000000 ) ;
#14747=CARTESIAN_POINT ( 'NONE',  ( 0.8751705887134553219, 33.37254303619554463, -34.63284514348550402 ) ) ;
#14748=EDGE_LOOP ( 'NONE', ( #3118, #11131, #40274, #41796 ) ) ;
#14750=CARTESIAN_POINT ( 'NONE',  ( 0.2885700199627508344, 40.13549263616302909, 15.75356883787167739 ) ) ;
#14755=ORIENTED_EDGE ( 'NONE', *, *, #23632, .T. ) ;
#14766=CARTESIAN_POINT ( 'NONE',  ( 0.6001305935487422083, -23.60027211631801691, -41.92422178329160687 ) ) ;
#14770=ORIENTED_EDGE ( 'NONE', *, *, #49804, .T. ) ;
#14776=CARTESIAN_POINT ( 'NONE',  ( 0.6041374136657476912, 47.71861871402581556, 6.106202762793639494 ) ) ;
#14782=CARTESIAN_POINT ( 'NONE',  ( -6.001507490154110336, 7.196845540359404048, -17.41542759839256860 ) ) ;
#14787=CARTESIAN_POINT ( 'NONE',  ( 0.5980894510889457338, 41.31170365136888023, -24.66136644716778292 ) ) ;
#14791=DIRECTION ( 'NONE',  ( 1.000000000000000000, 0.000000000000000000, 0.000000000000000000 ) ) ;
#14795=LINE ( 'NONE', #58283, #37682 ) ;
#14797=B_SPLINE_CURVE_WITH_KNOTS ( 'NONE', 3,
 ( #28589, #22989, #51778, #8876, #19219, #38330 ),
 .UNSPECIFIED., .F., .F.,
 ( 4, 2, 4 ),
 ( 8.609910155989501895E-17, 0.0002293366620881446324, 0.0004586733241762031791 ),
 .UNSPECIFIED. ) ;
#14802=ORIENTED_EDGE ( 'NONE', *, *, #20954, .T. ) ;
#14803=VECTOR ( 'NONE', #56814, 1000.000000000000114 ) ;
#14811=EDGE_LOOP ( 'NONE', ( #9181, #11047, #42779, #25006 ) ) ;
#14817=ORIENTED_EDGE ( 'NONE', *, *, #10779, .F. ) ;
#14825=LINE ( 'NONE', #42419, #60560 ) ;
#14830=COLOUR_RGB ( '', 0.31764706, 0.68627451, 0.89019608) ;
#14832=CARTESIAN_POINT ( 'NONE',  ( -6.016104459813371719, 11.46679299034602018, -14.95258000663120157 ) ) ;
#14834=CARTESIAN_POINT ( 'NONE',  ( 4.322998006666165516, -45.10383234877044600, 16.38761975793128656 ) ) ;
#14837=CARTESIAN_POINT ( 'NONE',  ( 0.1073791018717578927, 5.147744207006301309, 42.81622261970996135 ) ) ;
#14841=CARTESIAN_POINT ( 'NONE',  ( 0.1073791018717483448, 40.02496097243036388, 16.05399293000829175 ) ) ;
#14842=B_SPLINE_CURVE_WITH_KNOTS ( 'NONE', 3,
 ( #59786, #16571, #59462, #40401, #50086, #31910, #31592, #54761, #31284, #35698, #3071, #46031, #45403, #16896, #36315, #50680, #26579, #45710, #2452 ),
 .UNSPECIFIED., .F., .F.,
 ( 4, 3, 3, 3, 3, 3, 4 ),
 ( 1.161276725443423652E-16, 0.0002618519381806260252, 0.0003927759815485984689, 0.0005237000248299447311, 0.0006546240681325002104, 0.0007855481115631340102, 0.0009699050456655109419 ),
 .UNSPECIFIED. ) ;
#14844=ORIENTED_EDGE ( 'NONE', *, *, #55667, .T. ) ;
#14847=CARTESIAN_POINT ( 'NONE',  ( 0.6001305935487315502, -46.60388846085731984, 11.94532529598297010 ) ) ;
#14850=VECTOR ( 'NONE', #29032, 1000.000000000000000 ) ;
#14854=FACE_OUTER_BOUND ( 'NONE', #2775, .T. ) ;
#14856=CARTESIAN_POINT ( 'NONE',  ( 0.1084644655670282953, -39.68806829486960197, 16.86976209534710236 ) ) ;
#14860=CARTESIAN_POINT ( 'NONE',  ( 5.880360259849752858, 3.184717612777935525, -47.86623372148046229 ) ) ;
#14861=CARTESIAN_POINT ( 'NONE',  ( 0.1313383488274153799, -17.09007684155478302, -39.59253935480791853 ) ) ;
#14864=FACE_OUTER_BOUND ( 'NONE', #10818, .T. ) ;
#14870=VECTOR ( 'NONE', #28482, 1000.000000000000114 ) ;
#14871=EDGE_CURVE ( 'NONE', #5563, #25568, #910, .T. ) ;
#14888=DIRECTION ( 'NONE',  ( 0.000000000000000000, 0.000000000000000000, 1.000000000000000000 ) ) ;
#14889=ORIENTED_EDGE ( 'NONE', *, *, #48583, .T. ) ;
#14890=VERTEX_POINT ( 'NONE', #15342 ) ;
#14894=VERTEX_POINT ( 'NONE', #10636 ) ;
#14900=ORIENTED_EDGE ( 'NONE', *, *, #32630, .T. ) ;
#14908=EDGE_CURVE ( 'NONE', #31680, #53617, #48839, .T. ) ;
#14914=FACE_OUTER_BOUND ( 'NONE', #28385, .T. ) ;
#14920=CARTESIAN_POINT ( 'NONE',  ( -6.016489644550736315, 9.425415887801086967, 16.31649074174280045 ) ) ;
#14927=CARTESIAN_POINT ( 'NONE',  ( 0.1081432562775997419, -37.13343246403911024, -21.92800090985256745 ) ) ;
#14930=CARTESIAN_POINT ( 'NONE',  ( -6.017396004339686577, 13.32329839588573606, -13.32495836419610669 ) ) ;
#14932=CARTESIAN_POINT ( 'NONE',  ( -6.010958268070873523, 9.434296419346207330, 16.31164801516945317 ) ) ;
#14935=CARTESIAN_POINT ( 'NONE',  ( 4.549368137175248350, -24.02461520945298545, 35.57418903283073064 ) ) ;
#14936=CARTESIAN_POINT ( 'NONE',  ( 0.5998501479064708430, -47.76154736470761719, 5.759754759339972274 ) ) ;
#14939=CARTESIAN_POINT ( 'NONE',  ( -6.017396004339687465, -7.212050743684302212, 17.40836349643165093 ) ) ;
#14943=CARTESIAN_POINT ( 'NONE',  ( 0.6031356219577718170, 29.21669799774962684, -38.21934428970583753 ) ) ;
#14960=CARTESIAN_POINT ( 'NONE',  ( 0.1313383488274159905, -41.81465294768286611, -10.54394128763545346 ) ) ;
#14962=CARTESIAN_POINT ( 'NONE',  ( 0.2224561200757608770, -25.64288022150858737, -34.66601556960344510 ) ) ;
#14963=CARTESIAN_POINT ( 'NONE',  ( 0.1073791018717483448, 11.62916352156094035, 41.52698815987171344 ) ) ;
#14971=CARTESIAN_POINT ( 'NONE',  ( -6.015611763856276717, 18.68122482568283260, -2.465697960550860657 ) ) ;
#14973=ORIENTED_EDGE ( 'NONE', *, *, #59241, .T. ) ;
#14976=CARTESIAN_POINT ( 'NONE',  ( 0.1064266379913941379, -10.61815631313391073, 41.79703901861799409 ) ) ;
#14981=EDGE_LOOP ( 'NONE', ( #22592, #9654, #2986, #56702 ) ) ;
#14988=CARTESIAN_POINT ( 'NONE',  ( 0.6031356755773454870, 34.01711753073210787, 34.01708126935054111 ) ) ;
#14995=DIRECTION ( 'NONE',  ( 0.000000000000000000, 0.000000000000000000, 1.000000000000000000 ) ) ;
#15006=CARTESIAN_POINT ( 'NONE',  ( 4.322998006666179727, -45.10383234877022574, -16.38761975793193315 ) ) ;
#15015=CARTESIAN_POINT ( 'NONE',  ( 2.301529144917014769, -13.67115311794032451, -46.04684498357975997 ) ) ;
#15022=EDGE_CURVE ( 'NONE', #40637, #6465, #40099, .T. ) ;
#15023=CARTESIAN_POINT ( 'NONE',  ( 0.3622758884714600280, -42.62881903538205108, -6.444611261694439541 ) ) ;
#15027=CARTESIAN_POINT ( 'NONE',  ( 3.238931869106853600, -42.34694073502594591, 7.419701784410414724 ) ) ;
#15028=CARTESIAN_POINT ( 'NONE',  ( 0.5980894510889448457, -6.974827154144452201, 47.60453381548680341 ) ) ;
#15033=LINE ( 'NONE', #1510, #190 ) ;
#15037=B_SPLINE_CURVE_WITH_KNOTS ( 'NONE', 3,
 ( #7074, #45341, #2693, #31217, #45641, #40646 ),
 .UNSPECIFIED., .F., .F.,
 ( 4, 2, 4 ),
 ( 1.267283937151336631E-16, 0.0002450741128632354321, 0.0004901482257263441210 ),
 .UNSPECIFIED. ) ;
#15042=VECTOR ( 'NONE', #45241, 1000.000000000000227 ) ;
#15051=CARTESIAN_POINT ( 'NONE',  ( 0.3622758884714730732, -31.06363466427707820, -29.89648521331620756 ) ) ;
#15054=VERTEX_POINT ( 'NONE', #41026 ) ;
#15060=CARTESIAN_POINT ( 'NONE',  ( 0.8751705887134553219, 41.19904111682508585, -24.81530984069164703 ) ) ;
#15065=CARTESIAN_POINT ( 'NONE',  ( 0.3622758884714730732, 33.69533458712344753, -26.89560658783350178 ) ) ;
#15068=DIRECTION ( 'NONE',  ( -1.000000000000000000, -0.000000000000000000, -0.000000000000000000 ) ) ;
#15070=B_SPLINE_CURVE_WITH_KNOTS ( 'NONE', 3,
 ( #3209, #13258, #32361, #47085 ),
 .UNSPECIFIED., .F., .F.,
 ( 4, 4 ),
 ( 1.998817200139820460E-17, 0.004444306975806115029 ),
 .UNSPECIFIED. ) ;
#15072=CARTESIAN_POINT ( 'NONE',  ( 4.691466044806102076, 36.88741755356034702, 25.04870410140802406 ) ) ;
#15076=VERTEX_POINT ( 'NONE', #40710 ) ;
#15078=B_SPLINE_CURVE_WITH_KNOTS ( 'NONE', 3,
 ( #7145, #49158, #35707, #12206 ),
 .UNSPECIFIED., .F., .F.,
 ( 4, 4 ),
 ( 0.000000000000000000, 0.005014147105413698652 ),
 .UNSPECIFIED. ) ;
#15082=ORIENTED_EDGE ( 'NONE', *, *, #33975, .T. ) ;
#15091=EDGE_CURVE ( 'NONE', #56469, #58608, #19221, .T. ) ;
#15094=CARTESIAN_POINT ( 'NONE',  ( 0.5980894510889448457, 0.7015180096004866028, -48.10766805928368939 ) ) ;
#15096=CARTESIAN_POINT ( 'NONE',  ( -6.015611763856276717, 14.94556629257425584, 11.47596948473816170 ) ) ;
#15098=CARTESIAN_POINT ( 'NONE',  ( 0.8751705887134553219, -46.67919521768879321, -11.58504748649183647 ) ) ;
#15103=CARTESIAN_POINT ( 'NONE',  ( 0.6001305935487422083, 44.24520387813801392, 18.89378601236078481 ) ) ;
#15105=( BOUNDED_SURFACE ( )  B_SPLINE_SURFACE ( 3, 1, ( 
 ( #24940, #1714 ),
 ( #1105, #29936 ),
 ( #49042, #38434 ),
 ( #57483, #14625 ) ),
 .UNSPECIFIED., .F., .F., .F. ) 
 B_SPLINE_SURFACE_WITH_KNOTS ( ( 4, 4 ),
 ( 2, 2 ),
 ( 0.000000000000000000, 1.000000000000000000 ),
 ( 0.000000000000000000, 1.000000000000000000 ),
 .UNSPECIFIED. ) 
 GEOMETRIC_REPRESENTATION_ITEM ( )  RATIONAL_B_SPLINE_SURFACE ( (
 ( 1.000000000000000000, 1.000000000000000000),
 ( 0.7223157951917480446, 0.9931996967497186413),
 ( 0.7223157951917480446, 0.9931996967497186413),
 ( 1.000000000000000000, 1.000000000000000000) ) ) 
 REPRESENTATION_ITEM ( '' )  SURFACE ( )  );
#15108=ORIENTED_EDGE ( 'NONE', *, *, #54004, .F. ) ;
#15111=CARTESIAN_POINT ( 'NONE',  ( 0.5998501479064708430, 28.86886762351073088, 38.48283596222038483 ) ) ;
#15113=CARTESIAN_POINT ( 'NONE',  ( -2.569797478183790229, -2.353985772484857630, 14.44232325624822622 ) ) ;
#15118=CARTESIAN_POINT ( 'NONE',  ( 0.3622758884714600280, -40.13994584881793770, 15.73321244754782811 ) ) ;
#15119=CARTESIAN_POINT ( 'NONE',  ( -6.010958268070873523, 4.863021950010647743, 18.20513189769810225 ) ) ;
#15121=CARTESIAN_POINT ( 'NONE',  ( 0.7048096507298579061, 24.78213711671599029, -41.23648859290900504 ) ) ;
#15122=B_SPLINE_CURVE_WITH_KNOTS ( 'NONE', 3,
 ( #15786, #48982, #10778, #6641, #26096, #44612, #34899, #49906, #34584, #59289, #39924, #1965, #54264, #58347, #1649, #40532 ),
 .UNSPECIFIED., .F., .F.,
 ( 4, 3, 3, 3, 3, 4 ),
 ( 2.081781105835003155E-17, 0.0002618515315864400794, 0.0003927756766341976660, 0.0005236998216950558300, 0.0007855159896329891398, 0.001047349442285927437 ),
 .UNSPECIFIED. ) ;
#15123=ORIENTED_EDGE ( 'NONE', *, *, #57961, .T. ) ;
#15127=CARTESIAN_POINT ( 'NONE',  ( 0.6001305935487422083, 34.38748867424667566, 33.64689939321953460 ) ) ;
#15130=EDGE_CURVE ( 'NONE', #37162, #34651, #47613, .T. ) ;
#15139=CARTESIAN_POINT ( 'NONE',  ( 4.322998006666179727, 45.10383234877009784, 16.38761975793224934 ) ) ;
#15161=CARTESIAN_POINT ( 'NONE',  ( 3.238741278300273141, -38.11287256318076544, 19.89284324544627935 ) ) ;
#15165=CARTESIAN_POINT ( 'NONE',  ( -6.015611763856276717, -2.465697960551179513, 18.68122482568278997 ) ) ;
#15170=CARTESIAN_POINT ( 'NONE',  ( 0.1095718737110178143, 30.67477146794372800, -30.31138510522961838 ) ) ;
#15182=CARTESIAN_POINT ( 'NONE',  ( 3.238741278300275805, 9.350673766180220170, 41.96285461600083977 ) ) ;
#15185=CARTESIAN_POINT ( 'NONE',  ( 0.7048096507298579061, -13.26491767067547478, 46.24547838151344337 ) ) ;
#15187=CARTESIAN_POINT ( 'NONE',  ( 0.8751705887134553219, -7.160166390003972481, -47.55935879196468363 ) ) ;
#15192=CARTESIAN_POINT ( 'NONE',  ( 3.238741278300274029, 14.74792908357247256, 40.38334873621888477 ) ) ;
#15195=CARTESIAN_POINT ( 'NONE',  ( -6.016489644550737204, 17.40716454747929731, 7.215050741358106201 ) ) ;
#15196=ORIENTED_EDGE ( 'NONE', *, *, #3513, .F. ) ;
#15198=B_SPLINE_CURVE_WITH_KNOTS ( 'NONE', 3,
 ( #5087, #58019, #709, #48338 ),
 .UNSPECIFIED., .F., .F.,
 ( 4, 4 ),
 ( 0.000000000000000000, 0.005014147105413699519 ),
 .UNSPECIFIED. ) ;
#15199=CARTESIAN_POINT ( 'NONE',  ( 4.549368137175248350, 42.06008734272396765, -8.582197505783977221 ) ) ;
#15208=CARTESIAN_POINT ( 'NONE',  ( -6.015611763856276717, -7.205255340944484388, -17.41126425312545223 ) ) ;
#15217=FACE_OUTER_BOUND ( 'NONE', #50120, .T. ) ;
#15219=DIRECTION ( 'NONE',  ( 0.1024043820194936449, -0.7971196296869297315, -0.5950744814819213246 ) ) ;
#15220=CARTESIAN_POINT ( 'NONE',  ( 4.549368137175248350, 32.41327393324100825, 28.14399996863509301 ) ) ;
#15221=ORIENTED_EDGE ( 'NONE', *, *, #58457, .T. ) ;
#15230=CARTESIAN_POINT ( 'NONE',  ( 0.8760168074886960365, -23.27577685234568960, -42.09738177923946267 ) ) ;
#15232=EDGE_CURVE ( 'NONE', #52654, #18536, #12443, .T. ) ;
#15233=ORIENTED_EDGE ( 'NONE', *, *, #20841, .F. ) ;
#15236=CARTESIAN_POINT ( 'NONE',  ( -6.016761891674564211, 16.31696541414285306, -9.424569481870079812 ) ) ;
#15238=EDGE_CURVE ( 'NONE', #52918, #60249, #42862, .T. ) ;
#15239=CARTESIAN_POINT ( 'NONE',  ( -6.016761891674565099, -7.214149619366484245, 17.40752468084780702 ) ) ;
#15242=CARTESIAN_POINT ( 'NONE',  ( 0.6029303876144825880, 29.38970229176903359, -38.08638053211507923 ) ) ;
#15245=ORIENTED_EDGE ( 'NONE', *, *, #47041, .F. ) ;
#15249=ORIENTED_EDGE ( 'NONE', *, *, #33975, .F. ) ;
#15258=CARTESIAN_POINT ( 'NONE',  ( 0.6030672727741701600, 38.21927534816984462, -29.21669544497209969 ) ) ;
#15269=CARTESIAN_POINT ( 'NONE',  ( 0.1100053167205930355, 16.66867746965590413, 39.77279469894219943 ) ) ;
#15281=EDGE_CURVE ( 'NONE', #19329, #30492, #52024, .T. ) ;
#15290=CARTESIAN_POINT ( 'NONE',  ( 0.5980894510889448457, -19.05812566676535269, 44.17723055703920210 ) ) ;
#15294=CARTESIAN_POINT ( 'NONE',  ( 0.8751705887134553219, -28.56654290188682666, 38.69254731947783199 ) ) ;
#15299=CARTESIAN_POINT ( 'NONE',  ( 4.549368137175248350, 8.166781970325731166, -42.14271863032826104 ) ) ;
#15305=EDGE_CURVE ( 'NONE', #21442, #25607, #14668, .T. ) ;
#15314=FACE_OUTER_BOUND ( 'NONE', #40307, .T. ) ;
#15316=CARTESIAN_POINT ( 'NONE',  ( 3.680882792899936362, -36.90742604464144705, 30.65151321162936782 ) ) ;
#15321=CARTESIAN_POINT ( 'NONE',  ( 0.1104177457020372732, 30.49705356371264031, 30.49013195371466267 ) ) ;
#15322=CIRCLE ( 'NONE', #35308, 47.91270532121795611 ) ;
#15324=CARTESIAN_POINT ( 'NONE',  ( 0.6041374136657475802, -38.27243465845360504, 29.14743607025020466 ) ) ;
#15342=CARTESIAN_POINT ( 'NONE',  ( 4.975801465491694664, 42.71626295676232843, 21.70134120755216145 ) ) ;
#15358=ORIENTED_EDGE ( 'NONE', *, *, #51649, .F. ) ;
#15365=VERTEX_POINT ( 'NONE', #8012 ) ;
#15366=CARTESIAN_POINT ( 'NONE',  ( -5.995132425357893702, 17.41298668506980718, -7.203480333238889699 ) ) ;
#15370=CARTESIAN_POINT ( 'NONE',  ( 0.6254311100348657337, -28.73641524052546004, -38.58047947916320197 ) ) ;
#15377=( BOUNDED_SURFACE ( )  B_SPLINE_SURFACE ( 3, 1, ( 
 ( #13920, #38340 ),
 ( #5394, #23298 ),
 ( #14832, #33023 ),
 ( #18603, #43660 ) ),
 .UNSPECIFIED., .F., .F., .F. ) 
 B_SPLINE_SURFACE_WITH_KNOTS ( ( 4, 4 ),
 ( 2, 2 ),
 ( 0.000000000000000000, 1.000000000000000000 ),
 ( 0.000000000000000000, 1.000000000000000000 ),
 .UNSPECIFIED. ) 
 GEOMETRIC_REPRESENTATION_ITEM ( )  RATIONAL_B_SPLINE_SURFACE ( (
 ( 1.000000000000000000, 1.000000000000000000),
 ( 0.9953040768229013402, 0.8617119497784988535),
 ( 0.9953040768229013402, 0.8617119497784988535),
 ( 1.000000000000000000, 1.000000000000000000) ) ) 
 REPRESENTATION_ITEM ( '' )  SURFACE ( )  );
#15378=EDGE_LOOP ( 'NONE', ( #13229, #18664, #55240, #57871 ) ) ;
#15388=ORIENTED_EDGE ( 'NONE', *, *, #1330, .T. ) ;
#15390=CARTESIAN_POINT ( 'NONE',  ( 4.975801465491695552, 0.000000000000000000, 0.000000000000000000 ) ) ;
#15392=CARTESIAN_POINT ( 'NONE',  ( -6.010958268070873523, 13.33459572764757617, 13.31406649671967379 ) ) ;
#15400=CARTESIAN_POINT ( 'NONE',  ( 0.6025881611877910160, 18.61132239451786319, -44.36157157392734973 ) ) ;
#15403=CARTESIAN_POINT ( 'NONE',  ( 0.8760168074886965917, 0.8912768426706281222, -48.09529047980637273 ) ) ;
#15421=PRODUCT_DEFINITION_CONTEXT ( 'detailed design', #18800, 'design' ) ;
#15434=CARTESIAN_POINT ( 'NONE',  ( 0.3622758884714600280, 43.10531414739104150, 0.8252992914329575491 ) ) ;
#15439=CARTESIAN_POINT ( 'NONE',  ( 0.1103936448916675722, 0.03072591687002976246, 43.12443171339901937 ) ) ;
#15450=CARTESIAN_POINT ( 'NONE',  ( 4.549368137175248350, -3.018832571116875751, 42.82045902618767030 ) ) ;
#15452=CARTESIAN_POINT ( 'NONE',  ( 0.3622758884714730732, -31.06363466427707820, -29.89648521331620756 ) ) ;
#15455=CARTESIAN_POINT ( 'NONE',  ( 0.1073791018717578927, 42.68962945260945929, 6.109314776652849943 ) ) ;
#15458=ORIENTED_EDGE ( 'NONE', *, *, #30827, .T. ) ;
#15463=B_SPLINE_CURVE_WITH_KNOTS ( 'NONE', 3,
 ( #53187, #53485, #31548, #30934, #45989, #55031 ),
 .UNSPECIFIED., .F., .F.,
 ( 4, 2, 4 ),
 ( 1.870559545977334001E-17, 0.0002293319059085097372, 0.0004586638118170007720 ),
 .UNSPECIFIED. ) ;
#15465=CARTESIAN_POINT ( 'NONE',  ( 0.1100053167205930771, 34.10339839758286473, -26.39466280306232449 ) ) ;
#15471=CARTESIAN_POINT ( 'NONE',  ( 4.549368137175248350, -40.71620287708334018, -13.59764261105737404 ) ) ;
#15475=ORIENTED_EDGE ( 'NONE', *, *, #41972, .F. ) ;
#15482=CARTESIAN_POINT ( 'NONE',  ( -6.001507490154111224, 7.225628667346816414, -17.40350523682687722 ) ) ;
#15487=( BOUNDED_SURFACE ( )  B_SPLINE_SURFACE ( 3, 1, ( 
 ( #127, #4209 ),
 ( #18658, #48084 ),
 ( #4517, #42782 ),
 ( #24266, #23966 ) ),
 .UNSPECIFIED., .F., .F., .F. ) 
 B_SPLINE_SURFACE_WITH_KNOTS ( ( 4, 4 ),
 ( 2, 2 ),
 ( 0.000000000000000000, 1.000000000000000000 ),
 ( 0.000000000000000000, 1.000000000000000000 ),
 .UNSPECIFIED. ) 
 GEOMETRIC_REPRESENTATION_ITEM ( )  RATIONAL_B_SPLINE_SURFACE ( (
 ( 1.000000000000000000, 1.000000000000000000),
 ( 0.7223157951917476005, 0.9931996967497186413),
 ( 0.7223157951917476005, 0.9931996967497186413),
 ( 1.000000000000000000, 1.000000000000000000) ) ) 
 REPRESENTATION_ITEM ( '' )  SURFACE ( )  );
#15489=CARTESIAN_POINT ( 'NONE',  ( -6.015611763856276717, 4.870987357968431297, -18.20278301740931681 ) ) ;
#15494=CARTESIAN_POINT ( 'NONE',  ( 0.1073791018717578927, -43.12183934961191056, -0.4849339620931655825 ) ) ;
#15499=CARTESIAN_POINT ( 'NONE',  ( 0.1092355843206037486, -11.45151637801156497, 41.57624119012368880 ) ) ;
#15501=CARTESIAN_POINT ( 'NONE',  ( 4.549368137175248350, 0.000000000000000000, 0.000000000000000000 ) ) ;
#15502=ORIENTED_EDGE ( 'NONE', *, *, #33601, .T. ) ;
#15504=VERTEX_POINT ( 'NONE', #43096 ) ;
#15505=CARTESIAN_POINT ( 'NONE',  ( -6.016761891674564211, -18.20023637398602290, 4.880293656734900232 ) ) ;
#15520=CARTESIAN_POINT ( 'NONE',  ( 2.643462169533613793, 46.02269433264232390, -13.76277278785512692 ) ) ;
#15522=CARTESIAN_POINT ( 'NONE',  ( -2.569797478183783568, -11.87678401312189003, -8.547745408040752224 ) ) ;
#15524=EDGE_CURVE ( 'NONE', #10739, #25025, #51893, .T. ) ;
#15525=CIRCLE ( 'NONE', #50519, 47.91270532121795611 ) ;
#15542=CARTESIAN_POINT ( 'NONE',  ( -6.016761891674564211, -7.207804629151436160, 17.41015286184800459 ) ) ;
#15545=CARTESIAN_POINT ( 'NONE',  ( 0.8760168074887090262, -46.68716261866168082, -11.58706983520309741 ) ) ;
#15553=EDGE_CURVE ( 'NONE', #12288, #44917, #24585, .T. ) ;
#15556=CARTESIAN_POINT ( 'NONE',  ( 50.00005079999999680, 12.80000000000000071, 3.000000000000000000 ) ) ;
#15557=CARTESIAN_POINT ( 'NONE',  ( 4.549368137175248350, 0.000000000000000000, 0.000000000000000000 ) ) ;
#15558=CARTESIAN_POINT ( 'NONE',  ( 0.5980894510889457338, 44.71414919659881093, 17.76188940524963300 ) ) ;
#15559=CARTESIAN_POINT ( 'NONE',  ( 0.6017666602106489515, 37.95277954208636118, -29.56224131406230171 ) ) ;
#15563=CARTESIAN_POINT ( 'NONE',  ( 0.6025881611877910160, -0.2181813582441801125, 48.10699274197334319 ) ) ;
#15565=EDGE_CURVE ( 'NONE', #28832, #60778, #26486, .T. ) ;
#15575=DIRECTION ( 'NONE',  ( 0.1024043820194936449, -0.7126273545981441915, -0.6940285268068283608 ) ) ;
#15577=CARTESIAN_POINT ( 'NONE',  ( 0.5998501479064699549, 11.94461217097469685, -46.60114184914306179 ) ) ;
#15578=B_SPLINE_CURVE_WITH_KNOTS ( 'NONE', 3,
 ( #15577, #10563, #44113, #43801, #34377, #53451 ),
 .UNSPECIFIED., .F., .F.,
 ( 4, 2, 4 ),
 ( 1.764953265579307567E-18, 0.0002450742804987340135, 0.0004901485609974661839 ),
 .UNSPECIFIED. ) ;
#15581=CARTESIAN_POINT ( 'NONE',  ( 0.2224561200757615154, -4.874377913226201287, -42.84309024201774463 ) ) ;
#15583=CARTESIAN_POINT ( 'NONE',  ( 2.643462169533613793, -28.13401304854749085, 38.93558293168490536 ) ) ;
#15587=CARTESIAN_POINT ( 'NONE',  ( 0.1313383488274115496, 37.02311703718855540, -22.11173226734854325 ) ) ;
#15605=EDGE_LOOP ( 'NONE', ( #28972, #43608, #56693, #38857, #24437, #7820 ) ) ;
#15607=CARTESIAN_POINT ( 'NONE',  ( 0.6031356755825967308, -1.709377936827843777E-05, -48.10744332413644031 ) ) ;
#15620=CARTESIAN_POINT ( 'NONE',  ( 4.549368137175248350, 0.000000000000000000, 0.000000000000000000 ) ) ;
#15623=B_SPLINE_CURVE_WITH_KNOTS ( 'NONE', 3,
 ( #58813, #2421, #1802, #51892, #8986, #13706, #51572, #60351, #28096, #55657, #26863, #36907, #3956, #41296, #50965, #23398, #27787, #56278, #8664 ),
 .UNSPECIFIED., .F., .F.,
 ( 4, 3, 3, 3, 3, 3, 4 ),
 ( 1.165802754517233128E-16, 0.0002618519381806228810, 0.0003927759815485970052, 0.0005237000248299436469, 0.0006546240681324961988, 0.0007855481115631307576, 0.0009699050456655114840 ),
 .UNSPECIFIED. ) ;
#15628=CARTESIAN_POINT ( 'NONE',  ( -2.569797478183790229, 5.182550149005106022, 13.68441171582018079 ) ) ;
#15630=CARTESIAN_POINT ( 'NONE',  ( -6.015611763856276717, -2.465697960550925938, -18.68122482568282550 ) ) ;
#15633=CARTESIAN_POINT ( 'NONE',  ( 0.8751705887134423323, 46.67919521768887847, -11.58504748649151317 ) ) ;
#15638=CARTESIAN_POINT ( 'NONE',  ( 4.549368137175248350, -13.59764261105721950, -40.71620287708339703 ) ) ;
#15639=CARTESIAN_POINT ( 'NONE',  ( 0.8751705887134423323, -5.393078191592370452, -47.79200036674278351 ) ) ;
#15640=CARTESIAN_POINT ( 'NONE',  ( 0.8751705887134423323, -37.60752970653809513, -29.98056538504947710 ) ) ;
#15645=CARTESIAN_POINT ( 'NONE',  ( -6.016761891674564211, -17.40752468084787452, 7.214149619366299504 ) ) ;
#15648=EDGE_CURVE ( 'NONE', #30211, #5781, #37724, .T. ) ;
#15651=CARTESIAN_POINT ( 'NONE',  ( 4.549368137175248350, 0.000000000000000000, 0.000000000000000000 ) ) ;
#15652=DIRECTION ( 'NONE',  ( 0.1024043820194936311, 0.9573600124648758980, -0.2701391291102754333 ) ) ;
#15655=ADVANCED_FACE ( 'NONE', ( #26120 ), #35996, .F. ) ;
#15658=EDGE_CURVE ( 'NONE', #26755, #22273, #28055, .T. ) ;
#15659=CARTESIAN_POINT ( 'NONE',  ( -2.708315649062910779, -14.20182604343562360, 3.532515819624108655 ) ) ;
#15663=CARTESIAN_POINT ( 'NONE',  ( 4.975801465491695552, 0.000000000000000000, 0.000000000000000000 ) ) ;
#15668=CARTESIAN_POINT ( 'NONE',  ( 4.833616638992205949, 41.67905425467705527, -20.04871863793763964 ) ) ;
#15671=CARTESIAN_POINT ( 'NONE',  ( 0.7048096507298635682, 47.80151517212779311, 5.442192462019629140 ) ) ;
#15673=ORIENTED_EDGE ( 'NONE', *, *, #7431, .F. ) ;
#15680=CARTESIAN_POINT ( 'NONE',  ( 4.549368137175248350, 28.14399996863453168, 32.41327393324149853 ) ) ;
#15687=ADVANCED_FACE ( 'NONE', ( #40257 ), #12379, .F. ) ;
#15692=CARTESIAN_POINT ( 'NONE',  ( 0.6017667736363750963, 44.31084570541175083, 18.73201910948677096 ) ) ;
#15693=ORIENTED_EDGE ( 'NONE', *, *, #45962, .F. ) ;
#15706=VECTOR ( 'NONE', #39989, 999.9999999999998863 ) ;
#15710=VECTOR ( 'NONE', #23907, 1000.000000000000000 ) ;
#15716=CARTESIAN_POINT ( 'NONE',  ( 5.880360259849752858, -39.86101557989652378, -26.69116321728556329 ) ) ;
#15724=CARTESIAN_POINT ( 'NONE',  ( 0.6254087463353920073, 47.60024110474252979, -6.960754339421318271 ) ) ;
#15731=CARTESIAN_POINT ( 'NONE',  ( -2.708315649062916552, -7.087851317224052039, 12.80362818457433427 ) ) ;
#15737=VERTEX_POINT ( 'NONE', #42325 ) ;
#15740=( BOUNDED_SURFACE ( )  B_SPLINE_SURFACE ( 3, 1, ( 
 ( #38185, #28757 ),
 ( #33163, #15290 ),
 ( #14676, #34396 ),
 ( #24063, #42884 ) ),
 .UNSPECIFIED., .F., .F., .F. ) 
 B_SPLINE_SURFACE_WITH_KNOTS ( ( 4, 4 ),
 ( 2, 2 ),
 ( 0.000000000000000000, 1.000000000000000000 ),
 ( 0.000000000000000000, 1.000000000000000000 ),
 .UNSPECIFIED. ) 
 GEOMETRIC_REPRESENTATION_ITEM ( )  RATIONAL_B_SPLINE_SURFACE ( (
 ( 1.000000000000000000, 1.000000000000000000),
 ( 0.9953040768229013402, 0.8617119497784988535),
 ( 0.9953040768229013402, 0.8617119497784988535),
 ( 1.000000000000000000, 1.000000000000000000) ) ) 
 REPRESENTATION_ITEM ( '' )  SURFACE ( )  );
#15745=ORIENTED_EDGE ( 'NONE', *, *, #37223, .F. ) ;
#15752=DIRECTION ( 'NONE',  ( -0.1024043820194934368, -0.1167898032637205152, -0.9878630899050874214 ) ) ;
#15764=CARTESIAN_POINT ( 'NONE',  ( 0.1104177457020373426, 41.65628910360723580, 11.15670205480019028 ) ) ;
#15773=ORIENTED_EDGE ( 'NONE', *, *, #17196, .F. ) ;
#15776=CARTESIAN_POINT ( 'NONE',  ( 0.6001305935487315502, -18.89378601236034427, -44.24520387813821287 ) ) ;
#15779=CARTESIAN_POINT ( 'NONE',  ( 0.8760168074887090262, 5.394043284319505638, -47.80016357497244428 ) ) ;
#15780=EDGE_CURVE ( 'NONE', #40551, #54789, #49675, .T. ) ;
#15786=CARTESIAN_POINT ( 'NONE',  ( 0.5998501479064708430, -6.798102206414489146, 47.62484632993676570 ) ) ;
#15792=CARTESIAN_POINT ( 'NONE',  ( -6.015611763856276717, -14.95313250337422062, -11.46610900684738432 ) ) ;
#15811=CARTESIAN_POINT ( 'NONE',  ( -6.015611763856276717, 11.47596948473832690, -14.94556629257413327 ) ) ;
#15814=ORIENTED_EDGE ( 'NONE', *, *, #23451, .F. ) ;
#15818=CARTESIAN_POINT ( 'NONE',  ( 0.8760168074887090262, 13.30888447662015928, 46.22580377597790147 ) ) ;
#15820=CARTESIAN_POINT ( 'NONE',  ( 0.6254087463353933396, 19.04342133627982747, 44.17672642933511895 ) ) ;
#15824=ORIENTED_EDGE ( 'NONE', *, *, #52464, .F. ) ;
#15827=CARTESIAN_POINT ( 'NONE',  ( -6.015611763856276717, -9.416239407363189429, -16.32183393015606754 ) ) ;
#15828=CIRCLE ( 'NONE', #16871, 47.91270532121795611 ) ;
#15830=ORIENTED_EDGE ( 'NONE', *, *, #44014, .T. ) ;
#15834=CARTESIAN_POINT ( 'NONE',  ( 4.975801465491695552, 36.39623109580423943, 31.15993731089136887 ) ) ;
#15835=ORIENTED_EDGE ( 'NONE', *, *, #20545, .F. ) ;
#15839=( BOUNDED_SURFACE ( )  B_SPLINE_SURFACE ( 3, 1, ( 
 ( #59989, #50584 ),
 ( #22096, #36519 ),
 ( #55585, #12715 ),
 ( #9849, #61519 ) ),
 .UNSPECIFIED., .F., .F., .F. ) 
 B_SPLINE_SURFACE_WITH_KNOTS ( ( 4, 4 ),
 ( 2, 2 ),
 ( 0.000000000000000000, 1.000000000000000000 ),
 ( 0.000000000000000000, 1.000000000000000000 ),
 .UNSPECIFIED. ) 
 GEOMETRIC_REPRESENTATION_ITEM ( )  RATIONAL_B_SPLINE_SURFACE ( (
 ( 1.000000000000000000, 1.000000000000000000),
 ( 0.9751682680413298332, 0.9999560080971552356),
 ( 0.9751682680413298332, 0.9999560080971552356),
 ( 1.000000000000000000, 1.000000000000000000) ) ) 
 REPRESENTATION_ITEM ( '' )  SURFACE ( )  );
#15849=FACE_OUTER_BOUND ( 'NONE', #47574, .T. ) ;
#15850=CARTESIAN_POINT ( 'NONE',  ( -6.016104459813371719, 16.31603998697582725, -9.426230926598471171 ) ) ;
#15852=CARTESIAN_POINT ( 'NONE',  ( 5.880360259849752858, -47.87242051977163726, 3.090325311464702462 ) ) ;
#15855=CARTESIAN_POINT ( 'NONE',  ( 0.8751705887134553219, 44.76769609654211735, 17.57879340691559378 ) ) ;
#15864=ADVANCED_FACE ( 'NONE', ( #19133 ), #50767, .F. ) ;
#15870=CARTESIAN_POINT ( 'NONE',  ( 0.5998501479064699549, 37.84527566984857572, -29.69975237324574024 ) ) ;
#15874=CARTESIAN_POINT ( 'NONE',  ( 0.6023143664670691511, -0.2618215695310947000, 48.10676742339276046 ) ) ;
#15876=CARTESIAN_POINT ( 'NONE',  ( 0.6254087463353912302, -29.82831063981306485, -37.74264085326048956 ) ) ;
#15878=ORIENTED_EDGE ( 'NONE', *, *, #32413, .F. ) ;
#15881=AXIS2_PLACEMENT_3D ( 'NONE', #9502, #56492, #3555 ) ;
#15884=EDGE_CURVE ( 'NONE', #19530, #25568, #32498, .T. ) ;
#15890=VERTEX_POINT ( 'NONE', #24735 ) ;
#15892=AXIS2_PLACEMENT_3D ( 'NONE', #38923, #50449, #2823 ) ;
#15893=CARTESIAN_POINT ( 'NONE',  ( 0.1103310638050661596, -11.08182869403265514, -41.67627416617910541 ) ) ;
#15895=ORIENTED_EDGE ( 'NONE', *, *, #34454, .F. ) ;
#15896=CARTESIAN_POINT ( 'NONE',  ( 0.1103936448916680718, -0.01291577404971127989, 43.12443171339901937 ) ) ;
#15900=VERTEX_POINT ( 'NONE', #5900 ) ;
#15910=EDGE_CURVE ( 'NONE', #55102, #9584, #8621, .T. ) ;
#15911=CARTESIAN_POINT ( 'NONE',  ( -6.017396004339687465, -17.40926186480783855, 7.209881890566491869 ) ) ;
#15918=ORIENTED_EDGE ( 'NONE', *, *, #49210, .F. ) ;
#15926=DIRECTION ( 'NONE',  ( -1.000000000000000000, -0.000000000000000000, -0.000000000000000000 ) ) ;
#15947=CARTESIAN_POINT ( 'NONE',  ( 0.6041374136657475802, -41.74951251761589788, 23.90252055111250584 ) ) ;
#15955=CARTESIAN_POINT ( 'NONE',  ( 0.1313383488274134925, 0.6377633466094576598, 43.11882601516400371 ) ) ;
#15960=CARTESIAN_POINT ( 'NONE',  ( 3.238741278300274029, -18.12697907494920102, 38.98370040185395879 ) ) ;
#15968=CARTESIAN_POINT ( 'NONE',  ( 0.2230388203127608715, -29.94794547692467646, 31.02270543585776608 ) ) ;
#15974=ORIENTED_EDGE ( 'NONE', *, *, #59318, .F. ) ;
#15981=ORIENTED_EDGE ( 'NONE', *, *, #27078, .F. ) ;
#15984=CARTESIAN_POINT ( 'NONE',  ( 0.5998501479064708430, -0.5236536531318284338, 48.10473956285918717 ) ) ;
#15985=CARTESIAN_POINT ( 'NONE',  ( 0.1073791018717483448, 37.10214135362888754, -21.98088480513627729 ) ) ;
#15986=EDGE_CURVE ( 'NONE', #29832, #23990, #16575, .T. ) ;
#15991=CARTESIAN_POINT ( 'NONE',  ( 0.2885700199627521112, 33.71073713194521559, -26.88157179738468017 ) ) ;
#15992=ORIENTED_EDGE ( 'NONE', *, *, #46218, .T. ) ;
#15997=CARTESIAN_POINT ( 'NONE',  ( 0.6009452777970412107, 24.43074291040848323, 41.44251326863938090 ) ) ;
#16003=ORIENTED_EDGE ( 'NONE', *, *, #35961, .T. ) ;
#16015=VECTOR ( 'NONE', #11844, 999.9999999999998863 ) ;
#16026=CARTESIAN_POINT ( 'NONE',  ( 0.7246131072078513258, -42.06185227555128137, 23.33689307364176457 ) ) ;
#16033=LINE ( 'NONE', #1283, #43212 ) ;
#16034=VERTEX_POINT ( 'NONE', #12204 ) ;
#16037=CARTESIAN_POINT ( 'NONE',  ( 0.6254311100348688424, 28.73641524052521490, 38.58047947916339382 ) ) ;
#16041=CARTESIAN_POINT ( 'NONE',  ( 4.549368137175248350, -42.82045902618774136, 3.018832571115817487 ) ) ;
#16047=FACE_OUTER_BOUND ( 'NONE', #30446, .T. ) ;
#16063=CARTESIAN_POINT ( 'NONE',  ( 0.6017666602106489515, -18.08695057064621992, 44.57804174182690815 ) ) ;
#16066=LINE ( 'NONE', #11358, #17265 ) ;
#16081=ORIENTED_EDGE ( 'NONE', *, *, #4331, .F. ) ;
#16084=CARTESIAN_POINT ( 'NONE',  ( 0.1100053167205930632, 34.32189548568247517, 26.10991185395899450 ) ) ;
#16087=CARTESIAN_POINT ( 'NONE',  ( 0.2885700199627512785, -43.10898996868492361, 0.8047882683537324056 ) ) ;
#16088=DIRECTION ( 'NONE',  ( 0.000000000000000000, 0.000000000000000000, 1.000000000000000000 ) ) ;
#16090=CARTESIAN_POINT ( 'NONE',  ( -6.016761891674565099, 11.46828378093559131, 14.95139917749708758 ) ) ;
#16091=CARTESIAN_POINT ( 'NONE',  ( -6.001507490154111224, -18.19774963328904960, -4.892199142591494798 ) ) ;
#16094=CARTESIAN_POINT ( 'NONE',  ( 1.827326673878743035, -20.44853789448427506, -37.88339879236853136 ) ) ;
#16096=DIRECTION ( 'NONE',  ( 0.1024043820194936449, -0.8679729669084581545, -0.4859385467930429359 ) ) ;
#16103=CARTESIAN_POINT ( 'NONE',  ( 0.2230388203127608715, 43.11276071378623698, -0.7599700551095819323 ) ) ;
#16104=FACE_OUTER_BOUND ( 'NONE', #21433, .T. ) ;
#16105=( BOUNDED_SURFACE ( )  B_SPLINE_SURFACE ( 3, 1, ( 
 ( #10314, #38843 ),
 ( #48221, #58826 ),
 ( #29714, #15947 ),
 ( #29407, #35371 ) ),
 .UNSPECIFIED., .F., .F., .F. ) 
 B_SPLINE_SURFACE_WITH_KNOTS ( ( 4, 4 ),
 ( 2, 2 ),
 ( 0.000000000000000000, 1.000000000000000000 ),
 ( 0.000000000000000000, 1.000000000000000000 ),
 .UNSPECIFIED. ) 
 GEOMETRIC_REPRESENTATION_ITEM ( )  RATIONAL_B_SPLINE_SURFACE ( (
 ( 1.000000000000000000, 1.000000000000000000),
 ( 0.9751682680413298332, 0.9999560080971552356),
 ( 0.9751682680413298332, 0.9999560080971552356),
 ( 1.000000000000000000, 1.000000000000000000) ) ) 
 REPRESENTATION_ITEM ( '' )  SURFACE ( )  );
#16110=CARTESIAN_POINT ( 'NONE',  ( 0.8760168074887076939, 46.68716261866160266, 11.58706983520341893 ) ) ;
#16114=ORIENTED_EDGE ( 'NONE', *, *, #23346, .T. ) ;
#16115=CARTESIAN_POINT ( 'NONE',  ( 3.680882792899938138, -32.59085259319712691, 35.20667105325160406 ) ) ;
#16117=CARTESIAN_POINT ( 'NONE',  ( 0.1103878639767399417, -37.32258098927782441, 21.60424693647491878 ) ) ;
#16121=( BOUNDED_SURFACE ( )  B_SPLINE_SURFACE ( 3, 1, ( 
 ( #54591, #11720 ),
 ( #1978, #41164 ),
 ( #31429, #26727 ),
 ( #7927, #59928 ) ),
 .UNSPECIFIED., .F., .F., .F. ) 
 B_SPLINE_SURFACE_WITH_KNOTS ( ( 4, 4 ),
 ( 2, 2 ),
 ( 0.000000000000000000, 1.000000000000000000 ),
 ( 0.000000000000000000, 1.000000000000000000 ),
 .UNSPECIFIED. ) 
 GEOMETRIC_REPRESENTATION_ITEM ( )  RATIONAL_B_SPLINE_SURFACE ( (
 ( 1.000000000000000000, 1.000000000000000000),
 ( 0.9751682680413298332, 0.9999560080971552356),
 ( 0.9751682680413298332, 0.9999560080971552356),
 ( 1.000000000000000000, 1.000000000000000000) ) ) 
 REPRESENTATION_ITEM ( '' )  SURFACE ( )  );
#16126=EDGE_LOOP ( 'NONE', ( #37310, #61065, #23238, #37045 ) ) ;
#16129=EDGE_CURVE ( 'NONE', #30020, #50038, #23202, .T. ) ;
#16145=LINE ( 'NONE', #59966, #32783 ) ;
#16148=ORIENTED_EDGE ( 'NONE', *, *, #6842, .T. ) ;
#16152=CARTESIAN_POINT ( 'NONE',  ( 4.691466044806102076, -44.46979273209132799, -3.249105306918271374 ) ) ;
#16155=ORIENTED_EDGE ( 'NONE', *, *, #45632, .F. ) ;
#16156=CARTESIAN_POINT ( 'NONE',  ( 0.2885697896453124911, 39.51953439758086262, 17.24062360132728955 ) ) ;
#16166=CARTESIAN_POINT ( 'NONE',  ( 0.1084644655670281982, -41.75632203164224876, -10.77688306151788922 ) ) ;
#16172=LINE ( 'NONE', #44092, #46379 ) ;
#16178=ADVANCED_FACE ( 'NONE', ( #19062 ), #31580, .F. ) ;
#16186=CARTESIAN_POINT ( 'NONE',  ( 0.1103310638050661874, 16.42686748615350112, 39.87325896099748235 ) ) ;
#16187=ORIENTED_EDGE ( 'NONE', *, *, #14351, .F. ) ;
#16188=CARTESIAN_POINT ( 'NONE',  ( 0.6001305935487315502, 41.92422178329169924, -23.60027211631785349 ) ) ;
#16190=CARTESIAN_POINT ( 'NONE',  ( -6.017396004339687465, -14.95000090562889383, 11.47005965438133046 ) ) ;
#16193=VERTEX_POINT ( 'NONE', #5830 ) ;
#16195=CARTESIAN_POINT ( 'NONE',  ( 0.1102847568649952675, -11.25043675627769701, -41.63105453442833692 ) ) ;
#16197=VERTEX_POINT ( 'NONE', #5225 ) ;
#16204=EDGE_CURVE ( 'NONE', #59574, #19392, #53317, .T. ) ;
#16208=ORIENTED_EDGE ( 'NONE', *, *, #20241, .F. ) ;
#16236=CARTESIAN_POINT ( 'NONE',  ( 0.1103744047535531458, -5.590449877750299557, -42.76053735246610188 ) ) ;
#16241=CARTESIAN_POINT ( 'NONE',  ( 4.691466044806103852, -19.42108863068406066, 40.13652286047860684 ) ) ;
#16247=CARTESIAN_POINT ( 'NONE',  ( 4.975801465491695552, -20.67815041659169495, 43.22084481528186473 ) ) ;
#16252=LINE ( 'NONE', #53517, #60831 ) ;
#16259=EDGE_LOOP ( 'NONE', ( #4678, #12622, #35857, #47314 ) ) ;
#16262=CARTESIAN_POINT ( 'NONE',  ( 0.1102144999581332885, 43.12427761225339395, 0.1260305566213565931 ) ) ;
#16265=CARTESIAN_POINT ( 'NONE',  ( 0.1102847568649952675, -41.63105453442844350, 11.25043675627726181 ) ) ;
#16266=EDGE_LOOP ( 'NONE', ( #33612, #14257, #5424, #54782 ) ) ;
#16275=EDGE_CURVE ( 'NONE', #12288, #4388, #49550, .T. ) ;
#16276=ORIENTED_EDGE ( 'NONE', *, *, #61491, .F. ) ;
#16277=CARTESIAN_POINT ( 'NONE',  ( 4.549368137175248350, 0.000000000000000000, 0.000000000000000000 ) ) ;
#16280=EDGE_CURVE ( 'NONE', #5623, #43495, #13751, .T. ) ;
#16282=DIRECTION ( 'NONE',  ( 0.000000000000000000, 0.000000000000000000, -1.000000000000000000 ) ) ;
#16290=ORIENTED_EDGE ( 'NONE', *, *, #24116, .F. ) ;
#16294=DIRECTION ( 'NONE',  ( -0.1024043820194934507, -0.5950744814819135531, -0.7971196296869356157 ) ) ;
#16296=ORIENTED_EDGE ( 'NONE', *, *, #47913, .F. ) ;
#16302=CARTESIAN_POINT ( 'NONE',  ( 0.09136607875274982415, 0.000000000000000000, 3.000000000000000000 ) ) ;
#16307=CARTESIAN_POINT ( 'NONE',  ( 0.7954190325252782356, -0.8690070772085950468, -48.09103420665682194 ) ) ;
#16308=DIRECTION ( 'NONE',  ( 0.000000000000000000, 0.000000000000000000, -1.000000000000000000 ) ) ;
#16310=CARTESIAN_POINT ( 'NONE',  ( 0.8760168074887090262, -33.37827814204149490, 34.63873394077429424 ) ) ;
#16311=ORIENTED_EDGE ( 'NONE', *, *, #9148, .F. ) ;
#16314=AXIS2_PLACEMENT_3D ( 'NONE', #37362, #37996, #36 ) ;
#16317=CARTESIAN_POINT ( 'NONE',  ( 4.549368137175248350, 0.000000000000000000, 0.000000000000000000 ) ) ;
#16328=ADVANCED_FACE ( 'NONE', ( #45957 ), #20783, .F. ) ;
#16329=CARTESIAN_POINT ( 'NONE',  ( 0.1310142868023689566, 33.82067078731310517, 26.75450212504333436 ) ) ;
#16331=ORIENTED_EDGE ( 'NONE', *, *, #44797, .T. ) ;
#16336=CARTESIAN_POINT ( 'NONE',  ( 3.680882792899938138, -22.36818923730799114, 42.44216617524777746 ) ) ;
#16340=CARTESIAN_POINT ( 'NONE',  ( 1.827326673878743479, -42.82501343454098475, 4.394636550975911327 ) ) ;
#16355=CARTESIAN_POINT ( 'NONE',  ( -6.017396004339686577, 16.31924478664274858, 9.420565012089484824 ) ) ;
#16357=CARTESIAN_POINT ( 'NONE',  ( 0.1097557419366048670, 0.2231007852153696347, 43.12388302211984126 ) ) ;
#16361=CARTESIAN_POINT ( 'NONE',  ( 0.5998501479064699549, -17.92509395669137362, 44.64337787626217846 ) ) ;
#16363=CARTESIAN_POINT ( 'NONE',  ( 0.1100053167205930771, -30.36644426605161229, 30.62023953839029744 ) ) ;
#16365=ORIENTED_EDGE ( 'NONE', *, *, #59609, .F. ) ;
#16369=CARTESIAN_POINT ( 'NONE',  ( 0.1081432562775999223, 41.54352569227145864, 11.56998286599550241 ) ) ;
#16379=ORIENTED_EDGE ( 'NONE', *, *, #42254, .T. ) ;
#16382=CARTESIAN_POINT ( 'NONE',  ( 0.5998501479064699549, 28.86886762351124958, -38.48283596222000114 ) ) ;
#16383=CARTESIAN_POINT ( 'NONE',  ( 0.1097557419366048670, -39.75589591229798714, 16.70891382096300148 ) ) ;
#16389=CARTESIAN_POINT ( 'NONE',  ( -6.015611763856276717, -14.95313250337437871, 11.46610900684717471 ) ) ;
#16391=CARTESIAN_POINT ( 'NONE',  ( 4.833616638992205949, -20.04871863793778175, -41.67905425467698421 ) ) ;
#16395=CARTESIAN_POINT ( 'NONE',  ( 0.7245667037590742821, 5.464144792999380940, -47.79072416626839725 ) ) ;
#16399=CARTESIAN_POINT ( 'NONE',  ( 4.975801465491694664, 21.70134120755201224, -42.71626295676241369 ) ) ;
#16401=CARTESIAN_POINT ( 'NONE',  ( 4.975801465491694664, -36.39623109580487892, 31.15993731089061924 ) ) ;
#16412=CARTESIAN_POINT ( 'NONE',  ( 0.1064266418746774023, 30.88821921809848092, -30.09411284098539952 ) ) ;
#16419=CARTESIAN_POINT ( 'NONE',  ( 0.1100247026804066219, -37.43141430507386502, 21.41511734445733595 ) ) ;
#16423=CARTESIAN_POINT ( 'NONE',  ( 0.6009453534118440743, -23.67490308139376509, -41.87889766923446189 ) ) ;
#16427=LINE ( 'NONE', #20514, #33067 ) ;
#16430=ORIENTED_EDGE ( 'NONE', *, *, #43234, .F. ) ;
#16433=CARTESIAN_POINT ( 'NONE',  ( 5.880360259849752858, 26.61251048557193499, 39.91356965504157017 ) ) ;
#16452=ORIENTED_EDGE ( 'NONE', *, *, #11252, .T. ) ;
#16456=CONICAL_SURFACE ( 'NONE', #47496, 43.12527911185304674, 0.04450589592585017101 ) ;
#16457=B_SPLINE_CURVE_WITH_KNOTS ( 'NONE', 3,
 ( #3777, #32011, #3168, #41426 ),
 .UNSPECIFIED., .F., .F.,
 ( 4, 4 ),
 ( 1.854207614396248247E-17, 0.004444306975806115896 ),
 .UNSPECIFIED. ) ;
#16462=CARTESIAN_POINT ( 'NONE',  ( 0.1095718737110178143, -41.58781525899402709, -11.40943879390634308 ) ) ;
#16472=CARTESIAN_POINT ( 'NONE',  ( 0.7245667037590702853, -28.62745028382845902, 38.65590879674336122 ) ) ;
#16478=CARTESIAN_POINT ( 'NONE',  ( 0.6027935024548038978, 41.74929432965617337, -23.90242449907770350 ) ) ;
#16485=CARTESIAN_POINT ( 'NONE',  ( 0.2224561200757598778, -34.66601556960367247, 25.64288022150822499 ) ) ;
#16487=ADVANCED_FACE ( 'NONE', ( #39921 ), #49138, .F. ) ;
#16490=ORIENTED_EDGE ( 'NONE', *, *, #10807, .T. ) ;
#16493=FACE_OUTER_BOUND ( 'NONE', #10429, .T. ) ;
#16497=CARTESIAN_POINT ( 'NONE',  ( 0.5980894510889448457, -17.76188940524917115, -44.71414919659899567 ) ) ;
#16505=CARTESIAN_POINT ( 'NONE',  ( 0.3622758884714730732, 36.91764744403321430, -22.26738722580129348 ) ) ;
#16507=ORIENTED_EDGE ( 'NONE', *, *, #45361, .F. ) ;
#16509=DIRECTION ( 'NONE',  ( 0.000000000000000000, 0.000000000000000000, 1.000000000000000000 ) ) ;
#16510=EDGE_LOOP ( 'NONE', ( #55816, #51558, #11656, #21112 ) ) ;
#16525=VERTEX_POINT ( 'NONE', #22635 ) ;
#16530=CARTESIAN_POINT ( 'NONE',  ( 4.549368137175248350, 35.57418903283115696, -24.02461520945233531 ) ) ;
#16531=ORIENTED_EDGE ( 'NONE', *, *, #17196, .T. ) ;
#16534=CARTESIAN_POINT ( 'NONE',  ( 0.1073791018717483448, 10.69234304550053949, -41.77800844988504991 ) ) ;
#16535=ORIENTED_EDGE ( 'NONE', *, *, #7696, .F. ) ;
#16536=B_SPLINE_CURVE_WITH_KNOTS ( 'NONE', 3,
 ( #57186, #5187, #24319, #19635, #38753, #5491 ),
 .UNSPECIFIED., .F., .F.,
 ( 4, 2, 4 ),
 ( 1.870559545977334001E-17, 0.0002293319059085096288, 0.0004586638118170005551 ),
 .UNSPECIFIED. ) ;
#16543=LINE ( 'NONE', #49742, #52771 ) ;
#16544=VECTOR ( 'NONE', #23370, 1000.000000000000114 ) ;
#16545=ORIENTED_EDGE ( 'NONE', *, *, #4438, .F. ) ;
#16547=CARTESIAN_POINT ( 'NONE',  ( 4.975801465491695552, -20.67815041659169495, 43.22084481528186473 ) ) ;
#16553=VECTOR ( 'NONE', #28622, 1000.000000000000000 ) ;
#16562=CARTESIAN_POINT ( 'NONE',  ( 4.549368137175248350, 0.000000000000000000, 0.000000000000000000 ) ) ;
#16567=CARTESIAN_POINT ( 'NONE',  ( -6.016489644550736315, -18.68142234211826036, 2.463898142942696268 ) ) ;
#16568=CARTESIAN_POINT ( 'NONE',  ( 0.3622758884714600280, -17.25816669465019615, 39.50828911766968332 ) ) ;
#16570=ORIENTED_EDGE ( 'NONE', *, *, #774, .T. ) ;
#16571=CARTESIAN_POINT ( 'NONE',  ( 0.1084644655670281843, 10.77688306151803666, -41.75632203164222034 ) ) ;
#16573=FACE_BOUND ( 'NONE', #15605, .T. ) ;
#16575=LINE ( 'NONE', #46034, #32246 ) ;
#16577=ORIENTED_EDGE ( 'NONE', *, *, #27745, .T. ) ;
#16595=CARTESIAN_POINT ( 'NONE',  ( 0.1084644655670281566, -26.56696682929032249, -33.96951444491416083 ) ) ;
#16598=ORIENTED_EDGE ( 'NONE', *, *, #49006, .T. ) ;
#16609=B_SPLINE_CURVE_WITH_KNOTS ( 'NONE', 3,
 ( #13930, #28005, #13299, #8572, #60571, #26767 ),
 .UNSPECIFIED., .F., .F.,
 ( 4, 2, 4 ),
 ( 2.032850612904068153E-17, 0.0002293319059085113093, 0.0004586638118170022899 ),
 .UNSPECIFIED. ) ;
#16615=ORIENTED_EDGE ( 'NONE', *, *, #4088, .F. ) ;
#16617=CARTESIAN_POINT ( 'NONE',  ( 0.6001305935487422083, -48.10757715638248300, -0.5236757026887532973 ) ) ;
#16620=ORIENTED_EDGE ( 'NONE', *, *, #23807, .F. ) ;
#16621=CARTESIAN_POINT ( 'NONE',  ( 0.1101816497532063094, -42.77304337559939285, -5.494186916735566584 ) ) ;
#16622=CARTESIAN_POINT ( 'NONE',  ( 0.5998501479064699549, 37.84527566984857572, -29.69975237324574024 ) ) ;
#16634=CARTESIAN_POINT ( 'NONE',  ( 4.975801465491695552, 45.18341283946458020, -15.94009207553003016 ) ) ;
#16643=CARTESIAN_POINT ( 'NONE',  ( 0.5980894510889457338, -23.44630161211615871, 42.01322166096878874 ) ) ;
#16656=CARTESIAN_POINT ( 'NONE',  ( 4.549368137175248350, 42.84816078363926550, 2.596185425822091553 ) ) ;
#16659=B_SPLINE_CURVE_WITH_KNOTS ( 'NONE', 3,
 ( #26760, #12999, #3550, #8256, #18306, #22684, #17370, #31782, #59961, #60879, #27691, #12373, #37415, #36804, #50558, #37114 ),
 .UNSPECIFIED., .F., .F.,
 ( 4, 3, 3, 3, 3, 4 ),
 ( 1.962735358247464152E-17, 0.0002618515315864422478, 0.0003927756766341962565, 0.0005236998216950601668, 0.0007855159896329882725, 0.001047349442285927870 ),
 .UNSPECIFIED. ) ;
#16661=CARTESIAN_POINT ( 'NONE',  ( 1.827326673878742813, 37.88339879236860952, -20.44853789448414361 ) ) ;
#16665=ORIENTED_EDGE ( 'NONE', *, *, #26186, .F. ) ;
#16677=CARTESIAN_POINT ( 'NONE',  ( 0.1103310638050662151, -30.55179781598017641, 30.43528225250887331 ) ) ;
#16679=CARTESIAN_POINT ( 'NONE',  ( 0.5988103564986354543, 13.03604522143292854, 46.30780741915673104 ) ) ;
#16684=CARTESIAN_POINT ( 'NONE',  ( 0.1092565886968784733, 41.73439049602436057, 10.86136484717984274 ) ) ;
#16686=DIRECTION ( 'NONE',  ( -0.1024043820194934645, 0.6940285268068259183, 0.7126273545981466340 ) ) ;
#16687=( BOUNDED_SURFACE ( )  B_SPLINE_SURFACE ( 3, 1, ( 
 ( #220, #48475 ),
 ( #29070, #19680 ),
 ( #5539, #37887 ),
 ( #61939, #57542 ) ),
 .UNSPECIFIED., .F., .F., .F. ) 
 B_SPLINE_SURFACE_WITH_KNOTS ( ( 4, 4 ),
 ( 2, 2 ),
 ( 0.000000000000000000, 1.000000000000000000 ),
 ( 0.000000000000000000, 1.000000000000000000 ),
 .UNSPECIFIED. ) 
 GEOMETRIC_REPRESENTATION_ITEM ( )  RATIONAL_B_SPLINE_SURFACE ( (
 ( 1.000000000000000000, 1.000000000000000000),
 ( 0.7223157951917476005, 0.9931996967497186413),
 ( 0.7223157951917476005, 0.9931996967497186413),
 ( 1.000000000000000000, 1.000000000000000000) ) ) 
 REPRESENTATION_ITEM ( '' )  SURFACE ( )  );
#16688=CARTESIAN_POINT ( 'NONE',  ( 0.8751705887134423323, -47.79200036674284036, 5.393078191591890835 ) ) ;
#16689=ORIENTED_EDGE ( 'NONE', *, *, #26186, .T. ) ;
#16690=CARTESIAN_POINT ( 'NONE',  ( 4.975801465491695552, 0.000000000000000000, 47.91270532121795611 ) ) ;
#16692=ADVANCED_FACE ( 'NONE', ( #12684 ), #29185, .F. ) ;
#16699=CARTESIAN_POINT ( 'NONE',  ( 0.1073791018717578927, -37.58707531572220262, 21.14095454447495115 ) ) ;
#16703=B_SPLINE_CURVE_WITH_KNOTS ( 'NONE', 3,
 ( #56441, #13555, #37685, #5044, #43310, #14484 ),
 .UNSPECIFIED., .F., .F.,
 ( 4, 2, 4 ),
 ( 1.554159946372743606E-17, 0.0002293319059085096559, 0.0004586638118170038077 ),
 .UNSPECIFIED. ) ;
#16707=CARTESIAN_POINT ( 'NONE',  ( 0.6031356219577718170, 12.36679943215660948, -46.49081620741443999 ) ) ;
#16713=CARTESIAN_POINT ( 'NONE',  ( 0.6017667736363749853, -33.76945004754892921, -34.26315558341178757 ) ) ;
#16716=CARTESIAN_POINT ( 'NONE',  ( 0.1313383488274129651, 43.11882601516400371, -0.6377633466096090942 ) ) ;
#16718=FACE_OUTER_BOUND ( 'NONE', #32933, .T. ) ;
#16722=EDGE_LOOP ( 'NONE', ( #47589, #56280, #38162, #44070 ) ) ;
#16726=CONICAL_SURFACE ( 'NONE', #1667, 42.92674063221959813, 1.485477209440487556 ) ;
#16727=FACE_OUTER_BOUND ( 'NONE', #13618, .T. ) ;
#16732=CARTESIAN_POINT ( 'NONE',  ( 0.1098349054025746230, -37.45309339978498286, 21.37724154645436769 ) ) ;
#16733=VERTEX_POINT ( 'NONE', #3549 ) ;
#16740=B_SPLINE_CURVE_WITH_KNOTS ( 'NONE', 3,
 ( #1815, #44170, #6187, #53810 ),
 .UNSPECIFIED., .F., .F.,
 ( 4, 4 ),
 ( 0.000000000000000000, 0.005014147105413707325 ),
 .UNSPECIFIED. ) ;
#16742=CARTESIAN_POINT ( 'NONE',  ( 3.238931869106854489, 40.38337734129182621, 14.74782013370860767 ) ) ;
#16753=ORIENTED_EDGE ( 'NONE', *, *, #55805, .F. ) ;
#16754=CARTESIAN_POINT ( 'NONE',  ( 0.6001305935487422083, -12.95698906763841052, 46.33281397023041848 ) ) ;
#16760=CARTESIAN_POINT ( 'NONE',  ( 0.5998501479064699549, -18.89267974119636406, -44.24259072156078787 ) ) ;
#16762=EDGE_CURVE ( 'NONE', #29999, #58236, #45444, .T. ) ;
#16768=ADVANCED_FACE ( 'NONE', ( #23002 ), #42029, .F. ) ;
#16778=CARTESIAN_POINT ( 'NONE',  ( -6.015611763856276717, -0.006214430185273883862, 18.84324252354755203 ) ) ;
#16782=B_SPLINE_CURVE_WITH_KNOTS ( 'NONE', 3,
 ( #19681, #61940, #23753, #19371 ),
 .UNSPECIFIED., .F., .F.,
 ( 4, 4 ),
 ( 1.999757930724971929E-17, 0.004444306975806117631 ),
 .UNSPECIFIED. ) ;
#16788=ADVANCED_FACE ( 'NONE', ( #33334 ), #29924, .F. ) ;
#16802=VECTOR ( 'NONE', #26185, 1000.000000000000114 ) ;
#16806=ORIENTED_EDGE ( 'NONE', *, *, #50824, .T. ) ;
#16809=CARTESIAN_POINT ( 'NONE',  ( -6.015611763856276717, 7.216738110653281524, 17.40650793417846032 ) ) ;
#16812=LINE ( 'NONE', #27423, #54500 ) ;
#16814=CARTESIAN_POINT ( 'NONE',  ( 0.1101816497532062955, 41.61967362528556436, -11.29256821151170342 ) ) ;
#16820=CARTESIAN_POINT ( 'NONE',  ( 0.1084644655670279484, -11.54510651093232454, -41.55047717876500712 ) ) ;
#16823=B_SPLINE_CURVE_WITH_KNOTS ( 'NONE', 3,
 ( #8499, #60813, #57036, #37052, #14163, #51104 ),
 .UNSPECIFIED., .F., .F.,
 ( 4, 2, 4 ),
 ( 8.583542049204267543E-17, 0.0002293366620881436024, 0.0004586733241762013360 ),
 .UNSPECIFIED. ) ;
#16841=DIRECTION ( 'NONE',  ( 0.000000000000000000, 0.000000000000000000, 1.000000000000000000 ) ) ;
#16845=CARTESIAN_POINT ( 'NONE',  ( 0.1064266418746777354, -30.88821921809869053, 30.09411284098518280 ) ) ;
#16854=CARTESIAN_POINT ( 'NONE',  ( 0.1100053167205930355, -26.10991185395913305, 34.32189548568238280 ) ) ;
#16865=CARTESIAN_POINT ( 'NONE',  ( 0.1095718737110177449, 30.31138510522951535, 30.67477146794383458 ) ) ;
#16871=AXIS2_PLACEMENT_3D ( 'NONE', #41530, #60595, #17711 ) ;
#16875=FACE_OUTER_BOUND ( 'NONE', #27852, .T. ) ;
#16877=CARTESIAN_POINT ( 'NONE',  ( 0.3622758884714600280, 33.69533458712307095, 26.89560658783397074 ) ) ;
#16896=CARTESIAN_POINT ( 'NONE',  ( 0.1098349054025745952, 11.36734385884004972, -41.59932877996187273 ) ) ;
#16901=CONICAL_SURFACE ( 'NONE', #720, 42.92674063221959813, 1.485477209440487556 ) ;
#16902=VERTEX_POINT ( 'NONE', #24522 ) ;
#16914=CARTESIAN_POINT ( 'NONE',  ( 0.7954196712028465122, -46.67728755034892174, 11.60747899261438398 ) ) ;
#16918=ORIENTED_EDGE ( 'NONE', *, *, #54547, .F. ) ;
#16923=VERTEX_POINT ( 'NONE', #25441 ) ;
#16926=CARTESIAN_POINT ( 'NONE',  ( 4.691466044806103852, 43.66525414675643191, -9.025781474741004118 ) ) ;
#16931=CARTESIAN_POINT ( 'NONE',  ( 0.6031357023905875581, 44.42879114414631658, 18.45021748202297829 ) ) ;
#16933=DIRECTION ( 'NONE',  ( 1.000000000000000000, 0.000000000000000000, 0.000000000000000000 ) ) ;
#16935=DIRECTION ( 'NONE',  ( 0.000000000000000000, 0.000000000000000000, 1.000000000000000000 ) ) ;
#16939=CARTESIAN_POINT ( 'NONE',  ( 0.1064266418746777076, -33.86837517279528953, -26.69589626339699961 ) ) ;
#16940=CARTESIAN_POINT ( 'NONE',  ( 3.238741278300274029, -23.06029422819029051, 36.28414388564855386 ) ) ;
#16941=CARTESIAN_POINT ( 'NONE',  ( 4.549368137175248350, -2.596185425822241211, 42.84816078363925840 ) ) ;
#16942=VERTEX_POINT ( 'NONE', #30759 ) ;
#16948=CARTESIAN_POINT ( 'NONE',  ( -6.016104459813374383, -14.94608397322076243, -11.47525878590931825 ) ) ;
#16949=ORIENTED_EDGE ( 'NONE', *, *, #34244, .T. ) ;
#16951=CARTESIAN_POINT ( 'NONE',  ( 0.5998501479064708430, 44.24259072156059602, 18.89267974119682947 ) ) ;
#16954=SURFACE_SIDE_STYLE ('',( #6888 ) ) ;
#16958=ORIENTED_EDGE ( 'NONE', *, *, #60103, .T. ) ;
#16962=CARTESIAN_POINT ( 'NONE',  ( 0.1073791018717483448, 21.14095454447559419, -37.58707531572184735 ) ) ;
#16965=CARTESIAN_POINT ( 'NONE',  ( 0.7245667037590793891, -44.12005358974319336, 19.16327388243984231 ) ) ;
#16969=EDGE_CURVE ( 'NONE', #37162, #35170, #16066, .T. ) ;
#16986=VERTEX_POINT ( 'NONE', #1940 ) ;
#16987=ORIENTED_EDGE ( 'NONE', *, *, #292, .T. ) ;
#16990=B_SPLINE_CURVE_WITH_KNOTS ( 'NONE', 3,
 ( #9715, #58230, #52931, #38871 ),
 .UNSPECIFIED., .F., .F.,
 ( 4, 4 ),
 ( 7.152448122690996019E-18, 0.005014147105413701254 ),
 .UNSPECIFIED. ) ;
#16994=EDGE_CURVE ( 'NONE', #9584, #23847, #11035, .T. ) ;
#17012=CARTESIAN_POINT ( 'NONE',  ( 0.6017666602106489515, -41.83584962818300568, -23.75081624637607192 ) ) ;
#17019=CARTESIAN_POINT ( 'NONE',  ( 0.6041374136657475802, -47.71861871402593636, 6.106202762792685590 ) ) ;
#17023=CARTESIAN_POINT ( 'NONE',  ( 0.8760168074887076939, 37.61398439004533856, -29.98565522133307226 ) ) ;
#17025=CARTESIAN_POINT ( 'NONE',  ( 0.8760168074887090262, 33.37827814204125332, -34.63873394077453582 ) ) ;
#17028=CARTESIAN_POINT ( 'NONE',  ( -6.015611763856276717, -17.41126425312542736, 7.205255340944552778 ) ) ;
#17032=CARTESIAN_POINT ( 'NONE',  ( 0.5988103564986355654, -18.96890181990859858, -44.21009236284874078 ) ) ;
#17034=CARTESIAN_POINT ( 'NONE',  ( 0.1092565886968785011, -0.3103822814776921457, -43.12345370280014123 ) ) ;
#17037=CARTESIAN_POINT ( 'NONE',  ( -5.995132425357893702, -18.68405145320025795, 2.451215106828278589 ) ) ;
#17040=B_SPLINE_CURVE_WITH_KNOTS ( 'NONE', 3,
 ( #8206, #45526, #7583, #41453, #60823, #2581, #50510, #21702, #3197, #40845, #55198, #60510, #12023, #50203, #12634, #17943 ),
 .UNSPECIFIED., .F., .F.,
 ( 4, 3, 3, 3, 3, 4 ),
 ( 1.995049841954898532E-17, 0.0002618515315864428442, 0.0003927756766341985875, 0.0005236998216950575647, 0.0007855159896329908745, 0.001047349442285928304 ),
 .UNSPECIFIED. ) ;
#17048=ADVANCED_FACE ( 'NONE', ( #45822 ), #3784, .T. ) ;
#17049=VECTOR ( 'NONE', #3610, 1000.000000000000000 ) ;
#17050=VERTEX_POINT ( 'NONE', #60488 ) ;
#17053=EDGE_CURVE ( 'NONE', #16986, #15504, #2799, .T. ) ;
#17060=CARTESIAN_POINT ( 'NONE',  ( 0.1087620492084205859, 0.3620418170786780521, -43.12302841504342155 ) ) ;
#17061=VERTEX_POINT ( 'NONE', #55484 ) ;
#17064=CARTESIAN_POINT ( 'NONE',  ( 0.5998501479064708430, 48.10473956285918717, 0.5236536531316605680 ) ) ;
#17068=CARTESIAN_POINT ( 'NONE',  ( 4.322998006666165516, -2.120302895116613850, 47.94177812210860878 ) ) ;
#17072=EDGE_CURVE ( 'NONE', #5670, #24199, #47643, .T. ) ;
#17075=DIRECTION ( 'NONE',  ( 0.09835009131224566048, -0.4908642831975305043, -0.8656670924898598463 ) ) ;
#17088=CARTESIAN_POINT ( 'NONE',  ( 0.5980894510889457338, -0.7015180096001567556, -48.10766805928368939 ) ) ;
#17089=EDGE_CURVE ( 'NONE', #44899, #40739, #23792, .T. ) ;
#17098=VERTEX_POINT ( 'NONE', #52638 ) ;
#17099=FACE_OUTER_BOUND ( 'NONE', #60910, .T. ) ;
#17103=CARTESIAN_POINT ( 'NONE',  ( -5.995132425357893702, 0.008513469643070757306, -18.84415457712583475 ) ) ;
#17105=CARTESIAN_POINT ( 'NONE',  ( 0.1064266418746776244, 37.06314021531080272, 22.04679912212841941 ) ) ;
#17109=CARTESIAN_POINT ( 'NONE',  ( 0.8751705887134423323, -48.08707113907595243, -0.8911681664086732457 ) ) ;
#17113=CARTESIAN_POINT ( 'NONE',  ( -6.010958268070873523, -18.19761767765833227, 4.891065400978321875 ) ) ;
#17115=DIRECTION ( 'NONE',  ( -1.000000000000000000, -0.000000000000000000, -0.000000000000000000 ) ) ;
#17119=CARTESIAN_POINT ( 'NONE',  ( 0.1073791018717483448, 41.52698815987167791, -11.62916352156108779 ) ) ;
#17126=CARTESIAN_POINT ( 'NONE',  ( 0.1103744047535531458, -39.82693656558422646, -16.53879706351759538 ) ) ;
#17128=ORIENTED_EDGE ( 'NONE', *, *, #10005, .T. ) ;
#17133=AXIS2_PLACEMENT_3D ( 'NONE', #48911, #1278, #14184 ) ;
#17134=DIRECTION ( 'NONE',  ( 0.000000000000000000, 0.000000000000000000, 1.000000000000000000 ) ) ;
#17139=CARTESIAN_POINT ( 'NONE',  ( -6.016761891674565099, -18.84319130225482297, -0.003433883959981760738 ) ) ;
#17140=ORIENTED_EDGE ( 'NONE', *, *, #53307, .T. ) ;
#17149=CARTESIAN_POINT ( 'NONE',  ( 0.1073791018717483448, 42.81622261970987608, 5.147744207007008299 ) ) ;
#17152=CARTESIAN_POINT ( 'NONE',  ( 4.975801465491694664, 39.51822597168457918, 27.09127437476394817 ) ) ;
#17156=CARTESIAN_POINT ( 'NONE',  ( 0.1102144999581333024, -26.35238362727865891, 34.13606714958004318 ) ) ;
#17157=ORIENTED_EDGE ( 'NONE', *, *, #53388, .T. ) ;
#17168=CARTESIAN_POINT ( 'NONE',  ( 0.1073791018717578927, 41.77800844988514939, -10.69234304550012027 ) ) ;
#17187=CARTESIAN_POINT ( 'NONE',  ( 4.322998006666165516, 39.32552843303850665, -27.50295597456410590 ) ) ;
#17196=EDGE_CURVE ( 'NONE', #57388, #58295, #1245, .T. ) ;
#17197=CARTESIAN_POINT ( 'NONE',  ( -6.010958268070873523, 18.68413620842264322, 2.445171577615829150 ) ) ;
#17206=EDGE_CURVE ( 'NONE', #37185, #41488, #32009, .T. ) ;
#17207=CARTESIAN_POINT ( 'NONE',  ( 0.8751705887134553219, 34.63284514348538323, 33.37254303619566542 ) ) ;
#17208=VERTEX_POINT ( 'NONE', #20380 ) ;
#17214=EDGE_LOOP ( 'NONE', ( #5856, #13676, #51033, #20136 ) ) ;
#17218=VERTEX_POINT ( 'NONE', #5621 ) ;
#17221=CARTESIAN_POINT ( 'NONE',  ( 5.880360259849752858, -3.090325311464535485, -47.87242051977165147 ) ) ;
#17238=CARTESIAN_POINT ( 'NONE',  ( 0.1092565886968784872, -21.83052579204436938, -37.19081526480817246 ) ) ;
#17245=ORIENTED_EDGE ( 'NONE', *, *, #48055, .T. ) ;
#17247=ORIENTED_EDGE ( 'NONE', *, *, #11984, .T. ) ;
#17256=CARTESIAN_POINT ( 'NONE',  ( 4.975801465491695552, 0.000000000000000000, 0.000000000000000000 ) ) ;
#17258=CARTESIAN_POINT ( 'NONE',  ( 4.833616638992205949, -20.86133030530319843, 41.27831852777605093 ) ) ;
#17265=VECTOR ( 'NONE', #26071, 1000.000000000000114 ) ;
#17267=DIRECTION ( 'NONE',  ( -1.000000000000000000, -0.000000000000000000, -0.000000000000000000 ) ) ;
#17269=ORIENTED_EDGE ( 'NONE', *, *, #12447, .T. ) ;
#17285=CARTESIAN_POINT ( 'NONE',  ( 0.6009453534118439633, 28.93865405070896912, 38.43042294376924417 ) ) ;
#17287=ORIENTED_EDGE ( 'NONE', *, *, #40139, .T. ) ;
#17294=CARTESIAN_POINT ( 'NONE',  ( -6.010958268070873523, 16.31164801516942120, 9.434296419346264173 ) ) ;
#17305=( BOUNDED_SURFACE ( )  B_SPLINE_SURFACE ( 3, 1, ( 
 ( #6264, #11318 ),
 ( #10706, #54508 ),
 ( #53584, #16643 ),
 ( #39230, #58280 ) ),
 .UNSPECIFIED., .F., .F., .F. ) 
 B_SPLINE_SURFACE_WITH_KNOTS ( ( 4, 4 ),
 ( 2, 2 ),
 ( 0.000000000000000000, 1.000000000000000000 ),
 ( 0.000000000000000000, 1.000000000000000000 ),
 .UNSPECIFIED. ) 
 GEOMETRIC_REPRESENTATION_ITEM ( )  RATIONAL_B_SPLINE_SURFACE ( (
 ( 1.000000000000000000, 1.000000000000000000),
 ( 0.9953040768229005630, 0.8617119497784937465),
 ( 0.9953040768229005630, 0.8617119497784937465),
 ( 1.000000000000000000, 1.000000000000000000) ) ) 
 REPRESENTATION_ITEM ( '' )  SURFACE ( )  );
#17313=CARTESIAN_POINT ( 'NONE',  ( 0.6009453534118438522, -41.44251633523874290, -24.43073772334902927 ) ) ;
#17318=CARTESIAN_POINT ( 'NONE',  ( -6.016761891674564211, -16.32039929810250456, -9.418621820384668553 ) ) ;
#17323=CARTESIAN_POINT ( 'NONE',  ( 4.549368137175248350, -18.79584381673505789, -38.59302160394747006 ) ) ;
#17329=B_SPLINE_CURVE_WITH_KNOTS ( 'NONE', 3,
 ( #46185, #16742, #40882, #59632 ),
 .UNSPECIFIED., .F., .F.,
 ( 4, 4 ),
 ( 6.254634441385501517E-18, 0.004566006591234648103 ),
 .UNSPECIFIED. ) ;
#17332=CARTESIAN_POINT ( 'NONE',  ( 0.6031356755773454870, -6.279306815850496548, -47.69587413076371263 ) ) ;
#17345=ORIENTED_EDGE ( 'NONE', *, *, #14908, .T. ) ;
#17350=UNCERTAINTY_MEASURE_WITH_UNIT (LENGTH_MEASURE( 1.000000000000000082E-05 ), #20710, 'distance_accuracy_value', 'NONE');
#17351=VERTEX_POINT ( 'NONE', #46062 ) ;
#17356=CARTESIAN_POINT ( 'NONE',  ( 4.975801465491695552, -47.76942479135487929, 3.702618843596635401 ) ) ;
#17363=CARTESIAN_POINT ( 'NONE',  ( 0.1103744047535531458, 21.52865142340085569, 37.36621271144544920 ) ) ;
#17364=EDGE_LOOP ( 'NONE', ( #44500, #42561, #52899, #32869 ) ) ;
#17366=CARTESIAN_POINT ( 'NONE',  ( 0.5998501479064699549, 23.59887241503354716, -41.92175333043595487 ) ) ;
#17370=CARTESIAN_POINT ( 'NONE',  ( 0.6029303876144825880, 34.10953954078140526, -33.92442033626747389 ) ) ;
#17377=EDGE_CURVE ( 'NONE', #15900, #56955, #37117, .T. ) ;
#17382=CARTESIAN_POINT ( 'NONE',  ( 0.8760168074887076939, 11.58706983520325551, -46.68716261866165240 ) ) ;
#17384=VERTEX_POINT ( 'NONE', #47273 ) ;
#17388=CARTESIAN_POINT ( 'NONE',  ( 0.5998501479064699549, -41.39809967730504781, 24.50586714782532027 ) ) ;
#17390=CARTESIAN_POINT ( 'NONE',  ( 0.2230388203127612601, 42.64472907182729955, -6.380812898001128275 ) ) ;
#17394=CARTESIAN_POINT ( 'NONE',  ( 4.549368137175248350, -35.80950303116083688, -23.67244292351627521 ) ) ;
#17399=DIRECTION ( 'NONE',  ( -0.1024043820194934507, -0.6940285268068210334, -0.7126273545981514079 ) ) ;
#17410=ORIENTED_EDGE ( 'NONE', *, *, #20106, .T. ) ;
#17412=CARTESIAN_POINT ( 'NONE',  ( 0.8760168074886960365, 46.68716261866176609, -11.58706983520277589 ) ) ;
#17414=LINE ( 'NONE', #22419, #16802 ) ;
#17417=DIRECTION ( 'NONE',  ( -0.1024043820194934645, 0.2701391291102920866, -0.9573600124648712351 ) ) ;
#17419=CARTESIAN_POINT ( 'NONE',  ( 0.5998501479064708430, -29.69975237324642237, 37.84527566984805702 ) ) ;
#17421=ORIENTED_EDGE ( 'NONE', *, *, #39220, .T. ) ;
#17447=EDGE_LOOP ( 'NONE', ( #937, #33625, #24198, #14755, #26392, #61416, #157, #52150, #11926, #51382, #22626, #32069, #54402, #31197, #52930, #50015, #29018, #37464, #42644, #49245, #12246, #12602, #40355, #2548, #32089, #40983, #53188, #55711, #54627, #2379, #6851, #57137, #10417, #38911, #14005, #11105, #45415, #32176, #20741, #59205, #49338, #51007, #33608, #49083, #57100, #51945, #57093, #40122, #29680, #51550, #39880, #33191, #43753, #19520, #52852, #25697, #52936, #14802, #23462, #58970, #49405, #46213, #58760, #59328, #37882, #22692, #31207, #48142, #58700, #33630, #23528, #20048, #45458, #36084, #54640, #30433, #5972, #26116, #35092, #36747, #54786, #12833, #40043, #35282, #8359, #6184, #29091, #15388, #58322, #60534, #54091, #48050, #18750, #38873, #258, #5022, #41580, #44125, #38127, #42038, #3219, #54515, #21892, #56779, #56110, #48741, #49422, #52343, #7801, #35706, #38970, #37806, #25498, #50583, #6232, #55868, #31970, #11801, #52527, #22986, #38354, #8356, #43189, #420, #49933, #27666, #22816, #47099, #20382, #26857, #5942, #54007, #44406, #59859, #61764, #2297, #2172, #45211, #3854, #55787, #19006, #20826, #51980, #53192, #44509, #17748, #9481, #57321 ) ) ;
#17449=VERTEX_POINT ( 'NONE', #4016 ) ;
#17452=CARTESIAN_POINT ( 'NONE',  ( 0.6041374136657475802, -0.1745662470647943998, 48.10739871142803992 ) ) ;
#17453=CARTESIAN_POINT ( 'NONE',  ( 0.7048096507298635682, -17.62869676200438818, 44.76417498422286201 ) ) ;
#17456=CARTESIAN_POINT ( 'NONE',  ( -6.016104459813374383, 17.41090761020846145, -7.206059014949892649 ) ) ;
#17464=CARTESIAN_POINT ( 'NONE',  ( 0.7954196712028457350, -24.79809944608804528, 41.21355366240420182 ) ) ;
#17468=CARTESIAN_POINT ( 'NONE',  ( 0.7954196712028480665, -37.62416450255270206, -29.96539649507072056 ) ) ;
#17479=CARTESIAN_POINT ( 'NONE',  ( 0.7954190325252784577, -47.56618055754181285, 7.138712176114637487 ) ) ;
#17480=B_SPLINE_CURVE_WITH_KNOTS ( 'NONE', 3,
 ( #10289, #1174, #60047, #40669, #6783, #55028 ),
 .UNSPECIFIED., .F., .F.,
 ( 4, 2, 4 ),
 ( 2.032850612904068461E-17, 0.0002293319059085090867, 0.0004586638118169978446 ),
 .UNSPECIFIED. ) ;
#17481=CARTESIAN_POINT ( 'NONE',  ( 4.549368137175248350, 32.41327393324100825, 28.14399996863509301 ) ) ;
#17485=CARTESIAN_POINT ( 'NONE',  ( 0.6041374136657475802, 48.10739871142803992, 0.1745662470646264230 ) ) ;
#17487=EDGE_CURVE ( 'NONE', #4699, #49434, #48296, .T. ) ;
#17488=CARTESIAN_POINT ( 'NONE',  ( 0.3622758884714730732, -40.13994584881772454, -15.73321244754840720 ) ) ;
#17489=LINE ( 'NONE', #40392, #54838 ) ;
#17502=CARTESIAN_POINT ( 'NONE',  ( 0.8760168074886960365, 47.56749362999704545, 7.161346975773865253 ) ) ;
#17513=DIRECTION ( 'NONE',  ( 0.1024043820194936588, 0.6940285268068309144, -0.7126273545981417490 ) ) ;
#17516=CARTESIAN_POINT ( 'NONE',  ( -6.017396004339687465, -7.209881890566424367, -17.40926186480786697 ) ) ;
#17521=CARTESIAN_POINT ( 'NONE',  ( 4.975801465491694664, -42.71626295676247764, -21.70134120755185947 ) ) ;
#17528=CARTESIAN_POINT ( 'NONE',  ( 4.549368137175248350, 0.000000000000000000, 0.000000000000000000 ) ) ;
#17532=CARTESIAN_POINT ( 'NONE',  ( 0.6009452777970409887, 44.61081509289878966, 18.00606236585388231 ) ) ;
#17538=VECTOR ( 'NONE', #30216, 1000.000000000000000 ) ;
#17539=VERTEX_POINT ( 'NONE', #34414 ) ;
#17542=CARTESIAN_POINT ( 'NONE',  ( -6.016761891674564211, 18.84319130225482297, -0.003433883959849463787 ) ) ;
#17544=CARTESIAN_POINT ( 'NONE',  ( 0.3622758884714730732, -42.62881903538215056, 6.444611261693867554 ) ) ;
#17546=DIRECTION ( 'NONE',  ( -0.1024043820194934507, 0.9239750460186177961, -0.3684880688409037930 ) ) ;
#17559=B_SPLINE_CURVE_WITH_KNOTS ( 'NONE', 3,
 ( #26062, #51316, #2232, #13437 ),
 .UNSPECIFIED., .F., .F.,
 ( 4, 4 ),
 ( 0.000000000000000000, 0.004445488388166990781 ),
 .UNSPECIFIED. ) ;
#17572=CARTESIAN_POINT ( 'NONE',  ( 0.09136607875274982415, 0.000000000000000000, 0.000000000000000000 ) ) ;
#17577=CARTESIAN_POINT ( 'NONE',  ( 4.549368137175248350, 2.596185425821941894, -42.84816078363927971 ) ) ;
#17583=EDGE_CURVE ( 'NONE', #12277, #226, #15463, .T. ) ;
#17590=CARTESIAN_POINT ( 'NONE',  ( 0.6009452777970413218, 29.63106797105363555, 37.89911497740580870 ) ) ;
#17595=CARTESIAN_POINT ( 'NONE',  ( 0.5998501479064708430, 41.92175333043619645, -23.59887241503310307 ) ) ;
#17597=CARTESIAN_POINT ( 'NONE',  ( 0.8760168074887090262, -42.09738177923938451, -23.27577685234583527 ) ) ;
#17600=CARTESIAN_POINT ( 'NONE',  ( 0.8751705887134553219, 17.57879340691544101, -44.76769609654218129 ) ) ;
#17601=ORIENTED_EDGE ( 'NONE', *, *, #23551, .T. ) ;
#17606=ORIENTED_EDGE ( 'NONE', *, *, #28160, .T. ) ;
#17608=ORIENTED_EDGE ( 'NONE', *, *, #42674, .F. ) ;
#17609=CARTESIAN_POINT ( 'NONE',  ( 4.549368137175248350, -42.06008734272402450, 8.582197505783685898 ) ) ;
#17614=ORIENTED_EDGE ( 'NONE', *, *, #56055, .F. ) ;
#17615=LINE ( 'NONE', #46443, #56552 ) ;
#17619=EDGE_CURVE ( 'NONE', #4129, #48896, #2009, .T. ) ;
#17620=AXIS2_PLACEMENT_3D ( 'NONE', #22674, #41806, #26751 ) ;
#17622=ORIENTED_EDGE ( 'NONE', *, *, #37151, .T. ) ;
#17626=CARTESIAN_POINT ( 'NONE',  ( -6.017396004339686577, -16.31924478664268463, -9.420565012089598511 ) ) ;
#17629=CARTESIAN_POINT ( 'NONE',  ( 0.3622758884714600280, -0.8252992914331080954, 43.10531414739104150 ) ) ;
#17633=CARTESIAN_POINT ( 'NONE',  ( 4.549368137175248350, 0.000000000000000000, 0.000000000000000000 ) ) ;
#17635=CARTESIAN_POINT ( 'NONE',  ( -2.708315649062916552, -1.648584381067149218, 14.54141329178159303 ) ) ;
#17638=DIRECTION ( 'NONE',  ( 0.000000000000000000, 0.000000000000000000, 1.000000000000000000 ) ) ;
#17646=ORIENTED_EDGE ( 'NONE', *, *, #50700, .F. ) ;
#17652=DIRECTION ( 'NONE',  ( 0.1024043820194936311, 0.8679729669084546018, 0.4859385467930489311 ) ) ;
#17653=CARTESIAN_POINT ( 'NONE',  ( 0.8751705887134553219, 37.60752970653828697, -29.98056538504921065 ) ) ;
#17655=ORIENTED_EDGE ( 'NONE', *, *, #20203, .F. ) ;
#17662=AXIS2_PLACEMENT_3D ( 'NONE', #23616, #52415, #53337 ) ;
#17674=CARTESIAN_POINT ( 'NONE',  ( 2.643462169533600914, -1.382267876918794602, 48.01657676222234983 ) ) ;
#17678=EDGE_CURVE ( 'NONE', #54789, #50134, #45269, .T. ) ;
#17688=EDGE_CURVE ( 'NONE', #46133, #61654, #43106, .T. ) ;
#17692=VERTEX_POINT ( 'NONE', #60652 ) ;
#17693=B_SPLINE_CURVE_WITH_KNOTS ( 'NONE', 3,
 ( #60065, #36284, #50059, #55352, #41299, #55662, #12792, #12474, #55975, #27175, #50659, #35983, #36910, #41599, #32190, #31883, #50968, #8357, #35673 ),
 .UNSPECIFIED., .F., .F.,
 ( 4, 3, 3, 3, 3, 3, 4 ),
 ( 1.149162571898268292E-16, 0.0002618519381806262963, 0.0003927759815485972221, 0.0005237000248299437553, 0.0006546240681324991262, 0.0007855481115631330344, 0.0009699050456655103998 ),
 .UNSPECIFIED. ) ;
#17696=CARTESIAN_POINT ( 'NONE',  ( 4.975801465491694664, 8.787181743659507660, 47.10002938642145409 ) ) ;
#17707=ORIENTED_EDGE ( 'NONE', *, *, #700, .F. ) ;
#17710=FACE_OUTER_BOUND ( 'NONE', #6472, .T. ) ;
#17711=DIRECTION ( 'NONE',  ( 0.000000000000000000, 0.000000000000000000, 1.000000000000000000 ) ) ;
#17713=CARTESIAN_POINT ( 'NONE',  ( 0.8751705887134423323, -5.393078191592370452, -47.79200036674278351 ) ) ;
#17714=B_SPLINE_CURVE_WITH_KNOTS ( 'NONE', 3,
 ( #26403, #49910, #35521, #11709, #6035, #6965 ),
 .UNSPECIFIED., .F., .F.,
 ( 4, 2, 4 ),
 ( 8.583542049204266310E-17, 0.0002293366620881449576, 0.0004586733241762040465 ),
 .UNSPECIFIED. ) ;
#17716=CARTESIAN_POINT ( 'NONE',  ( 0.7245667037590787229, 17.64710816761261114, -44.74806999162972687 ) ) ;
#17718=CARTESIAN_POINT ( 'NONE',  ( 0.6025881611877910160, -44.52856035602921736, 18.20817581200337898 ) ) ;
#17720=CIRCLE ( 'NONE', #32752, 47.91270532121795611 ) ;
#17731=CARTESIAN_POINT ( 'NONE',  ( 0.1092355843206037486, 5.926758618547972368, -42.71527351115373961 ) ) ;
#17741=CARTESIAN_POINT ( 'NONE',  ( 0.2885697896453112699, 11.93479333319024605, -41.43179225254754527 ) ) ;
#17744=( BOUNDED_SURFACE ( )  B_SPLINE_SURFACE ( 3, 1, ( 
 ( #21828, #45967 ),
 ( #51543, #27758 ),
 ( #37179, #56249 ),
 ( #17139, #40967 ) ),
 .UNSPECIFIED., .F., .F., .F. ) 
 B_SPLINE_SURFACE_WITH_KNOTS ( ( 4, 4 ),
 ( 2, 2 ),
 ( 0.000000000000000000, 1.000000000000000000 ),
 ( 0.000000000000000000, 1.000000000000000000 ),
 .UNSPECIFIED. ) 
 GEOMETRIC_REPRESENTATION_ITEM ( )  RATIONAL_B_SPLINE_SURFACE ( (
 ( 1.000000000000000000, 1.000000000000000000),
 ( 0.9953040768229005630, 0.8617119497784937465),
 ( 0.9953040768229005630, 0.8617119497784937465),
 ( 1.000000000000000000, 1.000000000000000000) ) ) 
 REPRESENTATION_ITEM ( '' )  SURFACE ( )  );
#17748=ORIENTED_EDGE ( 'NONE', *, *, #20203, .T. ) ;
#17749=CIRCLE ( 'NONE', #52745, 47.91270532121795611 ) ;
#17751=CARTESIAN_POINT ( 'NONE',  ( 0.1073791018717483448, 34.50606437925512182, 25.86618856530722610 ) ) ;
#17760=ORIENTED_EDGE ( 'NONE', *, *, #33779, .F. ) ;
#17765=FACE_OUTER_BOUND ( 'NONE', #52317, .T. ) ;
#17766=( BOUNDED_SURFACE ( )  B_SPLINE_SURFACE ( 3, 1, ( 
 ( #41931, #42243 ),
 ( #57514, #27807 ),
 ( #51918, #61606 ),
 ( #61303, #52525 ) ),
 .UNSPECIFIED., .F., .F., .F. ) 
 B_SPLINE_SURFACE_WITH_KNOTS ( ( 4, 4 ),
 ( 2, 2 ),
 ( 0.000000000000000000, 1.000000000000000000 ),
 ( 0.000000000000000000, 1.000000000000000000 ),
 .UNSPECIFIED. ) 
 GEOMETRIC_REPRESENTATION_ITEM ( )  RATIONAL_B_SPLINE_SURFACE ( (
 ( 1.000000000000000000, 1.000000000000000000),
 ( 0.9953040768229005630, 0.8617119497784937465),
 ( 0.9953040768229005630, 0.8617119497784937465),
 ( 1.000000000000000000, 1.000000000000000000) ) ) 
 REPRESENTATION_ITEM ( '' )  SURFACE ( )  );
#17771=EDGE_CURVE ( 'NONE', #11109, #10420, #24442, .T. ) ;
#17783=CARTESIAN_POINT ( 'NONE',  ( 2.301430502907646058, 46.71331171933233151, -11.18388433759668743 ) ) ;
#17785=ORIENTED_EDGE ( 'NONE', *, *, #4051, .T. ) ;
#17797=CARTESIAN_POINT ( 'NONE',  ( -6.017396004339687465, -18.84316306185412415, -0.001173774849179927806 ) ) ;
#17799=CARTESIAN_POINT ( 'NONE',  ( 0.1064266379913941102, -40.05351204369895868, -15.98292486309322769 ) ) ;
#17811=CARTESIAN_POINT ( 'NONE',  ( -6.010958268070873523, -18.68413620842262191, -2.445171577615958824 ) ) ;
#17816=EDGE_CURVE ( 'NONE', #24396, #27042, #49853, .T. ) ;
#17819=CARTESIAN_POINT ( 'NONE',  ( 0.6029303876144825880, 24.16699908817961884, -41.59667219751857914 ) ) ;
#17832=CARTESIAN_POINT ( 'NONE',  ( 0.2885697896453105482, -15.75356890148129452, -40.13549262224773884 ) ) ;
#17842=DIRECTION ( 'NONE',  ( 0.000000000000000000, 0.000000000000000000, 1.000000000000000000 ) ) ;
#17847=CARTESIAN_POINT ( 'NONE',  ( -6.016489644550736315, -16.32089497094054664, -9.417787539062418389 ) ) ;
#17856=ORIENTED_EDGE ( 'NONE', *, *, #17487, .T. ) ;
#17860=CARTESIAN_POINT ( 'NONE',  ( 0.1092355843206037486, -42.71527351115375382, -5.926758618547823154 ) ) ;
#17866=CARTESIAN_POINT ( 'NONE',  ( -6.016761891674564211, -14.95139917749696501, -11.46828378093574941 ) ) ;
#17883=B_SPLINE_CURVE_WITH_KNOTS ( 'NONE', 3,
 ( #5729, #48369, #34907, #5431, #33983, #28640 ),
 .UNSPECIFIED., .F., .F.,
 ( 4, 2, 4 ),
 ( 1.268664800107929448E-16, 0.0002450741128632319085, 0.0004901482257263369653 ),
 .UNSPECIFIED. ) ;
#17885=FACE_OUTER_BOUND ( 'NONE', #12049, .T. ) ;
#17891=DIRECTION ( 'NONE',  ( 0.1024043820194936449, -0.01315135725335844948, -0.9946559125373960475 ) ) ;
#17893=CARTESIAN_POINT ( 'NONE',  ( 0.5988103622719994634, -38.53259676306939951, 28.80261254779972901 ) ) ;
#17902=ORIENTED_EDGE ( 'NONE', *, *, #59435, .F. ) ;
#17910=ORIENTED_EDGE ( 'NONE', *, *, #60290, .T. ) ;
#17915=B_SPLINE_CURVE_WITH_KNOTS ( 'NONE', 3,
 ( #15299, #25602, #44740, #1780 ),
 .UNSPECIFIED., .F., .F.,
 ( 4, 4 ),
 ( 0.000000000000000000, 0.005014147105413696050 ),
 .UNSPECIFIED. ) ;
#17919=EDGE_CURVE ( 'NONE', #33426, #46173, #22113, .T. ) ;
#17925=ORIENTED_EDGE ( 'NONE', *, *, #2763, .T. ) ;
#17927=ORIENTED_EDGE ( 'NONE', *, *, #61372, .F. ) ;
#17932=CARTESIAN_POINT ( 'NONE',  ( 0.6001305935487422083, -29.70149728382463650, 37.84751346122805415 ) ) ;
#17943=CARTESIAN_POINT ( 'NONE',  ( 0.5998501479064699549, 5.759754759340783181, -47.76154736470751772 ) ) ;
#17953=CARTESIAN_POINT ( 'NONE',  ( 0.1073791018717483448, -16.05399293000841254, 40.02496097243031414 ) ) ;
#17955=CARTESIAN_POINT ( 'NONE',  ( 0.1101816497532063094, -21.44450189183895006, 37.41460501058178068 ) ) ;
#17969=ADVANCED_FACE ( 'NONE', ( #46140 ), #5207, .F. ) ;
#17970=ORIENTED_EDGE ( 'NONE', *, *, #8604, .F. ) ;
#17973=ADVANCED_FACE ( 'NONE', ( #60199 ), #33232, .F. ) ;
#17978=( BOUNDED_SURFACE ( )  B_SPLINE_SURFACE ( 3, 1, ( 
 ( #4586, #56612 ),
 ( #57210, #43797 ),
 ( #30569, #45021 ),
 ( #54360, #34372 ) ),
 .UNSPECIFIED., .F., .F., .F. ) 
 B_SPLINE_SURFACE_WITH_KNOTS ( ( 4, 4 ),
 ( 2, 2 ),
 ( 0.000000000000000000, 1.000000000000000000 ),
 ( 0.000000000000000000, 1.000000000000000000 ),
 .UNSPECIFIED. ) 
 GEOMETRIC_REPRESENTATION_ITEM ( )  RATIONAL_B_SPLINE_SURFACE ( (
 ( 1.000000000000000000, 1.000000000000000000),
 ( 0.9953040768229005630, 0.8617119497784937465),
 ( 0.9953040768229005630, 0.8617119497784937465),
 ( 1.000000000000000000, 1.000000000000000000) ) ) 
 REPRESENTATION_ITEM ( '' )  SURFACE ( )  );
#17991=CARTESIAN_POINT ( 'NONE',  ( 0.6017667736363749853, -48.10631678344241635, -0.3491025323178837403 ) ) ;
#18003=CARTESIAN_POINT ( 'NONE',  ( 4.549368137175248350, 24.02461520945223228, 35.57418903283122802 ) ) ;
#18009=CARTESIAN_POINT ( 'NONE',  ( 0.5988103622719992414, 46.62176011478423021, -11.86435782853384957 ) ) ;
#18014=B_SPLINE_CURVE_WITH_KNOTS ( 'NONE', 3,
 ( #39533, #38, #57652, #660 ),
 .UNSPECIFIED., .F., .F.,
 ( 4, 4 ),
 ( 2.292215966409847588E-17, 0.004564976165746187711 ),
 .UNSPECIFIED. ) ;
#18017=CARTESIAN_POINT ( 'NONE',  ( 0.2885700199627501683, -34.69058524452997005, -25.60460887553365694 ) ) ;
#18027=CARTESIAN_POINT ( 'NONE',  ( 4.975801465491694664, -45.55012473237763260, 14.85979367497093762 ) ) ;
#18040=CONICAL_SURFACE ( 'NONE', #44089, 43.12527911185304674, 0.04450589592585017101 ) ;
#18047=CARTESIAN_POINT ( 'NONE',  ( 0.5988103622719994634, -29.76496569135189674, 37.79415722405543931 ) ) ;
#18054=CARTESIAN_POINT ( 'NONE',  ( 0.6025881611877910160, 41.55278713510049471, 24.24244696985822856 ) ) ;
#18063=CARTESIAN_POINT ( 'NONE',  ( 0.6031356219577718170, -47.70727206974381573, -6.192730535895980992 ) ) ;
#18074=CARTESIAN_POINT ( 'NONE',  ( 0.6001305935487422083, -33.64689939321966250, 34.38748867424655487 ) ) ;
#18076=CARTESIAN_POINT ( 'NONE',  ( -6.016761891674564211, 0.003433883959783673098, 18.84319130225482297 ) ) ;
#18094=ORIENTED_EDGE ( 'NONE', *, *, #21356, .F. ) ;
#18098=CARTESIAN_POINT ( 'NONE',  ( -2.569797478183790229, -8.547745408040713144, -11.87678401312191845 ) ) ;
#18099=CARTESIAN_POINT ( 'NONE',  ( 4.549368137175248350, -32.13400537129904677, -28.46244473166662559 ) ) ;
#18100=CARTESIAN_POINT ( 'NONE',  ( -6.010958268070873523, -18.84344976839986785, 0.01451635840156647282 ) ) ;
#18103=B_SPLINE_CURVE_WITH_KNOTS ( 'NONE', 3,
 ( #39509, #58562, #15692, #34796, #10991, #6236, #45439, #40435, #16931, #13154, #7486, #55412, #41064, #3105, #17532, #54799 ),
 .UNSPECIFIED., .F., .F.,
 ( 4, 3, 3, 3, 3, 4 ),
 ( 2.194378057379452319E-17, 0.0002618515315864391579, 0.0003927756766341943049, 0.0005236998216950536616, 0.0007855159896329885977, 0.001047349442285928304 ),
 .UNSPECIFIED. ) ;
#18104=CARTESIAN_POINT ( 'NONE',  ( 3.680882792899937694, -10.62117075007680711, 46.78529781139670263 ) ) ;
#18106=CARTESIAN_POINT ( 'NONE',  ( 0.1104177457020372871, -5.624018123398955460, 42.75615561261992070 ) ) ;
#18116=EDGE_CURVE ( 'NONE', #56965, #4682, #7907, .T. ) ;
#18119=CARTESIAN_POINT ( 'NONE',  ( -6.015611763856276717, 18.68284711750058591, 2.453375430804133117 ) ) ;
#18120=B_SPLINE_CURVE_WITH_KNOTS ( 'NONE', 3,
 ( #55751, #46088, #50147, #55444, #32278, #31038 ),
 .UNSPECIFIED., .F., .F.,
 ( 4, 2, 4 ),
 ( 1.870559545977334001E-17, 0.0002293319059085111467, 0.0004586638118170035909 ),
 .UNSPECIFIED. ) ;
#18127=CARTESIAN_POINT ( 'NONE',  ( 0.6023142530420679819, 23.82662387835867079, -41.79260242564376426 ) ) ;
#18136=CARTESIAN_POINT ( 'NONE',  ( -6.016761891674564211, -7.214149619366230226, -17.40752468084790650 ) ) ;
#18141=( BOUNDED_SURFACE ( )  B_SPLINE_SURFACE ( 3, 1, ( 
 ( #50046, #45669 ),
 ( #17456, #2723 ),
 ( #12460, #21850 ),
 ( #40990, #60053 ) ),
 .UNSPECIFIED., .F., .F., .F. ) 
 B_SPLINE_SURFACE_WITH_KNOTS ( ( 4, 4 ),
 ( 2, 2 ),
 ( 0.000000000000000000, 1.000000000000000000 ),
 ( 0.000000000000000000, 1.000000000000000000 ),
 .UNSPECIFIED. ) 
 GEOMETRIC_REPRESENTATION_ITEM ( )  RATIONAL_B_SPLINE_SURFACE ( (
 ( 1.000000000000000000, 1.000000000000000000),
 ( 0.9953040768229005630, 0.8617119497784937465),
 ( 0.9953040768229005630, 0.8617119497784937465),
 ( 1.000000000000000000, 1.000000000000000000) ) ) 
 REPRESENTATION_ITEM ( '' )  SURFACE ( )  );
#18144=B_SPLINE_CURVE_WITH_KNOTS ( 'NONE', 3,
 ( #58109, #44372, #19624, #2955, #26153, #45290 ),
 .UNSPECIFIED., .F., .F.,
 ( 4, 2, 4 ),
 ( 1.426045310262811165E-18, 0.0002450742804987334172, 0.0004901485609974654250 ),
 .UNSPECIFIED. ) ;
#18148=B_SPLINE_CURVE_WITH_KNOTS ( 'NONE', 3,
 ( #53356, #1651, #1968, #11090 ),
 .UNSPECIFIED., .F., .F.,
 ( 4, 4 ),
 ( 0.000000000000000000, 0.005014147105413696050 ),
 .UNSPECIFIED. ) ;
#18149=ORIENTED_EDGE ( 'NONE', *, *, #5242, .F. ) ;
#18158=CARTESIAN_POINT ( 'NONE',  ( 4.975801465491694664, -27.09127437476410805, 39.51822597168447260 ) ) ;
#18161=EDGE_LOOP ( 'NONE', ( #41113, #12996, #29518, #15233 ) ) ;
#18165=CARTESIAN_POINT ( 'NONE',  ( 4.549368137175248350, 0.000000000000000000, 0.000000000000000000 ) ) ;
#18167=EDGE_CURVE ( 'NONE', #11343, #59975, #43784, .T. ) ;
#18168=CARTESIAN_POINT ( 'NONE',  ( 0.1073791018717483448, -33.91564619577824402, 26.63563652260111070 ) ) ;
#18177=CARTESIAN_POINT ( 'NONE',  ( 0.1073791018717483448, 39.65380858626214433, -16.95003405440273525 ) ) ;
#18178=ORIENTED_EDGE ( 'NONE', *, *, #25166, .T. ) ;
#18181=ADVANCED_FACE ( 'NONE', ( #44843 ), #18764, .F. ) ;
#18196=ORIENTED_EDGE ( 'NONE', *, *, #54172, .T. ) ;
#18204=ORIENTED_EDGE ( 'NONE', *, *, #43734, .F. ) ;
#18209=CARTESIAN_POINT ( 'NONE',  ( 0.6025881611877910160, 29.11258673756362114, 38.29866377863849891 ) ) ;
#18213=CARTESIAN_POINT ( 'NONE',  ( 0.2230388203127624258, 40.12182516270778621, 15.79641846944932304 ) ) ;
#18222=CARTESIAN_POINT ( 'NONE',  ( 4.975801465491694664, 15.94009207553051510, -45.18341283946441678 ) ) ;
#18226=CARTESIAN_POINT ( 'NONE',  ( 4.975801465491694664, -32.01766832630337944, 35.64402118370901462 ) ) ;
#18227=DIRECTION ( 'NONE',  ( 0.000000000000000000, 0.000000000000000000, 1.000000000000000000 ) ) ;
#18238=CARTESIAN_POINT ( 'NONE',  ( 0.1064266379913938465, -37.62465837278060121, -21.07422113734149605 ) ) ;
#18246=CARTESIAN_POINT ( 'NONE',  ( 0.8760168074886960365, -19.22870327415332525, 44.09317760313719958 ) ) ;
#18251=CARTESIAN_POINT ( 'NONE',  ( 4.975801465491695552, 0.000000000000000000, 0.000000000000000000 ) ) ;
#18252=AXIS2_PLACEMENT_3D ( 'NONE', #36575, #11855, #51258 ) ;
#18255=FACE_OUTER_BOUND ( 'NONE', #28344, .T. ) ;
#18265=ADVANCED_FACE ( 'NONE', ( #12551 ), #54411, .F. ) ;
#18268=CARTESIAN_POINT ( 'NONE',  ( -6.016489644550737204, -9.417787539062134172, -16.32089497094071717 ) ) ;
#18274=EDGE_CURVE ( 'NONE', #19530, #41175, #31643, .T. ) ;
#18276=ORIENTED_EDGE ( 'NONE', *, *, #19804, .T. ) ;
#18277=LINE ( 'NONE', #28575, #48301 ) ;
#18282=CARTESIAN_POINT ( 'NONE',  ( 0.6017667736363749853, -37.95278695280790515, -29.56223180955317886 ) ) ;
#18284=CARTESIAN_POINT ( 'NONE',  ( 4.975801465491695552, -8.787181743660504196, 47.10002938642126935 ) ) ;
#18286=EDGE_LOOP ( 'NONE', ( #19621, #50971, #10799, #44867 ) ) ;
#18287=ORIENTED_EDGE ( 'NONE', *, *, #25997, .F. ) ;
#18290=DIRECTION ( 'NONE',  ( 0.09835009131224564660, 0.1222230102474879260, 0.9876177374393978470 ) ) ;
#18291=FACE_OUTER_BOUND ( 'NONE', #19814, .T. ) ;
#18294=CARTESIAN_POINT ( 'NONE',  ( 0.1102847568649952675, -30.55869130182088611, -30.42833243501139862 ) ) ;
#18295=EDGE_LOOP ( 'NONE', ( #35724, #43954, #11531, #49496 ) ) ;
#18298=CARTESIAN_POINT ( 'NONE',  ( 0.6027935024548037868, -48.10716172909472022, -0.1745403365869804269 ) ) ;
#18306=CARTESIAN_POINT ( 'NONE',  ( 0.6025881611877910160, 34.17105830828415236, -33.86250327239859814 ) ) ;
#18309=ORIENTED_EDGE ( 'NONE', *, *, #48130, .F. ) ;
#18311=CARTESIAN_POINT ( 'NONE',  ( 4.975801465491695552, 0.000000000000000000, 0.000000000000000000 ) ) ;
#18312=CARTESIAN_POINT ( 'NONE',  ( 0.1101816497532063371, 39.78963561881064948, -16.62841624476636682 ) ) ;
#18319=B_SPLINE_CURVE_WITH_KNOTS ( 'NONE', 3,
 ( #25913, #39730, #58779, #35022 ),
 .UNSPECIFIED., .F., .F.,
 ( 4, 4 ),
 ( 1.999757930724972237E-17, 0.004444306975806117631 ),
 .UNSPECIFIED. ) ;
#18322=CARTESIAN_POINT ( 'NONE',  ( 0.1073791018717483448, -5.147744207007177053, 42.81622261970985477 ) ) ;
#18326=CARTESIAN_POINT ( 'NONE',  ( 0.5998501479064699549, -6.798102206413803472, -47.62484632993685807 ) ) ;
#18328=CARTESIAN_POINT ( 'NONE',  ( -5.995132425357893702, -4.885449473615459226, 18.19985213254570766 ) ) ;
#18330=CARTESIAN_POINT ( 'NONE',  ( -2.708315649062916552, 9.116606751444184198, 11.44805714186574619 ) ) ;
#18331=CARTESIAN_POINT ( 'NONE',  ( -2.569797478183783568, -14.24379821351254982, -3.352038560005866863 ) ) ;
#18332=CARTESIAN_POINT ( 'NONE',  ( 0.5998501479064699549, 29.69975237324562656, 37.84527566984866809 ) ) ;
#18333=ADVANCED_FACE ( 'NONE', ( #46995 ), #58809, .F. ) ;
#18340=CARTESIAN_POINT ( 'NONE',  ( 0.8760168074886965917, 29.98565522133346661, -37.61398439004502592 ) ) ;
#18341=CARTESIAN_POINT ( 'NONE',  ( 2.301430502907646058, -4.990893951996671518, -47.77346269870098894 ) ) ;
#18346=EDGE_CURVE ( 'NONE', #42579, #6671, #14093, .T. ) ;
#18353=CARTESIAN_POINT ( 'NONE',  ( 0.1092565886968784594, -43.12345370280014123, 0.3103822814778426920 ) ) ;
#18355=FACE_OUTER_BOUND ( 'NONE', #49393, .T. ) ;
#18360=CARTESIAN_POINT ( 'NONE',  ( 0.6031357023905875581, -44.42879114414645159, -18.45021748202266920 ) ) ;
#18370=CARTESIAN_POINT ( 'NONE',  ( 0.7048096507298635682, 17.62869676200410396, -44.76417498422297570 ) ) ;
#18372=CARTESIAN_POINT ( 'NONE',  ( 4.549368137175248350, -42.82045902618774136, 3.018832571115817487 ) ) ;
#18374=DIRECTION ( 'NONE',  ( 0.000000000000000000, 0.000000000000000000, 1.000000000000000000 ) ) ;
#18376=CARTESIAN_POINT ( 'NONE',  ( 4.549368137175248350, 42.14271863032822552, 8.166781970325878603 ) ) ;
#18394=( BOUNDED_SURFACE ( )  B_SPLINE_SURFACE ( 3, 1, ( 
 ( #36042, #55104 ),
 ( #31312, #50415 ),
 ( #26607, #21922 ),
 ( #9043, #13772 ) ),
 .UNSPECIFIED., .F., .F., .F. ) 
 B_SPLINE_SURFACE_WITH_KNOTS ( ( 4, 4 ),
 ( 2, 2 ),
 ( 0.000000000000000000, 1.000000000000000000 ),
 ( 0.000000000000000000, 1.000000000000000000 ),
 .UNSPECIFIED. ) 
 GEOMETRIC_REPRESENTATION_ITEM ( )  RATIONAL_B_SPLINE_SURFACE ( (
 ( 1.000000000000000000, 1.000000000000000000),
 ( 0.9751682680413298332, 0.9999560080971552356),
 ( 0.9751682680413298332, 0.9999560080971552356),
 ( 1.000000000000000000, 1.000000000000000000) ) ) 
 REPRESENTATION_ITEM ( '' )  SURFACE ( )  );
#18396=CARTESIAN_POINT ( 'NONE',  ( 0.5998501479064699549, -29.69975237324587169, -37.84527566984847624 ) ) ;
#18400=CARTESIAN_POINT ( 'NONE',  ( 0.1100053167205930910, 16.33707796615706442, -39.91014771056761390 ) ) ;
#18407=EDGE_CURVE ( 'NONE', #37210, #38521, #16543, .T. ) ;
#18415=CARTESIAN_POINT ( 'NONE',  ( 0.6031356755773454870, 47.69588082432148468, 6.279255973231509635 ) ) ;
#18418=CARTESIAN_POINT ( 'NONE',  ( 0.1084644655670280594, -5.234391617064312108, 42.80575641816238885 ) ) ;
#18428=B_SPLINE_CURVE_WITH_KNOTS ( 'NONE', 3,
 ( #57618, #14750, #18213, #32936, #33865, #10042 ),
 .UNSPECIFIED., .F., .F.,
 ( 4, 2, 4 ),
 ( 8.461795104084953648E-17, 0.0002293366620881437921, 0.0004586733241762029623 ),
 .UNSPECIFIED. ) ;
#18433=VECTOR ( 'NONE', #6092, 1000.000000000000227 ) ;
#18439=CARTESIAN_POINT ( 'NONE',  ( 4.322998006666179727, 47.94177812210864431, -2.120302895115782515 ) ) ;
#18448=ORIENTED_EDGE ( 'NONE', *, *, #45014, .T. ) ;
#18458=VERTEX_POINT ( 'NONE', #1192 ) ;
#18463=ADVANCED_FACE ( 'NONE', ( #5874 ), #43672, .F. ) ;
#18465=CARTESIAN_POINT ( 'NONE',  ( 4.975801465491694664, -47.84403947906841381, 2.564218696447319257 ) ) ;
#18477=CARTESIAN_POINT ( 'NONE',  ( 0.5998501479064708430, 24.50586714782604858, -41.39809967730462859 ) ) ;
#18479=CARTESIAN_POINT ( 'NONE',  ( 4.549368137175248350, -42.14271863032838894, 8.166781970325002860 ) ) ;
#18485=CARTESIAN_POINT ( 'NONE',  ( 4.975801465491695552, 21.70134120755140827, 42.71626295676271212 ) ) ;
#18486=ADVANCED_FACE ( 'NONE', ( #39446 ), #28819, .F. ) ;
#18488=CARTESIAN_POINT ( 'NONE',  ( 4.691466044806102076, -36.88741755356052465, -25.04870410140776116 ) ) ;
#18495=EDGE_LOOP ( 'NONE', ( #5526, #46709, #2068, #56186 ) ) ;
#18497=LINE ( 'NONE', #22274, #52882 ) ;
#18499=CARTESIAN_POINT ( 'NONE',  ( -6.015611763856276717, 16.32183393015609951, -9.416239407363130809 ) ) ;
#18502=CARTESIAN_POINT ( 'NONE',  ( 4.833616638992208614, 9.466882727841500866, 45.27110352095250789 ) ) ;
#18512=CARTESIAN_POINT ( 'NONE',  ( 4.549368137175248350, 2.596185425821941894, -42.84816078363927971 ) ) ;
#18517=DIRECTION ( 'NONE',  ( 0.000000000000000000, 0.000000000000000000, 1.000000000000000000 ) ) ;
#18523=CARTESIAN_POINT ( 'NONE',  ( 4.549368137175248350, 35.57418903283115696, -24.02461520945233531 ) ) ;
#18531=ORIENTED_EDGE ( 'NONE', *, *, #12697, .T. ) ;
#18533=VERTEX_POINT ( 'NONE', #36585 ) ;
#18536=VERTEX_POINT ( 'NONE', #55349 ) ;
#18543=CARTESIAN_POINT ( 'NONE',  ( 0.1073791018717483448, 30.83464511437097499, 30.14884492832400298 ) ) ;
#18546=CARTESIAN_POINT ( 'NONE',  ( -6.010958268070873523, 7.197664668556679857, -17.41463273278770885 ) ) ;
#18549=EDGE_CURVE ( 'NONE', #44283, #56469, #44438, .T. ) ;
#18551=CARTESIAN_POINT ( 'NONE',  ( -6.016489644550737204, -16.32089497094068520, 9.417787539062191016 ) ) ;
#18552=VECTOR ( 'NONE', #18290, 1000.000000000000000 ) ;
#18555=CARTESIAN_POINT ( 'NONE',  ( 0.09136607875274982415, 1.224646799147353256E-15, -10.00000000000000000 ) ) ;
#18557=CARTESIAN_POINT ( 'NONE',  ( 0.8760168074886960365, 42.09738177923954083, -23.27577685234554394 ) ) ;
#18571=ORIENTED_EDGE ( 'NONE', *, *, #9760, .F. ) ;
#18573=CARTESIAN_POINT ( 'NONE',  ( 4.322998006666179727, -45.75942687572307932, 14.45630056002860364 ) ) ;
#18574=CARTESIAN_POINT ( 'NONE',  ( 4.975801465491695552, -32.01766832630288206, -35.64402118370946937 ) ) ;
#18585=ORIENTED_EDGE ( 'NONE', *, *, #48302, .T. ) ;
#18590=EDGE_CURVE ( 'NONE', #60753, #38461, #335, .T. ) ;
#18593=VERTEX_POINT ( 'NONE', #60352 ) ;
#18596=EDGE_CURVE ( 'NONE', #58608, #2051, #36287, .T. ) ;
#18601=EDGE_CURVE ( 'NONE', #61780, #20011, #48190, .T. ) ;
#18603=CARTESIAN_POINT ( 'NONE',  ( -6.015611763856276717, 11.46610900684744472, -14.95313250337417799 ) ) ;
#18613=CARTESIAN_POINT ( 'NONE',  ( 0.8751705887134423323, 24.81530984069208401, -41.19904111682483716 ) ) ;
#18616=CARTESIAN_POINT ( 'NONE',  ( 3.680974057930773924, -47.94008194857089222, -1.849713332883580197 ) ) ;
#18620=B_SPLINE_CURVE_WITH_KNOTS ( 'NONE', 3,
 ( #9854, #39931, #58989, #28956, #34908, #24569, #43390, #19571, #57745, #33984, #29255, #48370, #5432, #43701, #48675, #53360 ),
 .UNSPECIFIED., .F., .F.,
 ( 4, 3, 3, 3, 3, 4 ),
 ( 2.194378057379452319E-17, 0.0002618515315864421394, 0.0003927756766341980454, 0.0005236998216950549626, 0.0007855159896329901156, 0.001047349442285927437 ),
 .UNSPECIFIED. ) ;
#18625=CARTESIAN_POINT ( 'NONE',  ( 4.833616638992205949, 8.578242093415124003, 45.44786513329600552 ) ) ;
#18632=CARTESIAN_POINT ( 'NONE',  ( 0.1073791018717578927, 40.02496097243057704, -16.05399293000775529 ) ) ;
#18643=EDGE_CURVE ( 'NONE', #35726, #7624, #19793, .T. ) ;
#18644=B_SPLINE_CURVE_WITH_KNOTS ( 'NONE', 3,
 ( #56259, #22455, #41895, #14305, #47501, #42817 ),
 .UNSPECIFIED., .F., .F.,
 ( 4, 2, 4 ),
 ( 2.224174099750402954E-17, 0.0002293319059085117972, 0.0004586638118170013141 ),
 .UNSPECIFIED. ) ;
#18646=CARTESIAN_POINT ( 'NONE',  ( -6.016104459813371719, -17.41090761020830868, -7.206059014950265684 ) ) ;
#18651=CARTESIAN_POINT ( 'NONE',  ( 0.6031357023905875581, -46.45693331047449703, -12.49325238079521760 ) ) ;
#18658=CARTESIAN_POINT ( 'NONE',  ( -6.001507490154111224, -14.95933060264881753, 11.45906331631425878 ) ) ;
#18663=B_SPLINE_CURVE_WITH_KNOTS ( 'NONE', 3,
 ( #53508, #58511, #34745, #15640 ),
 .UNSPECIFIED., .F., .F.,
 ( 4, 4 ),
 ( 0.000000000000000000, 0.004445488388166995986 ),
 .UNSPECIFIED. ) ;
#18664=ORIENTED_EDGE ( 'NONE', *, *, #4601, .F. ) ;
#18670=ADVANCED_FACE ( 'NONE', ( #38444 ), #58437, .F. ) ;
#18672=EDGE_CURVE ( 'NONE', #58253, #47464, #35805, .T. ) ;
#18674=DIRECTION ( 'NONE',  ( 0.1024043820194936449, 0.3927886084231570485, 0.9139094329506647352 ) ) ;
#18676=EDGE_CURVE ( 'NONE', #28479, #57072, #22066, .T. ) ;
#18678=CARTESIAN_POINT ( 'NONE',  ( -6.010958268070873523, 13.31406649671981413, -13.33459572764743584 ) ) ;
#18679=ORIENTED_EDGE ( 'NONE', *, *, #29340, .F. ) ;
#18682=LINE ( 'NONE', #58094, #55643 ) ;
#18685=ORIENTED_EDGE ( 'NONE', *, *, #18407, .T. ) ;
#18690=ORIENTED_EDGE ( 'NONE', *, *, #45884, .F. ) ;
#18692=CONICAL_SURFACE ( 'NONE', #38694, 42.92674063221959813, 1.485477209440487556 ) ;
#18696=EDGE_CURVE ( 'NONE', #9817, #31225, #46920, .T. ) ;
#18698=VERTEX_POINT ( 'NONE', #37521 ) ;
#18702=ORIENTED_EDGE ( 'NONE', *, *, #34006, .F. ) ;
#18703=CARTESIAN_POINT ( 'NONE',  ( 0.6028618097248862329, -29.42431480658704501, -38.05975027458327276 ) ) ;
#18706=CARTESIAN_POINT ( 'NONE',  ( 0.6031356755773454870, 47.69587413076373394, -6.279306815850331347 ) ) ;
#18708=CARTESIAN_POINT ( 'NONE',  ( 0.1103878639767399278, 16.45816205842763935, -39.86034920885569477 ) ) ;
#18709=ORIENTED_EDGE ( 'NONE', *, *, #12348, .F. ) ;
#18717=CARTESIAN_POINT ( 'NONE',  ( -6.016761891674564211, -14.95139917749696501, -11.46828378093574941 ) ) ;
#18720=CARTESIAN_POINT ( 'NONE',  ( 0.7954190325252781246, -41.21355377862716551, 24.79809930825913256 ) ) ;
#18721=CONICAL_SURFACE ( 'NONE', #12739, 42.92674063221959813, 1.485477209440487556 ) ;
#18735=B_SPLINE_CURVE_WITH_KNOTS ( 'NONE', 3,
 ( #35359, #20626, #59125, #12168, #11538, #11229, #44763, #11865, #59434, #16236, #54415, #49740, #6797, #12470, #31255, #25939, #35668, #54107, #2730 ),
 .UNSPECIFIED., .F., .F.,
 ( 4, 3, 3, 3, 3, 3, 4 ),
 ( 1.161956753697875813E-16, 0.0002618519381806249952, 0.0003927759815485967884, 0.0005237000248299413701, 0.0006546240681324970662, 0.0007855481115631314081, 0.0009699050456655111587 ),
 .UNSPECIFIED. ) ;
#18738=VECTOR ( 'NONE', #20076, 1000.000000000000000 ) ;
#18743=CIRCLE ( 'NONE', #55739, 42.92674063221959813 ) ;
#18746=EDGE_CURVE ( 'NONE', #51963, #27614, #58580, .T. ) ;
#18747=CARTESIAN_POINT ( 'NONE',  ( 5.880360259849752858, 15.37531919565172878, 45.44137230084887591 ) ) ;
#18750=ORIENTED_EDGE ( 'NONE', *, *, #33911, .T. ) ;
#18764=CONICAL_SURFACE ( 'NONE', #39803, 42.92674063221959813, 1.485477209440487556 ) ;
#18766=CARTESIAN_POINT ( 'NONE',  ( 0.8751705887134423323, 33.37254303619506857, 34.63284514348596588 ) ) ;
#18770=EDGE_CURVE ( 'NONE', #351, #42525, #53121, .T. ) ;
#18773=CARTESIAN_POINT ( 'NONE',  ( 4.691466044806102964, 43.66525414675629690, 9.025781474741620514 ) ) ;
#18778=CARTESIAN_POINT ( 'NONE',  ( -5.995132425357893702, 11.46484027925367499, 14.95525565067279139 ) ) ;
#18789=CARTESIAN_POINT ( 'NONE',  ( -6.016104459813374383, -16.31603998697563540, -9.426230926598815785 ) ) ;
#18790=EDGE_LOOP ( 'NONE', ( #54470, #54462, #58098, #59234 ) ) ;
#18799=CARTESIAN_POINT ( 'NONE',  ( 0.3622758884714730732, -42.62881903538215056, 6.444611261693867554 ) ) ;
#18800=APPLICATION_CONTEXT ( 'automotive_design' ) ;
#18805=CARTESIAN_POINT ( 'NONE',  ( 0.8760168074886960365, 24.81951362746078260, -41.20610493656884898 ) ) ;
#18806=CARTESIAN_POINT ( 'NONE',  ( 4.549368137175248350, 40.58005590356690817, -13.99871866169321599 ) ) ;
#18810=B_SPLINE_CURVE_WITH_KNOTS ( 'NONE', 3,
 ( #38042, #57087, #5077, #53013, #33626, #33325 ),
 .UNSPECIFIED., .F., .F.,
 ( 4, 2, 4 ),
 ( 3.511543213478341086E-18, 0.0002450742804987349893, 0.0004901485609974664008 ),
 .UNSPECIFIED. ) ;
#18812=B_SPLINE_CURVE_WITH_KNOTS ( 'NONE', 3,
 ( #58065, #5131, #57135, #33069 ),
 .UNSPECIFIED., .F., .F.,
 ( 4, 4 ),
 ( 2.292215966409847280E-17, 0.004564976165746185977 ),
 .UNSPECIFIED. ) ;
#18814=CARTESIAN_POINT ( 'NONE',  ( -6.001507490154111224, 14.95933060264889392, -11.45906331631416286 ) ) ;
#18818=CARTESIAN_POINT ( 'NONE',  ( 0.8751705887134423323, -38.69254731947852832, 28.56654290188588163 ) ) ;
#18827=EDGE_CURVE ( 'NONE', #5237, #44283, #11579, .T. ) ;
#18832=CARTESIAN_POINT ( 'NONE',  ( 0.6041374136657475802, -38.05989626241411372, -29.42442150067184059 ) ) ;
#18836=CARTESIAN_POINT ( 'NONE',  ( 0.5998501479064699549, 33.64490850298844293, -34.38546660123262200 ) ) ;
#18837=EDGE_CURVE ( 'NONE', #39132, #43794, #45212, .T. ) ;
#18840=CARTESIAN_POINT ( 'NONE',  ( -6.015611763856276717, 17.41126425312538117, 7.205255340944677123 ) ) ;
#18856=ADVANCED_FACE ( 'NONE', ( #19952 ), #35245, .F. ) ;
#18867=CARTESIAN_POINT ( 'NONE',  ( 4.975801465491695552, 0.000000000000000000, 0.000000000000000000 ) ) ;
#18872=CARTESIAN_POINT ( 'NONE',  ( 0.5980894510889448457, 48.10766805928368228, 0.7015180096006546906 ) ) ;
#18876=CARTESIAN_POINT ( 'NONE',  ( 0.6001305935487422083, -28.87057754790912156, -38.48510059944036499 ) ) ;
#18880=CARTESIAN_POINT ( 'NONE',  ( 0.5998501479064708430, -41.39809967730470674, -24.50586714782589937 ) ) ;
#18885=CARTESIAN_POINT ( 'NONE',  ( -6.016761891674564211, -11.47373234755493243, -14.94721834528426463 ) ) ;
#18887=DIRECTION ( 'NONE',  ( -1.000000000000000000, -0.000000000000000000, -0.000000000000000000 ) ) ;
#18898=ORIENTED_EDGE ( 'NONE', *, *, #46659, .T. ) ;
#18928=CARTESIAN_POINT ( 'NONE',  ( 0.1084644655670283925, 6.022910953206533691, 42.70194587816330767 ) ) ;
#18929=EDGE_CURVE ( 'NONE', #32930, #10204, #31817, .T. ) ;
#18930=ORIENTED_EDGE ( 'NONE', *, *, #49357, .F. ) ;
#18939=CARTESIAN_POINT ( 'NONE',  ( 0.5988103564986357874, 38.53259703935791691, 28.80261217992934419 ) ) ;
#18940=AXIS2_PLACEMENT_3D ( 'NONE', #37214, #32504, #40691 ) ;
#18941=EDGE_LOOP ( 'NONE', ( #57424, #31775, #23832, #39439 ) ) ;
#18945=CARTESIAN_POINT ( 'NONE',  ( 0.1073791018717483448, -39.65380858626227223, 16.95003405440244038 ) ) ;
#18946=FACE_OUTER_BOUND ( 'NONE', #60846, .T. ) ;
#18947=CARTESIAN_POINT ( 'NONE',  ( 0.6001305935487422083, 28.87057754790937381, -38.48510059944018735 ) ) ;
#18948=CARTESIAN_POINT ( 'NONE',  ( -6.015611763856276717, -4.882992715191428523, 18.19956619163656697 ) ) ;
#18954=CARTESIAN_POINT ( 'NONE',  ( -6.015611763856276717, 2.465697960551318069, -18.68122482568277221 ) ) ;
#18957=B_SPLINE_CURVE_WITH_KNOTS ( 'NONE', 3,
 ( #40272, #60868, #50859, #60556, #31451, #60248, #51464, #56176, #36795, #17363, #8247, #21747, #55867, #41184, #32392, #13285, #36174, #55239, #22363 ),
 .UNSPECIFIED., .F., .F.,
 ( 4, 3, 3, 3, 3, 3, 4 ),
 ( 1.149162571898268292E-16, 0.0002618519381806292778, 0.0003927759815485966258, 0.0005237000248299431048, 0.0006546240681324950062, 0.0007855481115631322755, 0.0009699050456655125682 ),
 .UNSPECIFIED. ) ;
#18960=CARTESIAN_POINT ( 'NONE',  ( 0.8751705887134423323, -33.37254303619531726, -34.63284514348573850 ) ) ;
#18982=DIRECTION ( 'NONE',  ( 0.000000000000000000, 0.000000000000000000, -1.000000000000000000 ) ) ;
#18983=DIRECTION ( 'NONE',  ( 0.09835009131224552170, -0.2650256080583695550, -0.9592125346408710840 ) ) ;
#18989=CONICAL_SURFACE ( 'NONE', #1909, 42.92674063221959813, 1.485477209440487556 ) ;
#18998=CARTESIAN_POINT ( 'NONE',  ( -2.569797478183790229, -6.924386868080758539, -12.89088113963433457 ) ) ;
#19003=LINE ( 'NONE', #38119, #57732 ) ;
#19005=EDGE_CURVE ( 'NONE', #23785, #33784, #52813, .T. ) ;
#19006=ORIENTED_EDGE ( 'NONE', *, *, #43228, .T. ) ;
#19010=FACE_OUTER_BOUND ( 'NONE', #15378, .T. ) ;
#19017=ORIENTED_EDGE ( 'NONE', *, *, #60703, .F. ) ;
#19020=CARTESIAN_POINT ( 'NONE',  ( 4.975801465491694664, -26.14269827151650816, -40.15204426031524321 ) ) ;
#19026=CARTESIAN_POINT ( 'NONE',  ( 0.6023143664670691511, 29.49326149840232247, -38.00627775314932677 ) ) ;
#19034=ORIENTED_EDGE ( 'NONE', *, *, #32303, .T. ) ;
#19037=CARTESIAN_POINT ( 'NONE',  ( 0.1073791018717483448, -39.65380858626227223, 16.95003405440244038 ) ) ;
#19039=CARTESIAN_POINT ( 'NONE',  ( 0.8751705887134423323, 47.79200036674280483, -5.393078191592203474 ) ) ;
#19041=B_SPLINE_CURVE_WITH_KNOTS ( 'NONE', 3,
 ( #30255, #1427, #830, #6729 ),
 .UNSPECIFIED., .F., .F.,
 ( 4, 4 ),
 ( 0.000000000000000000, 0.005014147105413705591 ),
 .UNSPECIFIED. ) ;
#19046=CARTESIAN_POINT ( 'NONE',  ( 0.6028618097248862329, 47.71844004092979930, 6.106174977919211599 ) ) ;
#19047=CARTESIAN_POINT ( 'NONE',  ( 0.8751705887134553219, 28.56654290188653178, -38.69254731947804515 ) ) ;
#19048=EDGE_CURVE ( 'NONE', #32640, #44566, #61645, .T. ) ;
#19056=CARTESIAN_POINT ( 'NONE',  ( 0.6028618097248864549, -38.05975027458356408, 29.42431480658666132 ) ) ;
#19059=B_SPLINE_CURVE_WITH_KNOTS ( 'NONE', 3,
 ( #9224, #23949, #48067, #24247, #9850, #5427, #19567, #28951, #52748, #42460, #24563, #743, #8923, #38378, #43385, #57740, #43074, #61520, #33365 ),
 .UNSPECIFIED., .F., .F.,
 ( 4, 3, 3, 3, 3, 3, 4 ),
 ( 1.138109825968292890E-16, 0.0002618519381806256457, 0.0003927759815485970594, 0.0005237000248299464658, 0.0006546240681324991262, 0.0007855481115631363954, 0.0009699050456655126766 ),
 .UNSPECIFIED. ) ;
#19062=FACE_OUTER_BOUND ( 'NONE', #26938, .T. ) ;
#19067=EDGE_CURVE ( 'NONE', #32330, #27931, #13758, .T. ) ;
#19072=CARTESIAN_POINT ( 'NONE',  ( -6.016104459813371719, -13.32794178584988209, -13.32039631884698494 ) ) ;
#19076=DIRECTION ( 'NONE',  ( 0.000000000000000000, 0.000000000000000000, -1.000000000000000000 ) ) ;
#19088=CARTESIAN_POINT ( 'NONE',  ( -4.908599999999998964, 9.539392014169456147, 3.000000000000000000 ) ) ;
#19092=ORIENTED_EDGE ( 'NONE', *, *, #46640, .T. ) ;
#19100=CARTESIAN_POINT ( 'NONE',  ( 0.1097557419366048670, 30.65094619415025434, 30.33543403792248228 ) ) ;
#19101=CARTESIAN_POINT ( 'NONE',  ( 0.1087620492084205165, -34.43219573047449700, 25.96440931622072767 ) ) ;
#19102=B_SPLINE_CURVE_WITH_KNOTS ( 'NONE', 3,
 ( #33141, #13726, #9311, #28412, #47539, #23727 ),
 .UNSPECIFIED., .F., .F.,
 ( 4, 2, 4 ),
 ( 1.553373257785006303E-17, 0.0002293319059085063220, 0.0004586638118169971399 ),
 .UNSPECIFIED. ) ;
#19107=EDGE_CURVE ( 'NONE', #42620, #29913, #56205, .T. ) ;
#19109=CARTESIAN_POINT ( 'NONE',  ( 0.8760168074886965917, 37.61398439004493355, 29.98565522133359806 ) ) ;
#19115=CARTESIAN_POINT ( 'NONE',  ( 0.6023142530420679819, 0.2618396477460823712, 48.10676733004997629 ) ) ;
#19124=EDGE_CURVE ( 'NONE', #32260, #57388, #39958, .T. ) ;
#19133=FACE_OUTER_BOUND ( 'NONE', #11360, .T. ) ;
#19138=( BOUNDED_SURFACE ( )  B_SPLINE_SURFACE ( 3, 1, ( 
 ( #182, #61589 ),
 ( #37523, #23712 ),
 ( #56592, #47839 ),
 ( #52508, #9597 ) ),
 .UNSPECIFIED., .F., .F., .F. ) 
 B_SPLINE_SURFACE_WITH_KNOTS ( ( 4, 4 ),
 ( 2, 2 ),
 ( 0.000000000000000000, 1.000000000000000000 ),
 ( 0.000000000000000000, 1.000000000000000000 ),
 .UNSPECIFIED. ) 
 GEOMETRIC_REPRESENTATION_ITEM ( )  RATIONAL_B_SPLINE_SURFACE ( (
 ( 1.000000000000000000, 1.000000000000000000),
 ( 0.7223157951917480446, 0.9931996967497186413),
 ( 0.7223157951917480446, 0.9931996967497186413),
 ( 1.000000000000000000, 1.000000000000000000) ) ) 
 REPRESENTATION_ITEM ( '' )  SURFACE ( )  );
#19152=ORIENTED_EDGE ( 'NONE', *, *, #6824, .T. ) ;
#19157=CARTESIAN_POINT ( 'NONE',  ( 0.6001305935487422083, 46.33281397023046821, 12.95698906763824709 ) ) ;
#19158=VERTEX_POINT ( 'NONE', #58978 ) ;
#19162=ORIENTED_EDGE ( 'NONE', *, *, #6777, .T. ) ;
#19164=CARTESIAN_POINT ( 'NONE',  ( 0.8760168074886960365, -42.09738177923970426, 23.27577685234524907 ) ) ;
#19170=CARTESIAN_POINT ( 'NONE',  ( -6.016761891674564211, 11.46828378093580980, -14.95139917749692415 ) ) ;
#19175=CARTESIAN_POINT ( 'NONE',  ( 0.2224561200757577961, -40.12166550582823277, 15.79689521915794614 ) ) ;
#19178=LINE ( 'NONE', #9754, #37870 ) ;
#19184=EDGE_CURVE ( 'NONE', #11109, #5908, #34823, .T. ) ;
#19185=CARTESIAN_POINT ( 'NONE',  ( -6.016104459813374383, -2.454244026260969047, -18.68271063303497215 ) ) ;
#19190=CARTESIAN_POINT ( 'NONE',  ( 0.6027935024548037868, 48.10716172909472022, 0.1745403365873163526 ) ) ;
#19200=ORIENTED_EDGE ( 'NONE', *, *, #21868, .T. ) ;
#19212=CARTESIAN_POINT ( 'NONE',  ( 0.6027935024548038978, -38.05972402498757390, -29.42425667880423035 ) ) ;
#19213=ORIENTED_EDGE ( 'NONE', *, *, #27355, .F. ) ;
#19214=CARTESIAN_POINT ( 'NONE',  ( 0.5998501479064708430, -6.798102206414489146, 47.62484632993676570 ) ) ;
#19216=ORIENTED_EDGE ( 'NONE', *, *, #49006, .F. ) ;
#19218=VERTEX_POINT ( 'NONE', #34274 ) ;
#19219=CARTESIAN_POINT ( 'NONE',  ( 0.1064266379913942628, 15.98292486309336624, -40.05351204369889473 ) ) ;
#19220=CARTESIAN_POINT ( 'NONE',  ( 4.549368137175248350, 0.000000000000000000, 0.000000000000000000 ) ) ;
#19221=B_SPLINE_CURVE_WITH_KNOTS ( 'NONE', 3,
 ( #58840, #22500, #4285, #32844 ),
 .UNSPECIFIED., .F., .F.,
 ( 4, 4 ),
 ( 0.000000000000000000, 0.004445488388166993383 ),
 .UNSPECIFIED. ) ;
#19225=EDGE_CURVE ( 'NONE', #24495, #38023, #31720, .T. ) ;
#19235=FACE_OUTER_BOUND ( 'NONE', #21139, .T. ) ;
#19265=FACE_OUTER_BOUND ( 'NONE', #4833, .T. ) ;
#19266=DIRECTION ( 'NONE',  ( -1.000000000000000000, -0.000000000000000000, -0.000000000000000000 ) ) ;
#19268=CARTESIAN_POINT ( 'NONE',  ( 2.643462169533600914, -48.01657676222236404, -1.382267876918291893 ) ) ;
#19272=VERTEX_POINT ( 'NONE', #18477 ) ;
#19279=ORIENTED_EDGE ( 'NONE', *, *, #50439, .F. ) ;
#19281=CARTESIAN_POINT ( 'NONE',  ( 0.2885697896453102151, -29.91358794843040769, -31.05173034173360591 ) ) ;
#19290=CARTESIAN_POINT ( 'NONE',  ( 0.5998501479064708430, 41.92175333043619645, -23.59887241503310307 ) ) ;
#19294=ORIENTED_EDGE ( 'NONE', *, *, #32618, .T. ) ;
#19295=CARTESIAN_POINT ( 'NONE',  ( 4.833616638992208614, -46.11947910922911831, 3.476827473557080772 ) ) ;
#19321=CARTESIAN_POINT ( 'NONE',  ( 4.833616638992205949, 20.86133030530291421, -41.27831852777620725 ) ) ;
#19323=FACE_OUTER_BOUND ( 'NONE', #5076, .T. ) ;
#19324=CARTESIAN_POINT ( 'NONE',  ( 0.1100247026804066219, 16.65964013375385733, -39.77655614012837759 ) ) ;
#19327=FACE_OUTER_BOUND ( 'NONE', #12929, .T. ) ;
#19329=VERTEX_POINT ( 'NONE', #14104 ) ;
#19330=ADVANCED_FACE ( 'NONE', ( #5578 ), #38854, .F. ) ;
#19333=CARTESIAN_POINT ( 'NONE',  ( -6.016104459813371719, -7.215917642688938649, -17.40682403289256541 ) ) ;
#19352=B_SPLINE_CURVE_WITH_KNOTS ( 'NONE', 3,
 ( #38123, #9575, #38420, #37187 ),
 .UNSPECIFIED., .F., .F.,
 ( 4, 4 ),
 ( 2.343940034265377226E-17, 0.004564976165746189446 ),
 .UNSPECIFIED. ) ;
#19353=CARTESIAN_POINT ( 'NONE',  ( 4.322998006666165516, -47.80838462754068274, 4.155494336617899798 ) ) ;
#19354=B_SPLINE_CURVE_WITH_KNOTS ( 'NONE', 3,
 ( #5466, #21132, #54307, #6374, #11129, #6687 ),
 .UNSPECIFIED., .F., .F.,
 ( 4, 2, 4 ),
 ( 1.260375116100749216E-16, 0.0002450741128632348900, 0.0004901482257263436873 ),
 .UNSPECIFIED. ) ;
#19359=EDGE_LOOP ( 'NONE', ( #41075, #24376, #1598, #43121 ) ) ;
#19366=CARTESIAN_POINT ( 'NONE',  ( 0.6001305935487422083, -44.64600790884068005, 17.92615948558462691 ) ) ;
#19371=CARTESIAN_POINT ( 'NONE',  ( 4.975801465491694664, -40.15204426031552032, 26.14269827151608894 ) ) ;
#19376=ORIENTED_EDGE ( 'NONE', *, *, #48974, .T. ) ;
#19392=VERTEX_POINT ( 'NONE', #37923 ) ;
#19400=CARTESIAN_POINT ( 'NONE',  ( -6.016761891674565099, -16.31696541414265766, -9.424569481870424426 ) ) ;
#19406=CARTESIAN_POINT ( 'NONE',  ( 4.549368137175248350, -42.14271863032827525, -8.166781970325585505 ) ) ;
#19418=CARTESIAN_POINT ( 'NONE',  ( 3.680974057930775700, 22.36814223828908865, 42.44218549341218250 ) ) ;
#19419=CARTESIAN_POINT ( 'NONE',  ( -2.569797478183783568, 9.259773107242914136, 11.33042594333551278 ) ) ;
#19426=CARTESIAN_POINT ( 'NONE',  ( 0.1073791018717483448, 37.58707531572176919, 21.14095454447572564 ) ) ;
#19431=DIRECTION ( 'NONE',  ( 0.09835009131224567436, 0.9632152266566422760, -0.2500873580884609981 ) ) ;
#19435=ORIENTED_EDGE ( 'NONE', *, *, #286, .T. ) ;
#19445=VERTEX_POINT ( 'NONE', #15639 ) ;
#19447=AXIS2_PLACEMENT_3D ( 'NONE', #47162, #23042, #50595 ) ;
#19448=VERTEX_POINT ( 'NONE', #34744 ) ;
#19449=EDGE_CURVE ( 'NONE', #3592, #34476, #16740, .T. ) ;
#19462=CARTESIAN_POINT ( 'NONE',  ( 5.880360259849739535, -43.00389496650629440, 21.25991003419878211 ) ) ;
#19475=CARTESIAN_POINT ( 'NONE',  ( 0.5998501479064699549, 38.48283596221989455, 28.86886762351138103 ) ) ;
#19479=CARTESIAN_POINT ( 'NONE',  ( 0.6017667736363750963, 18.73201910948661819, -44.31084570541182188 ) ) ;
#19484=CARTESIAN_POINT ( 'NONE',  ( 4.975801465491695552, 20.67815041659141784, -43.22084481528199973 ) ) ;
#19489=FACE_OUTER_BOUND ( 'NONE', #21134, .T. ) ;
#19511=ORIENTED_EDGE ( 'NONE', *, *, #28160, .F. ) ;
#19516=ORIENTED_EDGE ( 'NONE', *, *, #46483, .T. ) ;
#19520=ORIENTED_EDGE ( 'NONE', *, *, #34303, .T. ) ;
#19528=CARTESIAN_POINT ( 'NONE',  ( 0.6028618097248863439, -48.10721794025128162, 0.1745704727164173742 ) ) ;
#19530=VERTEX_POINT ( 'NONE', #8365 ) ;
#19534=CARTESIAN_POINT ( 'NONE',  ( 0.8760168074886960365, -44.77533136581894269, 17.58183840866320935 ) ) ;
#19537=ADVANCED_FACE ( 'NONE', ( #12180 ), #24428, .F. ) ;
#19538=CARTESIAN_POINT ( 'NONE',  ( 0.1102144999581332746, 5.503895401229410567, 42.77179372778545030 ) ) ;
#19539=B_SPLINE_CURVE_WITH_KNOTS ( 'NONE', 3,
 ( #8040, #2712, #21840, #60041, #12770, #17149 ),
 .UNSPECIFIED., .F., .F.,
 ( 4, 2, 4 ),
 ( 8.554130121340520410E-17, 0.0002293366620881447950, 0.0004586733241762040465 ),
 .UNSPECIFIED. ) ;
#19546=VERTEX_POINT ( 'NONE', #46308 ) ;
#19548=CARTESIAN_POINT ( 'NONE',  ( 4.975801465491695552, 39.51822597168496287, -27.09127437476339395 ) ) ;
#19551=VECTOR ( 'NONE', #57769, 1000.000000000000114 ) ;
#19553=VERTEX_POINT ( 'NONE', #45692 ) ;
#19554=DIRECTION ( 'NONE',  ( 0.000000000000000000, 0.000000000000000000, 1.000000000000000000 ) ) ;
#19560=CARTESIAN_POINT ( 'NONE',  ( 0.1064266379913940130, -17.02047542254822687, -39.62374453032489896 ) ) ;
#19561=CARTESIAN_POINT ( 'NONE',  ( 2.301430502907647391, 28.20897229937352435, 38.87758534782515341 ) ) ;
#19563=CARTESIAN_POINT ( 'NONE',  ( 0.5998501479064708430, -47.76154736470761719, 5.759754759339972274 ) ) ;
#19564=FACE_OUTER_BOUND ( 'NONE', #6275, .T. ) ;
#19567=CARTESIAN_POINT ( 'NONE',  ( 0.1102847568649952675, -34.26895182984680588, -26.17930421801138863 ) ) ;
#19569=CARTESIAN_POINT ( 'NONE',  ( 0.6001305935487315502, -0.5236757026892772116, 48.10757715638247589 ) ) ;
#19571=CARTESIAN_POINT ( 'NONE',  ( 0.6030672727741701600, -46.49075153683480721, 12.36682345648100423 ) ) ;
#19576=EDGE_CURVE ( 'NONE', #23785, #10647, #49683, .T. ) ;
#19579=DIRECTION ( 'NONE',  ( -1.000000000000000000, -0.000000000000000000, -0.000000000000000000 ) ) ;
#19589=B_SPLINE_CURVE_WITH_KNOTS ( 'NONE', 3,
 ( #34813, #21319, #10687, #20395, #16307, #11618 ),
 .UNSPECIFIED., .F., .F.,
 ( 4, 2, 4 ),
 ( 1.426045310262811165E-18, 0.0002450742804987333088, 0.0004901485609974652081 ),
 .UNSPECIFIED. ) ;
#19590=B_SPLINE_CURVE_WITH_KNOTS ( 'NONE', 3,
 ( #53386, #39324, #13747, #27824, #58385, #34615 ),
 .UNSPECIFIED., .F., .F.,
 ( 4, 2, 4 ),
 ( 0.000000000000000000, 0.0002450742804987331462, 0.0004901485609974662924 ),
 .UNSPECIFIED. ) ;
#19593=VECTOR ( 'NONE', #43042, 1000.000000000000114 ) ;
#19594=CARTESIAN_POINT ( 'NONE',  ( 0.1073791018717578927, 30.14884492832347718, 30.83464511437148659 ) ) ;
#19600=CARTESIAN_POINT ( 'NONE',  ( 0.7954190325252783467, -17.60078418395023547, 44.76287681188600942 ) ) ;
#19605=VERTEX_POINT ( 'NONE', #56601 ) ;
#19610=CARTESIAN_POINT ( 'NONE',  ( 0.2230388203127617042, 37.71673103297339935, 20.89822698305281534 ) ) ;
#19621=ORIENTED_EDGE ( 'NONE', *, *, #11262, .F. ) ;
#19624=CARTESIAN_POINT ( 'NONE',  ( 0.6254087463353913412, 48.10157520235527073, -0.6881259009462784570 ) ) ;
#19627=VERTEX_POINT ( 'NONE', #51906 ) ;
#19629=CARTESIAN_POINT ( 'NONE',  ( 0.6025881611877911270, -47.72390913208169394, 6.062907795288557722 ) ) ;
#19633=FACE_OUTER_BOUND ( 'NONE', #5849, .T. ) ;
#19635=CARTESIAN_POINT ( 'NONE',  ( 0.2224561200757608492, 10.42482236669245665, 41.84032767736803748 ) ) ;
#19651=ADVANCED_FACE ( 'NONE', ( #23408 ), #34874, .F. ) ;
#19655=CARTESIAN_POINT ( 'NONE',  ( 0.8760168074886960365, 19.22870327415304104, -44.09317760313732748 ) ) ;
#19666=CARTESIAN_POINT ( 'NONE',  ( -6.001507490154111224, 11.48377994779722755, -14.94036486426001353 ) ) ;
#19667=DIRECTION ( 'NONE',  ( -1.000000000000000000, -0.000000000000000000, -0.000000000000000000 ) ) ;
#19668=ORIENTED_EDGE ( 'NONE', *, *, #47053, .T. ) ;
#19674=AXIS2_PLACEMENT_3D ( 'NONE', #49054, #39070, #30548 ) ;
#19675=VERTEX_POINT ( 'NONE', #47847 ) ;
#19676=CARTESIAN_POINT ( 'NONE',  ( 0.5980894510889448457, 33.52121017007780068, 34.51330645350414272 ) ) ;
#19677=CARTESIAN_POINT ( 'NONE',  ( 0.6030672727741701600, 33.95535904584739484, 34.07876014368871864 ) ) ;
#19680=CARTESIAN_POINT ( 'NONE',  ( 4.322998006666179727, 40.45864630878519108, -25.80712523194233299 ) ) ;
#19681=CARTESIAN_POINT ( 'NONE',  ( 0.8751705887134553219, -41.19904111682524928, 24.81530984069135570 ) ) ;
#19688=CARTESIAN_POINT ( 'NONE',  ( 3.238931869106855377, -36.28407486357536982, 23.06038324659503758 ) ) ;
#19689=( BOUNDED_SURFACE ( )  B_SPLINE_SURFACE ( 3, 1, ( 
 ( #3755, #42329 ),
 ( #4059, #31992 ),
 ( #46404, #3450 ),
 ( #22588, #23198 ) ),
 .UNSPECIFIED., .F., .F., .F. ) 
 B_SPLINE_SURFACE_WITH_KNOTS ( ( 4, 4 ),
 ( 2, 2 ),
 ( 0.000000000000000000, 1.000000000000000000 ),
 ( 0.000000000000000000, 1.000000000000000000 ),
 .UNSPECIFIED. ) 
 GEOMETRIC_REPRESENTATION_ITEM ( )  RATIONAL_B_SPLINE_SURFACE ( (
 ( 1.000000000000000000, 1.000000000000000000),
 ( 0.7223157951917480446, 0.9931996967497186413),
 ( 0.7223157951917480446, 0.9931996967497186413),
 ( 1.000000000000000000, 1.000000000000000000) ) ) 
 REPRESENTATION_ITEM ( '' )  SURFACE ( )  );
#19697=CARTESIAN_POINT ( 'NONE',  ( 5.880360259849752858, -31.59460303415958293, -36.09847387447848632 ) ) ;
#19698=CARTESIAN_POINT ( 'NONE',  ( 5.880360259849752858, -45.41096578730637390, -15.46489389606739984 ) ) ;
#19699=EDGE_CURVE ( 'NONE', #61648, #14372, #39168, .T. ) ;
#19704=CARTESIAN_POINT ( 'NONE',  ( 4.549368137175248350, -8.582197505784725067, 42.06008734272381133 ) ) ;
#19711=ORIENTED_EDGE ( 'NONE', *, *, #42155, .F. ) ;
#19714=FACE_OUTER_BOUND ( 'NONE', #10183, .T. ) ;
#19716=CARTESIAN_POINT ( 'NONE',  ( 0.8751705887134423323, -19.22545746485690188, 44.08562551107050353 ) ) ;
#19719=ORIENTED_EDGE ( 'NONE', *, *, #9474, .F. ) ;
#19720=CARTESIAN_POINT ( 'NONE',  ( -6.016761891674564211, 2.456125503350979677, -18.68243340030200272 ) ) ;
#19721=CARTESIAN_POINT ( 'NONE',  ( 4.549368137175248350, 2.596185425821331272, 42.84816078363931524 ) ) ;
#19728=EDGE_CURVE ( 'NONE', #60297, #36895, #57876, .T. ) ;
#19733=EDGE_LOOP ( 'NONE', ( #17345, #61636, #11985, #18702 ) ) ;
#19745=CARTESIAN_POINT ( 'NONE',  ( 0.8751705887134553219, 33.37254303619554463, -34.63284514348550402 ) ) ;
#19750=VECTOR ( 'NONE', #47687, 1000.000000000000227 ) ;
#19751=ORIENTED_EDGE ( 'NONE', *, *, #15232, .T. ) ;
#19752=CARTESIAN_POINT ( 'NONE',  ( 0.6041374136657476912, -38.27243465845322135, -29.14743607025070204 ) ) ;
#19769=CARTESIAN_POINT ( 'NONE',  ( 0.8760168074887090262, -7.161346975773370538, -47.56749362999710939 ) ) ;
#19775=ORIENTED_EDGE ( 'NONE', *, *, #31764, .F. ) ;
#19776=CARTESIAN_POINT ( 'NONE',  ( 0.5998501479064699549, 6.798102206413494386, 47.62484632993690781 ) ) ;
#19778=CARTESIAN_POINT ( 'NONE',  ( 0.3622758884714600280, -39.50828911766986096, -17.25816669464980890 ) ) ;
#19779=ORIENTED_EDGE ( 'NONE', *, *, #51726, .T. ) ;
#19782=B_SPLINE_CURVE_WITH_KNOTS ( 'NONE', 3,
 ( #15294, #48790, #29676, #10277 ),
 .UNSPECIFIED., .F., .F.,
 ( 4, 4 ),
 ( 2.122407100861210668E-17, 0.004444306975806114161 ),
 .UNSPECIFIED. ) ;
#19788=CARTESIAN_POINT ( 'NONE',  ( 1.827119703190780653, 15.32887915442596594, -40.22835835992449205 ) ) ;
#19793=B_SPLINE_CURVE_WITH_KNOTS ( 'NONE', 3,
 ( #50656, #45379, #55046, #12170, #31257, #56590 ),
 .UNSPECIFIED., .F., .F.,
 ( 4, 2, 4 ),
 ( 8.546004838552221719E-17, 0.0002293366620881438192, 0.0004586733241762021491 ),
 .UNSPECIFIED. ) ;
#19802=CARTESIAN_POINT ( 'NONE',  ( -2.708315649062910779, 14.63219292706382646, 0.2635547933244035690 ) ) ;
#19804=EDGE_CURVE ( 'NONE', #41909, #32930, #36678, .T. ) ;
#19808=CARTESIAN_POINT ( 'NONE',  ( 0.8760168074886965917, -11.58706983520293221, -46.68716261866173056 ) ) ;
#19813=EDGE_CURVE ( 'NONE', #26300, #36881, #45820, .T. ) ;
#19814=EDGE_LOOP ( 'NONE', ( #59870, #54816, #33378, #54021 ) ) ;
#19827=VERTEX_POINT ( 'NONE', #37293 ) ;
#19835=CARTESIAN_POINT ( 'NONE',  ( 0.6023142530420679819, -29.07781306567130386, 38.32506243004142021 ) ) ;
#19838=VERTEX_POINT ( 'NONE', #14716 ) ;
#19849=ADVANCED_FACE ( 'NONE', ( #37607 ), #31726, .F. ) ;
#19851=CARTESIAN_POINT ( 'NONE',  ( 4.975801465491695552, -46.87746200127462970, 9.906103548667402947 ) ) ;
#19852=CARTESIAN_POINT ( 'NONE',  ( 4.549368137175248350, 0.000000000000000000, 0.000000000000000000 ) ) ;
#19865=DIRECTION ( 'NONE',  ( 0.1024043820194936311, 0.1428674944015942416, 0.9844298967354739860 ) ) ;
#19866=CARTESIAN_POINT ( 'NONE',  ( 0.1101816497532063233, -39.78963561881077737, 16.62841624476607194 ) ) ;
#19872=CARTESIAN_POINT ( 'NONE',  ( 4.549368137175248350, 32.13400537129925283, -28.46244473166639111 ) ) ;
#19873=CARTESIAN_POINT ( 'NONE',  ( 0.7954196712028458460, 19.20650004025001678, -44.09776749253662587 ) ) ;
#19874=CARTESIAN_POINT ( 'NONE',  ( 0.6029303876144825880, -18.28892193312832859, -44.49541906039121386 ) ) ;
#19890=( BOUNDED_SURFACE ( )  B_SPLINE_SURFACE ( 3, 1, ( 
 ( #3558, #32407 ),
 ( #56190, #60887 ),
 ( #23312, #36191 ),
 ( #51481, #55255 ) ),
 .UNSPECIFIED., .F., .F., .F. ) 
 B_SPLINE_SURFACE_WITH_KNOTS ( ( 4, 4 ),
 ( 2, 2 ),
 ( 0.000000000000000000, 1.000000000000000000 ),
 ( 0.000000000000000000, 1.000000000000000000 ),
 .UNSPECIFIED. ) 
 GEOMETRIC_REPRESENTATION_ITEM ( )  RATIONAL_B_SPLINE_SURFACE ( (
 ( 1.000000000000000000, 1.000000000000000000),
 ( 0.9953040768229005630, 0.8617119497784937465),
 ( 0.9953040768229005630, 0.8617119497784937465),
 ( 1.000000000000000000, 1.000000000000000000) ) ) 
 REPRESENTATION_ITEM ( '' )  SURFACE ( )  );
#19893=EDGE_CURVE ( 'NONE', #31073, #49600, #36836, .T. ) ;
#19894=CARTESIAN_POINT ( 'NONE',  ( -6.016761891674564211, 4.873659902332621918, -18.20201388312090529 ) ) ;
#19900=CARTESIAN_POINT ( 'NONE',  ( 4.975801465491694664, 36.39623109580467997, -31.15993731089085017 ) ) ;
#19913=ADVANCED_FACE ( 'NONE', ( #43541 ), #32873, .F. ) ;
#19914=CARTESIAN_POINT ( 'NONE',  ( 0.6023143664670691511, -23.82663958122407522, -41.79259346737314473 ) ) ;
#19917=CARTESIAN_POINT ( 'NONE',  ( 4.322998006666179727, 14.45630056002876174, 45.75942687572302958 ) ) ;
#19919=CARTESIAN_POINT ( 'NONE',  ( 0.3622758884714730732, -41.42293301073634382, 11.95365414648425428 ) ) ;
#19927=AXIS2_PLACEMENT_3D ( 'NONE', #3269, #22714, #45930 ) ;
#19932=ORIENTED_EDGE ( 'NONE', *, *, #33530, .T. ) ;
#19935=CARTESIAN_POINT ( 'NONE',  ( 0.1098349054025746646, -37.23978094195836519, -21.74670956129746813 ) ) ;
#19945=CARTESIAN_POINT ( 'NONE',  ( 0.1073791018717483448, -6.109314776652422729, -42.68962945260951614 ) ) ;
#19950=CARTESIAN_POINT ( 'NONE',  ( 0.2230388203127631752, 26.84831060237797118, 33.74101226470672543 ) ) ;
#19952=FACE_OUTER_BOUND ( 'NONE', #18286, .T. ) ;
#19962=CARTESIAN_POINT ( 'NONE',  ( 0.5980894510889448457, 17.76188940524884075, 44.71414919659913068 ) ) ;
#19965=CARTESIAN_POINT ( 'NONE',  ( 0.7954196712028472893, 17.60078400783960006, 44.76287685048092868 ) ) ;
#19967=FACE_OUTER_BOUND ( 'NONE', #6869, .T. ) ;
#19971=CARTESIAN_POINT ( 'NONE',  ( 4.833616638992208614, -38.20222678111956327, 26.07076047129070773 ) ) ;
#19972=ORIENTED_EDGE ( 'NONE', *, *, #50439, .T. ) ;
#19979=CARTESIAN_POINT ( 'NONE',  ( 0.8760168074886965917, 42.09738177923954794, -23.27577685234553684 ) ) ;
#19987=ADVANCED_FACE ( 'NONE', ( #22489 ), #4832, .F. ) ;
#19988=B_SPLINE_CURVE_WITH_KNOTS ( 'NONE', 3,
 ( #49164, #608, #5302, #38555, #33855, #57606 ),
 .UNSPECIFIED., .F., .F.,
 ( 4, 2, 4 ),
 ( 1.253517773560139088E-16, 0.0002450741128632347274, 0.0004901482257263441210 ),
 .UNSPECIFIED. ) ;
#19989=CARTESIAN_POINT ( 'NONE',  ( 4.691466044806103852, 24.49380602310813870, -37.25818859570281916 ) ) ;
#19996=DIRECTION ( 'NONE',  ( -0.1024043820194934507, 0.9573600124648741216, 0.2701391291102821501 ) ) ;
#19998=CARTESIAN_POINT ( 'NONE',  ( 4.549368137175248350, -40.71620287708334018, -13.59764261105737404 ) ) ;
#19999=ORIENTED_EDGE ( 'NONE', *, *, #30418, .T. ) ;
#20000=CARTESIAN_POINT ( 'NONE',  ( 0.5998501479064699549, -38.48283596222010061, -28.86886762351111457 ) ) ;
#20011=VERTEX_POINT ( 'NONE', #26254 ) ;
#20013=ORIENTED_EDGE ( 'NONE', *, *, #55771, .T. ) ;
#20018=VERTEX_POINT ( 'NONE', #21880 ) ;
#20028=CARTESIAN_POINT ( 'NONE',  ( 0.1084644655670281704, 30.77359411724684435, 30.21121552071008054 ) ) ;
#20030=CARTESIAN_POINT ( 'NONE',  ( -6.016761891674564211, 14.94721834528430371, -11.47373234755488092 ) ) ;
#20040=CARTESIAN_POINT ( 'NONE',  ( 0.3622758884714730732, 22.26738722580116558, 36.91764744403329246 ) ) ;
#20043=CARTESIAN_POINT ( 'NONE',  ( 0.5980894510889457338, 46.28687279963691736, -13.12879507229240161 ) ) ;
#20048=ORIENTED_EDGE ( 'NONE', *, *, #55087, .T. ) ;
#20056=CARTESIAN_POINT ( 'NONE',  ( 4.975801465491695552, 0.000000000000000000, 0.000000000000000000 ) ) ;
#20058=B_SPLINE_CURVE_WITH_KNOTS ( 'NONE', 3,
 ( #4801, #61815, #52737, #14861, #19560, #38676 ),
 .UNSPECIFIED., .F., .F.,
 ( 4, 2, 4 ),
 ( 8.471125239557413953E-17, 0.0002293366620881436566, 0.0004586733241762026370 ),
 .UNSPECIFIED. ) ;
#20061=VERTEX_POINT ( 'NONE', #19047 ) ;
#20071=CARTESIAN_POINT ( 'NONE',  ( 0.7954196712028462901, -28.58653687859139225, -38.68220069891160051 ) ) ;
#20076=DIRECTION ( 'NONE',  ( -0.1024043820194934507, -0.9139094329506576297, -0.3927886084231733688 ) ) ;
#20078=ADVANCED_FACE ( 'NONE', ( #38158 ), #22424, .F. ) ;
#20083=CARTESIAN_POINT ( 'NONE',  ( 4.975801465491694664, -47.76942479135482955, -3.702618843597289544 ) ) ;
#20086=CARTESIAN_POINT ( 'NONE',  ( 0.5998501479064708430, -12.95623334615534716, 46.33007877220716608 ) ) ;
#20089=EDGE_CURVE ( 'NONE', #33107, #26859, #38392, .T. ) ;
#20090=EDGE_LOOP ( 'NONE', ( #32598, #5072, #36358, #49264 ) ) ;
#20091=VECTOR ( 'NONE', #27800, 1000.000000000000000 ) ;
#20096=CARTESIAN_POINT ( 'NONE',  ( 0.6254087463353935616, 37.74264085326059615, -29.82831063981293340 ) ) ;
#20101=CARTESIAN_POINT ( 'NONE',  ( 0.5998501479064708430, 18.89267974119668025, -44.24259072156067418 ) ) ;
#20106=EDGE_CURVE ( 'NONE', #12273, #61654, #14700, .T. ) ;
#20112=B_SPLINE_CURVE_WITH_KNOTS ( 'NONE', 3,
 ( #28179, #27567, #32590, #31654, #42005, #46691 ),
 .UNSPECIFIED., .F., .F.,
 ( 4, 2, 4 ),
 ( 8.559238840292261462E-17, 0.0002293366620881445782, 0.0004586733241762035586 ),
 .UNSPECIFIED. ) ;
#20116=ADVANCED_FACE ( 'NONE', ( #33448 ), #18721, .F. ) ;
#20122=FACE_OUTER_BOUND ( 'NONE', #20811, .T. ) ;
#20123=ORIENTED_EDGE ( 'NONE', *, *, #34798, .T. ) ;
#20125=LINE ( 'NONE', #15113, #1281 ) ;
#20133=VERTEX_POINT ( 'NONE', #195 ) ;
#20136=ORIENTED_EDGE ( 'NONE', *, *, #25688, .F. ) ;
#20140=DIRECTION ( 'NONE',  ( 0.000000000000000000, 0.000000000000000000, -1.000000000000000000 ) ) ;
#20141=CARTESIAN_POINT ( 'NONE',  ( -6.016761891674564211, 16.32039929810256851, 9.418621820384554866 ) ) ;
#20150=CARTESIAN_POINT ( 'NONE',  ( 0.1087620492084205581, -30.74858804150707670, 30.23658359364767989 ) ) ;
#20154=ORIENTED_EDGE ( 'NONE', *, *, #58457, .F. ) ;
#20170=CARTESIAN_POINT ( 'NONE',  ( 4.549368137175248350, -38.40568845698290801, 19.17571786012255686 ) ) ;
#20172=B_SPLINE_CURVE_WITH_KNOTS ( 'NONE', 3,
 ( #13318, #50578, #17390, #51813, #37137, #22703 ),
 .UNSPECIFIED., .F., .F.,
 ( 4, 2, 4 ),
 ( 8.510565793060200234E-17, 0.0002293366620881444426, 0.0004586733241762037754 ),
 .UNSPECIFIED. ) ;
#20180=CARTESIAN_POINT ( 'NONE',  ( 0.6031356755773454870, -18.40994522247727971, -44.44547243635314970 ) ) ;
#20188=CARTESIAN_POINT ( 'NONE',  ( 0.6027935024548037868, -24.20473723001725830, 41.57475399306878217 ) ) ;
#20190=LINE ( 'NONE', #30176, #44700 ) ;
#20193=ADVANCED_FACE ( 'NONE', ( #19967 ), #47733, .F. ) ;
#20195=FACE_OUTER_BOUND ( 'NONE', #57817, .T. ) ;
#20198=ORIENTED_EDGE ( 'NONE', *, *, #14134, .F. ) ;
#20199=ORIENTED_EDGE ( 'NONE', *, *, #29909, .F. ) ;
#20203=EDGE_CURVE ( 'NONE', #38470, #17692, #25595, .T. ) ;
#20206=CARTESIAN_POINT ( 'NONE',  ( 1.827119703190778877, -15.32887915442621818, 40.22835835992437836 ) ) ;
#20213=CARTESIAN_POINT ( 'NONE',  ( 4.833616638992205949, -15.29495699393755359, 43.64812679991092637 ) ) ;
#20221=CARTESIAN_POINT ( 'NONE',  ( 4.549368137175248350, 42.14271863032833920, -8.166781970325278195 ) ) ;
#20222=CARTESIAN_POINT ( 'NONE',  ( 2.643462169533613793, -22.81120928486525301, 42.27470921730900244 ) ) ;
#20225=CARTESIAN_POINT ( 'NONE',  ( 0.7245667037590763915, 44.74806999162964871, 17.64710816761277812 ) ) ;
#20228=ORIENTED_EDGE ( 'NONE', *, *, #60760, .F. ) ;
#20230=CARTESIAN_POINT ( 'NONE',  ( 0.6001305935487422083, -44.24520387813817024, -18.89378601236048283 ) ) ;
#20235=ORIENTED_EDGE ( 'NONE', *, *, #8999, .F. ) ;
#20238=ORIENTED_EDGE ( 'NONE', *, *, #54998, .T. ) ;
#20239=CARTESIAN_POINT ( 'NONE',  ( -5.995132425357893702, 9.429450169547955340, 16.31525984181036293 ) ) ;
#20241=EDGE_CURVE ( 'NONE', #22663, #3284, #166, .T. ) ;
#20244=CARTESIAN_POINT ( 'NONE',  ( 0.5998501479064699549, -5.759754759341138453, 47.76154736470748219 ) ) ;
#20245=EDGE_CURVE ( 'NONE', #35307, #35477, #9712, .T. ) ;
#20246=CARTESIAN_POINT ( 'NONE',  ( 0.8760168074886965917, -42.09738177923971136, 23.27577685234524196 ) ) ;
#20247=CARTESIAN_POINT ( 'NONE',  ( 0.2230388203127610935, -22.21453373073364546, -36.95676097786368786 ) ) ;
#20249=CARTESIAN_POINT ( 'NONE',  ( -6.010958268070873523, 18.84344976839986785, 0.01451635840169903692 ) ) ;
#20250=DIRECTION ( 'NONE',  ( 1.000000000000000000, 0.000000000000000000, 0.000000000000000000 ) ) ;
#20253=CARTESIAN_POINT ( 'NONE',  ( 0.1073791018717483448, -21.14095454447585709, 37.58707531572169813 ) ) ;
#20258=CARTESIAN_POINT ( 'NONE',  ( 4.549368137175248350, -32.13400537129945178, 28.46244473166616729 ) ) ;
#20274=CARTESIAN_POINT ( 'NONE',  ( 0.5998501479064708430, 28.86886762351073088, 38.48283596222038483 ) ) ;
#20281=ORIENTED_EDGE ( 'NONE', *, *, #23880, .F. ) ;
#20288=CARTESIAN_POINT ( 'NONE',  ( 0.1098349054025746369, -0.2133124578267739657, 43.12395110775227636 ) ) ;
#20293=CARTESIAN_POINT ( 'NONE',  ( 0.6017666602106489515, 34.26316403931513577, 33.76944145963986443 ) ) ;
#20299=CIRCLE ( 'NONE', #16314, 42.92674063221959813 ) ;
#20302=CARTESIAN_POINT ( 'NONE',  ( 0.5998501479064699549, -0.5236536531311584142, -48.10473956285919428 ) ) ;
#20305=CARTESIAN_POINT ( 'NONE',  ( 0.1073791018717483448, 21.14095454447559419, -37.58707531572184735 ) ) ;
#20309=ORIENTED_EDGE ( 'NONE', *, *, #30346, .F. ) ;
#20312=EDGE_CURVE ( 'NONE', #497, #42276, #60629, .T. ) ;
#20315=CARTESIAN_POINT ( 'NONE',  ( -6.016761891674564211, 7.207804629151548070, -17.41015286184795130 ) ) ;
#20322=LINE ( 'NONE', #6794, #5151 ) ;
#20324=CARTESIAN_POINT ( 'NONE',  ( 4.975801465491695552, -42.71626295676279028, 21.70134120755125906 ) ) ;
#20331=CARTESIAN_POINT ( 'NONE',  ( 0.6028618097248862329, 12.61968633793851247, 46.42282207635408042 ) ) ;
#20333=CARTESIAN_POINT ( 'NONE',  ( -6.015611763856276717, -17.41126425312532433, -7.205255340944797027 ) ) ;
#20336=CARTESIAN_POINT ( 'NONE',  ( 3.238931869106855377, -18.12707634097797538, -38.98364358950738051 ) ) ;
#20340=CARTESIAN_POINT ( 'NONE',  ( 4.549368137175248350, -42.06008734272390370, -8.582197505784284530 ) ) ;
#20344=CARTESIAN_POINT ( 'NONE',  ( 0.8751705887134423323, 11.58504748649134974, 46.67919521768892110 ) ) ;
#20375=LINE ( 'NONE', #53250, #8698 ) ;
#20380=CARTESIAN_POINT ( 'NONE',  ( 0.5998501479064699549, 47.76154736470750350, 5.759754759340949271 ) ) ;
#20382=ORIENTED_EDGE ( 'NONE', *, *, #480, .T. ) ;
#20383=EDGE_CURVE ( 'NONE', #46057, #41641, #27043, .T. ) ;
#20389=ORIENTED_EDGE ( 'NONE', *, *, #33627, .T. ) ;
#20393=CARTESIAN_POINT ( 'NONE',  ( 2.301529144917015213, 4.990866136406635789, -47.77346141661145396 ) ) ;
#20395=CARTESIAN_POINT ( 'NONE',  ( 0.7245667037590756143, -0.8205429720401278271, -48.09508190954919371 ) ) ;
#20399=CARTESIAN_POINT ( 'NONE',  ( 0.6023142530420679819, 18.16775455049945265, -44.54505940664467545 ) ) ;
#20402=VECTOR ( 'NONE', #32094, 1000.000000000000000 ) ;
#20404=CARTESIAN_POINT ( 'NONE',  ( -6.016761891674564211, 0.003433883959783673098, 18.84319130225482297 ) ) ;
#20431=ORIENTED_EDGE ( 'NONE', *, *, #31371, .T. ) ;
#20450=ORIENTED_EDGE ( 'NONE', *, *, #17377, .T. ) ;
#20465=CARTESIAN_POINT ( 'NONE',  ( 0.1100247026804066219, -39.90641708963723744, 16.34612806822689635 ) ) ;
#20473=CARTESIAN_POINT ( 'NONE',  ( -6.016761891674565099, -14.95139917749712488, 11.46828378093553980 ) ) ;
#20474=VECTOR ( 'NONE', #16686, 1000.000000000000114 ) ;
#20484=CARTESIAN_POINT ( 'NONE',  ( 0.5998501479064708430, -44.24259072156073813, -18.89267974119652749 ) ) ;
#20488=CARTESIAN_POINT ( 'NONE',  ( 0.5998501479064708430, -47.62484632993683675, -6.798102206413969562 ) ) ;
#20492=ORIENTED_EDGE ( 'NONE', *, *, #19449, .T. ) ;
#20494=CARTESIAN_POINT ( 'NONE',  ( 0.1102144999581333162, -43.12427761225339395, -0.1260305566210554729 ) ) ;
#20496=CARTESIAN_POINT ( 'NONE',  ( 1.827326673878743701, 15.32882202537219563, 40.22837085190317907 ) ) ;
#20497=ADVANCED_FACE ( 'NONE', ( #5735 ), #45515, .F. ) ;
#20499=ORIENTED_EDGE ( 'NONE', *, *, #21648, .F. ) ;
#20501=CARTESIAN_POINT ( 'NONE',  ( 0.3622758884714600280, 0.8252992914328071139, -43.10531414739104861 ) ) ;
#20502=CARTESIAN_POINT ( 'NONE',  ( 0.6017667736363748743, 5.933018439714683900, 47.74032759880257260 ) ) ;
#20513=( BOUNDED_SURFACE ( )  B_SPLINE_SURFACE ( 3, 1, ( 
 ( #10816, #25210 ),
 ( #58698, #21437 ),
 ( #1377, #35557 ),
 ( #35247, #6070 ) ),
 .UNSPECIFIED., .F., .F., .F. ) 
 B_SPLINE_SURFACE_WITH_KNOTS ( ( 4, 4 ),
 ( 2, 2 ),
 ( 0.000000000000000000, 1.000000000000000000 ),
 ( 0.000000000000000000, 1.000000000000000000 ),
 .UNSPECIFIED. ) 
 GEOMETRIC_REPRESENTATION_ITEM ( )  RATIONAL_B_SPLINE_SURFACE ( (
 ( 1.000000000000000000, 1.000000000000000000),
 ( 0.9953040768229013402, 0.8617119497784988535),
 ( 0.9953040768229013402, 0.8617119497784988535),
 ( 1.000000000000000000, 1.000000000000000000) ) ) 
 REPRESENTATION_ITEM ( '' )  SURFACE ( )  );
#20514=CARTESIAN_POINT ( 'NONE',  ( -2.708315649062916552, 0.2635547933241593199, 14.63219292706383179 ) ) ;
#20525=CARTESIAN_POINT ( 'NONE',  ( 0.5998501479064699549, 44.64337787626223530, 17.92509395669123862 ) ) ;
#20527=DIRECTION ( 'NONE',  ( -1.000000000000000000, -0.000000000000000000, -0.000000000000000000 ) ) ;
#20529=CONICAL_SURFACE ( 'NONE', #61506, 42.92674063221959813, 1.485477209440487556 ) ;
#20535=VERTEX_POINT ( 'NONE', #7598 ) ;
#20536=CARTESIAN_POINT ( 'NONE',  ( -2.569797478183790229, -12.89088113963440740, 6.924386868080623536 ) ) ;
#20544=CARTESIAN_POINT ( 'NONE',  ( 3.238931869106854489, 1.828840280768788240, 42.95312220797018199 ) ) ;
#20545=EDGE_CURVE ( 'NONE', #5168, #21617, #26258, .T. ) ;
#20549=CARTESIAN_POINT ( 'NONE',  ( 2.643462169533613793, -46.73820883660198433, -11.09243630552516890 ) ) ;
#20551=VERTEX_POINT ( 'NONE', #11398 ) ;
#20552=CARTESIAN_POINT ( 'NONE',  ( 4.549368137175248350, -38.40568845698290801, 19.17571786012255686 ) ) ;
#20556=CARTESIAN_POINT ( 'NONE',  ( 0.8751705887134423323, -0.8911681664091769539, 48.08707113907594533 ) ) ;
#20567=DIRECTION ( 'NONE',  ( -1.000000000000000000, -0.000000000000000000, -0.000000000000000000 ) ) ;
#20569=ORIENTED_EDGE ( 'NONE', *, *, #32189, .T. ) ;
#20576=CARTESIAN_POINT ( 'NONE',  ( 0.7048096507298579061, 42.08020459959980997, -23.32077812596837418 ) ) ;
#20577=CARTESIAN_POINT ( 'NONE',  ( 0.5988103564986356764, 0.6065102550366653356, 48.10388392110854028 ) ) ;
#20578=CARTESIAN_POINT ( 'NONE',  ( 5.880360259849739535, -47.86623372148051914, 3.184717612777128171 ) ) ;
#20585=CARTESIAN_POINT ( 'NONE',  ( 0.1101816497532063233, -39.89358705406974082, -16.37745527993575578 ) ) ;
#20586=CARTESIAN_POINT ( 'NONE',  ( 0.1073791018717578927, -21.98088480513690968, 37.10214135362851096 ) ) ;
#20587=ORIENTED_EDGE ( 'NONE', *, *, #6824, .F. ) ;
#20590=ORIENTED_EDGE ( 'NONE', *, *, #56949, .F. ) ;
#20593=DIRECTION ( 'NONE',  ( -1.000000000000000000, -0.000000000000000000, -0.000000000000000000 ) ) ;
#20598=ORIENTED_EDGE ( 'NONE', *, *, #56272, .F. ) ;
#20603=EDGE_LOOP ( 'NONE', ( #26928, #44220, #9553, #30821 ) ) ;
#20611=CARTESIAN_POINT ( 'NONE',  ( 0.3622758884714730732, 37.74294673546557988, 20.83792692158985460 ) ) ;
#20615=ORIENTED_EDGE ( 'NONE', *, *, #4718, .F. ) ;
#20616=CARTESIAN_POINT ( 'NONE',  ( 0.8751705887134423323, 38.69254731947834358, -28.56654290188613032 ) ) ;
#20626=CARTESIAN_POINT ( 'NONE',  ( 0.1084644655670282121, -6.022910953206811691, -42.70194587816327214 ) ) ;
#20628=CARTESIAN_POINT ( 'NONE',  ( -6.017396004339687465, 14.95000090562897022, -11.47005965438123631 ) ) ;
#20633=CARTESIAN_POINT ( 'NONE',  ( 0.1073791018717483448, -21.98088480513640874, -37.10214135362880228 ) ) ;
#20634=CARTESIAN_POINT ( 'NONE',  ( 4.322998006666165516, 43.48102276965671820, 20.30542865297664079 ) ) ;
#20640=B_SPLINE_CURVE_WITH_KNOTS ( 'NONE', 3,
 ( #35285, #54662, #11471, #11788 ),
 .UNSPECIFIED., .F., .F.,
 ( 4, 4 ),
 ( 0.000000000000000000, 0.005014147105413705591 ),
 .UNSPECIFIED. ) ;
#20645=EDGE_CURVE ( 'NONE', #5544, #60819, #21830, .T. ) ;
#20649=EDGE_CURVE ( 'NONE', #3284, #16197, #15070, .T. ) ;
#20651=CIRCLE ( 'NONE', #9641, 47.91270532121795611 ) ;
#20653=ADVANCED_FACE ( 'NONE', ( #12960 ), #37631, .F. ) ;
#20659=CARTESIAN_POINT ( 'NONE',  ( 0.1073791018717483448, -41.52698815987176317, 11.62916352156079824 ) ) ;
#20667=ORIENTED_EDGE ( 'NONE', *, *, #41082, .T. ) ;
#20684=VERTEX_POINT ( 'NONE', #22648 ) ;
#20685=ORIENTED_EDGE ( 'NONE', *, *, #26487, .T. ) ;
#20686=LINE ( 'NONE', #1243, #12405 ) ;
#20689=CARTESIAN_POINT ( 'NONE',  ( 0.7048096507298579061, 34.61049487267059277, -33.41730025321717079 ) ) ;
#20697=EDGE_CURVE ( 'NONE', #23596, #28479, #41779, .T. ) ;
#20699=ORIENTED_EDGE ( 'NONE', *, *, #32821, .T. ) ;
#20710=( LENGTH_UNIT ( ) NAMED_UNIT ( * ) SI_UNIT ( .MILLI., .METRE. ) );
#20714=CARTESIAN_POINT ( 'NONE',  ( 4.691466044806103852, 42.11359095667489782, -14.64802401911184759 ) ) ;
#20716=CARTESIAN_POINT ( 'NONE',  ( 0.1064266379913945265, 6.185137063632448751, 42.67882137217593197 ) ) ;
#20718=CARTESIAN_POINT ( 'NONE',  ( 0.7954196712028454019, -42.08256091708719993, 23.29293472883116678 ) ) ;
#20725=CARTESIAN_POINT ( 'NONE',  ( -2.708315649062916552, 13.41752550814510414, -5.842990691604468267 ) ) ;
#20726=ORIENTED_EDGE ( 'NONE', *, *, #1824, .F. ) ;
#20727=ADVANCED_FACE ( 'NONE', ( #33600 ), #7585, .F. ) ;
#20734=CARTESIAN_POINT ( 'NONE',  ( 4.975801465491694664, 14.85979367497109571, 45.55012473237758996 ) ) ;
#20735=B_SPLINE_CURVE_WITH_KNOTS ( 'NONE', 3,
 ( #16382, #35506, #54565, #11695, #30777, #49897 ),
 .UNSPECIFIED., .F., .F.,
 ( 4, 2, 4 ),
 ( 0.000000000000000000, 0.0002450742804987342304, 0.0004901485609974684608 ),
 .UNSPECIFIED. ) ;
#20738=VERTEX_POINT ( 'NONE', #54128 ) ;
#20741=ORIENTED_EDGE ( 'NONE', *, *, #55727, .T. ) ;
#20742=EDGE_CURVE ( 'NONE', #42579, #17351, #5377, .T. ) ;
#20745=AXIS2_PLACEMENT_3D ( 'NONE', #7399, #40660, #16841 ) ;
#20747=ORIENTED_EDGE ( 'NONE', *, *, #22412, .F. ) ;
#20748=CARTESIAN_POINT ( 'NONE',  ( 0.1101816497532062816, 11.29256821151155954, 41.61967362528560699 ) ) ;
#20750=EDGE_LOOP ( 'NONE', ( #10171, #41478, #25304, #37034 ) ) ;
#20760=CARTESIAN_POINT ( 'NONE',  ( 0.3622758884714730732, 11.95365414648439462, 41.42293301073630118 ) ) ;
#20764=CARTESIAN_POINT ( 'NONE',  ( 0.1095718737110178975, 41.58781525899394182, 11.40943879390663263 ) ) ;
#20774=VERTEX_POINT ( 'NONE', #11568 ) ;
#20775=ORIENTED_EDGE ( 'NONE', *, *, #9631, .F. ) ;
#20781=CARTESIAN_POINT ( 'NONE',  ( 0.3622758884714730732, -43.10531414739105571, 0.8252992914326598983 ) ) ;
#20783=( BOUNDED_SURFACE ( )  B_SPLINE_SURFACE ( 3, 1, ( 
 ( #3607, #55933 ),
 ( #60619, #46561 ),
 ( #47177, #41874 ),
 ( #60311, #22741 ) ),
 .UNSPECIFIED., .F., .F., .F. ) 
 B_SPLINE_SURFACE_WITH_KNOTS ( ( 4, 4 ),
 ( 2, 2 ),
 ( 0.000000000000000000, 1.000000000000000000 ),
 ( 0.000000000000000000, 1.000000000000000000 ),
 .UNSPECIFIED. ) 
 GEOMETRIC_REPRESENTATION_ITEM ( )  RATIONAL_B_SPLINE_SURFACE ( (
 ( 1.000000000000000000, 1.000000000000000000),
 ( 0.9953040768229013402, 0.8617119497784988535),
 ( 0.9953040768229013402, 0.8617119497784988535),
 ( 1.000000000000000000, 1.000000000000000000) ) ) 
 REPRESENTATION_ITEM ( '' )  SURFACE ( )  );
#20787=FACE_OUTER_BOUND ( 'NONE', #47470, .T. ) ;
#20788=FACE_OUTER_BOUND ( 'NONE', #56018, .T. ) ;
#20793=CARTESIAN_POINT ( 'NONE',  ( 0.7954190325252784577, 5.415566973723242583, -47.79303692714236007 ) ) ;
#20794=CARTESIAN_POINT ( 'NONE',  ( 0.8751705887134553219, 33.37254303619554463, -34.63284514348550402 ) ) ;
#20798=CARTESIAN_POINT ( 'NONE',  ( 0.1103573494271549854, -0.06145187104197965405, -43.12440049163654976 ) ) ;
#20800=CARTESIAN_POINT ( 'NONE',  ( 0.3622758884714730732, -22.26738722580142138, -36.91764744403313614 ) ) ;
#20808=CARTESIAN_POINT ( 'NONE',  ( 4.549368137175248350, 13.99871866169305434, 40.58005590356696501 ) ) ;
#20811=EDGE_LOOP ( 'NONE', ( #46805, #28144, #48327, #15918 ) ) ;
#20812=CARTESIAN_POINT ( 'NONE',  ( 0.1095718737110178698, -11.40943879390677651, 41.58781525899390630 ) ) ;
#20815=ORIENTED_EDGE ( 'NONE', *, *, #4899, .F. ) ;
#20816=EDGE_LOOP ( 'NONE', ( #6315, #32160, #59791, #42642 ) ) ;
#20824=DIRECTION ( 'NONE',  ( 1.000000000000000000, 0.000000000000000000, 0.000000000000000000 ) ) ;
#20826=ORIENTED_EDGE ( 'NONE', *, *, #8687, .T. ) ;
#20828=ORIENTED_EDGE ( 'NONE', *, *, #38205, .T. ) ;
#20830=LINE ( 'NONE', #35867, #7523 ) ;
#20831=AXIS2_PLACEMENT_3D ( 'NONE', #50899, #7995, #31180 ) ;
#20833=CARTESIAN_POINT ( 'NONE',  ( 4.833616638992208614, 20.86133030530232801, 41.27831852777651278 ) ) ;
#20841=EDGE_CURVE ( 'NONE', #45571, #45978, #59458, .T. ) ;
#20845=EDGE_LOOP ( 'NONE', ( #57459, #27518, #51147, #53293 ) ) ;
#20850=CARTESIAN_POINT ( 'NONE',  ( 0.6041374136657475802, 12.61972904329599210, -46.42299778158143653 ) ) ;
#20854=CARTESIAN_POINT ( 'NONE',  ( 0.6025881611877910160, -41.77096849334466810, 23.86454577211492278 ) ) ;
#20857=CARTESIAN_POINT ( 'NONE',  ( -5.995132425357893702, -2.451215106828474877, 18.68405145320023308 ) ) ;
#20863=ORIENTED_EDGE ( 'NONE', *, *, #19813, .F. ) ;
#20868=FACE_OUTER_BOUND ( 'NONE', #38724, .T. ) ;
#20869=CARTESIAN_POINT ( 'NONE',  ( 0.2885700199627512785, -0.8047882683535816373, -43.10898996868493072 ) ) ;
#20871=CARTESIAN_POINT ( 'NONE',  ( 0.7954190325252793459, 46.67728753507125816, 11.60747917225601000 ) ) ;
#20884=CARTESIAN_POINT ( 'NONE',  ( 0.5980894510889448457, 42.01322166096920085, -23.44630161211543395 ) ) ;
#20890=CARTESIAN_POINT ( 'NONE',  ( 0.1102144999581333440, -11.03964818279745153, -41.68747259405346028 ) ) ;
#20891=CARTESIAN_POINT ( 'NONE',  ( 4.549368137175248350, 8.582197505784431968, -42.06008734272388239 ) ) ;
#20899=CARTESIAN_POINT ( 'NONE',  ( 0.3622758884714600280, -36.91764744403305087, -22.26738722580154217 ) ) ;
#20901=EDGE_LOOP ( 'NONE', ( #31015, #21898, #38197, #40876 ) ) ;
#20902=CARTESIAN_POINT ( 'NONE',  ( 0.7954196712028460681, 23.29293472883130889, 42.08256091708710755 ) ) ;
#20906=ORIENTED_EDGE ( 'NONE', *, *, #34798, .F. ) ;
#20907=DIRECTION ( 'NONE',  ( -1.000000000000000000, -0.000000000000000000, -0.000000000000000000 ) ) ;
#20913=VERTEX_POINT ( 'NONE', #60086 ) ;
#20920=ORIENTED_EDGE ( 'NONE', *, *, #47258, .T. ) ;
#20925=ORIENTED_EDGE ( 'NONE', *, *, #25688, .T. ) ;
#20931=CARTESIAN_POINT ( 'NONE',  ( 4.549368137175248350, -42.06008734272390370, -8.582197505784284530 ) ) ;
#20941=FACE_OUTER_BOUND ( 'NONE', #19733, .T. ) ;
#20948=ORIENTED_EDGE ( 'NONE', *, *, #7265, .T. ) ;
#20954=EDGE_CURVE ( 'NONE', #49864, #4461, #45701, .T. ) ;
#20958=CARTESIAN_POINT ( 'NONE',  ( 0.8760168074886965917, 47.80016357497249402, -5.394043284319003817 ) ) ;
#20964=CARTESIAN_POINT ( 'NONE',  ( 0.1073791018717483448, -25.86618856530736466, 34.50606437925502945 ) ) ;
#20967=CARTESIAN_POINT ( 'NONE',  ( 0.1073791018717578927, -5.147744207006579309, -42.81622261970993293 ) ) ;
#20968=ORIENTED_EDGE ( 'NONE', *, *, #30480, .F. ) ;
#20979=ORIENTED_EDGE ( 'NONE', *, *, #55583, .F. ) ;
#20983=CARTESIAN_POINT ( 'NONE',  ( 0.5988103622719989083, -28.80261254780011271, -38.53259676306911530 ) ) ;
#20987=DIRECTION ( 'NONE',  ( -1.000000000000000000, -0.000000000000000000, -0.000000000000000000 ) ) ;
#20990=ORIENTED_EDGE ( 'NONE', *, *, #235, .T. ) ;
#20995=CARTESIAN_POINT ( 'NONE',  ( -6.016104459813371719, -13.32039631884693875, 13.32794178584992828 ) ) ;
#21000=B_SPLINE_CURVE_WITH_KNOTS ( 'NONE', 3,
 ( #763, #20496, #15192, #20808 ),
 .UNSPECIFIED., .F., .F.,
 ( 4, 4 ),
 ( 2.343940034265377226E-17, 0.004564976165746188579 ),
 .UNSPECIFIED. ) ;
#21016=ORIENTED_EDGE ( 'NONE', *, *, #3513, .T. ) ;
#21019=EDGE_CURVE ( 'NONE', #11417, #19272, #4284, .T. ) ;
#21020=CARTESIAN_POINT ( 'NONE',  ( 4.549368137175248350, 32.13400537129885493, 28.46244473166684941 ) ) ;
#21024=CARTESIAN_POINT ( 'NONE',  ( 0.2230388203127582347, -25.64246103889320594, 34.66629317821121958 ) ) ;
#21029=CARTESIAN_POINT ( 'NONE',  ( 0.5988103564986357874, 47.61318305157295327, -6.880138274944463284 ) ) ;
#21034=VERTEX_POINT ( 'NONE', #42549 ) ;
#21037=CARTESIAN_POINT ( 'NONE',  ( 0.5980894510889457338, -47.60453381548698104, 6.974827154143293129 ) ) ;
#21040=LINE ( 'NONE', #21974, #28310 ) ;
#21042=EDGE_CURVE ( 'NONE', #49963, #49511, #26905, .T. ) ;
#21043=CARTESIAN_POINT ( 'NONE',  ( 0.6023142530420679819, -12.70386526143740369, -46.39979989577476260 ) ) ;
#21048=EDGE_LOOP ( 'NONE', ( #11116, #20598, #1549, #46569 ) ) ;
#21050=CARTESIAN_POINT ( 'NONE',  ( -6.015611763856276717, 14.94556629257441038, -11.47596948473795919 ) ) ;
#21054=ORIENTED_EDGE ( 'NONE', *, *, #37491, .F. ) ;
#21059=CONICAL_SURFACE ( 'NONE', #32112, 42.92674063221959813, 1.485477209440487556 ) ;
#21064=CARTESIAN_POINT ( 'NONE',  ( 0.1073791018717483448, -30.14884492832410601, 30.83464511437086841 ) ) ;
#21082=CARTESIAN_POINT ( 'NONE',  ( 0.1087620492084205859, 33.99140154262268965, 26.53886348603014511 ) ) ;
#21101=VECTOR ( 'NONE', #4154, 1000.000000000000114 ) ;
#21104=CARTESIAN_POINT ( 'NONE',  ( -6.010958268070873523, -18.68413620842265743, 2.445171577615698144 ) ) ;
#21107=B_SPLINE_CURVE_WITH_KNOTS ( 'NONE', 3,
 ( #12949, #32048, #26400, #27640 ),
 .UNSPECIFIED., .F., .F.,
 ( 4, 4 ),
 ( 0.000000000000000000, 0.005014147105413699519 ),
 .UNSPECIFIED. ) ;
#21110=CARTESIAN_POINT ( 'NONE',  ( -6.016489644550736315, 18.68257207665196162, 2.455165042129801023 ) ) ;
#21112=ORIENTED_EDGE ( 'NONE', *, *, #15022, .F. ) ;
#21115=CARTESIAN_POINT ( 'NONE',  ( 0.1102847568649952675, -37.30068345220706760, 21.64199720113177605 ) ) ;
#21119=ADVANCED_FACE ( 'NONE', ( #5823 ), #26817, .F. ) ;
#21122=CYLINDRICAL_SURFACE ( 'NONE', #47972, 10.00000000000000000 ) ;
#21127=( BOUNDED_SURFACE ( )  B_SPLINE_SURFACE ( 3, 1, ( 
 ( #52952, #61719 ),
 ( #47054, #14458 ),
 ( #37657, #57630 ),
 ( #23845, #14766 ) ),
 .UNSPECIFIED., .F., .F., .F. ) 
 B_SPLINE_SURFACE_WITH_KNOTS ( ( 4, 4 ),
 ( 2, 2 ),
 ( 0.000000000000000000, 1.000000000000000000 ),
 ( 0.000000000000000000, 1.000000000000000000 ),
 .UNSPECIFIED. ) 
 GEOMETRIC_REPRESENTATION_ITEM ( )  RATIONAL_B_SPLINE_SURFACE ( (
 ( 1.000000000000000000, 1.000000000000000000),
 ( 0.9751682680413298332, 0.9999560080971552356),
 ( 0.9751682680413298332, 0.9999560080971552356),
 ( 1.000000000000000000, 1.000000000000000000) ) ) 
 REPRESENTATION_ITEM ( '' )  SURFACE ( )  );
#21128=B_SPLINE_CURVE_WITH_KNOTS ( 'NONE', 3,
 ( #4725, #33287, #52055, #32982 ),
 .UNSPECIFIED., .F., .F.,
 ( 4, 4 ),
 ( 0.000000000000000000, 0.005014147105413701254 ),
 .UNSPECIFIED. ) ;
#21129=CARTESIAN_POINT ( 'NONE',  ( -2.569797478183790229, -5.182550149005207274, -13.68441171582014348 ) ) ;
#21132=CARTESIAN_POINT ( 'NONE',  ( 0.7954196712028477334, 44.76287685048084342, -17.60078400783977415 ) ) ;
#21134=EDGE_LOOP ( 'NONE', ( #5295, #30983, #360, #14678 ) ) ;
#21135=FACE_OUTER_BOUND ( 'NONE', #26443, .T. ) ;
#21137=CARTESIAN_POINT ( 'NONE',  ( 0.6028618097248863439, 46.51318640245697367, 12.28244208173076757 ) ) ;
#21139=EDGE_LOOP ( 'NONE', ( #28490, #50414, #6791, #8920 ) ) ;
#21151=CARTESIAN_POINT ( 'NONE',  ( 1.827326673878745256, 25.21837361081542639, 34.89023127623428877 ) ) ;
#21156=CARTESIAN_POINT ( 'NONE',  ( 0.1084644655670283647, -42.70194587816332898, 6.022910953206383589 ) ) ;
#21162=CARTESIAN_POINT ( 'NONE',  ( 0.1092565886968783900, -41.73439049602443873, -10.86136484717955142 ) ) ;
#21171=EDGE_CURVE ( 'NONE', #21806, #24433, #34375, .T. ) ;
#21177=CARTESIAN_POINT ( 'NONE',  ( 0.6023142530420679819, -44.34465601638714105, 18.65157113320472604 ) ) ;
#21178=CARTESIAN_POINT ( 'NONE',  ( 0.6031357023905875581, 41.68407605450313014, -24.01594909943223044 ) ) ;
#21187=EDGE_LOOP ( 'NONE', ( #32588, #16208, #61855, #27975 ) ) ;
#21189=CARTESIAN_POINT ( 'NONE',  ( 0.7245667037590765025, 0.8205429720397920956, 48.09508190954921503 ) ) ;
#21190=CARTESIAN_POINT ( 'NONE',  ( 0.1092355843206037486, 41.73183925352180523, -10.87081649985046283 ) ) ;
#21192=EDGE_LOOP ( 'NONE', ( #60858, #12082, #40825, #36472 ) ) ;
#21195=CARTESIAN_POINT ( 'NONE',  ( 2.301529144917015213, -47.43735140118869253, 7.543875168382339957 ) ) ;
#21200=ORIENTED_EDGE ( 'NONE', *, *, #31635, .F. ) ;
#21201=CARTESIAN_POINT ( 'NONE',  ( 0.1102144999581333162, -0.1260305566215071948, 43.12427761225339395 ) ) ;
#21208=CARTESIAN_POINT ( 'NONE',  ( 4.975801465491695552, 0.000000000000000000, 0.000000000000000000 ) ) ;
#21214=ORIENTED_EDGE ( 'NONE', *, *, #2332, .F. ) ;
#21216=CARTESIAN_POINT ( 'NONE',  ( 0.6029303876144825880, 44.49541906039127781, -18.28892193312817227 ) ) ;
#21218=CARTESIAN_POINT ( 'NONE',  ( 50.00005079999999680, 9.539392014169456147, -3.000000000000000000 ) ) ;
#21222=ORIENTED_EDGE ( 'NONE', *, *, #50625, .T. ) ;
#21227=CARTESIAN_POINT ( 'NONE',  ( 0.1102847568649952675, -26.17930421801176877, 34.26895182984652877 ) ) ;
#21229=CARTESIAN_POINT ( 'NONE',  ( -6.017396004339687465, 7.212050743684414122, -17.40836349643160119 ) ) ;
#21239=CARTESIAN_POINT ( 'NONE',  ( 0.7954190325252765703, -37.62416463577130088, 29.96539637359152053 ) ) ;
#21242=CARTESIAN_POINT ( 'NONE',  ( 0.2885697896453119915, 41.84838128162059689, -10.38006191081376350 ) ) ;
#21249=CARTESIAN_POINT ( 'NONE',  ( -6.016761891674564211, 11.47373234755503013, 14.94721834528419002 ) ) ;
#21254=CARTESIAN_POINT ( 'NONE',  ( 0.8751705887134553219, -47.55935879196475469, 7.160166390003496417 ) ) ;
#21268=CARTESIAN_POINT ( 'NONE',  ( 0.1098349054025746507, 43.12395110775227636, 0.2133124578266234195 ) ) ;
#21285=CARTESIAN_POINT ( 'NONE',  ( 0.3622758884714730732, 6.444611261694017657, 42.62881903538212924 ) ) ;
#21292=CARTESIAN_POINT ( 'NONE',  ( 4.549368137175248350, 28.46244473166628097, 32.13400537129935230 ) ) ;
#21301=CARTESIAN_POINT ( 'NONE',  ( 0.7245667037590793891, 34.58857005974907395, 33.42814706018032922 ) ) ;
#21302=CARTESIAN_POINT ( 'NONE',  ( 4.549368137175248350, -13.99871866169335810, -40.58005590356685843 ) ) ;
#21309=CARTESIAN_POINT ( 'NONE',  ( 4.549368137175248350, -3.018832571116875751, 42.82045902618767030 ) ) ;
#21310=VERTEX_POINT ( 'NONE', #40326 ) ;
#21313=CARTESIAN_POINT ( 'NONE',  ( -2.708315649062910779, -12.54007339125010034, -7.544341609839931628 ) ) ;
#21315=CARTESIAN_POINT ( 'NONE',  ( 4.833616638992208614, -2.572717262758311918, 46.17873762321148945 ) ) ;
#21318=DIRECTION ( 'NONE',  ( 1.000000000000000000, 0.000000000000000000, 0.000000000000000000 ) ) ;
#21319=CARTESIAN_POINT ( 'NONE',  ( 0.5988103564986355654, -0.6065102550370011780, -48.10388392110853317 ) ) ;
#21328=( NAMED_UNIT ( * ) SI_UNIT ( $, .STERADIAN. ) SOLID_ANGLE_UNIT ( ) );
#21329=CARTESIAN_POINT ( 'NONE',  ( 4.549368137175248350, 28.46244473166673927, -32.13400537129894730 ) ) ;
#21331=ORIENTED_EDGE ( 'NONE', *, *, #23142, .T. ) ;
#21332=DIRECTION ( 'NONE',  ( 0.000000000000000000, 0.000000000000000000, 1.000000000000000000 ) ) ;
#21349=CARTESIAN_POINT ( 'NONE',  ( 0.6254087463353926735, 47.77987801197954809, 5.596276562478490924 ) ) ;
#21355=CARTESIAN_POINT ( 'NONE',  ( 0.7048096507298635682, 34.61049487267014513, 33.41730025321766107 ) ) ;
#21356=EDGE_CURVE ( 'NONE', #53671, #44040, #27680, .T. ) ;
#21360=EDGE_CURVE ( 'NONE', #39423, #32449, #16812, .T. ) ;
#21361=ORIENTED_EDGE ( 'NONE', *, *, #47299, .T. ) ;
#21364=ORIENTED_EDGE ( 'NONE', *, *, #17206, .T. ) ;
#21365=CARTESIAN_POINT ( 'NONE',  ( 0.8751705887134423323, 42.09020928323375443, -23.27176129838382224 ) ) ;
#21372=ORIENTED_EDGE ( 'NONE', *, *, #2000, .F. ) ;
#21373=CARTESIAN_POINT ( 'NONE',  ( 0.6025881611877910160, -18.61132239451814741, 44.36157157392723605 ) ) ;
#21377=ORIENTED_EDGE ( 'NONE', *, *, #37467, .F. ) ;
#21378=CIRCLE ( 'NONE', #39422, 48.35291015139245019 ) ;
#21379=ORIENTED_EDGE ( 'NONE', *, *, #61021, .F. ) ;
#21380=CARTESIAN_POINT ( 'NONE',  ( 0.1103744047535531458, 41.64495780681022552, 11.19884698423381231 ) ) ;
#21383=VERTEX_POINT ( 'NONE', #2682 ) ;
#21388=VERTEX_POINT ( 'NONE', #60008 ) ;
#21394=EDGE_CURVE ( 'NONE', #3337, #46926, #57486, .T. ) ;
#21398=CARTESIAN_POINT ( 'NONE',  ( 0.6027935024548037868, 12.61964268015556989, -46.42277558035030438 ) ) ;
#21403=CARTESIAN_POINT ( 'NONE',  ( -6.001507490154110336, -14.95933060264865766, -11.45906331631447017 ) ) ;
#21405=CONICAL_SURFACE ( 'NONE', #56401, 42.92674063221959813, 1.485477209440487556 ) ;
#21413=EDGE_LOOP ( 'NONE', ( #24587, #40833, #16958, #9886 ) ) ;
#21416=CARTESIAN_POINT ( 'NONE',  ( -6.016761891674565099, -18.20023637398595540, -4.880293656735155139 ) ) ;
#21431=CARTESIAN_POINT ( 'NONE',  ( 0.8751705887134423323, -47.79200036674284036, 5.393078191591890835 ) ) ;
#21433=EDGE_LOOP ( 'NONE', ( #55457, #50143, #11277, #23360 ) ) ;
#21435=B_SPLINE_CURVE_WITH_KNOTS ( 'NONE', 3,
 ( #34246, #5999, #2240, #1618, #21373, #29524, #44583, #6610, #29837, #53618, #54235, #59255, #39265, #16063, #10745, #16361 ),
 .UNSPECIFIED., .F., .F.,
 ( 4, 3, 3, 3, 3, 4 ),
 ( 1.868480190406682863E-17, 0.0002618515315864458257, 0.0003927756766342040086, 0.0005236998216950610342, 0.0007855159896329934766, 0.001047349442285930689 ),
 .UNSPECIFIED. ) ;
#21437=CARTESIAN_POINT ( 'NONE',  ( 0.5980894510889448457, 19.05812566676507203, -44.17723055703932289 ) ) ;
#21441=CARTESIAN_POINT ( 'NONE',  ( 0.8760168074887090262, 24.81951362746020706, 41.20610493656918294 ) ) ;
#21442=VERTEX_POINT ( 'NONE', #3599 ) ;
#21444=CARTESIAN_POINT ( 'NONE',  ( 0.3622758884714730732, -4.808133778522197588, 42.84426538328723666 ) ) ;
#21445=DIRECTION ( 'NONE',  ( -1.000000000000000000, -0.000000000000000000, -0.000000000000000000 ) ) ;
#21452=VECTOR ( 'NONE', #51027, 1000.000000000000000 ) ;
#21459=DIRECTION ( 'NONE',  ( 0.09835009131224549395, 0.3736726418952318052, -0.9223318362920749358 ) ) ;
#21461=CARTESIAN_POINT ( 'NONE',  ( 0.2885700199627506679, -22.25146206940439697, -36.93108631019287458 ) ) ;
#21465=CARTESIAN_POINT ( 'NONE',  ( 5.880360259849752858, -47.04104239318760250, -9.405269135695077054 ) ) ;
#21477=CARTESIAN_POINT ( 'NONE',  ( 0.8751705887134553219, 17.57879340691544101, -44.76769609654218129 ) ) ;
#21484=ORIENTED_EDGE ( 'NONE', *, *, #19184, .F. ) ;
#21493=EDGE_CURVE ( 'NONE', #55243, #28634, #23659, .T. ) ;
#21496=EDGE_LOOP ( 'NONE', ( #13538, #7809, #36225, #51593 ) ) ;
#21510=( BOUNDED_SURFACE ( )  B_SPLINE_SURFACE ( 3, 1, ( 
 ( #58636, #6010 ),
 ( #11683, #53626 ),
 ( #6943, #49256 ),
 ( #58960, #44592 ) ),
 .UNSPECIFIED., .F., .F., .F. ) 
 B_SPLINE_SURFACE_WITH_KNOTS ( ( 4, 4 ),
 ( 2, 2 ),
 ( 0.000000000000000000, 1.000000000000000000 ),
 ( 0.000000000000000000, 1.000000000000000000 ),
 .UNSPECIFIED. ) 
 GEOMETRIC_REPRESENTATION_ITEM ( )  RATIONAL_B_SPLINE_SURFACE ( (
 ( 1.000000000000000000, 1.000000000000000000),
 ( 0.7223157951917476005, 0.9931996967497186413),
 ( 0.7223157951917476005, 0.9931996967497186413),
 ( 1.000000000000000000, 1.000000000000000000) ) ) 
 REPRESENTATION_ITEM ( '' )  SURFACE ( )  );
#21516=CARTESIAN_POINT ( 'NONE',  ( -2.708315649062910779, 0.2635547933243524432, -14.63219292706382646 ) ) ;
#21525=CARTESIAN_POINT ( 'NONE',  ( 0.6028618097248863439, 44.37846879336933625, -18.57111736963403459 ) ) ;
#21530=ORIENTED_EDGE ( 'NONE', *, *, #55068, .T. ) ;
#21532=CARTESIAN_POINT ( 'NONE',  ( 0.6001305935487315502, -17.92615948558569272, 44.64600790884025372 ) ) ;
#21541=B_SPLINE_CURVE_WITH_KNOTS ( 'NONE', 3,
 ( #23964, #61232, #18353, #43091, #60929, #56228, #5742, #29885, #5136, #1665, #48998, #20494, #58368, #48687, #58676, #25488, #28968, #24890, #15494 ),
 .UNSPECIFIED., .F., .F.,
 ( 4, 3, 3, 3, 3, 3, 4 ),
 ( 1.157434093048479169E-16, 0.0002618519381806257000, 0.0003927759815485974931, 0.0005237000248299428879, 0.0006546240681324978251, 0.0007855481115631320586, 0.0009699050456655107250 ),
 .UNSPECIFIED. ) ;
#21547=EDGE_CURVE ( 'NONE', #19392, #56342, #28445, .T. ) ;
#21558=CARTESIAN_POINT ( 'NONE',  ( 0.5980894510889448457, -28.72954109785577259, -38.59343625445439585 ) ) ;
#21563=DIRECTION ( 'NONE',  ( -1.000000000000000000, -0.000000000000000000, -0.000000000000000000 ) ) ;
#21568=CARTESIAN_POINT ( 'NONE',  ( 0.3622758884714730732, -43.10531414739105571, 0.8252992914326598983 ) ) ;
#21570=DIRECTION ( 'NONE',  ( 0.000000000000000000, 0.000000000000000000, 1.000000000000000000 ) ) ;
#21576=EDGE_CURVE ( 'NONE', #22212, #54494, #50858, .T. ) ;
#21591=CARTESIAN_POINT ( 'NONE',  ( -2.708315649062910779, 12.80362818457445151, -7.087851317223837100 ) ) ;
#21592=CARTESIAN_POINT ( 'NONE',  ( 0.6023143664670691511, -29.49326149840261024, 38.00627775314912071 ) ) ;
#21604=CARTESIAN_POINT ( 'NONE',  ( 0.1092565886968784872, 11.46097737058305555, 41.57372480460688990 ) ) ;
#21605=B_SPLINE_CURVE_WITH_KNOTS ( 'NONE', 3,
 ( #33992, #53065, #23118, #3360 ),
 .UNSPECIFIED., .F., .F.,
 ( 4, 4 ),
 ( 0.000000000000000000, 0.005014147105413698652 ),
 .UNSPECIFIED. ) ;
#21606=ORIENTED_EDGE ( 'NONE', *, *, #56564, .T. ) ;
#21609=AXIS2_PLACEMENT_3D ( 'NONE', #16317, #7514, #49517 ) ;
#21611=CARTESIAN_POINT ( 'NONE',  ( 0.1100247026804066219, -16.65964013375411668, 39.77655614012826391 ) ) ;
#21613=ORIENTED_EDGE ( 'NONE', *, *, #8804, .F. ) ;
#21617=VERTEX_POINT ( 'NONE', #53674 ) ;
#21621=CARTESIAN_POINT ( 'NONE',  ( 5.880360259849739535, -9.312491912828475549, 47.05949693022690639 ) ) ;
#21624=CARTESIAN_POINT ( 'NONE',  ( 0.5998501479064699549, -34.38546660123274989, -33.64490850298832925 ) ) ;
#21635=ORIENTED_EDGE ( 'NONE', *, *, #11230, .F. ) ;
#21639=CARTESIAN_POINT ( 'NONE',  ( 4.549368137175248350, -3.018832571116246477, -42.82045902618772004 ) ) ;
#21646=CARTESIAN_POINT ( 'NONE',  ( -2.708315649062916552, 10.16016146078288607, -10.53288422393045920 ) ) ;
#21648=EDGE_CURVE ( 'NONE', #28915, #42044, #39330, .T. ) ;
#21654=CARTESIAN_POINT ( 'NONE',  ( 4.975801465491694664, 14.85979367497109571, 45.55012473237758996 ) ) ;
#21657=EDGE_CURVE ( 'NONE', #6741, #47578, #13369, .T. ) ;
#21666=ORIENTED_EDGE ( 'NONE', *, *, #39557, .T. ) ;
#21672=ORIENTED_EDGE ( 'NONE', *, *, #35528, .T. ) ;
#21692=LINE ( 'NONE', #11688, #4608 ) ;
#21693=CARTESIAN_POINT ( 'NONE',  ( -6.001507490154110336, -11.48377994779691136, -14.94036486426024801 ) ) ;
#21695=ORIENTED_EDGE ( 'NONE', *, *, #14463, .F. ) ;
#21697=ORIENTED_EDGE ( 'NONE', *, *, #25166, .F. ) ;
#21698=CARTESIAN_POINT ( 'NONE',  ( 0.2885697896453099376, 15.75356890148099609, 40.13549262224785252 ) ) ;
#21701=CARTESIAN_POINT ( 'NONE',  ( -6.017396004339687465, -16.31807101179363784, -9.422598049764795647 ) ) ;
#21702=CARTESIAN_POINT ( 'NONE',  ( 0.6030672727741701600, 6.365785297724776193, -47.68443224372865075 ) ) ;
#21707=CARTESIAN_POINT ( 'NONE',  ( 0.6009452777970410997, 12.02913818029312765, -46.57942614304346307 ) ) ;
#21708=EDGE_CURVE ( 'NONE', #52785, #20684, #60542, .T. ) ;
#21719=CARTESIAN_POINT ( 'NONE',  ( -6.016761891674564211, 18.68243340030203115, 2.456125503350775841 ) ) ;
#21724=STYLED_ITEM ( 'NONE', ( #59522 ), #25822 ) ;
#21725=AXIS2_PLACEMENT_3D ( 'NONE', #4092, #45828, #46134 ) ;
#21730=ORIENTED_EDGE ( 'NONE', *, *, #7912, .T. ) ;
#21731=ORIENTED_EDGE ( 'NONE', *, *, #10409, .F. ) ;
#21733=CARTESIAN_POINT ( 'NONE',  ( 0.1104177457020373010, -37.34442418285517817, 21.56646482560066858 ) ) ;
#21736=ORIENTED_EDGE ( 'NONE', *, *, #32998, .T. ) ;
#21741=ORIENTED_EDGE ( 'NONE', *, *, #19893, .F. ) ;
#21742=CARTESIAN_POINT ( 'NONE',  ( -6.016761891674564211, -2.456125503350841566, 18.68243340030202049 ) ) ;
#21747=CARTESIAN_POINT ( 'NONE',  ( 0.1102144999581332885, 21.45299314243942135, 37.40973521037469851 ) ) ;
#21750=ORIENTED_EDGE ( 'NONE', *, *, #14463, .T. ) ;
#21751=CARTESIAN_POINT ( 'NONE',  ( 0.3622758884714600280, 42.84426538328730771, -4.808133778521432866 ) ) ;
#21756=CARTESIAN_POINT ( 'NONE',  ( 0.8751705887134553219, 46.21789262997757675, -13.30665218149314200 ) ) ;
#21760=CARTESIAN_POINT ( 'NONE',  ( 0.6031357023905875581, 18.36962560204156247, 44.46217339385177780 ) ) ;
#21766=CARTESIAN_POINT ( 'NONE',  ( 0.2885700199627514451, -4.828949117912088695, 42.84523253167934342 ) ) ;
#21768=CARTESIAN_POINT ( 'NONE',  ( -6.016104459813374383, -4.882138007282878611, 18.19977249352309201 ) ) ;
#21770=VECTOR ( 'NONE', #29355, 1000.000000000000000 ) ;
#21779=EDGE_CURVE ( 'NONE', #51250, #37892, #18277, .T. ) ;
#21781=B_SPLINE_CURVE_WITH_KNOTS ( 'NONE', 3,
 ( #11781, #50580, #1721, #2345 ),
 .UNSPECIFIED., .F., .F.,
 ( 4, 4 ),
 ( 0.000000000000000000, 0.004445488388166992516 ),
 .UNSPECIFIED. ) ;
#21782=CARTESIAN_POINT ( 'NONE',  ( -5.995132425357893702, -16.32377331145314159, -9.414704407577975331 ) ) ;
#21783=CARTESIAN_POINT ( 'NONE',  ( -5.995132425357893702, 18.19985213254571477, 4.885449473615395277 ) ) ;
#21787=CARTESIAN_POINT ( 'NONE',  ( -6.017396004339686577, 2.460690056887785193, 18.68180398134251163 ) ) ;
#21798=DIRECTION ( 'NONE',  ( -0.1024043820194934507, -0.1428674944016075643, 0.9844298967354720986 ) ) ;
#21803=CARTESIAN_POINT ( 'NONE',  ( 0.6027935024548037868, 0.1745403365871484036, -48.10716172909472022 ) ) ;
#21806=VERTEX_POINT ( 'NONE', #12974 ) ;
#21812=CARTESIAN_POINT ( 'NONE',  ( 0.8751705887134423323, 41.19904111682474479, 24.81530984069222256 ) ) ;
#21817=CARTESIAN_POINT ( 'NONE',  ( 0.1103878639767399000, -11.20830530106163891, -41.64243544356624938 ) ) ;
#21819=CARTESIAN_POINT ( 'NONE',  ( 0.6027935024548037868, 41.57475399306886743, 24.20473723001711264 ) ) ;
#21823=ORIENTED_EDGE ( 'NONE', *, *, #19005, .F. ) ;
#21828=CARTESIAN_POINT ( 'NONE',  ( -6.015611763856276717, -18.84324252354755203, -0.006214430185339674118 ) ) ;
#21830=B_SPLINE_CURVE_WITH_KNOTS ( 'NONE', 3,
 ( #50831, #59608, #17034, #36149, #44620, #55213, #60220, #20798, #39936, #58993 ),
 .UNSPECIFIED., .F., .F.,
 ( 4, 3, 3, 4 ),
 ( 1.157434093048479169E-16, 0.0002618519381806257000, 0.0003927759815485975473, 0.0004849530346207898404 ),
 .UNSPECIFIED. ) ;
#21831=ORIENTED_EDGE ( 'NONE', *, *, #18549, .F. ) ;
#21832=CARTESIAN_POINT ( 'NONE',  ( 0.6025881611877910160, -47.66695236827171556, -6.495537368245704712 ) ) ;
#21835=CARTESIAN_POINT ( 'NONE',  ( -6.001507490154111224, 7.196845540359170457, 17.41542759839266452 ) ) ;
#21837=CARTESIAN_POINT ( 'NONE',  ( 0.1073791018717483448, -43.12183934961191056, 0.4849339620931858996 ) ) ;
#21840=CARTESIAN_POINT ( 'NONE',  ( 0.2230388203127615099, 42.84312106681675658, 4.873876086128395180 ) ) ;
#21846=DIRECTION ( 'NONE',  ( 0.000000000000000000, 0.000000000000000000, 1.000000000000000000 ) ) ;
#21848=CARTESIAN_POINT ( 'NONE',  ( 0.1084644655670280039, -25.93599432281523676, 34.45367667780522680 ) ) ;
#21850=CARTESIAN_POINT ( 'NONE',  ( 0.5980894510889457338, -44.17723055703965684, 19.05812566676427977 ) ) ;
#21861=ORIENTED_EDGE ( 'NONE', *, *, #31764, .T. ) ;
#21863=CARTESIAN_POINT ( 'NONE',  ( 3.238931869106853600, 12.88361013339106620, 41.01619136531531495 ) ) ;
#21864=EDGE_CURVE ( 'NONE', #55183, #5629, #20125, .T. ) ;
#21865=CARTESIAN_POINT ( 'NONE',  ( 4.549368137175248350, -18.79584381673559079, 38.59302160394720005 ) ) ;
#21868=EDGE_CURVE ( 'NONE', #12730, #41236, #11152, .T. ) ;
#21877=CARTESIAN_POINT ( 'NONE',  ( 0.6023143664670691511, 38.00627775314922729, 29.49326149840245392 ) ) ;
#21878=( BOUNDED_SURFACE ( )  B_SPLINE_SURFACE ( 3, 1, ( 
 ( #19894, #34288 ),
 ( #34914, #39009 ),
 ( #59300, #15185 ),
 ( #15489, #53366 ) ),
 .UNSPECIFIED., .F., .F., .F. ) 
 B_SPLINE_SURFACE_WITH_KNOTS ( ( 4, 4 ),
 ( 2, 2 ),
 ( 0.000000000000000000, 1.000000000000000000 ),
 ( 0.000000000000000000, 1.000000000000000000 ),
 .UNSPECIFIED. ) 
 GEOMETRIC_REPRESENTATION_ITEM ( )  RATIONAL_B_SPLINE_SURFACE ( (
 ( 1.000000000000000000, 1.000000000000000000),
 ( 0.9953040768229013402, 0.8617119497784988535),
 ( 0.9953040768229013402, 0.8617119497784988535),
 ( 1.000000000000000000, 1.000000000000000000) ) ) 
 REPRESENTATION_ITEM ( '' )  SURFACE ( )  );
#21880=CARTESIAN_POINT ( 'NONE',  ( 0.1073791018717483448, -30.83464511437118816, -30.14884492832378626 ) ) ;
#21883=CARTESIAN_POINT ( 'NONE',  ( 4.322998006666165516, 45.10383234877033232, -16.38761975793161696 ) ) ;
#21892=ORIENTED_EDGE ( 'NONE', *, *, #15884, .T. ) ;
#21898=ORIENTED_EDGE ( 'NONE', *, *, #42724, .F. ) ;
#21910=VERTEX_POINT ( 'NONE', #5973 ) ;
#21913=CARTESIAN_POINT ( 'NONE',  ( 0.1103744047535531458, -26.22174028894846032, -34.23648668783384608 ) ) ;
#21915=FACE_OUTER_BOUND ( 'NONE', #6017, .T. ) ;
#21921=ORIENTED_EDGE ( 'NONE', *, *, #21864, .T. ) ;
#21922=CARTESIAN_POINT ( 'NONE',  ( 0.6041374136657475802, -33.89363087703024746, -34.14050483116125179 ) ) ;
#21924=CARTESIAN_POINT ( 'NONE',  ( 3.680974057930774812, -25.57193971028188173, 40.59247216052809648 ) ) ;
#21929=CARTESIAN_POINT ( 'NONE',  ( 0.7245667037590747261, 7.091191019330228329, 47.57651946688181255 ) ) ;
#21938=CARTESIAN_POINT ( 'NONE',  ( 0.1098349054025746785, -42.72717686504326196, -5.840292671757516985 ) ) ;
#21943=ORIENTED_EDGE ( 'NONE', *, *, #43622, .T. ) ;
#21944=B_SPLINE_CURVE_WITH_KNOTS ( 'NONE', 3,
 ( #2403, #12449, #35029, #54088, #2084, #45054, #21216, #59103, #50631, #3019, #7721, #21525, #40661, #11210, #26842, #45977 ),
 .UNSPECIFIED., .F., .F.,
 ( 4, 3, 3, 3, 3, 4 ),
 ( 1.868480190406682863E-17, 0.0002618515315864400252, 0.0003927756766341985875, 0.0005236998216950590826, 0.0007855159896329929345, 0.001047349442285931773 ),
 .UNSPECIFIED. ) ;
#21945=EDGE_CURVE ( 'NONE', #199, #11845, #21040, .T. ) ;
#21949=CARTESIAN_POINT ( 'NONE',  ( 0.7246131072078564328, -5.464103862701177761, -47.79072675905339906 ) ) ;
#21955=CARTESIAN_POINT ( 'NONE',  ( 0.1103310638050661457, 21.63353985999688689, -37.30561229499308951 ) ) ;
#21959=CARTESIAN_POINT ( 'NONE',  ( 0.8751705887134553219, -44.08562551107095828, 19.22545746485582185 ) ) ;
#21964=B_SPLINE_CURVE_WITH_KNOTS ( 'NONE', 3,
 ( #40226, #38980, #15161, #20170 ),
 .UNSPECIFIED., .F., .F.,
 ( 4, 4 ),
 ( 2.230302957514598322E-17, 0.004564976165746189446 ),
 .UNSPECIFIED. ) ;
#21966=CARTESIAN_POINT ( 'NONE',  ( 0.7246131072078584312, 33.42811616637872163, 34.58859703353090964 ) ) ;
#21969=VECTOR ( 'NONE', #45264, 1000.000000000000114 ) ;
#21971=CARTESIAN_POINT ( 'NONE',  ( 0.6001305935487315502, -47.62765676940948367, 6.798494447611417968 ) ) ;
#21974=CARTESIAN_POINT ( 'NONE',  ( -2.569797478183783568, -8.547745408040883675, 11.87678401312179943 ) ) ;
#21976=LINE ( 'NONE', #30422, #43714 ) ;
#21979=EDGE_CURVE ( 'NONE', #60249, #28915, #11954, .T. ) ;
#21980=LINE ( 'NONE', #6917, #52528 ) ;
#21984=VERTEX_POINT ( 'NONE', #26350 ) ;
#21985=VERTEX_POINT ( 'NONE', #16656 ) ;
#21991=B_SPLINE_CURVE_WITH_KNOTS ( 'NONE', 3,
 ( #73, #14520, #56477, #24510, #33934, #52088, #18294, #28904, #37405, #13592, #32700, #51781, #9180, #28290, #47408, #4452, #23591, #42719, #34239 ),
 .UNSPECIFIED., .F., .F.,
 ( 4, 3, 3, 3, 3, 3, 4 ),
 ( 1.153344816771540786E-16, 0.0002618519381806285731, 0.0003927759815485985231, 0.0005237000248299445142, 0.0006546240681325007525, 0.0007855481115631309744, 0.0009699050456655139776 ),
 .UNSPECIFIED. ) ;
#22006=CARTESIAN_POINT ( 'NONE',  ( 4.549368137175248350, 18.79584381673534565, -38.59302160394733505 ) ) ;
#22009=CARTESIAN_POINT ( 'NONE',  ( 0.6001305935487315502, 11.94532529598313175, 46.60388846085727010 ) ) ;
#22013=AXIS2_PLACEMENT_3D ( 'NONE', #44471, #1201, #53808 ) ;
#22014=ORIENTED_EDGE ( 'NONE', *, *, #30480, .T. ) ;
#22028=CARTESIAN_POINT ( 'NONE',  ( 1.827326673878743923, -15.32882202537249583, -40.22837085190305828 ) ) ;
#22030=EDGE_CURVE ( 'NONE', #61620, #49895, #59725, .T. ) ;
#22032=CARTESIAN_POINT ( 'NONE',  ( 0.6029303876144825880, -33.92442033626760178, -34.10953954078129158 ) ) ;
#22054=CARTESIAN_POINT ( 'NONE',  ( 0.5980894510889457338, -33.52121017007851123, 34.51330645350343929 ) ) ;
#22055=EDGE_CURVE ( 'NONE', #17208, #15365, #38794, .T. ) ;
#22059=CARTESIAN_POINT ( 'NONE',  ( 0.5998501479064708430, -18.89267974119696447, 44.24259072156053918 ) ) ;
#22066=B_SPLINE_CURVE_WITH_KNOTS ( 'NONE', 3,
 ( #5189, #29023, #23709, #61889 ),
 .UNSPECIFIED., .F., .F.,
 ( 4, 4 ),
 ( 1.998817200139820460E-17, 0.004444306975806115029 ),
 .UNSPECIFIED. ) ;
#22070=CARTESIAN_POINT ( 'NONE',  ( -2.569797478183783568, -14.01151037928426035, 4.218948559326007874 ) ) ;
#22080=CARTESIAN_POINT ( 'NONE',  ( 0.2885700199627513340, 29.91358789498782045, -31.05173037893211330 ) ) ;
#22082=VERTEX_POINT ( 'NONE', #41713 ) ;
#22085=LINE ( 'NONE', #59978, #48680 ) ;
#22093=CARTESIAN_POINT ( 'NONE',  ( -6.017396004339687465, 2.458362590802789072, 18.68211039806564600 ) ) ;
#22096=CARTESIAN_POINT ( 'NONE',  ( -6.017396004339687465, 2.460690056888055643, -18.68180398134247255 ) ) ;
#22100=EDGE_CURVE ( 'NONE', #54494, #24199, #6271, .T. ) ;
#22108=ORIENTED_EDGE ( 'NONE', *, *, #56431, .T. ) ;
#22109=VERTEX_POINT ( 'NONE', #14127 ) ;
#22110=CARTESIAN_POINT ( 'NONE',  ( 2.643462169533600914, 46.73820883660206249, -11.09243630552484383 ) ) ;
#22113=B_SPLINE_CURVE_WITH_KNOTS ( 'NONE', 3,
 ( #47065, #7896, #36743, #22622 ),
 .UNSPECIFIED., .F., .F.,
 ( 4, 4 ),
 ( 2.033478910116247305E-17, 0.004444306975806115896 ),
 .UNSPECIFIED. ) ;
#22115=CARTESIAN_POINT ( 'NONE',  ( 0.6254087463353902310, -38.58044986685671063, -28.73645667569937245 ) ) ;
#22118=ORIENTED_EDGE ( 'NONE', *, *, #49394, .F. ) ;
#22122=B_SPLINE_CURVE_WITH_KNOTS ( 'NONE', 3,
 ( #29629, #6409, #54339, #25245 ),
 .UNSPECIFIED., .F., .F.,
 ( 4, 4 ),
 ( 4.670885906470169154E-18, 0.004566006591234646368 ),
 .UNSPECIFIED. ) ;
#22123=CARTESIAN_POINT ( 'NONE',  ( 0.6031356219577719280, 41.70591683999472110, 23.97811961689702542 ) ) ;
#22131=LINE ( 'NONE', #61554, #6936 ) ;
#22132=ORIENTED_EDGE ( 'NONE', *, *, #4432, .F. ) ;
#22133=ADVANCED_FACE ( 'NONE', ( #36703 ), #19689, .F. ) ;
#22138=ORIENTED_EDGE ( 'NONE', *, *, #21708, .T. ) ;
#22140=EDGE_CURVE ( 'NONE', #9409, #6250, #29772, .T. ) ;
#22145=DIRECTION ( 'NONE',  ( -1.000000000000000000, -0.000000000000000000, -0.000000000000000000 ) ) ;
#22149=EDGE_CURVE ( 'NONE', #35726, #3284, #56690, .T. ) ;
#22154=DIRECTION ( 'NONE',  ( -1.000000000000000000, -0.000000000000000000, -0.000000000000000000 ) ) ;
#22156=EDGE_CURVE ( 'NONE', #52389, #34292, #15322, .T. ) ;
#22157=( BOUNDED_SURFACE ( )  B_SPLINE_SURFACE ( 3, 1, ( 
 ( #33582, #37994 ),
 ( #28546, #18872 ),
 ( #13866, #8832 ),
 ( #57649, #47987 ) ),
 .UNSPECIFIED., .F., .F., .F. ) 
 B_SPLINE_SURFACE_WITH_KNOTS ( ( 4, 4 ),
 ( 2, 2 ),
 ( 0.000000000000000000, 1.000000000000000000 ),
 ( 0.000000000000000000, 1.000000000000000000 ),
 .UNSPECIFIED. ) 
 GEOMETRIC_REPRESENTATION_ITEM ( )  RATIONAL_B_SPLINE_SURFACE ( (
 ( 1.000000000000000000, 1.000000000000000000),
 ( 0.9953040768229013402, 0.8617119497784988535),
 ( 0.9953040768229013402, 0.8617119497784988535),
 ( 1.000000000000000000, 1.000000000000000000) ) ) 
 REPRESENTATION_ITEM ( '' )  SURFACE ( )  );
#22158=CARTESIAN_POINT ( 'NONE',  ( 0.1101816497532063510, -26.14462713083321077, 34.29544870207467966 ) ) ;
#22163=CARTESIAN_POINT ( 'NONE',  ( 4.975801465491694664, 47.10002938642141856, -8.787181743659651545 ) ) ;
#22167=CARTESIAN_POINT ( 'NONE',  ( 0.6001305935487315502, -44.64600790884068715, 17.92615948558460559 ) ) ;
#22193=LINE ( 'NONE', #14574, #43255 ) ;
#22208=EDGE_CURVE ( 'NONE', #58926, #54112, #53834, .T. ) ;
#22212=VERTEX_POINT ( 'NONE', #10030 ) ;
#22219=CARTESIAN_POINT ( 'NONE',  ( 2.301430502907644282, 34.86297247504474939, -33.04218380901183139 ) ) ;
#22220=ORIENTED_EDGE ( 'NONE', *, *, #25693, .T. ) ;
#22227=ORIENTED_EDGE ( 'NONE', *, *, #30712, .T. ) ;
#22231=EDGE_LOOP ( 'NONE', ( #43837, #27157, #51868, #8607 ) ) ;
#22249=CARTESIAN_POINT ( 'NONE',  ( -2.569797478183790229, -11.87678401312200371, 8.547745408040595905 ) ) ;
#22263=CARTESIAN_POINT ( 'NONE',  ( 0.1102847568649952675, -16.58813073670681604, -39.80641842112238749 ) ) ;
#22264=DIRECTION ( 'NONE',  ( 0.09835009131224552170, -0.9855991218957039779, 0.1375559175655126365 ) ) ;
#22268=VECTOR ( 'NONE', #8451, 1000.000000000000227 ) ;
#22269=CARTESIAN_POINT ( 'NONE',  ( 0.5980894510889448457, 28.72954109785552745, 38.59343625445455928 ) ) ;
#22273=VERTEX_POINT ( 'NONE', #602 ) ;
#22274=CARTESIAN_POINT ( 'NONE',  ( -2.569797478183783568, -0.4487456364277818133, -14.62602397812941213 ) ) ;
#22278=ORIENTED_EDGE ( 'NONE', *, *, #7952, .F. ) ;
#22292=CARTESIAN_POINT ( 'NONE',  ( 3.680974057930773924, 42.44218549341211144, -22.36814223828923787 ) ) ;
#22293=VERTEX_POINT ( 'NONE', #35084 ) ;
#22296=ORIENTED_EDGE ( 'NONE', *, *, #47556, .F. ) ;
#22299=VERTEX_POINT ( 'NONE', #40724 ) ;
#22305=ORIENTED_EDGE ( 'NONE', *, *, #32821, .F. ) ;
#22311=ORIENTED_EDGE ( 'NONE', *, *, #30602, .F. ) ;
#22320=CARTESIAN_POINT ( 'NONE',  ( 0.3622758884714600280, 15.73321244754796666, 40.13994584881788086 ) ) ;
#22322=CARTESIAN_POINT ( 'NONE',  ( 0.6001305935487422083, 41.92422178329137239, 23.60027211631843969 ) ) ;
#22335=CARTESIAN_POINT ( 'NONE',  ( 4.549368137175248350, -32.41327393324159800, 28.14399996863441800 ) ) ;
#22343=CARTESIAN_POINT ( 'NONE',  ( 4.975801465491695552, 26.14269827151680659, -40.15204426031507268 ) ) ;
#22344=CARTESIAN_POINT ( 'NONE',  ( 2.643462169533613793, 34.93025802711680683, 32.97543604874687873 ) ) ;
#22348=DIRECTION ( 'NONE',  ( 0.000000000000000000, 0.000000000000000000, 1.000000000000000000 ) ) ;
#22354=EDGE_CURVE ( 'NONE', #2002, #58167, #15078, .T. ) ;
#22363=CARTESIAN_POINT ( 'NONE',  ( 0.1073791018717578927, 21.14095454447508615, 37.58707531572213156 ) ) ;
#22370=CARTESIAN_POINT ( 'NONE',  ( 4.833616638992208614, 30.15290813935903103, -35.06988470649537959 ) ) ;
#22379=ORIENTED_EDGE ( 'NONE', *, *, #51400, .F. ) ;
#22381=CARTESIAN_POINT ( 'NONE',  ( 2.643462169533613793, -34.93025802711703420, -32.97543604874663714 ) ) ;
#22388=CARTESIAN_POINT ( 'NONE',  ( -6.016489644550737204, -0.004404229197908116067, 18.84320342686341121 ) ) ;
#22390=FACE_OUTER_BOUND ( 'NONE', #55025, .T. ) ;
#22399=CARTESIAN_POINT ( 'NONE',  ( 0.5998501479064699549, -0.5236536531311584142, -48.10473956285919428 ) ) ;
#22412=EDGE_CURVE ( 'NONE', #5908, #42065, #27052, .T. ) ;
#22413=CARTESIAN_POINT ( 'NONE',  ( 0.2885697896453107147, 6.424755442172600972, -42.63514065501009043 ) ) ;
#22419=CARTESIAN_POINT ( 'NONE',  ( -2.569797478183783568, -3.352038560006015189, 14.24379821351251429 ) ) ;
#22423=CARTESIAN_POINT ( 'NONE',  ( 0.1073791018717483448, 5.147744207006859973, -42.81622261970989030 ) ) ;
#22424=( BOUNDED_SURFACE ( )  B_SPLINE_SURFACE ( 3, 1, ( 
 ( #52214, #28730 ),
 ( #24030, #52522 ),
 ( #33139, #28112 ),
 ( #4278, #47851 ) ),
 .UNSPECIFIED., .F., .F., .F. ) 
 B_SPLINE_SURFACE_WITH_KNOTS ( ( 4, 4 ),
 ( 2, 2 ),
 ( 0.000000000000000000, 1.000000000000000000 ),
 ( 0.000000000000000000, 1.000000000000000000 ),
 .UNSPECIFIED. ) 
 GEOMETRIC_REPRESENTATION_ITEM ( )  RATIONAL_B_SPLINE_SURFACE ( (
 ( 1.000000000000000000, 1.000000000000000000),
 ( 0.7223157951917480446, 0.9931996967497186413),
 ( 0.7223157951917480446, 0.9931996967497186413),
 ( 1.000000000000000000, 1.000000000000000000) ) ) 
 REPRESENTATION_ITEM ( '' )  SURFACE ( )  );
#22430=CARTESIAN_POINT ( 'NONE',  ( 0.6031357023905874470, 41.64046004335383344, 24.09149424676630957 ) ) ;
#22440=ORIENTED_EDGE ( 'NONE', *, *, #11415, .T. ) ;
#22441=CARTESIAN_POINT ( 'NONE',  ( 2.643462169533613793, -47.78621045426871916, -4.896978544601982897 ) ) ;
#22443=VERTEX_POINT ( 'NONE', #37800 ) ;
#22445=CARTESIAN_POINT ( 'NONE',  ( 0.1064266379913941241, 34.55203636557774161, 25.80493164505215375 ) ) ;
#22451=VERTEX_POINT ( 'NONE', #57450 ) ;
#22455=CARTESIAN_POINT ( 'NONE',  ( 0.1064266418746777770, 25.80493189480185379, 34.55203617814598260 ) ) ;
#22462=VERTEX_POINT ( 'NONE', #9558 ) ;
#22467=CARTESIAN_POINT ( 'NONE',  ( 0.5998501479064699549, -37.84527566984877467, 29.69975237324549155 ) ) ;
#22468=CARTESIAN_POINT ( 'NONE',  ( 0.8760168074886965917, -44.77533136581894269, 17.58183840866320224 ) ) ;
#22471=CARTESIAN_POINT ( 'NONE',  ( 0.5998501479064708430, -11.94461217097437000, -46.60114184914313995 ) ) ;
#22472=VERTEX_POINT ( 'NONE', #43102 ) ;
#22482=CARTESIAN_POINT ( 'NONE',  ( 0.1064266418746778603, -11.70292610004353762, 41.50637583369802286 ) ) ;
#22489=FACE_OUTER_BOUND ( 'NONE', #61558, .T. ) ;
#22491=CONICAL_SURFACE ( 'NONE', #5462, 42.92674063221959813, 1.485477209440487556 ) ;
#22492=EDGE_CURVE ( 'NONE', #24440, #27931, #61850, .T. ) ;
#22498=AXIS2_PLACEMENT_3D ( 'NONE', #22911, #13514, #18517 ) ;
#22499=CARTESIAN_POINT ( 'NONE',  ( 0.8751705887134553219, -44.76769609654225235, -17.57879340691528469 ) ) ;
#22500=CARTESIAN_POINT ( 'NONE',  ( 3.680974057930773480, -10.62112035260209808, -46.78530430706934595 ) ) ;
#22509=CARTESIAN_POINT ( 'NONE',  ( -6.001507490154110336, -11.45906331631441866, 14.95933060264870029 ) ) ;
#22522=CARTESIAN_POINT ( 'NONE',  ( 0.8760168074887076939, -46.68716261866168082, -11.58706983520309208 ) ) ;
#22523=ORIENTED_EDGE ( 'NONE', *, *, #44485, .T. ) ;
#22524=CARTESIAN_POINT ( 'NONE',  ( 0.6001305935487422083, 17.92615948558477967, 44.64600790884061610 ) ) ;
#22525=CARTESIAN_POINT ( 'NONE',  ( 3.680974057930773924, 35.20670187740660140, -32.59081219553993236 ) ) ;
#22534=CARTESIAN_POINT ( 'NONE',  ( 0.8760168074887090262, -0.8912768426702896152, -48.09529047980637273 ) ) ;
#22537=ORIENTED_EDGE ( 'NONE', *, *, #59158, .T. ) ;
#22539=CARTESIAN_POINT ( 'NONE',  ( 4.975801465491695552, 46.87746200127456575, -9.906103548667728020 ) ) ;
#22540=CARTESIAN_POINT ( 'NONE',  ( 0.8751705887134423323, -24.81530984069236823, 41.19904111682465242 ) ) ;
#22543=CARTESIAN_POINT ( 'NONE',  ( -2.708315649062916552, -11.44805714186577639, 9.116606751444143342 ) ) ;
#22565=EDGE_LOOP ( 'NONE', ( #59151, #11549, #10681, #46916 ) ) ;
#22568=CARTESIAN_POINT ( 'NONE',  ( 0.7954190325252789018, 46.22745637125041895, -13.28627193046320620 ) ) ;
#22581=ORIENTED_EDGE ( 'NONE', *, *, #6430, .F. ) ;
#22586=CARTESIAN_POINT ( 'NONE',  ( 3.680974057930773036, 47.28851186370997084, 8.091325130366584517 ) ) ;
#22588=CARTESIAN_POINT ( 'NONE',  ( -5.995132425357893702, 4.885449473615331328, 18.19985213254573964 ) ) ;
#22592=ORIENTED_EDGE ( 'NONE', *, *, #40276, .F. ) ;
#22594=CARTESIAN_POINT ( 'NONE',  ( 0.7048096507298579061, -33.41730025321730579, -34.61049487267047908 ) ) ;
#22598=ORIENTED_EDGE ( 'NONE', *, *, #47647, .F. ) ;
#22602=FACE_OUTER_BOUND ( 'NONE', #29884, .T. ) ;
#22603=ORIENTED_EDGE ( 'NONE', *, *, #57664, .F. ) ;
#22608=ORIENTED_EDGE ( 'NONE', *, *, #61962, .T. ) ;
#22611=CARTESIAN_POINT ( 'NONE',  ( 4.833616638992208614, -30.15290813935929748, 35.06988470649517353 ) ) ;
#22612=CARTESIAN_POINT ( 'NONE',  ( 0.6254311100348634023, -41.31309618784398907, -24.64676532715779800 ) ) ;
#22619=CARTESIAN_POINT ( 'NONE',  ( 0.6001305935487422083, -28.87057754790966513, 38.48510059943998129 ) ) ;
#22622=CARTESIAN_POINT ( 'NONE',  ( 4.975801465491694664, 47.84403947906843513, -2.564218696446985302 ) ) ;
#22624=CARTESIAN_POINT ( 'NONE',  ( 0.3622758884714600280, -4.808133778521581192, -42.84426538328729350 ) ) ;
#22626=ORIENTED_EDGE ( 'NONE', *, *, #60033, .T. ) ;
#22627=CARTESIAN_POINT ( 'NONE',  ( 4.549368137175248350, -28.14399996863474129, -32.41327393324131378 ) ) ;
#22635=CARTESIAN_POINT ( 'NONE',  ( 0.1073791018717578927, 39.65380858626191696, 16.95003405440326816 ) ) ;
#22642=CARTESIAN_POINT ( 'NONE',  ( 0.2230388203127557090, -15.79641846944945094, 40.12182516270770805 ) ) ;
#22643=CARTESIAN_POINT ( 'NONE',  ( 4.975801465491695552, 46.87746200127456575, -9.906103548667728020 ) ) ;
#22648=CARTESIAN_POINT ( 'NONE',  ( 0.8751705887134553219, 42.09020928323342758, 23.27176129838440488 ) ) ;
#22649=CARTESIAN_POINT ( 'NONE',  ( 4.322998006666165516, 10.36018990813247775, 46.85697641700711813 ) ) ;
#22650=CARTESIAN_POINT ( 'NONE',  ( 4.975801465491695552, -21.70134120755170315, -42.71626295676257001 ) ) ;
#22652=ORIENTED_EDGE ( 'NONE', *, *, #61796, .F. ) ;
#22654=EDGE_CURVE ( 'NONE', #44040, #30112, #852, .T. ) ;
#22659=EDGE_CURVE ( 'NONE', #37338, #14715, #41486, .T. ) ;
#22663=VERTEX_POINT ( 'NONE', #60548 ) ;
#22665=CARTESIAN_POINT ( 'NONE',  ( 0.3622758884714600280, -26.89560658783410574, 33.69533458712297147 ) ) ;
#22674=CARTESIAN_POINT ( 'NONE',  ( 4.975801465491695552, 0.000000000000000000, 0.000000000000000000 ) ) ;
#22683=CARTESIAN_POINT ( 'NONE',  ( 0.6041374136657475802, 34.14050483116137258, -33.89363087703013377 ) ) ;
#22684=CARTESIAN_POINT ( 'NONE',  ( 0.6027935024548038978, 34.14031893787224448, -33.89348162668942166 ) ) ;
#22688=CARTESIAN_POINT ( 'NONE',  ( -6.017396004339687465, 9.422598049764850714, -16.31807101179360942 ) ) ;
#22690=B_SPLINE_CURVE_WITH_KNOTS ( 'NONE', 3,
 ( #53793, #6176, #43844, #30619 ),
 .UNSPECIFIED., .F., .F.,
 ( 4, 4 ),
 ( 6.992893892674702526E-18, 0.005014147105413695182 ),
 .UNSPECIFIED. ) ;
#22692=ORIENTED_EDGE ( 'NONE', *, *, #54001, .T. ) ;
#22702=CARTESIAN_POINT ( 'NONE',  ( -6.010958268070873523, -16.32616437357105710, -9.409153349053758220 ) ) ;
#22703=CARTESIAN_POINT ( 'NONE',  ( 0.1073791018717483448, 42.68962945260953035, -6.109314776652274404 ) ) ;
#22706=ADVANCED_FACE ( 'NONE', ( #31445 ), #59731, .F. ) ;
#22714=DIRECTION ( 'NONE',  ( -1.000000000000000000, -0.000000000000000000, -0.000000000000000000 ) ) ;
#22715=CARTESIAN_POINT ( 'NONE',  ( -6.015611763856276717, -18.68122482568278286, -2.465697960551244350 ) ) ;
#22718=CARTESIAN_POINT ( 'NONE',  ( -2.569797478183790229, -9.259773107243150392, 11.33042594333532271 ) ) ;
#22725=CARTESIAN_POINT ( 'NONE',  ( 0.3622758884714600280, 33.69533458712307095, 26.89560658783397074 ) ) ;
#22726=CARTESIAN_POINT ( 'NONE',  ( 0.6009452777970410997, -46.57942614304348439, -12.02913818029296422 ) ) ;
#22735=CARTESIAN_POINT ( 'NONE',  ( 0.1098349054025746785, 5.840292671757666199, -42.72717686504323353 ) ) ;
#22741=CARTESIAN_POINT ( 'NONE',  ( 0.8760168074886965917, 46.22580377597767409, 13.30888447662096929 ) ) ;
#22765=ORIENTED_EDGE ( 'NONE', *, *, #37568, .F. ) ;
#22772=CARTESIAN_POINT ( 'NONE',  ( 3.680882792899938138, 47.28852514876955837, -8.091276083384906670 ) ) ;
#22776=CARTESIAN_POINT ( 'NONE',  ( 4.549368137175248350, 0.000000000000000000, 0.000000000000000000 ) ) ;
#22779=CARTESIAN_POINT ( 'NONE',  ( 0.6027935024548037868, 47.71838037711334124, -6.106197519200991408 ) ) ;
#22780=VERTEX_POINT ( 'NONE', #42707 ) ;
#22789=CARTESIAN_POINT ( 'NONE',  ( 4.549368137175248350, 40.71620287708324781, 13.59764261105765826 ) ) ;
#22792=FACE_OUTER_BOUND ( 'NONE', #34074, .T. ) ;
#22799=CARTESIAN_POINT ( 'NONE',  ( 4.691466044806103852, -43.66525414675648875, 9.025781474740702137 ) ) ;
#22801=ORIENTED_EDGE ( 'NONE', *, *, #19107, .T. ) ;
#22808=CARTESIAN_POINT ( 'NONE',  ( 0.1064266418746775411, 26.69589626339711685, -33.86837517279519716 ) ) ;
#22816=ORIENTED_EDGE ( 'NONE', *, *, #60017, .T. ) ;
#22825=CARTESIAN_POINT ( 'NONE',  ( 4.549368137175248350, -42.84816078363928682, -2.596185425821792236 ) ) ;
#22833=ADVANCED_FACE ( 'NONE', ( #37100 ), #18989, .F. ) ;
#22835=ORIENTED_EDGE ( 'NONE', *, *, #47760, .T. ) ;
#22840=CARTESIAN_POINT ( 'NONE',  ( 4.833616638992205949, 45.27110352095233736, 9.466882727842298451 ) ) ;
#22845=CARTESIAN_POINT ( 'NONE',  ( 0.1102847568649952675, -16.41780866919068771, 39.87696813145900876 ) ) ;
#22847=ORIENTED_EDGE ( 'NONE', *, *, #14134, .T. ) ;
#22854=DIRECTION ( 'NONE',  ( 0.000000000000000000, 0.000000000000000000, 1.000000000000000000 ) ) ;
#22857=B_SPLINE_CURVE_WITH_KNOTS ( 'NONE', 3,
 ( #59846, #36076, #8151, #46089, #3135, #55134, #22263, #12260, #60445, #51055, #27266, #52285, #29111, #32592, #33833, #33214, #47926, #27882, #47010 ),
 .UNSPECIFIED., .F., .F.,
 ( 4, 3, 3, 3, 3, 3, 4 ),
 ( 1.153344816771540786E-16, 0.0002618519381806349699, 0.0003927759815486002036, 0.0005237000248299497184, 0.0006546240681325027040, 0.0007855481115631361786, 0.0009699050456655135440 ),
 .UNSPECIFIED. ) ;
#22858=CARTESIAN_POINT ( 'NONE',  ( 0.6001305935487422083, 41.40054608060292907, -24.50730504006414634 ) ) ;
#22870=( NAMED_UNIT ( * ) PLANE_ANGLE_UNIT ( ) SI_UNIT ( $, .RADIAN. ) );
#22872=ORIENTED_EDGE ( 'NONE', *, *, #28790, .T. ) ;
#22876=CARTESIAN_POINT ( 'NONE',  ( -6.010958268070873523, -9.409153349053701376, 16.32616437357108907 ) ) ;
#22877=CARTESIAN_POINT ( 'NONE',  ( 0.1073791018717578927, 21.98088480513665388, -37.10214135362866728 ) ) ;
#22888=AXIS2_PLACEMENT_3D ( 'NONE', #52991, #10094, #5362 ) ;
#22890=AXIS2_PLACEMENT_3D ( 'NONE', #389, #52720, #38655 ) ;
#22904=CARTESIAN_POINT ( 'NONE',  ( 4.549368137175248350, -8.166781970325423856, -42.14271863032831078 ) ) ;
#22909=EDGE_LOOP ( 'NONE', ( #39283, #29471, #52803, #14220 ) ) ;
#22911=CARTESIAN_POINT ( 'NONE',  ( 4.549368137175248350, 0.000000000000000000, 0.000000000000000000 ) ) ;
#22915=ORIENTED_EDGE ( 'NONE', *, *, #10005, .F. ) ;
#22917=CARTESIAN_POINT ( 'NONE',  ( -6.001507490154111224, 16.31148204059947204, 9.435425682280875748 ) ) ;
#22919=CARTESIAN_POINT ( 'NONE',  ( 0.8751705887134423323, 48.08707113907594533, 0.8911681664090089772 ) ) ;
#22926=CARTESIAN_POINT ( 'NONE',  ( 4.691466044806103852, 44.46979273209135641, -3.249105306917955627 ) ) ;
#22928=ORIENTED_EDGE ( 'NONE', *, *, #6123, .F. ) ;
#22930=CARTESIAN_POINT ( 'NONE',  ( 4.975801465491694664, -31.15993731089097452, -36.39623109580456628 ) ) ;
#22935=CARTESIAN_POINT ( 'NONE',  ( 1.827119703190779765, -6.838980420687682305, -42.50321986945166230 ) ) ;
#22941=CARTESIAN_POINT ( 'NONE',  ( 0.5998501479064708430, 47.76154736470757456, -5.759754759340284913 ) ) ;
#22948=CARTESIAN_POINT ( 'NONE',  ( 0.6001305935487422083, -47.76436356026972163, 5.760103278697227935 ) ) ;
#22952=CARTESIAN_POINT ( 'NONE',  ( 0.5998501479064708430, 38.48283596222029956, -28.86886762351084812 ) ) ;
#22958=CARTESIAN_POINT ( 'NONE',  ( 4.322998006666179727, 16.38761975793208947, -45.10383234877016889 ) ) ;
#22959=CARTESIAN_POINT ( 'NONE',  ( -6.016761891674565099, -11.46828378093549361, -14.95139917749716041 ) ) ;
#22965=CARTESIAN_POINT ( 'NONE',  ( 4.975801465491695552, 9.906103548667566372, 46.87746200127460128 ) ) ;
#22980=EDGE_LOOP ( 'NONE', ( #55773, #20747, #46954, #44261 ) ) ;
#22981=CARTESIAN_POINT ( 'NONE',  ( 0.6025881611877910160, -38.03302298778322665, -29.45877655626779656 ) ) ;
#22986=ORIENTED_EDGE ( 'NONE', *, *, #8686, .T. ) ;
#22989=CARTESIAN_POINT ( 'NONE',  ( 0.2885700199627520002, 15.75356883787153528, -40.13549263616307883 ) ) ;
#22994=CARTESIAN_POINT ( 'NONE',  ( 0.6009453534118439633, -48.10564080474284765, -0.4363813339956353898 ) ) ;
#22998=EDGE_CURVE ( 'NONE', #14276, #58372, #728, .T. ) ;
#23000=ORIENTED_EDGE ( 'NONE', *, *, #53462, .F. ) ;
#23002=FACE_OUTER_BOUND ( 'NONE', #61271, .T. ) ;
#23011=B_SPLINE_CURVE_WITH_KNOTS ( 'NONE', 3,
 ( #48393, #16423, #24590, #19914, #39025, #29279, #58080, #29587, #53382, #44043, #48699, #39321, #59011, #11118, #6063, #6364 ),
 .UNSPECIFIED., .F., .F.,
 ( 4, 3, 3, 3, 3, 4 ),
 ( 2.501947744657918636E-17, 0.0002618515315864388868, 0.0003927756766341969612, 0.0005236998216950529026, 0.0007855159896329866462, 0.001047349442285926135 ),
 .UNSPECIFIED. ) ;
#23012=CARTESIAN_POINT ( 'NONE',  ( 0.1073791018717483448, 39.65380858626214433, -16.95003405440273525 ) ) ;
#23019=ORIENTED_EDGE ( 'NONE', *, *, #12447, .F. ) ;
#23021=CARTESIAN_POINT ( 'NONE',  ( -6.016489644550736315, 18.84320342686341121, -0.004404229197841518298 ) ) ;
#23022=CARTESIAN_POINT ( 'NONE',  ( 4.549368137175248350, -42.14271863032827525, -8.166781970325585505 ) ) ;
#23027=CARTESIAN_POINT ( 'NONE',  ( 0.3622758884714600280, 42.84426538328730771, -4.808133778521432866 ) ) ;
#23035=B_SPLINE_CURVE_WITH_KNOTS ( 'NONE', 3,
 ( #23605, #51172, #28303, #47420 ),
 .UNSPECIFIED., .F., .F.,
 ( 4, 4 ),
 ( 5.553824967135426632E-18, 0.004566006591234645501 ),
 .UNSPECIFIED. ) ;
#23038=CARTESIAN_POINT ( 'NONE',  ( 0.1100247026804066219, 42.73303500775678998, 5.797046384220007731 ) ) ;
#23042=DIRECTION ( 'NONE',  ( -1.000000000000000000, -0.000000000000000000, -0.000000000000000000 ) ) ;
#23053=CARTESIAN_POINT ( 'NONE',  ( 0.6009453534118440743, -44.27682103112819334, -18.81239552212969457 ) ) ;
#23056=EDGE_LOOP ( 'NONE', ( #30708, #53711, #25845, #7005 ) ) ;
#23066=CIRCLE ( 'NONE', #1044, 42.92674063221959813 ) ;
#23068=ORIENTED_EDGE ( 'NONE', *, *, #12109, .F. ) ;
#23082=EDGE_LOOP ( 'NONE', ( #43201, #1103, #24743, #17646 ) ) ;
#23086=CARTESIAN_POINT ( 'NONE',  ( 4.549368137175248350, 28.46244473166673927, -32.13400537129894730 ) ) ;
#23095=CARTESIAN_POINT ( 'NONE',  ( 0.7048096507298579061, -44.76417498422327412, 17.62869676200329749 ) ) ;
#23100=CARTESIAN_POINT ( 'NONE',  ( -2.708315649062916552, 14.63219292706383001, -0.2635547933242103902 ) ) ;
#23101=CARTESIAN_POINT ( 'NONE',  ( 0.5998501479064699549, 29.69975237324562656, 37.84527566984866809 ) ) ;
#23106=CARTESIAN_POINT ( 'NONE',  ( 0.5998501479064708430, -23.59887241503325228, -41.92175333043611829 ) ) ;
#23107=B_SPLINE_CURVE_WITH_KNOTS ( 'NONE', 3,
 ( #43861, #904, #25033, #20040 ),
 .UNSPECIFIED., .F., .F.,
 ( 4, 4 ),
 ( 6.254634441385501517E-18, 0.004566006591234646368 ),
 .UNSPECIFIED. ) ;
#23109=CARTESIAN_POINT ( 'NONE',  ( 0.5988103564986354543, -41.35593036885951790, 24.57719524907170339 ) ) ;
#23110=FACE_OUTER_BOUND ( 'NONE', #7160, .T. ) ;
#23115=CARTESIAN_POINT ( 'NONE',  ( 0.5998501479064699549, -34.38546660123274989, -33.64490850298832925 ) ) ;
#23117=CARTESIAN_POINT ( 'NONE',  ( 0.8751705887134423323, 47.55935879196461968, 7.160166390004468973 ) ) ;
#23118=CARTESIAN_POINT ( 'NONE',  ( 4.691466044806102076, -43.79545162262314761, 8.371234562541101099 ) ) ;
#23121=CARTESIAN_POINT ( 'NONE',  ( 0.2885697896453115474, 26.88157175352887762, -33.71073718007512099 ) ) ;
#23126=CARTESIAN_POINT ( 'NONE',  ( 4.322998006666165516, 47.25487450103524623, 8.359821156456641589 ) ) ;
#23130=CARTESIAN_POINT ( 'NONE',  ( -6.001507490154111224, -4.862106078787797436, -18.20581304543303247 ) ) ;
#23132=CARTESIAN_POINT ( 'NONE',  ( 0.6031356219577719280, 23.97811961689687976, -41.70591683999481347 ) ) ;
#23137=CARTESIAN_POINT ( 'NONE',  ( -6.016489644550737204, -11.46752133529374973, -14.95199950534959754 ) ) ;
#23138=CARTESIAN_POINT ( 'NONE',  ( 0.2230388203127549596, 22.21453373073337900, 36.95676097786386549 ) ) ;
#23139=ORIENTED_EDGE ( 'NONE', *, *, #35309, .F. ) ;
#23141=CARTESIAN_POINT ( 'NONE',  ( 0.1104177457020372732, 26.25638621857945765, 34.20994892372218033 ) ) ;
#23142=EDGE_CURVE ( 'NONE', #20774, #60202, #24716, .T. ) ;
#23146=ORIENTED_EDGE ( 'NONE', *, *, #41759, .F. ) ;
#23149=( BOUNDED_SURFACE ( )  B_SPLINE_SURFACE ( 3, 1, ( 
 ( #51190, #3567 ),
 ( #23021, #51808 ),
 ( #55892, #38065 ),
 ( #52420, #52116 ) ),
 .UNSPECIFIED., .F., .F., .F. ) 
 B_SPLINE_SURFACE_WITH_KNOTS ( ( 4, 4 ),
 ( 2, 2 ),
 ( 0.000000000000000000, 1.000000000000000000 ),
 ( 0.000000000000000000, 1.000000000000000000 ),
 .UNSPECIFIED. ) 
 GEOMETRIC_REPRESENTATION_ITEM ( )  RATIONAL_B_SPLINE_SURFACE ( (
 ( 1.000000000000000000, 1.000000000000000000),
 ( 0.9953040768229013402, 0.8617119497784988535),
 ( 0.9953040768229013402, 0.8617119497784988535),
 ( 1.000000000000000000, 1.000000000000000000) ) ) 
 REPRESENTATION_ITEM ( '' )  SURFACE ( )  );
#23151=LINE ( 'NONE', #57241, #31151 ) ;
#23162=CARTESIAN_POINT ( 'NONE',  ( 0.5998501479064708430, -24.50586714782633280, 41.39809967730445095 ) ) ;
#23169=CARTESIAN_POINT ( 'NONE',  ( 0.1103310638050662013, -34.26302445194765056, 26.18709435931468121 ) ) ;
#23173=CARTESIAN_POINT ( 'NONE',  ( 0.3622758884714730732, -10.35929834645951964, 41.85013935980084199 ) ) ;
#23188=CARTESIAN_POINT ( 'NONE',  ( 4.549368137175248350, 35.80950303116100741, -23.67244292351601942 ) ) ;
#23189=EDGE_CURVE ( 'NONE', #32871, #48869, #61351, .T. ) ;
#23190=EDGE_CURVE ( 'NONE', #38885, #23714, #39140, .T. ) ;
#23198=CARTESIAN_POINT ( 'NONE',  ( 5.880360259849739535, -9.405269135694920735, -47.04104239318763803 ) ) ;
#23202=CIRCLE ( 'NONE', #31206, 43.12527911185304674 ) ;
#23207=EDGE_CURVE ( 'NONE', #35477, #2725, #3717, .T. ) ;
#23209=CARTESIAN_POINT ( 'NONE',  ( 0.6254311100348646235, 46.28443883864375152, 13.11433105842157509 ) ) ;
#23218=EDGE_CURVE ( 'NONE', #23536, #39132, #46008, .T. ) ;
#23233=B_SPLINE_CURVE_WITH_KNOTS ( 'NONE', 3,
 ( #24069, #4312, #61634, #18766 ),
 .UNSPECIFIED., .F., .F.,
 ( 4, 4 ),
 ( 0.000000000000000000, 0.004445488388166991649 ),
 .UNSPECIFIED. ) ;
#23238=ORIENTED_EDGE ( 'NONE', *, *, #30185, .T. ) ;
#23240=CARTESIAN_POINT ( 'NONE',  ( 0.5980894510889448457, 46.65000524237087376, -11.77356634613269470 ) ) ;
#23246=CARTESIAN_POINT ( 'NONE',  ( 2.643462169533613793, 43.83256147628732435, -19.65219740572143792 ) ) ;
#23263=DIRECTION ( 'NONE',  ( 0.1024043820194936172, 0.2447326578667328445, -0.9641676559171078464 ) ) ;
#23281=B_SPLINE_CURVE_WITH_KNOTS ( 'NONE', 3,
 ( #34903, #53965, #44613, #53355 ),
 .UNSPECIFIED., .F., .F.,
 ( 4, 4 ),
 ( 1.969819611697804288E-17, 0.004444306975806115896 ),
 .UNSPECIFIED. ) ;
#23282=CARTESIAN_POINT ( 'NONE',  ( 0.6023142530420679819, -38.32506243004171864, -29.07781306567088109 ) ) ;
#23286=ORIENTED_EDGE ( 'NONE', *, *, #26219, .F. ) ;
#23287=VERTEX_POINT ( 'NONE', #38830 ) ;
#23296=ORIENTED_EDGE ( 'NONE', *, *, #49157, .F. ) ;
#23298=CARTESIAN_POINT ( 'NONE',  ( 0.5980894510889448457, -29.84264441023806569, 37.73932204245466693 ) ) ;
#23303=CARTESIAN_POINT ( 'NONE',  ( -6.016489644550737204, 11.46752133529384565, 14.95199950534952293 ) ) ;
#23304=CARTESIAN_POINT ( 'NONE',  ( -6.015611763856276717, 2.453375430804066504, 18.68284711750059301 ) ) ;
#23305=EDGE_CURVE ( 'NONE', #43871, #58483, #4486, .T. ) ;
#23306=B_SPLINE_CURVE_WITH_KNOTS ( 'NONE', 3,
 ( #47772, #38388, #57436, #53066 ),
 .UNSPECIFIED., .F., .F.,
 ( 4, 4 ),
 ( 2.384850491544188529E-17, 0.004564976165746187711 ),
 .UNSPECIFIED. ) ;
#23308=CARTESIAN_POINT ( 'NONE',  ( -6.017396004339686577, 9.420565012089657131, -16.31924478664265621 ) ) ;
#23311=EDGE_CURVE ( 'NONE', #36718, #13235, #18735, .T. ) ;
#23312=CARTESIAN_POINT ( 'NONE',  ( -6.016489644550737204, -18.68257207665197939, 2.455165042129670905 ) ) ;
#23314=ORIENTED_EDGE ( 'NONE', *, *, #25556, .T. ) ;
#23321=CARTESIAN_POINT ( 'NONE',  ( 4.549368137175248350, 0.000000000000000000, 0.000000000000000000 ) ) ;
#23326=CARTESIAN_POINT ( 'NONE',  ( 1.827326673878743923, -33.38933471001457320, -27.17438009792320486 ) ) ;
#23328=DIRECTION ( 'NONE',  ( 0.1024043820194936449, -0.9641676559171085126, -0.2447326578667294861 ) ) ;
#23340=CARTESIAN_POINT ( 'NONE',  ( 4.975801465491694664, 47.76942479135480824, 3.702618843597622167 ) ) ;
#23341=EDGE_CURVE ( 'NONE', #49359, #42620, #61190, .T. ) ;
#23346=EDGE_CURVE ( 'NONE', #30431, #30079, #8166, .T. ) ;
#23348=ORIENTED_EDGE ( 'NONE', *, *, #53235, .T. ) ;
#23353=DIRECTION ( 'NONE',  ( 1.000000000000000000, 0.000000000000000000, 0.000000000000000000 ) ) ;
#23356=VECTOR ( 'NONE', #48552, 1000.000000000000000 ) ;
#23360=ORIENTED_EDGE ( 'NONE', *, *, #11424, .F. ) ;
#23361=EDGE_CURVE ( 'NONE', #58926, #14715, #25370, .T. ) ;
#23362=LINE ( 'NONE', #42485, #44337 ) ;
#23365=CARTESIAN_POINT ( 'NONE',  ( -6.016104459813374383, 13.32039631884684638, 13.32794178585002243 ) ) ;
#23366=CARTESIAN_POINT ( 'NONE',  ( 0.1064266379913941102, 10.61815631313362118, -41.79703901861807935 ) ) ;
#23370=DIRECTION ( 'NONE',  ( 0.09835009131224567436, -0.1222230102474943930, -0.9876177374393970698 ) ) ;
#23371=EDGE_LOOP ( 'NONE', ( #53850, #11685, #22118, #1689 ) ) ;
#23373=DIRECTION ( 'NONE',  ( 0.000000000000000000, 0.000000000000000000, 1.000000000000000000 ) ) ;
#23376=VECTOR ( 'NONE', #35679, 1000.000000000000114 ) ;
#23385=ORIENTED_EDGE ( 'NONE', *, *, #49210, .T. ) ;
#23393=CIRCLE ( 'NONE', #40409, 42.92674063221959813 ) ;
#23397=CARTESIAN_POINT ( 'NONE',  ( 4.549368137175248350, 0.000000000000000000, 0.000000000000000000 ) ) ;
#23398=CARTESIAN_POINT ( 'NONE',  ( 0.1092355843206037486, 26.49036028133781429, -34.02913268098563293 ) ) ;
#23401=DIRECTION ( 'NONE',  ( 0.000000000000000000, 0.000000000000000000, 1.000000000000000000 ) ) ;
#23408=FACE_OUTER_BOUND ( 'NONE', #54711, .T. ) ;
#23413=EDGE_CURVE ( 'NONE', #7392, #37162, #15623, .T. ) ;
#23425=CARTESIAN_POINT ( 'NONE',  ( 0.6017666602106488405, -37.95277954208655302, 29.56224131406205657 ) ) ;
#23426=B_SPLINE_CURVE_WITH_KNOTS ( 'NONE', 3,
 ( #55246, #50868, #22370, #60564 ),
 .UNSPECIFIED., .F., .F.,
 ( 4, 4 ),
 ( 0.000000000000000000, 0.005014147105413709060 ),
 .UNSPECIFIED. ) ;
#23432=EDGE_CURVE ( 'NONE', #40711, #12159, #52206, .T. ) ;
#23433=CARTESIAN_POINT ( 'NONE',  ( 4.549368137175248350, 0.000000000000000000, 0.000000000000000000 ) ) ;
#23439=CARTESIAN_POINT ( 'NONE',  ( 0.6041374136657475802, -44.51224464245012058, 18.24862627831457118 ) ) ;
#23443=CARTESIAN_POINT ( 'NONE',  ( 3.238931869106854489, 42.82436385108074717, 3.793313187127091979 ) ) ;
#23444=CARTESIAN_POINT ( 'NONE',  ( 0.1092355843206037486, 26.01340835034366705, 34.39511076960612002 ) ) ;
#23451=EDGE_CURVE ( 'NONE', #20684, #14890, #36599, .T. ) ;
#23458=CARTESIAN_POINT ( 'NONE',  ( 2.643462169533613793, 19.65219740572127094, 43.83256147628741672 ) ) ;
#23462=ORIENTED_EDGE ( 'NONE', *, *, #7655, .T. ) ;
#23463=CARTESIAN_POINT ( 'NONE',  ( -6.016489644550736315, -2.463898142942639424, -18.68142234211826747 ) ) ;
#23467=CARTESIAN_POINT ( 'NONE',  ( 0.8760168074887076939, 42.09738177923922819, 23.27577685234612304 ) ) ;
#23472=CARTESIAN_POINT ( 'NONE',  ( 0.7048096507298579061, 37.64898672361912446, 29.95256433478738600 ) ) ;
#23494=CARTESIAN_POINT ( 'NONE',  ( -6.016489644550737204, -4.872725758886062408, -18.20227673842149585 ) ) ;
#23504=CARTESIAN_POINT ( 'NONE',  ( 0.6001305935487315502, -5.760103278697686235, -47.76436356026965768 ) ) ;
#23516=ORIENTED_EDGE ( 'NONE', *, *, #9631, .T. ) ;
#23518=( BOUNDED_SURFACE ( )  B_SPLINE_SURFACE ( 3, 1, ( 
 ( #24487, #9770 ),
 ( #53287, #53899 ),
 ( #48913, #43625 ),
 ( #668, #19808 ) ),
 .UNSPECIFIED., .F., .F., .F. ) 
 B_SPLINE_SURFACE_WITH_KNOTS ( ( 4, 4 ),
 ( 2, 2 ),
 ( 0.000000000000000000, 1.000000000000000000 ),
 ( 0.000000000000000000, 1.000000000000000000 ),
 .UNSPECIFIED. ) 
 GEOMETRIC_REPRESENTATION_ITEM ( )  RATIONAL_B_SPLINE_SURFACE ( (
 ( 1.000000000000000000, 1.000000000000000000),
 ( 0.9953040768229013402, 0.8617119497784988535),
 ( 0.9953040768229013402, 0.8617119497784988535),
 ( 1.000000000000000000, 1.000000000000000000) ) ) 
 REPRESENTATION_ITEM ( '' )  SURFACE ( )  );
#23527=B_SPLINE_CURVE_WITH_KNOTS ( 'NONE', 3,
 ( #27321, #32969, #4713, #4402 ),
 .UNSPECIFIED., .F., .F.,
 ( 4, 4 ),
 ( 2.297383214701472214E-17, 0.004564976165746187711 ),
 .UNSPECIFIED. ) ;
#23528=ORIENTED_EDGE ( 'NONE', *, *, #49097, .T. ) ;
#23535=CARTESIAN_POINT ( 'NONE',  ( -6.016761891674565099, 11.47373234755524862, -14.94721834528402660 ) ) ;
#23536=VERTEX_POINT ( 'NONE', #24320 ) ;
#23537=CARTESIAN_POINT ( 'NONE',  ( 0.2230388203127589286, -37.71673103297349883, -20.89822698305252402 ) ) ;
#23539=ADVANCED_FACE ( 'NONE', ( #19323 ), #35985, .F. ) ;
#23548=CARTESIAN_POINT ( 'NONE',  ( 0.6001305935487315502, 41.40054608060292907, -24.50730504006414634 ) ) ;
#23551=EDGE_CURVE ( 'NONE', #35170, #1703, #52985, .T. ) ;
#23565=CARTESIAN_POINT ( 'NONE',  ( 3.680974057930773924, 10.62112035260176945, 46.78530430706942411 ) ) ;
#23572=EDGE_LOOP ( 'NONE', ( #55713, #33798, #39352, #42783 ) ) ;
#23573=EDGE_CURVE ( 'NONE', #52918, #45306, #60401, .T. ) ;
#23580=B_SPLINE_CURVE_WITH_KNOTS ( 'NONE', 3,
 ( #21020, #40161, #59208, #40771 ),
 .UNSPECIFIED., .F., .F.,
 ( 4, 4 ),
 ( 5.553824967135426632E-18, 0.004566006591234644633 ),
 .UNSPECIFIED. ) ;
#23583=CARTESIAN_POINT ( 'NONE',  ( 4.549368137175248350, 0.000000000000000000, 0.000000000000000000 ) ) ;
#23591=CARTESIAN_POINT ( 'NONE',  ( 0.1087620492084205026, -30.23658359364800319, -30.74858804150676050 ) ) ;
#23596=VERTEX_POINT ( 'NONE', #33122 ) ;
#23597=ADVANCED_FACE ( 'NONE', ( #2030 ), #40560, .F. ) ;
#23604=CARTESIAN_POINT ( 'NONE',  ( 0.1100247026804066219, 5.460606496326332326, 42.77732815928602150 ) ) ;
#23605=CARTESIAN_POINT ( 'NONE',  ( 4.549368137175248350, 28.46244473166673927, -32.13400537129894730 ) ) ;
#23608=ORIENTED_EDGE ( 'NONE', *, *, #34873, .T. ) ;
#23616=CARTESIAN_POINT ( 'NONE',  ( 4.549368137175248350, 0.000000000000000000, 0.000000000000000000 ) ) ;
#23622=DIRECTION ( 'NONE',  ( 0.000000000000000000, 0.000000000000000000, 1.000000000000000000 ) ) ;
#23630=CARTESIAN_POINT ( 'NONE',  ( 4.833616638992205949, -14.43699082351681540, -43.93936707042095691 ) ) ;
#23632=EDGE_CURVE ( 'NONE', #18593, #9726, #38826, .T. ) ;
#23633=CARTESIAN_POINT ( 'NONE',  ( -6.010958268070873523, 2.473955915502482394, -18.68034667844846552 ) ) ;
#23634=CARTESIAN_POINT ( 'NONE',  ( 0.8760168074886965917, -44.09317760313739143, -19.22870327415289182 ) ) ;
#23635=ORIENTED_EDGE ( 'NONE', *, *, #23341, .F. ) ;
#23640=CARTESIAN_POINT ( 'NONE',  ( -6.015611763856276717, -0.006214430185009750529, -18.84324252354755203 ) ) ;
#23642=CARTESIAN_POINT ( 'NONE',  ( 0.7048096507298579061, 44.11842270945945899, 19.18768066167137576 ) ) ;
#23649=CARTESIAN_POINT ( 'NONE',  ( 4.975801465491695552, 45.18341283946458020, -15.94009207553003016 ) ) ;
#23651=VERTEX_POINT ( 'NONE', #15855 ) ;
#23659=LINE ( 'NONE', #42784, #3483 ) ;
#23661=CARTESIAN_POINT ( 'NONE',  ( 0.1103744047535531458, 5.667281528142393832, -42.75042227379822180 ) ) ;
#23674=CARTESIAN_POINT ( 'NONE',  ( -6.001507490154110336, 13.31361390284178370, -13.33564355450094396 ) ) ;
#23678=CARTESIAN_POINT ( 'NONE',  ( 0.5998501479064708430, 46.33007877220720871, 12.95623334615518374 ) ) ;
#23679=CARTESIAN_POINT ( 'NONE',  ( 0.5988103622719989083, -6.880137819455214299, 47.61318311633112188 ) ) ;
#23690=EDGE_CURVE ( 'NONE', #47578, #39264, #20172, .T. ) ;
#23695=ORIENTED_EDGE ( 'NONE', *, *, #11690, .F. ) ;
#23709=CARTESIAN_POINT ( 'NONE',  ( 3.680882792899937250, 10.62117075007648204, -46.78529781139678079 ) ) ;
#23710=ORIENTED_EDGE ( 'NONE', *, *, #19107, .F. ) ;
#23712=CARTESIAN_POINT ( 'NONE',  ( 2.643462169533600914, -37.25264019563393703, -30.32726672320786676 ) ) ;
#23714=VERTEX_POINT ( 'NONE', #32423 ) ;
#23716=CARTESIAN_POINT ( 'NONE',  ( 0.8760168074887090262, 28.57146030081980470, -38.69913431881793286 ) ) ;
#23727=CARTESIAN_POINT ( 'NONE',  ( 0.3622758884714600280, 22.26738722580168073, -36.91764744403298693 ) ) ;
#23731=B_SPLINE_CURVE_WITH_KNOTS ( 'NONE', 3,
 ( #54887, #39911, #40843, #6324, #16084, #36133, #26703, #12317, #30158, #25459, #59904, #30461, #6630, #55196, #25779, #1956, #21082, #40225, #59275 ),
 .UNSPECIFIED., .F., .F.,
 ( 4, 3, 3, 3, 3, 3, 4 ),
 ( 1.138109825968292890E-16, 0.0002618519381806229352, 0.0003927759815485970052, 0.0005237000248299436469, 0.0006546240681325005356, 0.0007855481115631335765, 0.0009699050456655113756 ),
 .UNSPECIFIED. ) ;
#23735=EDGE_CURVE ( 'NONE', #13776, #27177, #8276, .T. ) ;
#23742=CARTESIAN_POINT ( 'NONE',  ( 4.975801465491695552, 21.70134120755140827, 42.71626295676271212 ) ) ;
#23745=CARTESIAN_POINT ( 'NONE',  ( 4.975801465491695552, 26.14269827151680659, -40.15204426031507268 ) ) ;
#23751=ORIENTED_EDGE ( 'NONE', *, *, #59597, .F. ) ;
#23752=CARTESIAN_POINT ( 'NONE',  ( 4.549368137175248350, 42.82045902618768451, 3.018832571116707442 ) ) ;
#23753=CARTESIAN_POINT ( 'NONE',  ( 3.680882792899936362, -40.59250320379031507, 25.57189948075115637 ) ) ;
#23757=CARTESIAN_POINT ( 'NONE',  ( 0.8751705887134423323, 29.98056538504960855, -37.60752970653798855 ) ) ;
#23778=DIRECTION ( 'NONE',  ( -1.000000000000000000, -0.000000000000000000, -0.000000000000000000 ) ) ;
#23779=CARTESIAN_POINT ( 'NONE',  ( -2.708315649062916552, -13.41752550814514677, 5.842990691604369680 ) ) ;
#23783=( BOUNDED_SURFACE ( )  B_SPLINE_SURFACE ( 3, 1, ( 
 ( #2390, #51238 ),
 ( #50621, #55317 ),
 ( #40652, #22441 ),
 ( #26831, #60628 ) ),
 .UNSPECIFIED., .F., .F., .F. ) 
 B_SPLINE_SURFACE_WITH_KNOTS ( ( 4, 4 ),
 ( 2, 2 ),
 ( 0.000000000000000000, 1.000000000000000000 ),
 ( 0.000000000000000000, 1.000000000000000000 ),
 .UNSPECIFIED. ) 
 GEOMETRIC_REPRESENTATION_ITEM ( )  RATIONAL_B_SPLINE_SURFACE ( (
 ( 1.000000000000000000, 1.000000000000000000),
 ( 0.7223157951917476005, 0.9931996967497186413),
 ( 0.7223157951917476005, 0.9931996967497186413),
 ( 1.000000000000000000, 1.000000000000000000) ) ) 
 REPRESENTATION_ITEM ( '' )  SURFACE ( )  );
#23785=VERTEX_POINT ( 'NONE', #14251 ) ;
#23786=AXIS2_PLACEMENT_3D ( 'NONE', #18165, #23778, #22854 ) ;
#23791=CARTESIAN_POINT ( 'NONE',  ( 0.3622758884714600280, -31.06363466427748321, 29.89648521331577058 ) ) ;
#23792=B_SPLINE_CURVE_WITH_KNOTS ( 'NONE', 3,
 ( #59885, #55178, #33563, #43279, #4696, #33875 ),
 .UNSPECIFIED., .F., .F.,
 ( 4, 2, 4 ),
 ( 1.268633296668913999E-16, 0.0002450741128632358658, 0.0004901482257263448800 ),
 .UNSPECIFIED. ) ;
#23796=CARTESIAN_POINT ( 'NONE',  ( 0.6031356755852232965, 8.546889573354048380E-06, 48.10744332413860747 ) ) ;
#23797=EDGE_LOOP ( 'NONE', ( #39753, #8241, #22928, #21054 ) ) ;
#23807=EDGE_CURVE ( 'NONE', #39562, #46978, #30992, .T. ) ;
#23811=CARTESIAN_POINT ( 'NONE',  ( 0.1103310638050661874, 37.30561229499300424, 21.63353985999701479 ) ) ;
#23819=EDGE_LOOP ( 'NONE', ( #19516, #43572, #26992, #33604 ) ) ;
#23832=ORIENTED_EDGE ( 'NONE', *, *, #28630, .F. ) ;
#23837=EDGE_CURVE ( 'NONE', #22451, #19448, #47795, .T. ) ;
#23840=CONICAL_SURFACE ( 'NONE', #2851, 42.92674063221959813, 1.485477209440487556 ) ;
#23844=EDGE_CURVE ( 'NONE', #19546, #351, #20058, .T. ) ;
#23845=CARTESIAN_POINT ( 'NONE',  ( -6.016761891674564211, 9.424569481870250343, 16.31696541414275359 ) ) ;
#23847=VERTEX_POINT ( 'NONE', #38071 ) ;
#23857=VECTOR ( 'NONE', #28796, 1000.000000000000114 ) ;
#23860=CARTESIAN_POINT ( 'NONE',  ( 0.3622758884714730732, -26.89560658783362612, -33.69533458712334806 ) ) ;
#23861=CARTESIAN_POINT ( 'NONE',  ( 5.880360259849739535, -21.17507050419543191, 43.04573319267409204 ) ) ;
#23869=CARTESIAN_POINT ( 'NONE',  ( -6.015611763856276717, -2.453375430803944823, -18.68284711750060723 ) ) ;
#23880=EDGE_CURVE ( 'NONE', #44114, #15737, #53642, .T. ) ;
#23881=DIRECTION ( 'NONE',  ( -0.1024043820194934368, -0.9844298967354715435, -0.1428674944016109227 ) ) ;
#23882=CARTESIAN_POINT ( 'NONE',  ( -6.001507490154110336, -18.68062548815627721, 2.475062734132372100 ) ) ;
#23884=VECTOR ( 'NONE', #47220, 999.9999999999997726 ) ;
#23892=( BOUNDED_SURFACE ( )  B_SPLINE_SURFACE ( 3, 1, ( 
 ( #10408, #39242 ),
 ( #5056, #48008 ),
 ( #5971, #38937 ),
 ( #29192, #39869 ) ),
 .UNSPECIFIED., .F., .F., .F. ) 
 B_SPLINE_SURFACE_WITH_KNOTS ( ( 4, 4 ),
 ( 2, 2 ),
 ( 0.000000000000000000, 1.000000000000000000 ),
 ( 0.000000000000000000, 1.000000000000000000 ),
 .UNSPECIFIED. ) 
 GEOMETRIC_REPRESENTATION_ITEM ( )  RATIONAL_B_SPLINE_SURFACE ( (
 ( 1.000000000000000000, 1.000000000000000000),
 ( 0.9953040768229013402, 0.8617119497784988535),
 ( 0.9953040768229013402, 0.8617119497784988535),
 ( 1.000000000000000000, 1.000000000000000000) ) ) 
 REPRESENTATION_ITEM ( '' )  SURFACE ( )  );
#23898=CARTESIAN_POINT ( 'NONE',  ( -6.016489644550736315, -9.417787539062361546, 16.32089497094057862 ) ) ;
#23899=ORIENTED_EDGE ( 'NONE', *, *, #35886, .F. ) ;
#23902=VERTEX_POINT ( 'NONE', #36370 ) ;
#23907=DIRECTION ( 'NONE',  ( -0.1024043820194934507, -0.7971196296869339504, 0.5950744814819157735 ) ) ;
#23914=ORIENTED_EDGE ( 'NONE', *, *, #50625, .F. ) ;
#23922=DIRECTION ( 'NONE',  ( 1.000000000000000000, 0.000000000000000000, 0.000000000000000000 ) ) ;
#23934=CARTESIAN_POINT ( 'NONE',  ( -6.015611763856276717, 13.31979030221817695, -13.32857883366819429 ) ) ;
#23938=CARTESIAN_POINT ( 'NONE',  ( -6.017396004339686577, -11.47005965438149033, 14.95000090562877482 ) ) ;
#23942=DIRECTION ( 'NONE',  ( -1.000000000000000000, -0.000000000000000000, -0.000000000000000000 ) ) ;
#23947=ORIENTED_EDGE ( 'NONE', *, *, #26769, .T. ) ;
#23949=CARTESIAN_POINT ( 'NONE',  ( 0.1084644655670284341, -34.45367667780550391, -25.93599432281485662 ) ) ;
#23953=CARTESIAN_POINT ( 'NONE',  ( -6.016489644550736315, -17.41053539857194465, -7.206912786933474813 ) ) ;
#23955=CARTESIAN_POINT ( 'NONE',  ( 4.975801465491695552, -45.55012473237743365, -14.85979367497158599 ) ) ;
#23964=CARTESIAN_POINT ( 'NONE',  ( 0.1073791018717483448, -43.12183934961191056, 0.4849339620931858996 ) ) ;
#23965=CARTESIAN_POINT ( 'NONE',  ( 0.1092355843206037486, 39.72582785521893101, 16.78033551728677963 ) ) ;
#23966=CARTESIAN_POINT ( 'NONE',  ( 0.8760168074887090262, 37.61398439004534566, -29.98565522133306871 ) ) ;
#23969=CARTESIAN_POINT ( 'NONE',  ( 4.549368137175248350, 32.41327393324141326, -28.14399996863463116 ) ) ;
#23973=VERTEX_POINT ( 'NONE', #61358 ) ;
#23974=ORIENTED_EDGE ( 'NONE', *, *, #38427, .T. ) ;
#23977=CARTESIAN_POINT ( 'NONE',  ( -6.016489644550737204, 13.32104266208099475, 13.32727118274442546 ) ) ;
#23978=CARTESIAN_POINT ( 'NONE',  ( 0.1073791018717483448, 10.69234304550053949, -41.77800844988504991 ) ) ;
#23980=EDGE_LOOP ( 'NONE', ( #20815, #43098, #19775, #21377 ) ) ;
#23989=DIRECTION ( 'NONE',  ( 0.000000000000000000, 0.000000000000000000, 1.000000000000000000 ) ) ;
#23990=VERTEX_POINT ( 'NONE', #57270 ) ;
#23991=VERTEX_POINT ( 'NONE', #27562 ) ;
#23992=CARTESIAN_POINT ( 'NONE',  ( -6.016104459813374383, -11.47525878590926673, 14.94608397322080506 ) ) ;
#23996=( BOUNDED_SURFACE ( )  B_SPLINE_SURFACE ( 3, 1, ( 
 ( #34517, #52984 ),
 ( #48600, #5656 ),
 ( #29182, #29490 ),
 ( #24800, #15103 ) ),
 .UNSPECIFIED., .F., .F., .F. ) 
 B_SPLINE_SURFACE_WITH_KNOTS ( ( 4, 4 ),
 ( 2, 2 ),
 ( 0.000000000000000000, 1.000000000000000000 ),
 ( 0.000000000000000000, 1.000000000000000000 ),
 .UNSPECIFIED. ) 
 GEOMETRIC_REPRESENTATION_ITEM ( )  RATIONAL_B_SPLINE_SURFACE ( (
 ( 1.000000000000000000, 1.000000000000000000),
 ( 0.9751682680413298332, 0.9999560080971552356),
 ( 0.9751682680413298332, 0.9999560080971552356),
 ( 1.000000000000000000, 1.000000000000000000) ) ) 
 REPRESENTATION_ITEM ( '' )  SURFACE ( )  );
#23999=CARTESIAN_POINT ( 'NONE',  ( -6.016761891674565099, 18.20201388312102253, -4.873659902332176053 ) ) ;
#24001=CARTESIAN_POINT ( 'NONE',  ( 2.643462169533600914, -22.81120928486466326, -42.27470921730932218 ) ) ;
#24005=CARTESIAN_POINT ( 'NONE',  ( 0.8751705887134553219, -33.37254303619578621, 34.63284514348527665 ) ) ;
#24015=CARTESIAN_POINT ( 'NONE',  ( 0.1087620492084205304, 16.83695155255833598, -39.70193592734187860 ) ) ;
#24019=VECTOR ( 'NONE', #8914, 999.9999999999998863 ) ;
#24023=CARTESIAN_POINT ( 'NONE',  ( 0.3622758884714730732, 4.808133778521878732, -42.84426538328727219 ) ) ;
#24030=CARTESIAN_POINT ( 'NONE',  ( -6.010958268070873523, 18.19761767765837135, -4.891065400978194866 ) ) ;
#24031=CARTESIAN_POINT ( 'NONE',  ( 0.3622758884714600280, -25.58609868863743841, -34.70015533914819628 ) ) ;
#24034=VERTEX_POINT ( 'NONE', #23791 ) ;
#24035=B_SPLINE_CURVE_WITH_KNOTS ( 'NONE', 3,
 ( #11760, #6696, #11138, #40587, #54945, #12378, #59648, #12079, #21760, #31464, #26451, #31152, #50261, #6383, #2636, #40900 ),
 .UNSPECIFIED., .F., .F.,
 ( 4, 3, 3, 3, 3, 4 ),
 ( 1.868480190406682863E-17, 0.0002618515315864384531, 0.0003927756766341935460, 0.0005236998216950533363, 0.0007855159896329884893, 0.001047349442285926352 ),
 .UNSPECIFIED. ) ;
#24043=EDGE_LOOP ( 'NONE', ( #29008, #16987, #5066, #30194 ) ) ;
#24044=CARTESIAN_POINT ( 'NONE',  ( 0.1310142868023693452, -4.996535778099055136, -42.83311553787491732 ) ) ;
#24056=ADVANCED_FACE ( 'NONE', ( #19714 ), #32033, .F. ) ;
#24059=EDGE_CURVE ( 'NONE', #44566, #61266, #10280, .T. ) ;
#24062=VECTOR ( 'NONE', #60521, 1000.000000000000114 ) ;
#24063=CARTESIAN_POINT ( 'NONE',  ( -6.015611763856276717, 7.205255340944849429, -17.41126425312530301 ) ) ;
#24067=CARTESIAN_POINT ( 'NONE',  ( 0.3622758884714600280, -15.73321244754826509, -40.13994584881776007 ) ) ;
#24068=ORIENTED_EDGE ( 'NONE', *, *, #36759, .T. ) ;
#24069=CARTESIAN_POINT ( 'NONE',  ( 4.975801465491695552, 32.01766832630263337, 35.64402118370968964 ) ) ;
#24070=ORIENTED_EDGE ( 'NONE', *, *, #42155, .T. ) ;
#24072=( BOUNDED_SURFACE ( )  B_SPLINE_SURFACE ( 3, 1, ( 
 ( #20333, #34743 ),
 ( #58206, #898 ),
 ( #34435, #20634 ),
 ( #48219, #24402 ) ),
 .UNSPECIFIED., .F., .F., .F. ) 
 B_SPLINE_SURFACE_WITH_KNOTS ( ( 4, 4 ),
 ( 2, 2 ),
 ( 0.000000000000000000, 1.000000000000000000 ),
 ( 0.000000000000000000, 1.000000000000000000 ),
 .UNSPECIFIED. ) 
 GEOMETRIC_REPRESENTATION_ITEM ( )  RATIONAL_B_SPLINE_SURFACE ( (
 ( 1.000000000000000000, 1.000000000000000000),
 ( 0.7223157951917480446, 0.9931996967497186413),
 ( 0.7223157951917480446, 0.9931996967497186413),
 ( 1.000000000000000000, 1.000000000000000000) ) ) 
 REPRESENTATION_ITEM ( '' )  SURFACE ( )  );
#24073=ORIENTED_EDGE ( 'NONE', *, *, #12006, .T. ) ;
#24076=CARTESIAN_POINT ( 'NONE',  ( 0.6027935024548037868, -34.14031893787248606, 33.89348162668918008 ) ) ;
#24080=CARTESIAN_POINT ( 'NONE',  ( 5.880360259849752858, 21.17507050419453662, 43.04573319267453968 ) ) ;
#24085=ORIENTED_EDGE ( 'NONE', *, *, #50559, .T. ) ;
#24088=ADVANCED_FACE ( 'NONE', ( #5577 ), #24072, .F. ) ;
#24089=DIRECTION ( 'NONE',  ( -0.1024043820194934368, -0.3684880688409071237, -0.9239750460186164638 ) ) ;
#24093=EDGE_LOOP ( 'NONE', ( #43724, #24770, #565, #57935 ) ) ;
#24095=CARTESIAN_POINT ( 'NONE',  ( -6.016489644550736315, -14.95199950534940037, -11.46752133529400375 ) ) ;
#24096=LINE ( 'NONE', #43225, #25008 ) ;
#24113=CARTESIAN_POINT ( 'NONE',  ( 0.1104177457020373149, 37.34931850022140054, 21.55798761925400697 ) ) ;
#24116=EDGE_CURVE ( 'NONE', #49729, #21388, #24096, .T. ) ;
#24118=CARTESIAN_POINT ( 'NONE',  ( -2.569797478183783568, 14.24379821351252495, 3.352038560005965451 ) ) ;
#24121=ORIENTED_EDGE ( 'NONE', *, *, #48130, .T. ) ;
#24127=CARTESIAN_POINT ( 'NONE',  ( -6.001507490154111224, 17.41542759839274268, -7.196845540358981275 ) ) ;
#24132=CARTESIAN_POINT ( 'NONE',  ( 4.975801465491694664, -45.55012473237763260, 14.85979367497093762 ) ) ;
#24138=ORIENTED_EDGE ( 'NONE', *, *, #29594, .T. ) ;
#24140=B_SPLINE_CURVE_WITH_KNOTS ( 'NONE', 3,
 ( #46189, #12675, #31774, #7953, #47111, #40886, #8558, #41492, #12991, #59952, #17060, #37407, #3853 ),
 .UNSPECIFIED., .F., .F.,
 ( 4, 3, 3, 3, 4 ),
 ( 0.0004849530346207898404, 0.0005237000248299429964, 0.0006546240681324979336, 0.0007855481115631321671, 0.0009699050456655107250 ),
 .UNSPECIFIED. ) ;
#24150=EDGE_CURVE ( 'NONE', #58621, #4984, #2987, .T. ) ;
#24153=CARTESIAN_POINT ( 'NONE',  ( 0.3622758884714730732, -37.74294673546571488, -20.83792692158958815 ) ) ;
#24156=CARTESIAN_POINT ( 'NONE',  ( 0.5998501479064708430, 12.95623334615502387, -46.33007877220726556 ) ) ;
#24159=CARTESIAN_POINT ( 'NONE',  ( -6.016489644550736315, -18.68257207665194741, -2.455165042129931141 ) ) ;
#24162=B_SPLINE_CURVE_WITH_KNOTS ( 'NONE', 3,
 ( #31809, #13024, #41222, #42159 ),
 .UNSPECIFIED., .F., .F.,
 ( 4, 4 ),
 ( 0.000000000000000000, 0.005014147105413705591 ),
 .UNSPECIFIED. ) ;
#24164=CARTESIAN_POINT ( 'NONE',  ( -6.015611763856276717, -16.32183393015603556, 9.416239407363246272 ) ) ;
#24169=CARTESIAN_POINT ( 'NONE',  ( 4.549368137175248350, 0.000000000000000000, 0.000000000000000000 ) ) ;
#24184=CARTESIAN_POINT ( 'NONE',  ( 0.6041374136657475802, 24.20487816031520723, -41.57494627055121583 ) ) ;
#24193=EDGE_LOOP ( 'NONE', ( #46728, #27314, #5451, #9053 ) ) ;
#24198=ORIENTED_EDGE ( 'NONE', *, *, #40897, .T. ) ;
#24199=VERTEX_POINT ( 'NONE', #12179 ) ;
#24202=ORIENTED_EDGE ( 'NONE', *, *, #4088, .T. ) ;
#24208=CARTESIAN_POINT ( 'NONE',  ( 4.975801465491694664, 47.10002938642141856, -8.787181743659651545 ) ) ;
#24212=VERTEX_POINT ( 'NONE', #60361 ) ;
#24217=ORIENTED_EDGE ( 'NONE', *, *, #44542, .T. ) ;
#24218=CARTESIAN_POINT ( 'NONE',  ( 0.6028618097248863439, -12.28244208173093099, 46.51318640245693103 ) ) ;
#24224=CARTESIAN_POINT ( 'NONE',  ( 0.6041374136657476912, 6.106202762793474292, -47.71861871402583688 ) ) ;
#24238=( BOUNDED_SURFACE ( )  B_SPLINE_SURFACE ( 3, 1, ( 
 ( #14564, #32742 ),
 ( #33059, #43073 ),
 ( #42459, #5117 ),
 ( #8595, #56826 ) ),
 .UNSPECIFIED., .F., .F., .F. ) 
 B_SPLINE_SURFACE_WITH_KNOTS ( ( 4, 4 ),
 ( 2, 2 ),
 ( 0.000000000000000000, 1.000000000000000000 ),
 ( 0.000000000000000000, 1.000000000000000000 ),
 .UNSPECIFIED. ) 
 GEOMETRIC_REPRESENTATION_ITEM ( )  RATIONAL_B_SPLINE_SURFACE ( (
 ( 1.000000000000000000, 1.000000000000000000),
 ( 0.9953040768229013402, 0.8617119497784988535),
 ( 0.9953040768229013402, 0.8617119497784988535),
 ( 1.000000000000000000, 1.000000000000000000) ) ) 
 REPRESENTATION_ITEM ( '' )  SURFACE ( )  );
#24239=CARTESIAN_POINT ( 'NONE',  ( 4.549368137175248350, -32.41327393324121431, -28.14399996863486209 ) ) ;
#24243=CARTESIAN_POINT ( 'NONE',  ( 0.1073791018717483448, 30.14884492832389284, -30.83464511437107447 ) ) ;
#24244=CARTESIAN_POINT ( 'NONE',  ( -6.015611763856276717, 17.41126425312538117, 7.205255340944677123 ) ) ;
#24247=CARTESIAN_POINT ( 'NONE',  ( 0.1097557419366048670, -34.34829179474817806, -26.07515889977806367 ) ) ;
#24249=CARTESIAN_POINT ( 'NONE',  ( -6.016104459813371719, -14.94608397322092586, 11.47525878590911041 ) ) ;
#24250=CARTESIAN_POINT ( 'NONE',  ( -5.995132425357893702, 7.219211173946727733, -17.40647075750109352 ) ) ;
#24252=DIRECTION ( 'NONE',  ( 0.1024043820194936449, 0.5950744814819241002, -0.7971196296869277331 ) ) ;
#24256=CARTESIAN_POINT ( 'NONE',  ( 0.5998501479064708430, -5.759754759340450114, -47.76154736470756745 ) ) ;
#24261=LINE ( 'NONE', #1355, #24332 ) ;
#24266=CARTESIAN_POINT ( 'NONE',  ( -6.015611763856276717, -14.95313250337437871, 11.46610900684717471 ) ) ;
#24267=ADVANCED_FACE ( 'NONE', ( #16875 ), #43302, .F. ) ;
#24269=CARTESIAN_POINT ( 'NONE',  ( 0.1097557419366048670, -10.94578341459299509, 41.71221507312528587 ) ) ;
#24274=ORIENTED_EDGE ( 'NONE', *, *, #26976, .F. ) ;
#24278=CARTESIAN_POINT ( 'NONE',  ( 0.2885697896453107147, 17.24062360132716165, -39.51953439758091946 ) ) ;
#24284=B_SPLINE_CURVE_WITH_KNOTS ( 'NONE', 3,
 ( #19020, #29017, #10220, #52811 ),
 .UNSPECIFIED., .F., .F.,
 ( 4, 4 ),
 ( 0.000000000000000000, 0.005014147105413696917 ),
 .UNSPECIFIED. ) ;
#24287=B_SPLINE_CURVE_WITH_KNOTS ( 'NONE', 3,
 ( #9541, #42777, #13647, #57437, #14270, #47463, #3590, #46864, #18651, #38090, #41858, #27735, #60926, #42472, #22726, #32439 ),
 .UNSPECIFIED., .F., .F.,
 ( 4, 3, 3, 3, 3, 4 ),
 ( 2.194378057379452319E-17, 0.0002618515315864434947, 0.0003927756766341995633, 0.0005236998216950572394, 0.0007855159896329905493, 0.001047349442285928087 ),
 .UNSPECIFIED. ) ;
#24290=CARTESIAN_POINT ( 'NONE',  ( 0.3622758884714600280, 10.35929834645864389, 41.85013935980105515 ) ) ;
#24294=CARTESIAN_POINT ( 'NONE',  ( 0.3622758884714730732, 37.74294673546557988, 20.83792692158985460 ) ) ;
#24295=CARTESIAN_POINT ( 'NONE',  ( 0.6027935024548037868, 46.42277558035024754, 12.61964268015572976 ) ) ;
#24298=VERTEX_POINT ( 'NONE', #23106 ) ;
#24299=CARTESIAN_POINT ( 'NONE',  ( 0.1310142868023686513, 4.996535778098778025, 42.83311553787493864 ) ) ;
#24306=CARTESIAN_POINT ( 'NONE',  ( -6.016489644550737204, 16.31649074174277203, 9.425415887801145587 ) ) ;
#24307=ORIENTED_EDGE ( 'NONE', *, *, #10559, .T. ) ;
#24309=EDGE_CURVE ( 'NONE', #56342, #32449, #52873, .T. ) ;
#24316=B_SPLINE_CURVE_WITH_KNOTS ( 'NONE', 3,
 ( #55410, #12536, #56033, #45437 ),
 .UNSPECIFIED., .F., .F.,
 ( 4, 4 ),
 ( 2.054184040232706591E-17, 0.004444306975806115896 ),
 .UNSPECIFIED. ) ;
#24319=CARTESIAN_POINT ( 'NONE',  ( 0.1310142868023677631, 10.54463319394675658, 41.81449350725031167 ) ) ;
#24320=CARTESIAN_POINT ( 'NONE',  ( 4.549368137175248350, 19.17571786012324608, -38.40568845698256695 ) ) ;
#24321=DIRECTION ( 'NONE',  ( -0.1024043820194934229, 0.9139094329506604053, 0.3927886084231669295 ) ) ;
#24329=CARTESIAN_POINT ( 'NONE',  ( 4.549368137175248350, 28.46244473166628097, 32.13400537129935230 ) ) ;
#24332=VECTOR ( 'NONE', #43398, 1000.000000000000000 ) ;
#24333=CARTESIAN_POINT ( 'NONE',  ( 5.880360259849752858, -26.61251048557221210, -39.91356965504138543 ) ) ;
#24340=CARTESIAN_POINT ( 'NONE',  ( 0.1073791018717578927, -26.63563652260192427, 33.91564619577761874 ) ) ;
#24345=CARTESIAN_POINT ( 'NONE',  ( -2.569797478183783568, -13.34095667500609217, 6.011723966603914171 ) ) ;
#24347=EDGE_CURVE ( 'NONE', #31565, #37013, #49999, .T. ) ;
#24355=CARTESIAN_POINT ( 'NONE',  ( 0.8760168074887090262, -28.57146030082009602, 38.69913431881773391 ) ) ;
#24358=EDGE_CURVE ( 'NONE', #18458, #32580, #60990, .T. ) ;
#24360=CONICAL_SURFACE ( 'NONE', #4339, 42.92674063221959813, 1.485477209440487556 ) ;
#24364=( BOUNDED_SURFACE ( )  B_SPLINE_SURFACE ( 3, 1, ( 
 ( #22959, #32668 ),
 ( #47082, #4120 ),
 ( #47685, #37687 ),
 ( #18885, #56752 ) ),
 .UNSPECIFIED., .F., .F., .F. ) 
 B_SPLINE_SURFACE_WITH_KNOTS ( ( 4, 4 ),
 ( 2, 2 ),
 ( 0.000000000000000000, 1.000000000000000000 ),
 ( 0.000000000000000000, 1.000000000000000000 ),
 .UNSPECIFIED. ) 
 GEOMETRIC_REPRESENTATION_ITEM ( )  RATIONAL_B_SPLINE_SURFACE ( (
 ( 1.000000000000000000, 1.000000000000000000),
 ( 0.9751682680413298332, 0.9999560080971552356),
 ( 0.9751682680413298332, 0.9999560080971552356),
 ( 1.000000000000000000, 1.000000000000000000) ) ) 
 REPRESENTATION_ITEM ( '' )  SURFACE ( )  );
#24367=ORIENTED_EDGE ( 'NONE', *, *, #39849, .T. ) ;
#24368=CARTESIAN_POINT ( 'NONE',  ( 0.6001305935487315502, 33.64689939321893775, 34.38748867424725830 ) ) ;
#24371=FACE_OUTER_BOUND ( 'NONE', #61453, .T. ) ;
#24376=ORIENTED_EDGE ( 'NONE', *, *, #23432, .F. ) ;
#24387=CARTESIAN_POINT ( 'NONE',  ( 4.549368137175248350, -13.99871866169335810, -40.58005590356685843 ) ) ;
#24390=ADVANCED_FACE ( 'NONE', ( #48750 ), #49012, .F. ) ;
#24392=CARTESIAN_POINT ( 'NONE',  ( 0.1095718737110178143, -21.33933464366394261, -37.47471772507211796 ) ) ;
#24395=CARTESIAN_POINT ( 'NONE',  ( -2.569797478183790229, 3.352038560005718981, 14.24379821351258535 ) ) ;
#24396=VERTEX_POINT ( 'NONE', #39079 ) ;
#24399=ORIENTED_EDGE ( 'NONE', *, *, #43944, .F. ) ;
#24400=DIRECTION ( 'NONE',  ( 1.000000000000000000, 0.000000000000000000, 0.000000000000000000 ) ) ;
#24402=CARTESIAN_POINT ( 'NONE',  ( 5.880360259849739535, 43.04573319267415599, 21.17507050419530401 ) ) ;
#24407=CARTESIAN_POINT ( 'NONE',  ( 0.2224561200757651791, 34.66601556960352326, -25.64288022150844526 ) ) ;
#24411=CARTESIAN_POINT ( 'NONE',  ( 0.8751705887134423323, 23.27176129838367302, 42.09020928323383259 ) ) ;
#24421=CARTESIAN_POINT ( 'NONE',  ( 0.7954190325252775695, -23.29293489839764320, 42.08256085583533945 ) ) ;
#24425=ADVANCED_FACE ( 'NONE', ( #10863 ), #49673, .F. ) ;
#24428=( BOUNDED_SURFACE ( )  B_SPLINE_SURFACE ( 3, 1, ( 
 ( #31266, #31576 ),
 ( #27182, #36293 ),
 ( #41608, #55054 ),
 ( #13406, #12799 ) ),
 .UNSPECIFIED., .F., .F., .F. ) 
 B_SPLINE_SURFACE_WITH_KNOTS ( ( 4, 4 ),
 ( 2, 2 ),
 ( 0.000000000000000000, 1.000000000000000000 ),
 ( 0.000000000000000000, 1.000000000000000000 ),
 .UNSPECIFIED. ) 
 GEOMETRIC_REPRESENTATION_ITEM ( )  RATIONAL_B_SPLINE_SURFACE ( (
 ( 1.000000000000000000, 1.000000000000000000),
 ( 0.9953040768229013402, 0.8617119497784988535),
 ( 0.9953040768229013402, 0.8617119497784988535),
 ( 1.000000000000000000, 1.000000000000000000) ) ) 
 REPRESENTATION_ITEM ( '' )  SURFACE ( )  );
#24433=VERTEX_POINT ( 'NONE', #24957 ) ;
#24436=CARTESIAN_POINT ( 'NONE',  ( 0.6254087463353893428, 33.52637152047081059, -34.49952850220934408 ) ) ;
#24437=ORIENTED_EDGE ( 'NONE', *, *, #9538, .F. ) ;
#24439=LINE ( 'NONE', #6530, #23356 ) ;
#24440=VERTEX_POINT ( 'NONE', #19039 ) ;
#24441=CARTESIAN_POINT ( 'NONE',  ( 2.301529144917015213, -46.04684498357990918, 13.67115311793984311 ) ) ;
#24442=B_SPLINE_CURVE_WITH_KNOTS ( 'NONE', 3,
 ( #41902, #24852, #60971, #23086 ),
 .UNSPECIFIED., .F., .F.,
 ( 4, 4 ),
 ( 0.000000000000000000, 0.005014147105413696917 ),
 .UNSPECIFIED. ) ;
#24443=ORIENTED_EDGE ( 'NONE', *, *, #59241, .F. ) ;
#24446=CARTESIAN_POINT ( 'NONE',  ( 0.6023143664670691511, -38.32505149877531636, 29.07782746490689973 ) ) ;
#24448=ORIENTED_EDGE ( 'NONE', *, *, #15305, .F. ) ;
#24453=B_SPLINE_CURVE_WITH_KNOTS ( 'NONE', 3,
 ( #8578, #18939, #57107, #14239, #60577, #27705 ),
 .UNSPECIFIED., .F., .F.,
 ( 4, 2, 4 ),
 ( 0.000000000000000000, 0.0002450742804987333630, 0.0004901485609974667260 ),
 .UNSPECIFIED. ) ;
#24459=CARTESIAN_POINT ( 'NONE',  ( 3.680974057930774812, 39.15945827951711067, -27.71659654258255046 ) ) ;
#24477=CARTESIAN_POINT ( 'NONE',  ( 0.3622758884714730732, 20.83792692158972670, -37.74294673546565804 ) ) ;
#24479=EDGE_CURVE ( 'NONE', #58937, #27859, #37258, .T. ) ;
#24487=CARTESIAN_POINT ( 'NONE',  ( -6.016761891674564211, 4.880293656734964181, 18.20023637398600869 ) ) ;
#24495=VERTEX_POINT ( 'NONE', #35905 ) ;
#24504=VERTEX_POINT ( 'NONE', #1731 ) ;
#24506=CARTESIAN_POINT ( 'NONE',  ( 0.1104177457020373426, 11.16615714989251096, 41.65375561851289632 ) ) ;
#24507=ORIENTED_EDGE ( 'NONE', *, *, #37068, .T. ) ;
#24510=CARTESIAN_POINT ( 'NONE',  ( 0.1097557419366048670, -30.65094619415046751, -30.33543403792227267 ) ) ;
#24516=ORIENTED_EDGE ( 'NONE', *, *, #49157, .T. ) ;
#24518=CARTESIAN_POINT ( 'NONE',  ( -6.016104459813371719, 14.94608397322100224, -11.47525878590901094 ) ) ;
#24522=CARTESIAN_POINT ( 'NONE',  ( 0.1073791018717578927, -41.52698815987159264, -11.62916352156135780 ) ) ;
#24533=CARTESIAN_POINT ( 'NONE',  ( 4.549368137175248350, -8.166781970326043805, 42.14271863032818999 ) ) ;
#24535=ORIENTED_EDGE ( 'NONE', *, *, #36764, .F. ) ;
#24553=B_SPLINE_CURVE_WITH_KNOTS ( 'NONE', 3,
 ( #33398, #13674, #9888, #48105 ),
 .UNSPECIFIED., .F., .F.,
 ( 4, 4 ),
 ( 2.010076909634645264E-17, 0.004444306975806113294 ),
 .UNSPECIFIED. ) ;
#24558=CARTESIAN_POINT ( 'NONE',  ( 2.643462169533613793, 32.97543604874675083, -34.93025802711691341 ) ) ;
#24560=ADVANCED_FACE ( 'NONE', ( #32745 ), #446, .F. ) ;
#24563=CARTESIAN_POINT ( 'NONE',  ( 0.1103310638050662290, -34.16271402810851043, -26.31782144882228636 ) ) ;
#24565=EDGE_CURVE ( 'NONE', #39339, #7638, #60287, .T. ) ;
#24568=CARTESIAN_POINT ( 'NONE',  ( 0.6023143664670691511, -24.28012784216906894, 41.53077189784221446 ) ) ;
#24569=CARTESIAN_POINT ( 'NONE',  ( 0.6027935024548037868, -46.51312430684514254, 12.28245664247765490 ) ) ;
#24575=CARTESIAN_POINT ( 'NONE',  ( 4.549368137175248350, -23.67244292351614376, -35.80950303116092925 ) ) ;
#24576=CARTESIAN_POINT ( 'NONE',  ( 0.6041374136657475802, -12.28249295042015277, -46.51335992032614541 ) ) ;
#24578=ORIENTED_EDGE ( 'NONE', *, *, #10779, .T. ) ;
#24580=CARTESIAN_POINT ( 'NONE',  ( 0.1064266379913943183, -33.86837498006642733, 26.69589650908227796 ) ) ;
#24585=LINE ( 'NONE', #61841, #37174 ) ;
#24587=ORIENTED_EDGE ( 'NONE', *, *, #6820, .T. ) ;
#24590=CARTESIAN_POINT ( 'NONE',  ( 0.6017667736363750963, -23.75082673020834534, -41.83584368312182988 ) ) ;
#24604=LINE ( 'NONE', #43740, #34836 ) ;
#24609=FACE_OUTER_BOUND ( 'NONE', #23819, .T. ) ;
#24612=CARTESIAN_POINT ( 'NONE',  ( 0.3622758884714600280, 4.808133778521302304, 42.84426538328732903 ) ) ;
#24613=CARTESIAN_POINT ( 'NONE',  ( 0.6001305935487422083, -44.64600790884043846, -17.92615948558524863 ) ) ;
#24618=CARTESIAN_POINT ( 'NONE',  ( -6.016761891674564211, 13.32172022638610365, -13.32657647165341253 ) ) ;
#24625=CARTESIAN_POINT ( 'NONE',  ( 1.827119703190779321, -25.21842556008211389, 34.89020442382214782 ) ) ;
#24626=EDGE_CURVE ( 'NONE', #20133, #19445, #52087, .T. ) ;
#24629=CARTESIAN_POINT ( 'NONE',  ( 4.322998006666179727, -47.94177812210863010, 2.120302895116117803 ) ) ;
#24634=ORIENTED_EDGE ( 'NONE', *, *, #12109, .T. ) ;
#24640=CONICAL_SURFACE ( 'NONE', #52656, 42.92674063221959813, 1.485477209440487556 ) ;
#24642=CARTESIAN_POINT ( 'NONE',  ( -5.995132425357893702, -11.47834865841106300, 14.94489030678147401 ) ) ;
#24646=CARTESIAN_POINT ( 'NONE',  ( -6.015611763856276717, -17.40650793417838571, -7.216738110653465377 ) ) ;
#24657=CARTESIAN_POINT ( 'NONE',  ( 0.1103878639767399417, 16.54784522866413354, 39.82320122342710533 ) ) ;
#24666=ADVANCED_FACE ( 'NONE', ( #13328 ), #26077, .F. ) ;
#24675=CARTESIAN_POINT ( 'NONE',  ( -2.569797478183790229, 4.218948559326250347, -14.01151037928418930 ) ) ;
#24688=ORIENTED_EDGE ( 'NONE', *, *, #37467, .T. ) ;
#24694=VECTOR ( 'NONE', #52601, 1000.000000000000114 ) ;
#24704=ADVANCED_FACE ( 'NONE', ( #29563 ), #45318, .F. ) ;
#24715=CARTESIAN_POINT ( 'NONE',  ( 0.3622758884714730732, -11.95365414648468594, -41.42293301073622303 ) ) ;
#24716=B_SPLINE_CURVE_WITH_KNOTS ( 'NONE', 3,
 ( #17544, #12863, #27249, #36662, #41672, #27862 ),
 .UNSPECIFIED., .F., .F.,
 ( 4, 2, 4 ),
 ( 8.484948815274053452E-17, 0.0002293366620881442529, 0.0004586733241762036670 ),
 .UNSPECIFIED. ) ;
#24717=DIRECTION ( 'NONE',  ( 0.000000000000000000, 0.000000000000000000, -1.000000000000000000 ) ) ;
#24721=B_SPLINE_CURVE_WITH_KNOTS ( 'NONE', 3,
 ( #40237, #26098, #2270, #40533 ),
 .UNSPECIFIED., .F., .F.,
 ( 4, 4 ),
 ( 2.043828937333572736E-17, 0.004444306975806114161 ),
 .UNSPECIFIED. ) ;
#24735=CARTESIAN_POINT ( 'NONE',  ( 4.549368137175248350, 42.84816078363930814, -2.596185425821480930 ) ) ;
#24737=ORIENTED_EDGE ( 'NONE', *, *, #7874, .T. ) ;
#24738=EDGE_CURVE ( 'NONE', #6825, #23990, #53993, .T. ) ;
#24743=ORIENTED_EDGE ( 'NONE', *, *, #45679, .T. ) ;
#24748=CARTESIAN_POINT ( 'NONE',  ( -6.017396004339687465, 14.94857180791993123, 11.47192209077592295 ) ) ;
#24751=ORIENTED_EDGE ( 'NONE', *, *, #57664, .T. ) ;
#24760=CARTESIAN_POINT ( 'NONE',  ( -6.016761891674564211, -18.20201388312091950, -4.873659902332557081 ) ) ;
#24770=ORIENTED_EDGE ( 'NONE', *, *, #20954, .F. ) ;
#24772=CARTESIAN_POINT ( 'NONE',  ( 0.6254311100348650676, -13.11433105842173852, 46.28443883864371600 ) ) ;
#24777=FACE_OUTER_BOUND ( 'NONE', #30232, .T. ) ;
#24787=ADVANCED_FACE ( 'NONE', ( #28953 ), #25715, .F. ) ;
#24790=( BOUNDED_SURFACE ( )  B_SPLINE_SURFACE ( 3, 1, ( 
 ( #13692, #52184 ),
 ( #14006, #46589 ),
 ( #42822, #3943 ),
 ( #18076, #3631 ) ),
 .UNSPECIFIED., .F., .F., .F. ) 
 B_SPLINE_SURFACE_WITH_KNOTS ( ( 4, 4 ),
 ( 2, 2 ),
 ( 0.000000000000000000, 1.000000000000000000 ),
 ( 0.000000000000000000, 1.000000000000000000 ),
 .UNSPECIFIED. ) 
 GEOMETRIC_REPRESENTATION_ITEM ( )  RATIONAL_B_SPLINE_SURFACE ( (
 ( 1.000000000000000000, 1.000000000000000000),
 ( 0.9751682680413298332, 0.9999560080971552356),
 ( 0.9751682680413298332, 0.9999560080971552356),
 ( 1.000000000000000000, 1.000000000000000000) ) ) 
 REPRESENTATION_ITEM ( '' )  SURFACE ( )  );
#24800=CARTESIAN_POINT ( 'NONE',  ( -6.016761891674564211, -17.41015286184797262, -7.207804629151495668 ) ) ;
#24807=CARTESIAN_POINT ( 'NONE',  ( 4.549368137175248350, 40.71620287708324781, 13.59764261105765826 ) ) ;
#24809=CARTESIAN_POINT ( 'NONE',  ( -6.017396004339686577, -9.420565012089543444, 16.31924478664272371 ) ) ;
#24814=ADVANCED_FACE ( 'NONE', ( #40853 ), #8880, .F. ) ;
#24818=CARTESIAN_POINT ( 'NONE',  ( -6.015611763856276717, -13.31979030221789984, -13.32857883366847318 ) ) ;
#24819=EDGE_CURVE ( 'NONE', #19445, #52485, #53967, .T. ) ;
#24821=EDGE_CURVE ( 'NONE', #25537, #15737, #43137, .T. ) ;
#24822=CARTESIAN_POINT ( 'NONE',  ( 4.549368137175248350, -28.14399996863522446, 32.41327393324091588 ) ) ;
#24824=EDGE_CURVE ( 'NONE', #61266, #12288, #17714, .T. ) ;
#24829=CARTESIAN_POINT ( 'NONE',  ( 0.6031357023905875581, -29.32055886552351254, 38.13964912630282811 ) ) ;
#24832=CARTESIAN_POINT ( 'NONE',  ( -6.017396004339687465, 16.31807101179370179, 9.422598049764681960 ) ) ;
#24837=CARTESIAN_POINT ( 'NONE',  ( 1.827119703190779765, 41.24693285842928958, -12.32825544177793731 ) ) ;
#24843=CARTESIAN_POINT ( 'NONE',  ( 0.1097557419366048670, 5.849988371690505673, 42.72583172879055269 ) ) ;
#24850=VERTEX_POINT ( 'NONE', #31109 ) ;
#24852=CARTESIAN_POINT ( 'NONE',  ( 4.833616638992205949, 30.83411269743563921, -34.47248434257878813 ) ) ;
#24858=ORIENTED_EDGE ( 'NONE', *, *, #14099, .F. ) ;
#24859=CARTESIAN_POINT ( 'NONE',  ( 0.5998501479064708430, -46.60114184914326074, 11.94461217097388328 ) ) ;
#24860=DIRECTION ( 'NONE',  ( -1.000000000000000000, 0.000000000000000000, -0.000000000000000000 ) ) ;
#24864=CARTESIAN_POINT ( 'NONE',  ( 0.1103744047535531458, 34.23648668783393845, -26.22174028894833953 ) ) ;
#24867=EDGE_CURVE ( 'NONE', #37278, #17539, #58987, .T. ) ;
#24875=CARTESIAN_POINT ( 'NONE',  ( 3.238741278300274029, -41.96285461600087530, 9.350673766180072732 ) ) ;
#24876=CARTESIAN_POINT ( 'NONE',  ( 4.549368137175248350, -38.40568845698262379, -19.17571786012310753 ) ) ;
#24881=CARTESIAN_POINT ( 'NONE',  ( 1.827326673878743701, 9.946825761453919057, 41.88502433275007775 ) ) ;
#24886=CARTESIAN_POINT ( 'NONE',  ( 0.1073791018717578927, 16.05399293000759542, 40.02496097243063389 ) ) ;
#24887=CARTESIAN_POINT ( 'NONE',  ( 0.7245667037590748372, -7.091191019330533862, -47.57651946688172018 ) ) ;
#24889=ORIENTED_EDGE ( 'NONE', *, *, #11307, .F. ) ;
#24890=CARTESIAN_POINT ( 'NONE',  ( 0.1081432562775998252, -43.12249629849792854, -0.4234896101210040564 ) ) ;
#24893=CARTESIAN_POINT ( 'NONE',  ( 4.549368137175248350, -35.57418903283131328, 24.02461520945210793 ) ) ;
#24899=EDGE_CURVE ( 'NONE', #36963, #59719, #1969, .T. ) ;
#24903=CARTESIAN_POINT ( 'NONE',  ( 0.6001305935487422083, 46.33281397023063874, -12.95698906763762537 ) ) ;
#24913=EDGE_CURVE ( 'NONE', #44423, #25842, #60834, .T. ) ;
#24917=CARTESIAN_POINT ( 'NONE',  ( 4.549368137175248350, -24.02461520945298545, 35.57418903283073064 ) ) ;
#24930=CARTESIAN_POINT ( 'NONE',  ( 0.1103744047535531458, -37.32746539760805149, -21.59576373962403650 ) ) ;
#24939=CARTESIAN_POINT ( 'NONE',  ( -6.016761891674564211, -4.873659902332494909, 18.20201388312094082 ) ) ;
#24940=CARTESIAN_POINT ( 'NONE',  ( -6.015611763856276717, 16.32183393015596451, 9.416239407363361735 ) ) ;
#24942=CARTESIAN_POINT ( 'NONE',  ( 0.6023143664670691511, -41.79259346737339342, 23.82663958122363823 ) ) ;
#24945=CARTESIAN_POINT ( 'NONE',  ( 0.2885700199627517781, -20.85752789928088191, 37.73587457854630856 ) ) ;
#24957=CARTESIAN_POINT ( 'NONE',  ( 0.8751705887134553219, -34.63284514348562482, -33.37254303619542384 ) ) ;
#24958=CARTESIAN_POINT ( 'NONE',  ( -6.016761891674565099, -17.40752468084777504, -7.214149619366543753 ) ) ;
#24959=CARTESIAN_POINT ( 'NONE',  ( 0.5998501479064708430, 38.48283596222029956, -28.86886762351084812 ) ) ;
#24961=CARTESIAN_POINT ( 'NONE',  ( 0.1073791018717483448, -41.77800844988507123, -10.69234304550039383 ) ) ;
#24965=CARTESIAN_POINT ( 'NONE',  ( -6.010958268070873523, -7.197664668556567946, 17.41463273278775858 ) ) ;
#24973=CARTESIAN_POINT ( 'NONE',  ( -2.569797478183783568, -6.924386868080936175, 12.89088113963424043 ) ) ;
#24986=( BOUNDED_SURFACE ( )  B_SPLINE_SURFACE ( 3, 1, ( 
 ( #3961, #51275 ),
 ( #60355, #50660 ),
 ( #27176, #46300 ),
 ( #41600, #60984 ) ),
 .UNSPECIFIED., .F., .F., .F. ) 
 B_SPLINE_SURFACE_WITH_KNOTS ( ( 4, 4 ),
 ( 2, 2 ),
 ( 0.000000000000000000, 1.000000000000000000 ),
 ( 0.000000000000000000, 1.000000000000000000 ),
 .UNSPECIFIED. ) 
 GEOMETRIC_REPRESENTATION_ITEM ( )  RATIONAL_B_SPLINE_SURFACE ( (
 ( 1.000000000000000000, 1.000000000000000000),
 ( 0.7223157951917476005, 0.9931996967497186413),
 ( 0.7223157951917476005, 0.9931996967497186413),
 ( 1.000000000000000000, 1.000000000000000000) ) ) 
 REPRESENTATION_ITEM ( '' )  SURFACE ( )  );
#24987=VERTEX_POINT ( 'NONE', #22643 ) ;
#24991=EDGE_CURVE ( 'NONE', #19627, #25537, #55208, .T. ) ;
#24993=CARTESIAN_POINT ( 'NONE',  ( 0.6017667736363750963, 33.76945004754868762, 34.26315558341202205 ) ) ;
#24994=ORIENTED_EDGE ( 'NONE', *, *, #14871, .F. ) ;
#25000=ORIENTED_EDGE ( 'NONE', *, *, #34459, .F. ) ;
#25003=CARTESIAN_POINT ( 'NONE',  ( 1.827119703190780653, -34.89020442382241072, -25.21842556008173375 ) ) ;
#25006=ORIENTED_EDGE ( 'NONE', *, *, #51608, .T. ) ;
#25008=VECTOR ( 'NONE', #57896, 1000.000000000000114 ) ;
#25011=CARTESIAN_POINT ( 'NONE',  ( -6.016761891674565099, 7.214149619366596156, -17.40752468084775373 ) ) ;
#25013=CARTESIAN_POINT ( 'NONE',  ( -6.010958268070873523, -14.94067681728541963, -11.48268200989212495 ) ) ;
#25015=ORIENTED_EDGE ( 'NONE', *, *, #34129, .F. ) ;
#25019=DIRECTION ( 'NONE',  ( 0.000000000000000000, 0.000000000000000000, 1.000000000000000000 ) ) ;
#25023=ORIENTED_EDGE ( 'NONE', *, *, #4051, .F. ) ;
#25025=VERTEX_POINT ( 'NONE', #47369 ) ;
#25033=CARTESIAN_POINT ( 'NONE',  ( 1.827119703190779765, 22.58367210012840687, 36.65069040194717331 ) ) ;
#25050=ADVANCED_FACE ( 'NONE', ( #42686 ), #4455, .F. ) ;
#25052=ORIENTED_EDGE ( 'NONE', *, *, #10970, .F. ) ;
#25053=CARTESIAN_POINT ( 'NONE',  ( 0.6001305935487315502, 47.76436356026960084, 5.760103278698184504 ) ) ;
#25057=CARTESIAN_POINT ( 'NONE',  ( 0.6254311100348660668, -46.64066536338349778, 11.78487556908926770 ) ) ;
#25060=CARTESIAN_POINT ( 'NONE',  ( 0.5988103564986354543, 41.35593036885933316, -24.57719524907199826 ) ) ;
#25063=EDGE_CURVE ( 'NONE', #10591, #56576, #58725, .T. ) ;
#25065=CARTESIAN_POINT ( 'NONE',  ( 0.2230388203127593172, -41.44703429209694434, 11.89247826311202516 ) ) ;
#25074=CARTESIAN_POINT ( 'NONE',  ( 0.6001305935487422083, -46.60388846085714931, -11.94532529598361670 ) ) ;
#25079=CARTESIAN_POINT ( 'NONE',  ( 0.8751705887134553219, -7.160166390003972481, -47.55935879196468363 ) ) ;
#25082=CARTESIAN_POINT ( 'NONE',  ( 0.5980894510889448457, 13.12879507229288478, -46.28687279963680368 ) ) ;
#25083=CARTESIAN_POINT ( 'NONE',  ( 2.301430502907644282, -46.04685681264155050, -13.67112791032026919 ) ) ;
#25085=CARTESIAN_POINT ( 'NONE',  ( 0.3622758884714730732, 17.25816669464937902, 39.50828911767005280 ) ) ;
#25087=CARTESIAN_POINT ( 'NONE',  ( 0.6031357023905875581, 18.45021748202282552, -44.42879114414639474 ) ) ;
#25091=ADVANCED_FACE ( 'NONE', ( #1901 ), #17305, .F. ) ;
#25092=LINE ( 'NONE', #54738, #29912 ) ;
#25097=EDGE_CURVE ( 'NONE', #35307, #58937, #42357, .T. ) ;
#25112=CARTESIAN_POINT ( 'NONE',  ( -6.016761891674565099, -9.424569481870369358, 16.31696541414269319 ) ) ;
#25114=EDGE_CURVE ( 'NONE', #9246, #58767, #40467, .T. ) ;
#25120=ORIENTED_EDGE ( 'NONE', *, *, #634, .T. ) ;
#25121=CARTESIAN_POINT ( 'NONE',  ( 0.8760168074887090262, -13.30888447662048435, -46.22580377597781620 ) ) ;
#25122=VERTEX_POINT ( 'NONE', #11965 ) ;
#25126=CARTESIAN_POINT ( 'NONE',  ( 0.1081432562775997142, 10.75186376283284062, 41.76274004527636663 ) ) ;
#25128=DIRECTION ( 'NONE',  ( -1.000000000000000000, -0.000000000000000000, -0.000000000000000000 ) ) ;
#25142=( BOUNDED_SURFACE ( )  B_SPLINE_SURFACE ( 3, 1, ( 
 ( #30692, #25074 ),
 ( #952, #44218 ),
 ( #34799, #5934 ),
 ( #1248, #30377 ) ),
 .UNSPECIFIED., .F., .F., .F. ) 
 B_SPLINE_SURFACE_WITH_KNOTS ( ( 4, 4 ),
 ( 2, 2 ),
 ( 0.000000000000000000, 1.000000000000000000 ),
 ( 0.000000000000000000, 1.000000000000000000 ),
 .UNSPECIFIED. ) 
 GEOMETRIC_REPRESENTATION_ITEM ( )  RATIONAL_B_SPLINE_SURFACE ( (
 ( 1.000000000000000000, 1.000000000000000000),
 ( 0.9751682680413298332, 0.9999560080971552356),
 ( 0.9751682680413298332, 0.9999560080971552356),
 ( 1.000000000000000000, 1.000000000000000000) ) ) 
 REPRESENTATION_ITEM ( '' )  SURFACE ( )  );
#25144=CARTESIAN_POINT ( 'NONE',  ( 2.301529144917014325, 30.25186323939223954, 37.31001381748743029 ) ) ;
#25153=CARTESIAN_POINT ( 'NONE',  ( 0.1073791018717578927, 37.58707531572206051, -21.14095454447521405 ) ) ;
#25154=ADVANCED_FACE ( 'NONE', ( #50155 ), #18040, .F. ) ;
#25158=CARTESIAN_POINT ( 'NONE',  ( 0.1104177457020372871, 34.20994892372210217, -26.25638621857955712 ) ) ;
#25159=EDGE_CURVE ( 'NONE', #38023, #32695, #51305, .T. ) ;
#25160=CARTESIAN_POINT ( 'NONE',  ( 4.322998006666179727, 4.155494336618708928, -47.80838462754061169 ) ) ;
#25166=EDGE_CURVE ( 'NONE', #12159, #9208, #48324, .T. ) ;
#25167=CARTESIAN_POINT ( 'NONE',  ( 0.1087620492084206275, 30.74858804150686709, -30.23658359364789305 ) ) ;
#25169=CARTESIAN_POINT ( 'NONE',  ( 0.5998501479064708430, -34.38546660123321175, 33.64490850298784608 ) ) ;
#25174=CARTESIAN_POINT ( 'NONE',  ( 0.5998501479064699549, -23.59887241503383493, 41.92175333043579144 ) ) ;
#25190=CARTESIAN_POINT ( 'NONE',  ( 0.3622758884714600280, -34.70015533914845918, 25.58609868863709380 ) ) ;
#25193=CARTESIAN_POINT ( 'NONE',  ( 0.1098349054025746369, -11.36734385884033927, 41.59932877996178746 ) ) ;
#25194=CARTESIAN_POINT ( 'NONE',  ( -6.016761891674565099, -13.32657647165364700, 13.32172022638586917 ) ) ;
#25198=CARTESIAN_POINT ( 'NONE',  ( -6.016761891674565099, -18.20201388312099056, 4.873659902332302174 ) ) ;
#25210=CARTESIAN_POINT ( 'NONE',  ( 0.6001305935487315502, 18.89378601236065691, -44.24520387813809208 ) ) ;
#25213=CARTESIAN_POINT ( 'NONE',  ( 4.549368137175248350, 2.596185425821331272, 42.84816078363931524 ) ) ;
#25215=CARTESIAN_POINT ( 'NONE',  ( 0.8760168074887090262, 46.22580377597785883, -13.30888447662032092 ) ) ;
#25233=CARTESIAN_POINT ( 'NONE',  ( 0.6030672727741701600, -47.70721108823352807, 6.192762795893642647 ) ) ;
#25237=CARTESIAN_POINT ( 'NONE',  ( 0.6027935024548037868, -41.74929432965634390, 23.90242449907741218 ) ) ;
#25245=CARTESIAN_POINT ( 'NONE',  ( 0.3622758884714730732, -40.13994584881772454, -15.73321244754840720 ) ) ;
#25253=CARTESIAN_POINT ( 'NONE',  ( 0.7048096507298579061, 17.62869676200345737, 44.76417498422321728 ) ) ;
#25261=DIRECTION ( 'NONE',  ( -1.000000000000000000, -0.000000000000000000, -0.000000000000000000 ) ) ;
#25263=CARTESIAN_POINT ( 'NONE',  ( 0.6009453534118439633, 0.4363813339958033111, -48.10564080474284765 ) ) ;
#25264=FACE_OUTER_BOUND ( 'NONE', #28828, .T. ) ;
#25265=VERTEX_POINT ( 'NONE', #20274 ) ;
#25273=( BOUNDED_SURFACE ( )  B_SPLINE_SURFACE ( 3, 1, ( 
 ( #42144, #8266 ),
 ( #3254, #8576 ),
 ( #32102, #22381 ),
 ( #36814, #27703 ) ),
 .UNSPECIFIED., .F., .F., .F. ) 
 B_SPLINE_SURFACE_WITH_KNOTS ( ( 4, 4 ),
 ( 2, 2 ),
 ( 0.000000000000000000, 1.000000000000000000 ),
 ( 0.000000000000000000, 1.000000000000000000 ),
 .UNSPECIFIED. ) 
 GEOMETRIC_REPRESENTATION_ITEM ( )  RATIONAL_B_SPLINE_SURFACE ( (
 ( 1.000000000000000000, 1.000000000000000000),
 ( 0.7223157951917476005, 0.9931996967497186413),
 ( 0.7223157951917476005, 0.9931996967497186413),
 ( 1.000000000000000000, 1.000000000000000000) ) ) 
 REPRESENTATION_ITEM ( '' )  SURFACE ( )  );
#25276=CARTESIAN_POINT ( 'NONE',  ( 0.1073791018717578927, -5.147744207006579309, -42.81622261970993293 ) ) ;
#25280=CARTESIAN_POINT ( 'NONE',  ( 0.2230388203127542934, 36.95676097786380154, -22.21453373073351756 ) ) ;
#25286=CARTESIAN_POINT ( 'NONE',  ( 0.3622758884714600280, 41.85013935980101962, -10.35929834645879133 ) ) ;
#25290=LINE ( 'NONE', #57232, #27717 ) ;
#25291=CARTESIAN_POINT ( 'NONE',  ( 4.975801465491694664, -47.84403947906841381, 2.564218696447319257 ) ) ;
#25293=ORIENTED_EDGE ( 'NONE', *, *, #12006, .F. ) ;
#25304=ORIENTED_EDGE ( 'NONE', *, *, #38102, .F. ) ;
#25322=EDGE_CURVE ( 'NONE', #47737, #35307, #34801, .T. ) ;
#25324=EDGE_CURVE ( 'NONE', #30112, #12663, #4138, .T. ) ;
#25335=FACE_OUTER_BOUND ( 'NONE', #52387, .T. ) ;
#25338=EDGE_CURVE ( 'NONE', #24433, #23785, #29564, .T. ) ;
#25349=CARTESIAN_POINT ( 'NONE',  ( 0.1081432562775997419, 43.12249629849793564, 0.4234896101213052044 ) ) ;
#25357=CARTESIAN_POINT ( 'NONE',  ( 4.691466044806102964, 40.13652286047893369, -19.42108863068337143 ) ) ;
#25364=VERTEX_POINT ( 'NONE', #55291 ) ;
#25366=DIRECTION ( 'NONE',  ( -1.000000000000000000, -0.000000000000000000, -0.000000000000000000 ) ) ;
#25367=DIRECTION ( 'NONE',  ( -0.1024043820194934645, -0.7126273545981489654, 0.6940285268068233648 ) ) ;
#25370=B_SPLINE_CURVE_WITH_KNOTS ( 'NONE', 3,
 ( #17168, #36281, #6179, #7109, #21242, #26235 ),
 .UNSPECIFIED., .F., .F.,
 ( 4, 2, 4 ),
 ( 2.032850612904068153E-17, 0.0002293319059085098999, 0.0004586638118169994709 ),
 .UNSPECIFIED. ) ;
#25373=DIRECTION ( 'NONE',  ( 0.000000000000000000, 0.000000000000000000, 1.000000000000000000 ) ) ;
#25374=ORIENTED_EDGE ( 'NONE', *, *, #31514, .F. ) ;
#25380=EDGE_LOOP ( 'NONE', ( #22138, #14109, #21613, #41554 ) ) ;
#25395=EDGE_CURVE ( 'NONE', #25122, #3613, #10159, .T. ) ;
#25398=CIRCLE ( 'NONE', #38397, 42.92674063221959813 ) ;
#25400=FILL_AREA_STYLE ('',( #30094 ) ) ;
#25401=CARTESIAN_POINT ( 'NONE',  ( -2.569797478183790229, -6.011723966604236580, 13.34095667500594828 ) ) ;
#25405=DIRECTION ( 'NONE',  ( -1.000000000000000000, -0.000000000000000000, -0.000000000000000000 ) ) ;
#25418=VECTOR ( 'NONE', #41541, 1000.000000000000227 ) ;
#25428=ORIENTED_EDGE ( 'NONE', *, *, #34244, .F. ) ;
#25436=B_SPLINE_CURVE_WITH_KNOTS ( 'NONE', 3,
 ( #25286, #51542, #3309, #27140 ),
 .UNSPECIFIED., .F., .F.,
 ( 4, 4 ),
 ( 2.276721302528256204E-17, 0.004564976165746189446 ),
 .UNSPECIFIED. ) ;
#25441=CARTESIAN_POINT ( 'NONE',  ( 4.975801465491694664, 20.67815041659077835, 43.22084481528228395 ) ) ;
#25453=CARTESIAN_POINT ( 'NONE',  ( 0.6009452777970410997, -41.87890062806020097, -23.67489783211079413 ) ) ;
#25454=EDGE_CURVE ( 'NONE', #5563, #41175, #55743, .T. ) ;
#25459=CARTESIAN_POINT ( 'NONE',  ( 0.1103744047535531458, 34.18931094755004807, 26.28322091066887722 ) ) ;
#25463=CARTESIAN_POINT ( 'NONE',  ( 0.1092355843206037486, 34.39511076960603475, -26.01340835034376653 ) ) ;
#25468=CARTESIAN_POINT ( 'NONE',  ( 4.549368137175248350, 0.000000000000000000, 0.000000000000000000 ) ) ;
#25471=CARTESIAN_POINT ( 'NONE',  ( 4.549368137175248350, -19.17571786012296187, -38.40568845698270195 ) ) ;
#25473=CARTESIAN_POINT ( 'NONE',  ( 0.6001305935487315502, 44.24520387813827682, -18.89378601236018795 ) ) ;
#25480=CARTESIAN_POINT ( 'NONE',  ( 4.549368137175248350, 8.582197505783829783, 42.06008734272398897 ) ) ;
#25482=B_SPLINE_CURVE_WITH_KNOTS ( 'NONE', 3,
 ( #20556, #44690, #40003, #48439, #44394, #823 ),
 .UNSPECIFIED., .F., .F.,
 ( 4, 2, 4 ),
 ( 1.267283937151336631E-16, 0.0002450741128632353779, 0.0004901482257263440126 ),
 .UNSPECIFIED. ) ;
#25486=VERTEX_POINT ( 'NONE', #34876 ) ;
#25487=ORIENTED_EDGE ( 'NONE', *, *, #46578, .F. ) ;
#25488=CARTESIAN_POINT ( 'NONE',  ( 0.1092355843206037486, -43.12343565949664992, -0.3005923759132368422 ) ) ;
#25490=LINE ( 'NONE', #30489, #61742 ) ;
#25493=CARTESIAN_POINT ( 'NONE',  ( 0.8751705887134553219, -33.37254303619578621, 34.63284514348527665 ) ) ;
#25494=CARTESIAN_POINT ( 'NONE',  ( 0.6001305935487315502, -28.87057754790966868, 38.48510059943998129 ) ) ;
#25496=VERTEX_POINT ( 'NONE', #24533 ) ;
#25498=ORIENTED_EDGE ( 'NONE', *, *, #22100, .T. ) ;
#25503=ADVANCED_FACE ( 'NONE', ( #49257 ), #44951, .F. ) ;
#25506=EDGE_CURVE ( 'NONE', #10647, #21806, #6337, .T. ) ;
#25507=CARTESIAN_POINT ( 'NONE',  ( 0.7048096507298635682, -48.10291524268441776, 0.8437160066905670108 ) ) ;
#25508=( BOUNDED_SURFACE ( )  B_SPLINE_SURFACE ( 3, 1, ( 
 ( #52741, #48063 ),
 ( #5114, #10152 ),
 ( #29247, #24558 ),
 ( #736, #17025 ) ),
 .UNSPECIFIED., .F., .F., .F. ) 
 B_SPLINE_SURFACE_WITH_KNOTS ( ( 4, 4 ),
 ( 2, 2 ),
 ( 0.000000000000000000, 1.000000000000000000 ),
 ( 0.000000000000000000, 1.000000000000000000 ),
 .UNSPECIFIED. ) 
 GEOMETRIC_REPRESENTATION_ITEM ( )  RATIONAL_B_SPLINE_SURFACE ( (
 ( 1.000000000000000000, 1.000000000000000000),
 ( 0.7223157951917476005, 0.9931996967497186413),
 ( 0.7223157951917476005, 0.9931996967497186413),
 ( 1.000000000000000000, 1.000000000000000000) ) ) 
 REPRESENTATION_ITEM ( '' )  SURFACE ( )  );
#25514=CARTESIAN_POINT ( 'NONE',  ( 4.975801465491694664, 2.564218696446817880, 47.84403947906844223 ) ) ;
#25515=DIRECTION ( 'NONE',  ( 0.09835009131224567436, -0.9592125346408703068, -0.2650256080583726637 ) ) ;
#25518=CARTESIAN_POINT ( 'NONE',  ( 0.8760168074886960365, 34.63873394077486978, -33.37827814204089805 ) ) ;
#25524=CARTESIAN_POINT ( 'NONE',  ( 0.2224561200757610435, 4.874377913225924175, 42.84309024201777305 ) ) ;
#25525=VECTOR ( 'NONE', #56547, 1000.000000000000114 ) ;
#25528=( BOUNDED_SURFACE ( )  B_SPLINE_SURFACE ( 3, 1, ( 
 ( #15645, #6814 ),
 ( #54122, #25641 ),
 ( #59451, #34747 ),
 ( #53817, #10947 ) ),
 .UNSPECIFIED., .F., .F., .F. ) 
 B_SPLINE_SURFACE_WITH_KNOTS ( ( 4, 4 ),
 ( 2, 2 ),
 ( 0.000000000000000000, 1.000000000000000000 ),
 ( 0.000000000000000000, 1.000000000000000000 ),
 .UNSPECIFIED. ) 
 GEOMETRIC_REPRESENTATION_ITEM ( )  RATIONAL_B_SPLINE_SURFACE ( (
 ( 1.000000000000000000, 1.000000000000000000),
 ( 0.9953040768229013402, 0.8617119497784988535),
 ( 0.9953040768229013402, 0.8617119497784988535),
 ( 1.000000000000000000, 1.000000000000000000) ) ) 
 REPRESENTATION_ITEM ( '' )  SURFACE ( )  );
#25535=CARTESIAN_POINT ( 'NONE',  ( -6.016761891674565099, 16.31696541414272161, 9.424569481870310739 ) ) ;
#25537=VERTEX_POINT ( 'NONE', #6314 ) ;
#25538=CARTESIAN_POINT ( 'NONE',  ( 0.7245667037590756143, -5.464144792999733546, 47.79072416626834752 ) ) ;
#25543=CARTESIAN_POINT ( 'NONE',  ( 0.5998501479064708430, -41.92175333043635987, 23.59887241503281174 ) ) ;
#25545=CARTESIAN_POINT ( 'NONE',  ( 0.8751705887134553219, -0.8911681664085087107, -48.08707113907594533 ) ) ;
#25546=CARTESIAN_POINT ( 'NONE',  ( 0.3622758884714600280, -10.35929834645893699, -41.85013935980099120 ) ) ;
#25553=CARTESIAN_POINT ( 'NONE',  ( -6.015611763856276717, 4.882992715191555533, -18.19956619163653500 ) ) ;
#25556=EDGE_CURVE ( 'NONE', #27976, #54850, #1151, .T. ) ;
#25559=CARTESIAN_POINT ( 'NONE',  ( 0.1313383488274128263, -0.6377633466097591963, -43.11882601516400371 ) ) ;
#25563=CARTESIAN_POINT ( 'NONE',  ( 0.5998501479064708430, -0.5236536531318284338, 48.10473956285918717 ) ) ;
#25568=VERTEX_POINT ( 'NONE', #34257 ) ;
#25569=CARTESIAN_POINT ( 'NONE',  ( 4.975801465491695552, 2.564218696447496004, -47.84403947906841381 ) ) ;
#25572=CARTESIAN_POINT ( 'NONE',  ( 0.1081432562775997419, 16.11101151263768827, 40.00205417854818535 ) ) ;
#25577=CARTESIAN_POINT ( 'NONE',  ( 4.975801465491695552, -15.94009207553018648, -45.18341283946452336 ) ) ;
#25581=CARTESIAN_POINT ( 'NONE',  ( 0.1097557419366048670, -11.37678103520307715, -41.59672960874308245 ) ) ;
#25592=EDGE_CURVE ( 'NONE', #23847, #27695, #10444, .T. ) ;
#25595=B_SPLINE_CURVE_WITH_KNOTS ( 'NONE', 3,
 ( #25563, #6422, #34992, #15874, #15563, #10548, #34670, #48756, #11172, #52839 ),
 .UNSPECIFIED., .F., .F.,
 ( 4, 3, 3, 4 ),
 ( 2.027574016683678720E-17, 0.0002618515315864106976, 0.0003927756766341516958, 0.0005236741812378729226 ),
 .UNSPECIFIED. ) ;
#25597=EDGE_CURVE ( 'NONE', #13939, #40478, #13172, .T. ) ;
#25602=CARTESIAN_POINT ( 'NONE',  ( 4.691466044806103852, 8.371234562541850721, -43.79545162262300551 ) ) ;
#25605=CARTESIAN_POINT ( 'NONE',  ( 0.1064266379913942906, 21.07422113734163460, -37.62465837278053726 ) ) ;
#25607=VERTEX_POINT ( 'NONE', #6945 ) ;
#25610=CARTESIAN_POINT ( 'NONE',  ( 4.549368137175248350, 0.000000000000000000, 0.000000000000000000 ) ) ;
#25612=B_SPLINE_CURVE_WITH_KNOTS ( 'NONE', 3,
 ( #24153, #47064, #23537, #9130, #18238, #47977 ),
 .UNSPECIFIED., .F., .F.,
 ( 4, 2, 4 ),
 ( 8.673136251825839020E-17, 0.0002293366620881421387, 0.0004586733241761975412 ),
 .UNSPECIFIED. ) ;
#25617=CARTESIAN_POINT ( 'NONE',  ( -6.015611763856276717, 17.40650793417844255, 7.216738110653344584 ) ) ;
#25626=CARTESIAN_POINT ( 'NONE',  ( 0.3622758884714600280, 29.89648521331588071, 31.06363466427737663 ) ) ;
#25632=CARTESIAN_POINT ( 'NONE',  ( 0.7048096507298579061, -28.61383451045671222, -38.67623024744037963 ) ) ;
#25641=CARTESIAN_POINT ( 'NONE',  ( 0.5980894510889448457, 44.71414919659906673, -17.76188940524901838 ) ) ;
#25643=DIRECTION ( 'NONE',  ( 0.1024043820194936311, 0.8548216096550996790, -0.5087173657443492258 ) ) ;
#25649=ORIENTED_EDGE ( 'NONE', *, *, #33587, .T. ) ;
#25662=EDGE_CURVE ( 'NONE', #8307, #37892, #7134, .T. ) ;
#25663=CARTESIAN_POINT ( 'NONE',  ( 4.975801465491694664, 43.22084481528220579, -20.67815041659094888 ) ) ;
#25666=EDGE_CURVE ( 'NONE', #34543, #39132, #37818, .T. ) ;
#25667=CARTESIAN_POINT ( 'NONE',  ( 3.238741278300273141, 41.01623499585995347, 12.88350628398754516 ) ) ;
#25668=EDGE_LOOP ( 'NONE', ( #26230, #7546, #33240, #43530 ) ) ;
#25670=ADVANCED_FACE ( 'NONE', ( #50498 ), #3368, .F. ) ;
#25678=ORIENTED_EDGE ( 'NONE', *, *, #52302, .F. ) ;
#25679=B_SPLINE_CURVE_WITH_KNOTS ( 'NONE', 3,
 ( #10215, #29931, #44073, #29311 ),
 .UNSPECIFIED., .F., .F.,
 ( 4, 4 ),
 ( 0.000000000000000000, 0.005014147105413694315 ),
 .UNSPECIFIED. ) ;
#25688=EDGE_CURVE ( 'NONE', #16902, #5739, #42247, .T. ) ;
#25690=CARTESIAN_POINT ( 'NONE',  ( 4.549368137175248350, 35.57418903283081590, 24.02461520945284690 ) ) ;
#25693=EDGE_CURVE ( 'NONE', #61173, #49729, #16823, .T. ) ;
#25695=ORIENTED_EDGE ( 'NONE', *, *, #50559, .F. ) ;
#25697=ORIENTED_EDGE ( 'NONE', *, *, #4438, .T. ) ;
#25707=ORIENTED_EDGE ( 'NONE', *, *, #29655, .F. ) ;
#25710=B_SPLINE_CURVE_WITH_KNOTS ( 'NONE', 3,
 ( #40727, #60101, #45417, #54457 ),
 .UNSPECIFIED., .F., .F.,
 ( 4, 4 ),
 ( 2.294131830766625192E-17, 0.004564976165746188579 ),
 .UNSPECIFIED. ) ;
#25713=SURFACE_STYLE_USAGE ( .BOTH. , #16954 ) ;
#25715=( BOUNDED_SURFACE ( )  B_SPLINE_SURFACE ( 3, 1, ( 
 ( #15792, #39610 ),
 ( #35212, #58663 ),
 ( #21403, #49282 ),
 ( #11392, #45537 ) ),
 .UNSPECIFIED., .F., .F., .F. ) 
 B_SPLINE_SURFACE_WITH_KNOTS ( ( 4, 4 ),
 ( 2, 2 ),
 ( 0.000000000000000000, 1.000000000000000000 ),
 ( 0.000000000000000000, 1.000000000000000000 ),
 .UNSPECIFIED. ) 
 GEOMETRIC_REPRESENTATION_ITEM ( )  RATIONAL_B_SPLINE_SURFACE ( (
 ( 1.000000000000000000, 1.000000000000000000),
 ( 0.7223157951917480446, 0.9931996967497186413),
 ( 0.7223157951917480446, 0.9931996967497186413),
 ( 1.000000000000000000, 1.000000000000000000) ) ) 
 REPRESENTATION_ITEM ( '' )  SURFACE ( )  );
#25730=CARTESIAN_POINT ( 'NONE',  ( -6.016489644550737204, 18.68257207665199715, -2.455165042129548336 ) ) ;
#25735=CARTESIAN_POINT ( 'NONE',  ( 0.6031357023905875581, -12.40899271757806765, -46.47951061918806204 ) ) ;
#25748=CARTESIAN_POINT ( 'NONE',  ( 0.1095718737110178281, 10.91304379105004330, 41.72082389913620659 ) ) ;
#25751=B_SPLINE_CURVE_WITH_KNOTS ( 'NONE', 3,
 ( #60620, #8626, #60943, #51535, #18054, #21819, #12426, #13669, #22430, #27132, #22123, #31842, #3920, #3301, #55934, #45636 ),
 .UNSPECIFIED., .F., .F.,
 ( 4, 3, 3, 3, 3, 4 ),
 ( 1.868480190406682863E-17, 0.0002618515315864432236, 0.0003927756766342012438, 0.0005236998216950576731, 0.0007855159896329925008, 0.001047349442285930472 ),
 .UNSPECIFIED. ) ;
#25753=ORIENTED_EDGE ( 'NONE', *, *, #6333, .T. ) ;
#25754=CARTESIAN_POINT ( 'NONE',  ( 0.1103936448916694457, -6.269440624735986453E-17, 43.12443171339902648 ) ) ;
#25756=CARTESIAN_POINT ( 'NONE',  ( -6.016761891674565099, 2.462934516564073917, -18.68153697670638991 ) ) ;
#25766=VECTOR ( 'NONE', #24321, 1000.000000000000000 ) ;
#25767=CARTESIAN_POINT ( 'NONE',  ( 0.1073791018717578927, 41.52698815987152159, 11.62916352156164557 ) ) ;
#25769=CARTESIAN_POINT ( 'NONE',  ( 0.2885697896453112143, -41.84838128162066795, 10.38006191081347218 ) ) ;
#25776=B_SPLINE_CURVE_WITH_KNOTS ( 'NONE', 3,
 ( #25787, #16391, #1964, #17323 ),
 .UNSPECIFIED., .F., .F.,
 ( 4, 4 ),
 ( 6.938893903907228378E-18, 0.005014147105413696050 ),
 .UNSPECIFIED. ) ;
#25778=CARTESIAN_POINT ( 'NONE',  ( 4.975801465491695552, 20.67815041659141784, -43.22084481528199973 ) ) ;
#25779=CARTESIAN_POINT ( 'NONE',  ( 0.1095718737110178281, 34.05592812063346031, 26.45591486700768513 ) ) ;
#25782=CARTESIAN_POINT ( 'NONE',  ( 0.1073791018717483448, -43.12183934961191056, 0.4849339620931858996 ) ) ;
#25787=CARTESIAN_POINT ( 'NONE',  ( 4.975801465491694664, -20.67815041659109809, -43.22084481528213473 ) ) ;
#25796=CARTESIAN_POINT ( 'NONE',  ( 0.5998501479064699549, -6.798102206413803472, -47.62484632993685807 ) ) ;
#25799=CARTESIAN_POINT ( 'NONE',  ( -6.015611763856276717, -4.882992715191171840, -18.19956619163663447 ) ) ;
#25803=ORIENTED_EDGE ( 'NONE', *, *, #37511, .F. ) ;
#25810=CARTESIAN_POINT ( 'NONE',  ( 4.549368137175248350, 42.14271863032833920, -8.166781970325278195 ) ) ;
#25812=AXIS2_PLACEMENT_3D ( 'NONE', #26786, #41524, #7983 ) ;
#25822=ADVANCED_BREP_SHAPE_REPRESENTATION ( '', ( #10540, #14677 ), #46738 ) ;
#25825=CARTESIAN_POINT ( 'NONE',  ( 0.5998501479064699549, -24.50586714782575726, -41.39809967730479201 ) ) ;
#25842=VERTEX_POINT ( 'NONE', #23162 ) ;
#25845=ORIENTED_EDGE ( 'NONE', *, *, #48302, .F. ) ;
#25849=ORIENTED_EDGE ( 'NONE', *, *, #41396, .F. ) ;
#25865=FACE_OUTER_BOUND ( 'NONE', #12912, .T. ) ;
#25873=CARTESIAN_POINT ( 'NONE',  ( 0.6028618097248863439, -44.37846879336947836, 18.57111736963370419 ) ) ;
#25875=CARTESIAN_POINT ( 'NONE',  ( 0.6009453534118439633, 41.87889766923454715, -23.67490308139361588 ) ) ;
#25878=CARTESIAN_POINT ( 'NONE',  ( 0.1073791018717578927, 6.109314776652701617, -42.68962945260948061 ) ) ;
#25883=VECTOR ( 'NONE', #21459, 999.9999999999998863 ) ;
#25885=CARTESIAN_POINT ( 'NONE',  ( 0.5998501479064708430, 0.5236536531314925913, -48.10473956285919428 ) ) ;
#25887=CARTESIAN_POINT ( 'NONE',  ( -6.016489644550736315, -16.31649074174283598, 9.425415887801030124 ) ) ;
#25889=CARTESIAN_POINT ( 'NONE',  ( 0.6001305935487422083, 38.48510059944047157, -28.87057754790898656 ) ) ;
#25892=ORIENTED_EDGE ( 'NONE', *, *, #33587, .F. ) ;
#25893=DIRECTION ( 'NONE',  ( 1.000000000000000000, 0.000000000000000000, 0.000000000000000000 ) ) ;
#25899=EDGE_LOOP ( 'NONE', ( #22847, #12413, #20228, #490 ) ) ;
#25902=EDGE_CURVE ( 'NONE', #20913, #36543, #4765, .T. ) ;
#25908=DIRECTION ( 'NONE',  ( 1.000000000000000000, 0.000000000000000000, 0.000000000000000000 ) ) ;
#25912=ORIENTED_EDGE ( 'NONE', *, *, #48091, .T. ) ;
#25913=CARTESIAN_POINT ( 'NONE',  ( 0.8751705887134553219, -24.81530984069179269, -41.19904111682499348 ) ) ;
#25921=ORIENTED_EDGE ( 'NONE', *, *, #10764, .T. ) ;
#25922=LINE ( 'NONE', #21218, #13196 ) ;
#25926=CARTESIAN_POINT ( 'NONE',  ( 0.6001305935487422083, 0.5236757026882734589, 48.10757715638249010 ) ) ;
#25931=CARTESIAN_POINT ( 'NONE',  ( 0.6001305935487422083, -18.89378601236091981, 44.24520387813797129 ) ) ;
#25938=CARTESIAN_POINT ( 'NONE',  ( 0.3622758884714600280, -37.74294673546600620, 20.83792692158906235 ) ) ;
#25939=CARTESIAN_POINT ( 'NONE',  ( 0.1092355843206037486, -5.330717085613026818, -42.79374386763043958 ) ) ;
#25946=EDGE_LOOP ( 'NONE', ( #6854, #24889, #52029, #59473 ) ) ;
#25948=CARTESIAN_POINT ( 'NONE',  ( 4.975801465491695552, 35.64402118370958306, -32.01766832630274706 ) ) ;
#25952=CARTESIAN_POINT ( 'NONE',  ( -2.569797478183790229, -14.24379821351259601, 3.352038560005669687 ) ) ;
#25955=CARTESIAN_POINT ( 'NONE',  ( 0.6041374136657476912, 48.10739871142803992, -0.1745662470639787467 ) ) ;
#25960=LINE ( 'NONE', #53215, #42858 ) ;
#25966=AXIS2_PLACEMENT_3D ( 'NONE', #23433, #44047, #37555 ) ;
#25970=ADVANCED_FACE ( 'NONE', ( #1484 ), #38180, .F. ) ;
#25971=CONICAL_SURFACE ( 'NONE', #47011, 42.92674063221959813, 1.485477209440487556 ) ;
#25972=CARTESIAN_POINT ( 'NONE',  ( 0.1104177457020373149, 43.12445244485484608, -0.004894317366372227286 ) ) ;
#25975=CARTESIAN_POINT ( 'NONE',  ( 0.1081432562775998668, -41.76274004527640926, 10.75186376283269851 ) ) ;
#25976=ORIENTED_EDGE ( 'NONE', *, *, #22998, .F. ) ;
#25981=CARTESIAN_POINT ( 'NONE',  ( 3.238931869106854933, 18.12707634097768761, 38.98364358950751551 ) ) ;
#25984=AXIS2_PLACEMENT_3D ( 'NONE', #47751, #411, #42756 ) ;
#25997=EDGE_CURVE ( 'NONE', #5948, #1788, #55035, .T. ) ;
#25998=VERTEX_POINT ( 'NONE', #16534 ) ;
#26000=CARTESIAN_POINT ( 'NONE',  ( -6.016761891674565099, -9.418621820384382559, -16.32039929810266798 ) ) ;
#26017=CARTESIAN_POINT ( 'NONE',  ( 0.7245667037590786119, 37.65687897229928183, -29.92941129926910904 ) ) ;
#26019=CARTESIAN_POINT ( 'NONE',  ( 0.6023143664670691511, -29.07782746490727988, -38.32505149877503214 ) ) ;
#26021=ORIENTED_EDGE ( 'NONE', *, *, #36173, .T. ) ;
#26022=CARTESIAN_POINT ( 'NONE',  ( 0.3622758884714730732, 4.808133778521878732, -42.84426538328727219 ) ) ;
#26030=CARTESIAN_POINT ( 'NONE',  ( 0.1073791018717483448, -25.86618856530736466, 34.50606437925502945 ) ) ;
#26032=EDGE_CURVE ( 'NONE', #5799, #44283, #12947, .T. ) ;
#26038=DIRECTION ( 'NONE',  ( 0.09835009131224566048, 0.8579344853044275077, 0.5042575517176716149 ) ) ;
#26049=CARTESIAN_POINT ( 'NONE',  ( 0.8751705887134423323, 7.160166390004303771, -47.55935879196464100 ) ) ;
#26054=CARTESIAN_POINT ( 'NONE',  ( -6.016761891674564211, 13.32657647165355286, 13.32172022638596509 ) ) ;
#26062=CARTESIAN_POINT ( 'NONE',  ( 4.975801465491695552, 43.22084481528192157, 20.67815041659156705 ) ) ;
#26066=ADVANCED_FACE ( 'NONE', ( #6789 ), #58918, .F. ) ;
#26071=DIRECTION ( 'NONE',  ( 0.09835009131224567436, 0.6119264800004780014, -0.7847759187265480607 ) ) ;
#26073=ORIENTED_EDGE ( 'NONE', *, *, #20089, .F. ) ;
#26077=( BOUNDED_SURFACE ( )  B_SPLINE_SURFACE ( 3, 1, ( 
 ( #3896, #34282 ),
 ( #44016, #1051 ),
 ( #24249, #43699 ),
 ( #43076, #47452 ) ),
 .UNSPECIFIED., .F., .F., .F. ) 
 B_SPLINE_SURFACE_WITH_KNOTS ( ( 4, 4 ),
 ( 2, 2 ),
 ( 0.000000000000000000, 1.000000000000000000 ),
 ( 0.000000000000000000, 1.000000000000000000 ),
 .UNSPECIFIED. ) 
 GEOMETRIC_REPRESENTATION_ITEM ( )  RATIONAL_B_SPLINE_SURFACE ( (
 ( 1.000000000000000000, 1.000000000000000000),
 ( 0.9953040768229013402, 0.8617119497784988535),
 ( 0.9953040768229013402, 0.8617119497784988535),
 ( 1.000000000000000000, 1.000000000000000000) ) ) 
 REPRESENTATION_ITEM ( '' )  SURFACE ( )  );
#26086=CARTESIAN_POINT ( 'NONE',  ( 0.1310142868023658203, 15.91230901232167838, 40.08041389954887279 ) ) ;
#26088=CARTESIAN_POINT ( 'NONE',  ( 4.549368137175248350, -13.99871866169391765, 40.58005590356665948 ) ) ;
#26089=DIRECTION ( 'NONE',  ( -1.000000000000000000, -0.000000000000000000, -0.000000000000000000 ) ) ;
#26095=FACE_OUTER_BOUND ( 'NONE', #58572, .T. ) ;
#26096=CARTESIAN_POINT ( 'NONE',  ( 0.6025881611877910160, -6.495537368246224297, 47.66695236827163740 ) ) ;
#26098=CARTESIAN_POINT ( 'NONE',  ( 2.301529144917015213, 7.543875168382506047, 47.43735140118867122 ) ) ;
#26099=CARTESIAN_POINT ( 'NONE',  ( 0.3622758884714600280, -41.85013935980108357, 10.35929834645850001 ) ) ;
#26104=CARTESIAN_POINT ( 'NONE',  ( 4.691466044806102076, -33.74235639413347343, 29.14742760351052198 ) ) ;
#26105=VECTOR ( 'NONE', #6417, 1000.000000000000114 ) ;
#26109=CARTESIAN_POINT ( 'NONE',  ( 2.643462169533613793, 47.42536612906428672, -7.637863311827113755 ) ) ;
#26116=ORIENTED_EDGE ( 'NONE', *, *, #5425, .T. ) ;
#26120=FACE_OUTER_BOUND ( 'NONE', #21048, .T. ) ;
#26126=CARTESIAN_POINT ( 'NONE',  ( 3.680882792899937250, -39.15943299201968841, -27.71664061799134515 ) ) ;
#26127=CARTESIAN_POINT ( 'NONE',  ( 0.8760168074887076939, -7.161346975773376755, -47.56749362999710939 ) ) ;
#26133=CARTESIAN_POINT ( 'NONE',  ( 0.5988103564986354543, -24.57719524907214037, -41.35593036885926921 ) ) ;
#26134=ORIENTED_EDGE ( 'NONE', *, *, #5508, .F. ) ;
#26137=CARTESIAN_POINT ( 'NONE',  ( 4.322998006666179727, -22.13465289016656712, 42.57894920390090476 ) ) ;
#26151=PLANE ( 'NONE',  #28517 ) ;
#26153=CARTESIAN_POINT ( 'NONE',  ( 0.7954190325252783467, 48.09103420665682194, -0.8690070772084271811 ) ) ;
#26154=CARTESIAN_POINT ( 'NONE',  ( -6.016761891674565099, -4.880293656735092078, 18.20023637398597671 ) ) ;
#26155=( BOUNDED_SURFACE ( )  B_SPLINE_SURFACE ( 3, 1, ( 
 ( #36629, #46645 ),
 ( #51009, #51312 ),
 ( #23137, #8102 ),
 ( #42266, #12214 ) ),
 .UNSPECIFIED., .F., .F., .F. ) 
 B_SPLINE_SURFACE_WITH_KNOTS ( ( 4, 4 ),
 ( 2, 2 ),
 ( 0.000000000000000000, 1.000000000000000000 ),
 ( 0.000000000000000000, 1.000000000000000000 ),
 .UNSPECIFIED. ) 
 GEOMETRIC_REPRESENTATION_ITEM ( )  RATIONAL_B_SPLINE_SURFACE ( (
 ( 1.000000000000000000, 1.000000000000000000),
 ( 0.9953040768229005630, 0.8617119497784937465),
 ( 0.9953040768229005630, 0.8617119497784937465),
 ( 1.000000000000000000, 1.000000000000000000) ) ) 
 REPRESENTATION_ITEM ( '' )  SURFACE ( )  );
#26158=CARTESIAN_POINT ( 'NONE',  ( 0.1102847568649952675, -42.74337176234133295, 5.720244683737878866 ) ) ;
#26159=CARTESIAN_POINT ( 'NONE',  ( 0.1064266379913941241, 25.80493164505204007, -34.55203636557783398 ) ) ;
#26160=DIRECTION ( 'NONE',  ( -1.000000000000000000, -0.000000000000000000, -0.000000000000000000 ) ) ;
#26164=CARTESIAN_POINT ( 'NONE',  ( 0.1103744047535531458, -41.64495780681030368, -11.19884698423352276 ) ) ;
#26175=B_SPLINE_CURVE_WITH_KNOTS ( 'NONE', 3,
 ( #40058, #16845, #30925, #2086, #7090, #2405 ),
 .UNSPECIFIED., .F., .F.,
 ( 4, 2, 4 ),
 ( 1.474357996003774831E-17, 0.0002293319059085077044, 0.0004586638118170006636 ),
 .UNSPECIFIED. ) ;
#26179=CARTESIAN_POINT ( 'NONE',  ( 0.1073791018717578927, 37.10214135362858912, 21.98088480513677823 ) ) ;
#26185=DIRECTION ( 'NONE',  ( 0.1024043820194936311, -0.2447326578667395336, 0.9641676559171059591 ) ) ;
#26186=EDGE_CURVE ( 'NONE', #9208, #45826, #61586, .T. ) ;
#26187=ORIENTED_EDGE ( 'NONE', *, *, #56045, .F. ) ;
#26215=ORIENTED_EDGE ( 'NONE', *, *, #42768, .F. ) ;
#26219=EDGE_CURVE ( 'NONE', #7367, #2003, #24284, .T. ) ;
#26220=ORIENTED_EDGE ( 'NONE', *, *, #37568, .T. ) ;
#26221=CARTESIAN_POINT ( 'NONE',  ( -6.016761891674565099, 0.003433883960047550993, -18.84319130225482297 ) ) ;
#26227=CARTESIAN_POINT ( 'NONE',  ( 2.643462169533613793, 38.93558293168500484, 28.13401304854733453 ) ) ;
#26229=CIRCLE ( 'NONE', #28198, 47.91270532121795611 ) ;
#26230=ORIENTED_EDGE ( 'NONE', *, *, #19576, .F. ) ;
#26235=CARTESIAN_POINT ( 'NONE',  ( 0.3622758884714600280, 41.85013935980101962, -10.35929834645879133 ) ) ;
#26237=CARTESIAN_POINT ( 'NONE',  ( 3.238931869106854489, 36.28407486357521350, -23.06038324659529337 ) ) ;
#26241=CARTESIAN_POINT ( 'NONE',  ( 4.975801465491695552, -46.87746200127462970, 9.906103548667402947 ) ) ;
#26246=CARTESIAN_POINT ( 'NONE',  ( 3.238741278300274029, 40.38334873621882082, -14.74792908357263066 ) ) ;
#26254=CARTESIAN_POINT ( 'NONE',  ( 0.5998501479064708430, -37.84527566984837677, -29.69975237324600315 ) ) ;
#26258=B_SPLINE_CURVE_WITH_KNOTS ( 'NONE', 3,
 ( #1975, #36455, #16103, #16716, #2596, #7923 ),
 .UNSPECIFIED., .F., .F.,
 ( 4, 2, 4 ),
 ( 8.560751122900633232E-17, 0.0002293366620881451474, 0.0004586733241762046970 ),
 .UNSPECIFIED. ) ;
#26269=CARTESIAN_POINT ( 'NONE',  ( 0.1100053167205931048, 43.12409768020066281, -0.1794603581039966034 ) ) ;
#26275=CARTESIAN_POINT ( 'NONE',  ( 0.3622758884714600280, -10.35929834645893699, -41.85013935980099120 ) ) ;
#26283=CARTESIAN_POINT ( 'NONE',  ( 4.975801465491694664, -26.14269827151650816, -40.15204426031524321 ) ) ;
#26285=CARTESIAN_POINT ( 'NONE',  ( 0.5998501479064708430, -46.60114184914326074, 11.94461217097388328 ) ) ;
#26291=B_SPLINE_CURVE_WITH_KNOTS ( 'NONE', 3,
 ( #54589, #13260, #61147, #8530, #42092, #31743, #2909, #26725, #50834, #55216, #12963, #12339, #3827, #50527, #32363, #55839 ),
 .UNSPECIFIED., .F., .F.,
 ( 4, 3, 3, 3, 3, 4 ),
 ( 1.868480190406682863E-17, 0.0002618515315864417057, 0.0003927756766341974491, 0.0005236998216950559384, 0.0007855159896329909830, 0.001047349442285930039 ),
 .UNSPECIFIED. ) ;
#26298=ORIENTED_EDGE ( 'NONE', *, *, #23361, .T. ) ;
#26300=VERTEX_POINT ( 'NONE', #42829 ) ;
#26305=CARTESIAN_POINT ( 'NONE',  ( 0.1103310638050662013, -16.57910240621667342, 39.81020119244053035 ) ) ;
#26306=CARTESIAN_POINT ( 'NONE',  ( 0.7048096507298579061, 41.23648859290891266, 24.78213711671612884 ) ) ;
#26311=VERTEX_POINT ( 'NONE', #9588 ) ;
#26313=CARTESIAN_POINT ( 'NONE',  ( -6.017396004339687465, 18.84316306185412415, 0.001173774849048346645 ) ) ;
#26314=CARTESIAN_POINT ( 'NONE',  ( -6.010958268070873523, 2.445171577616032987, -18.68413620842261835 ) ) ;
#26317=CARTESIAN_POINT ( 'NONE',  ( 4.549368137175248350, -28.46244473166695954, 32.13400537129875545 ) ) ;
#26320=EDGE_CURVE ( 'NONE', #35399, #49767, #60886, .T. ) ;
#26334=CARTESIAN_POINT ( 'NONE',  ( 4.549368137175248350, -2.596185425821630588, -42.84816078363929392 ) ) ;
#26338=EDGE_CURVE ( 'NONE', #6976, #7392, #51827, .T. ) ;
#26350=CARTESIAN_POINT ( 'NONE',  ( 0.5998501479064699549, -44.64337787626236320, -17.92509395669093308 ) ) ;
#26363=CARTESIAN_POINT ( 'NONE',  ( 0.7954196712028465122, 42.08256091708702940, -23.29293472883145455 ) ) ;
#26365=EDGE_CURVE ( 'NONE', #44145, #32619, #13103, .T. ) ;
#26367=( BOUNDED_SURFACE ( )  B_SPLINE_SURFACE ( 3, 1, ( 
 ( #15208, #8953 ),
 ( #33705, #52470 ),
 ( #56858, #28363 ),
 ( #33393, #4844 ) ),
 .UNSPECIFIED., .F., .F., .F. ) 
 B_SPLINE_SURFACE_WITH_KNOTS ( ( 4, 4 ),
 ( 2, 2 ),
 ( 0.000000000000000000, 1.000000000000000000 ),
 ( 0.000000000000000000, 1.000000000000000000 ),
 .UNSPECIFIED. ) 
 GEOMETRIC_REPRESENTATION_ITEM ( )  RATIONAL_B_SPLINE_SURFACE ( (
 ( 1.000000000000000000, 1.000000000000000000),
 ( 0.9953040768229005630, 0.8617119497784937465),
 ( 0.9953040768229005630, 0.8617119497784937465),
 ( 1.000000000000000000, 1.000000000000000000) ) ) 
 REPRESENTATION_ITEM ( '' )  SURFACE ( )  );
#26375=CARTESIAN_POINT ( 'NONE',  ( 4.975801465491695552, 47.76942479135485797, -3.702618843596948039 ) ) ;
#26382=CARTESIAN_POINT ( 'NONE',  ( 0.3622758884714730732, -6.444611261694294768, -42.62881903538208661 ) ) ;
#26384=CARTESIAN_POINT ( 'NONE',  ( 0.5998501479064708430, -47.76154736470761719, 5.759754759339972274 ) ) ;
#26386=CARTESIAN_POINT ( 'NONE',  ( 0.1073791018717578927, 25.86618856530665767, 34.50606437925554815 ) ) ;
#26391=VERTEX_POINT ( 'NONE', #48735 ) ;
#26392=ORIENTED_EDGE ( 'NONE', *, *, #42331, .T. ) ;
#26400=CARTESIAN_POINT ( 'NONE',  ( 4.691466044806102964, -42.11359095667479835, -14.64802401911215135 ) ) ;
#26403=CARTESIAN_POINT ( 'NONE',  ( 0.3622758884714730732, -11.95365414648468594, -41.42293301073622303 ) ) ;
#26409=EDGE_CURVE ( 'NONE', #13823, #5867, #288, .T. ) ;
#26411=CARTESIAN_POINT ( 'NONE',  ( 0.6041374136657476912, -47.71861871402585109, -6.106202762793307315 ) ) ;
#26414=ORIENTED_EDGE ( 'NONE', *, *, #47760, .F. ) ;
#26428=CARTESIAN_POINT ( 'NONE',  ( 0.5980894510889457338, -6.974827154143770080, -47.60453381548690288 ) ) ;
#26429=B_SPLINE_CURVE_WITH_KNOTS ( 'NONE', 3,
 ( #5541, #47881, #28761, #48477 ),
 .UNSPECIFIED., .F., .F.,
 ( 4, 4 ),
 ( 6.254634441385501517E-18, 0.004566006591234648103 ),
 .UNSPECIFIED. ) ;
#26433=CARTESIAN_POINT ( 'NONE',  ( 4.975801465491694664, -47.76942479135482955, -3.702618843597289544 ) ) ;
#26441=CARTESIAN_POINT ( 'NONE',  ( 4.549368137175248350, 42.82045902618772715, -3.018832571116098151 ) ) ;
#26443=EDGE_LOOP ( 'NONE', ( #11491, #31636, #37048, #18690 ) ) ;
#26451=CARTESIAN_POINT ( 'NONE',  ( 0.6031356219577718170, 18.49057407199394021, 44.41207482560214004 ) ) ;
#26472=CARTESIAN_POINT ( 'NONE',  ( 0.1073791018717483448, -41.77800844988507123, -10.69234304550039383 ) ) ;
#26473=CARTESIAN_POINT ( 'NONE',  ( 0.6041374136657475802, -6.106202762793164318, -47.71861871402587241 ) ) ;
#26478=CARTESIAN_POINT ( 'NONE',  ( 4.975801465491694664, 2.564218696446817880, 47.84403947906844223 ) ) ;
#26481=B_SPLINE_CURVE_WITH_KNOTS ( 'NONE', 3,
 ( #2329, #39664, #44983, #7021 ),
 .UNSPECIFIED., .F., .F.,
 ( 4, 4 ),
 ( 0.000000000000000000, 0.005014147105413705591 ),
 .UNSPECIFIED. ) ;
#26484=CARTESIAN_POINT ( 'NONE',  ( 0.6031356755773454870, -44.44547243635334866, 18.40994522247679654 ) ) ;
#26486=B_SPLINE_CURVE_WITH_KNOTS ( 'NONE', 3,
 ( #33385, #38706, #9242, #34299 ),
 .UNSPECIFIED., .F., .F.,
 ( 4, 4 ),
 ( 5.818439421673296370E-18, 0.004566006591234648970 ),
 .UNSPECIFIED. ) ;
#26487=EDGE_CURVE ( 'NONE', #34393, #22293, #14538, .T. ) ;
#26494=CARTESIAN_POINT ( 'NONE',  ( -2.569797478183783568, 14.55946937464481827, 1.464172661884213689 ) ) ;
#26518=CARTESIAN_POINT ( 'NONE',  ( 4.549368137175248350, -18.79584381673559079, 38.59302160394720005 ) ) ;
#26523=ADVANCED_FACE ( 'NONE', ( #31478 ), #5733, .F. ) ;
#26528=CARTESIAN_POINT ( 'NONE',  ( 0.5998501479064699549, 41.39809967730487017, -24.50586714782561160 ) ) ;
#26529=B_SPLINE_CURVE_WITH_KNOTS ( 'NONE', 3,
 ( #23012, #36495, #46828, #37123, #42140, #18312, #32099, #60572, #37423, #46508, #7968, #45904, #28007, #31788, #27699, #12380, #47129, #2950, #8573 ),
 .UNSPECIFIED., .F., .F.,
 ( 4, 3, 3, 3, 3, 3, 4 ),
 ( 1.180170631773780508E-16, 0.0002618519381806264589, 0.0003927759815485976015, 0.0005237000248299444058, 0.0006546240681324972830, 0.0007855481115631333597, 0.0009699050456655111587 ),
 .UNSPECIFIED. ) ;
#26536=CARTESIAN_POINT ( 'NONE',  ( 0.6041374136657476912, 0.1745662470638107422, 48.10739871142803992 ) ) ;
#26537=CARTESIAN_POINT ( 'NONE',  ( 0.8751705887134423323, -17.57879340691512837, -44.76769609654229498 ) ) ;
#26541=CARTESIAN_POINT ( 'NONE',  ( 0.3622758884714600280, -22.26738722580193652, 36.91764744403282350 ) ) ;
#26546=ORIENTED_EDGE ( 'NONE', *, *, #35502, .T. ) ;
#26549=CARTESIAN_POINT ( 'NONE',  ( 4.975801465491694664, -40.15204426031552032, 26.14269827151608894 ) ) ;
#26551=CARTESIAN_POINT ( 'NONE',  ( 1.827326673878743701, -36.65065268305642832, -22.58371678864569176 ) ) ;
#26554=VECTOR ( 'NONE', #25515, 1000.000000000000000 ) ;
#26560=DIRECTION ( 'NONE',  ( 0.1024043820194936449, -0.1167898032637411931, 0.9878630899050852010 ) ) ;
#26561=CARTESIAN_POINT ( 'NONE',  ( 1.827326673878743701, 40.22837085190311512, -15.32882202537235550 ) ) ;
#26563=CARTESIAN_POINT ( 'NONE',  ( 0.6041374136657476912, 38.27243465845302239, 29.14743607025096850 ) ) ;
#26577=ORIENTED_EDGE ( 'NONE', *, *, #22055, .T. ) ;
#26579=CARTESIAN_POINT ( 'NONE',  ( 0.1087620492084206553, 11.51076657762335032, -41.55994353650429929 ) ) ;
#26590=CARTESIAN_POINT ( 'NONE',  ( 4.975801465491695552, 9.906103548667566372, 46.87746200127460128 ) ) ;
#26607=CARTESIAN_POINT ( 'NONE',  ( -6.017396004339686577, 13.32495836419624702, 13.32329839588559750 ) ) ;
#26613=VERTEX_POINT ( 'NONE', #13942 ) ;
#26614=DIRECTION ( 'NONE',  ( 0.000000000000000000, 0.000000000000000000, -1.000000000000000000 ) ) ;
#26621=CARTESIAN_POINT ( 'NONE',  ( -6.017396004339686577, 18.84316306185412415, -0.001173774849047644949 ) ) ;
#26625=CARTESIAN_POINT ( 'NONE',  ( -6.016761891674565099, -16.32039929810263601, 9.418621820384437626 ) ) ;
#26629=CARTESIAN_POINT ( 'NONE',  ( -5.995132425357893702, 13.33084941932925993, -13.31880955509713260 ) ) ;
#26631=CARTESIAN_POINT ( 'NONE',  ( 0.5988103622719985752, 44.21009254328978244, 18.96890139670008679 ) ) ;
#26638=LINE ( 'NONE', #25401, #56609 ) ;
#26648=B_SPLINE_CURVE_WITH_KNOTS ( 'NONE', 3,
 ( #30460, #1955, #26086, #30776, #21698, #22320 ),
 .UNSPECIFIED., .F., .F.,
 ( 4, 2, 4 ),
 ( 1.553373257785006303E-17, 0.0002293319059085112009, 0.0004586638118170068977 ),
 .UNSPECIFIED. ) ;
#26649=FACE_OUTER_BOUND ( 'NONE', #32145, .T. ) ;
#26653=CARTESIAN_POINT ( 'NONE',  ( 0.7954196712028465122, 33.39101545667288207, 34.61997730204591761 ) ) ;
#26663=EDGE_LOOP ( 'NONE', ( #4342, #59015, #42985, #36533 ) ) ;
#26668=VERTEX_POINT ( 'NONE', #10142 ) ;
#26680=AXIS2_PLACEMENT_3D ( 'NONE', #53342, #28934, #24860 ) ;
#26681=ORIENTED_EDGE ( 'NONE', *, *, #32904, .F. ) ;
#26689=EDGE_CURVE ( 'NONE', #32871, #29523, #36960, .T. ) ;
#26694=CARTESIAN_POINT ( 'NONE',  ( 1.827326673878744367, 17.60663982372537717, -39.28486782721049053 ) ) ;
#26703=CARTESIAN_POINT ( 'NONE',  ( 0.1102847568649952675, 34.26895182984662824, 26.17930421801163021 ) ) ;
#26705=CARTESIAN_POINT ( 'NONE',  ( 3.238931869106855377, 38.98364358950744446, -18.12707634097783682 ) ) ;
#26710=CARTESIAN_POINT ( 'NONE',  ( -6.015611763856276717, 2.465697960551047618, 18.68122482568280773 ) ) ;
#26713=ADVANCED_FACE ( 'NONE', ( #58651 ), #27356, .F. ) ;
#26715=B_SPLINE_CURVE_WITH_KNOTS ( 'NONE', 3,
 ( #17696, #18625, #14245, #8272 ),
 .UNSPECIFIED., .F., .F.,
 ( 4, 4 ),
 ( 0.000000000000000000, 0.005014147105413694315 ),
 .UNSPECIFIED. ) ;
#26718=CARTESIAN_POINT ( 'NONE',  ( 4.549368137175248350, 3.018832571116558672, -42.82045902618769873 ) ) ;
#26719=CARTESIAN_POINT ( 'NONE',  ( 0.6030672727741701600, -6.192762795894120487, -47.70721108823347123 ) ) ;
#26722=AXIS2_PLACEMENT_3D ( 'NONE', #25468, #44611, #1648 ) ;
#26725=CARTESIAN_POINT ( 'NONE',  ( 0.6030672727741701600, 46.49075153683472905, -12.36682345648132753 ) ) ;
#26726=EDGE_CURVE ( 'NONE', #47783, #13269, #21964, .T. ) ;
#26727=CARTESIAN_POINT ( 'NONE',  ( 0.6041374136657475802, 47.71861871402589372, -6.106202762792999117 ) ) ;
#26735=CARTESIAN_POINT ( 'NONE',  ( 0.5998501479064708430, 34.38546660123297727, -33.64490850298808056 ) ) ;
#26737=ORIENTED_EDGE ( 'NONE', *, *, #52782, .F. ) ;
#26751=DIRECTION ( 'NONE',  ( 0.000000000000000000, 0.000000000000000000, 1.000000000000000000 ) ) ;
#26752=B_SPLINE_CURVE_WITH_KNOTS ( 'NONE', 3,
 ( #34919, #11106, #30189, #29268, #24580, #49296 ),
 .UNSPECIFIED., .F., .F.,
 ( 4, 2, 4 ),
 ( 8.699011523299071029E-17, 0.0002293366620881452287, 0.0004586733241762035044 ),
 .UNSPECIFIED. ) ;
#26753=CARTESIAN_POINT ( 'NONE',  ( 0.6030672727741701600, -48.10738703097480595, -0.08725775308904697158 ) ) ;
#26755=VERTEX_POINT ( 'NONE', #26088 ) ;
#26760=CARTESIAN_POINT ( 'NONE',  ( 0.5998501479064708430, 34.38546660123297727, -33.64490850298808056 ) ) ;
#26761=CARTESIAN_POINT ( 'NONE',  ( 0.8760168074887076939, -29.98565522133320371, -37.61398439004523198 ) ) ;
#26767=CARTESIAN_POINT ( 'NONE',  ( 0.3622758884714600280, -10.35929834645893699, -41.85013935980099120 ) ) ;
#26769=EDGE_CURVE ( 'NONE', #57844, #2002, #48914, .T. ) ;
#26772=CARTESIAN_POINT ( 'NONE',  ( 0.1103744047535531458, 42.76053735246612320, -5.590449877750151231 ) ) ;
#26780=DIRECTION ( 'NONE',  ( 0.09835009131224552170, 0.8579344853044343910, -0.5042575517176598465 ) ) ;
#26783=CARTESIAN_POINT ( 'NONE',  ( 0.6017666602106490625, -41.48673504406963275, 24.35550044372372369 ) ) ;
#26786=CARTESIAN_POINT ( 'NONE',  ( -4.908599999999998964, 0.000000000000000000, 0.000000000000000000 ) ) ;
#26795=CARTESIAN_POINT ( 'NONE',  ( -6.010958268070873523, 0.01451635840189641029, -18.84344976839986785 ) ) ;
#26799=CARTESIAN_POINT ( 'NONE',  ( 0.1310142868023685403, 37.02349354742214160, 22.11113027429300004 ) ) ;
#26807=EDGE_LOOP ( 'NONE', ( #61489, #5158, #40039, #14685 ) ) ;
#26809=FACE_OUTER_BOUND ( 'NONE', #12766, .T. ) ;
#26811=ADVANCED_FACE ( 'NONE', ( #41762 ), #1717, .F. ) ;
#26813=ORIENTED_EDGE ( 'NONE', *, *, #13563, .F. ) ;
#26816=CARTESIAN_POINT ( 'NONE',  ( 0.5998501479064708430, 44.24259072156059602, 18.89267974119682947 ) ) ;
#26817=( BOUNDED_SURFACE ( )  B_SPLINE_SURFACE ( 3, 1, ( 
 ( #30269, #16188 ),
 ( #25887, #20884 ),
 ( #44711, #20576 ),
 ( #11179, #19979 ) ),
 .UNSPECIFIED., .F., .F., .F. ) 
 B_SPLINE_SURFACE_WITH_KNOTS ( ( 4, 4 ),
 ( 2, 2 ),
 ( 0.000000000000000000, 1.000000000000000000 ),
 ( 0.000000000000000000, 1.000000000000000000 ),
 .UNSPECIFIED. ) 
 GEOMETRIC_REPRESENTATION_ITEM ( )  RATIONAL_B_SPLINE_SURFACE ( (
 ( 1.000000000000000000, 1.000000000000000000),
 ( 0.9953040768229013402, 0.8617119497784988535),
 ( 0.9953040768229013402, 0.8617119497784988535),
 ( 1.000000000000000000, 1.000000000000000000) ) ) 
 REPRESENTATION_ITEM ( '' )  SURFACE ( )  );
#26823=CONICAL_SURFACE ( 'NONE', #29807, 42.92674063221959813, 1.485477209440487556 ) ;
#26825=CARTESIAN_POINT ( 'NONE',  ( 4.549368137175248350, 3.018832571115968033, 42.82045902618773425 ) ) ;
#26829=CARTESIAN_POINT ( 'NONE',  ( 0.1064266418746772913, 11.70292610004324985, -41.50637583369811523 ) ) ;
#26831=CARTESIAN_POINT ( 'NONE',  ( -6.015611763856276717, 18.68122482568280063, 2.465697960551114232 ) ) ;
#26835=CARTESIAN_POINT ( 'NONE',  ( 0.6029303876144825880, -47.67862422489729113, -6.409038528275959656 ) ) ;
#26842=CARTESIAN_POINT ( 'NONE',  ( 0.6009452777970412107, 44.27681866781104247, -18.81240106508482057 ) ) ;
#26847=CARTESIAN_POINT ( 'NONE',  ( -6.017396004339686577, 7.212050743684176979, 17.40836349643169711 ) ) ;
#26849=EDGE_LOOP ( 'NONE', ( #10308, #13121, #38585, #61150 ) ) ;
#26851=CARTESIAN_POINT ( 'NONE',  ( 0.5988103622719991304, -17.84821742497965857, -44.67429504351052572 ) ) ;
#26852=CARTESIAN_POINT ( 'NONE',  ( 0.1100247026804066219, -26.38690693952982613, 34.10937070541699256 ) ) ;
#26856=CARTESIAN_POINT ( 'NONE',  ( 2.301529144917016101, 47.43735140118864280, -7.543875168382650820 ) ) ;
#26857=ORIENTED_EDGE ( 'NONE', *, *, #52758, .T. ) ;
#26858=B_SPLINE_CURVE_WITH_KNOTS ( 'NONE', 3,
 ( #30871, #54347, #7670, #16472, #50901, #35603 ),
 .UNSPECIFIED., .F., .F.,
 ( 4, 2, 4 ),
 ( 0.000000000000000000, 0.0002450742804987349893, 0.0004901485609974699786 ),
 .UNSPECIFIED. ) ;
#26859=VERTEX_POINT ( 'NONE', #55819 ) ;
#26863=CARTESIAN_POINT ( 'NONE',  ( 0.1103310638050661874, 26.31782144882240715, -34.16271402810842517 ) ) ;
#26888=CARTESIAN_POINT ( 'NONE',  ( -5.995132425357893702, -14.94489030678159480, 11.47834865841090490 ) ) ;
#26897=( BOUNDED_SURFACE ( )  B_SPLINE_SURFACE ( 3, 1, ( 
 ( #24250, #53968 ),
 ( #15482, #28955 ),
 ( #34283, #427 ),
 ( #9853, #43700 ) ),
 .UNSPECIFIED., .F., .F., .F. ) 
 B_SPLINE_SURFACE_WITH_KNOTS ( ( 4, 4 ),
 ( 2, 2 ),
 ( 0.000000000000000000, 1.000000000000000000 ),
 ( 0.000000000000000000, 1.000000000000000000 ),
 .UNSPECIFIED. ) 
 GEOMETRIC_REPRESENTATION_ITEM ( )  RATIONAL_B_SPLINE_SURFACE ( (
 ( 1.000000000000000000, 1.000000000000000000),
 ( 0.7223157951917476005, 0.9931996967497186413),
 ( 0.7223157951917476005, 0.9931996967497186413),
 ( 1.000000000000000000, 1.000000000000000000) ) ) 
 REPRESENTATION_ITEM ( '' )  SURFACE ( )  );
#26898=ADVANCED_FACE ( 'NONE', ( #61427 ), #46585, .F. ) ;
#26899=CARTESIAN_POINT ( 'NONE',  ( -5.995132425357893702, 18.68405145320024019, 2.451215106828409596 ) ) ;
#26905=B_SPLINE_CURVE_WITH_KNOTS ( 'NONE', 3,
 ( #3980, #14347, #32525, #42861, #43169, #48162 ),
 .UNSPECIFIED., .F., .F.,
 ( 4, 2, 4 ),
 ( 1.267283937151336631E-16, 0.0002450741128632354321, 0.0004901482257263441210 ),
 .UNSPECIFIED. ) ;
#26907=EDGE_LOOP ( 'NONE', ( #23146, #24516, #845, #6294 ) ) ;
#26908=CARTESIAN_POINT ( 'NONE',  ( 1.827119703190778877, 6.838980420687405193, 42.50321986945171204 ) ) ;
#26911=( BOUNDED_SURFACE ( )  B_SPLINE_SURFACE ( 3, 1, ( 
 ( #8924, #28035 ),
 ( #3581, #33366 ),
 ( #61217, #4195 ),
 ( #13956, #18340 ) ),
 .UNSPECIFIED., .F., .F., .F. ) 
 B_SPLINE_SURFACE_WITH_KNOTS ( ( 4, 4 ),
 ( 2, 2 ),
 ( 0.000000000000000000, 1.000000000000000000 ),
 ( 0.000000000000000000, 1.000000000000000000 ),
 .UNSPECIFIED. ) 
 GEOMETRIC_REPRESENTATION_ITEM ( )  RATIONAL_B_SPLINE_SURFACE ( (
 ( 1.000000000000000000, 1.000000000000000000),
 ( 0.9953040768229013402, 0.8617119497784988535),
 ( 0.9953040768229013402, 0.8617119497784988535),
 ( 1.000000000000000000, 1.000000000000000000) ) ) 
 REPRESENTATION_ITEM ( '' )  SURFACE ( )  );
#26916=FACE_OUTER_BOUND ( 'NONE', #31672, .T. ) ;
#26917=ORIENTED_EDGE ( 'NONE', *, *, #29485, .T. ) ;
#26920=( BOUNDED_SURFACE ( )  B_SPLINE_SURFACE ( 3, 1, ( 
 ( #49551, #35796 ),
 ( #59567, #44580 ),
 ( #10741, #40501 ),
 ( #25756, #39261 ) ),
 .UNSPECIFIED., .F., .F., .F. ) 
 B_SPLINE_SURFACE_WITH_KNOTS ( ( 4, 4 ),
 ( 2, 2 ),
 ( 0.000000000000000000, 1.000000000000000000 ),
 ( 0.000000000000000000, 1.000000000000000000 ),
 .UNSPECIFIED. ) 
 GEOMETRIC_REPRESENTATION_ITEM ( )  RATIONAL_B_SPLINE_SURFACE ( (
 ( 1.000000000000000000, 1.000000000000000000),
 ( 0.9953040768229005630, 0.8617119497784937465),
 ( 0.9953040768229005630, 0.8617119497784937465),
 ( 1.000000000000000000, 1.000000000000000000) ) ) 
 REPRESENTATION_ITEM ( '' )  SURFACE ( )  );
#26923=VERTEX_POINT ( 'NONE', #9440 ) ;
#26928=ORIENTED_EDGE ( 'NONE', *, *, #687, .F. ) ;
#26929=CARTESIAN_POINT ( 'NONE',  ( 0.6041374136657476912, 24.20487816031464234, 41.57494627055152847 ) ) ;
#26938=EDGE_LOOP ( 'NONE', ( #57168, #45227, #53920, #10380 ) ) ;
#26939=CARTESIAN_POINT ( 'NONE',  ( 0.1098349054025746091, 37.23978094195821598, 21.74670956129773458 ) ) ;
#26940=CARTESIAN_POINT ( 'NONE',  ( 0.6001305935487422083, -48.10757715638248300, 0.5236757026887773891 ) ) ;
#26943=ORIENTED_EDGE ( 'NONE', *, *, #17816, .T. ) ;
#26944=LINE ( 'NONE', #55122, #34576 ) ;
#26946=ORIENTED_EDGE ( 'NONE', *, *, #17583, .T. ) ;
#26954=ORIENTED_EDGE ( 'NONE', *, *, #30224, .F. ) ;
#26962=ADVANCED_FACE ( 'NONE', ( #5035 ), #59353, .F. ) ;
#26969=DIRECTION ( 'NONE',  ( 1.000000000000000000, 0.000000000000000000, 0.000000000000000000 ) ) ;
#26976=EDGE_CURVE ( 'NONE', #28210, #30576, #19178, .T. ) ;
#26977=CARTESIAN_POINT ( 'NONE',  ( 3.680974057930773036, 8.091325130366421092, -47.28851186370999216 ) ) ;
#26982=CARTESIAN_POINT ( 'NONE',  ( 4.549368137175248350, 32.13400537129885493, 28.46244473166684941 ) ) ;
#26987=EDGE_LOOP ( 'NONE', ( #20499, #45037, #24070, #2162 ) ) ;
#26988=ORIENTED_EDGE ( 'NONE', *, *, #40211, .F. ) ;
#26992=ORIENTED_EDGE ( 'NONE', *, *, #6578, .T. ) ;
#26995=CARTESIAN_POINT ( 'NONE',  ( 4.691466044806102076, 44.51344083442439370, -2.583163953528010204 ) ) ;
#26999=CARTESIAN_POINT ( 'NONE',  ( 4.549368137175248350, 42.82045902618772715, -3.018832571116098151 ) ) ;
#27000=LINE ( 'NONE', #41740, #27629 ) ;
#27018=CARTESIAN_POINT ( 'NONE',  ( 5.880360259849739535, 26.69116321728517249, 39.86101557989678668 ) ) ;
#27026=EDGE_CURVE ( 'NONE', #22462, #58253, #11532, .T. ) ;
#27028=DIRECTION ( 'NONE',  ( 0.000000000000000000, 0.000000000000000000, 1.000000000000000000 ) ) ;
#27035=CARTESIAN_POINT ( 'NONE',  ( 0.6031356219577718170, -6.365832241666245395, -47.68448279784252719 ) ) ;
#27037=CARTESIAN_POINT ( 'NONE',  ( 0.7048096507298579061, -41.23648859290909030, -24.78213711671583752 ) ) ;
#27038=CARTESIAN_POINT ( 'NONE',  ( 0.5998501479064699549, -46.60114184914309021, -11.94461217097453343 ) ) ;
#27042=VERTEX_POINT ( 'NONE', #30952 ) ;
#27043=B_SPLINE_CURVE_WITH_KNOTS ( 'NONE', 3,
 ( #37152, #37780, #47459, #42169 ),
 .UNSPECIFIED., .F., .F.,
 ( 4, 4 ),
 ( 0.000000000000000000, 0.004445488388166995118 ),
 .UNSPECIFIED. ) ;
#27046=CARTESIAN_POINT ( 'NONE',  ( 0.8751705887134423323, 34.63284514348585930, -33.37254303619518225 ) ) ;
#27048=EDGE_CURVE ( 'NONE', #6465, #42044, #28592, .T. ) ;
#27049=VERTEX_POINT ( 'NONE', #7426 ) ;
#27052=B_SPLINE_CURVE_WITH_KNOTS ( 'NONE', 3,
 ( #6837, #45110, #30984, #45410 ),
 .UNSPECIFIED., .F., .F.,
 ( 4, 4 ),
 ( 0.000000000000000000, 0.004445488388166993383 ),
 .UNSPECIFIED. ) ;
#27054=ORIENTED_EDGE ( 'NONE', *, *, #32973, .T. ) ;
#27056=CARTESIAN_POINT ( 'NONE',  ( 4.549368137175248350, 42.06008734272383975, 8.582197505784577629 ) ) ;
#27060=CARTESIAN_POINT ( 'NONE',  ( 0.7048096507298579061, 7.115188260603842352, -47.58126109679093929 ) ) ;
#27062=CARTESIAN_POINT ( 'NONE',  ( 50.00005079999999680, 0.000000000000000000, 0.000000000000000000 ) ) ;
#27063=ORIENTED_EDGE ( 'NONE', *, *, #18116, .T. ) ;
#27075=ORIENTED_EDGE ( 'NONE', *, *, #31277, .F. ) ;
#27077=CARTESIAN_POINT ( 'NONE',  ( 4.691466044806103852, 25.04870410140739523, 36.88741755356078045 ) ) ;
#27078=EDGE_CURVE ( 'NONE', #42733, #12539, #968, .T. ) ;
#27098=CARTESIAN_POINT ( 'NONE',  ( 0.7246131072078585422, -46.24389631750680962, -13.24054562911110722 ) ) ;
#27125=CARTESIAN_POINT ( 'NONE',  ( 0.1073791018717578927, 6.109314776652701617, -42.68962945260948061 ) ) ;
#27126=ORIENTED_EDGE ( 'NONE', *, *, #37879, .F. ) ;
#27132=CARTESIAN_POINT ( 'NONE',  ( 0.6031356755773454870, 41.66228085015293203, 24.05369945659548492 ) ) ;
#27140=CARTESIAN_POINT ( 'NONE',  ( 4.549368137175248350, 42.06008734272396765, -8.582197505783977221 ) ) ;
#27144=CARTESIAN_POINT ( 'NONE',  ( 4.975801465491695552, 0.000000000000000000, 0.000000000000000000 ) ) ;
#27151=EDGE_CURVE ( 'NONE', #23973, #50134, #39059, .T. ) ;
#27152=ORIENTED_EDGE ( 'NONE', *, *, #22492, .T. ) ;
#27157=ORIENTED_EDGE ( 'NONE', *, *, #13002, .F. ) ;
#27158=FACE_OUTER_BOUND ( 'NONE', #14344, .T. ) ;
#27164=ADVANCED_FACE ( 'NONE', ( #51576 ), #24986, .F. ) ;
#27167=( BOUNDED_SURFACE ( )  B_SPLINE_SURFACE ( 3, 1, ( 
 ( #45735, #55403 ),
 ( #7163, #12527 ),
 ( #55710, #51020 ),
 ( #51322, #8408 ) ),
 .UNSPECIFIED., .F., .F., .F. ) 
 B_SPLINE_SURFACE_WITH_KNOTS ( ( 4, 4 ),
 ( 2, 2 ),
 ( 0.000000000000000000, 1.000000000000000000 ),
 ( 0.000000000000000000, 1.000000000000000000 ),
 .UNSPECIFIED. ) 
 GEOMETRIC_REPRESENTATION_ITEM ( )  RATIONAL_B_SPLINE_SURFACE ( (
 ( 1.000000000000000000, 1.000000000000000000),
 ( 0.7223157951917480446, 0.9931996967497186413),
 ( 0.7223157951917480446, 0.9931996967497186413),
 ( 1.000000000000000000, 1.000000000000000000) ) ) 
 REPRESENTATION_ITEM ( '' )  SURFACE ( )  );
#27170=CARTESIAN_POINT ( 'NONE',  ( 0.5988103622719987973, -24.57719485303665863, 41.35593060299629542 ) ) ;
#27172=CARTESIAN_POINT ( 'NONE',  ( 0.6025881611877910160, 47.72390913208165131, -6.062907795288870361 ) ) ;
#27173=CARTESIAN_POINT ( 'NONE',  ( 0.6254311100348659558, -37.74260849418475061, -29.82834996731681443 ) ) ;
#27174=ORIENTED_EDGE ( 'NONE', *, *, #4216, .T. ) ;
#27175=CARTESIAN_POINT ( 'NONE',  ( 0.1103744047535531458, 37.36621271144537815, -21.52865142340098359 ) ) ;
#27176=CARTESIAN_POINT ( 'NONE',  ( -6.010958268070873523, 18.68413620842267520, -2.445171577615575575 ) ) ;
#27177=VERTEX_POINT ( 'NONE', #23101 ) ;
#27182=CARTESIAN_POINT ( 'NONE',  ( -6.016489644550736315, 18.68142234211827457, -2.463898142942573699 ) ) ;
#27185=CARTESIAN_POINT ( 'NONE',  ( 4.975801465491695552, -32.01766832630288206, -35.64402118370946937 ) ) ;
#27193=CARTESIAN_POINT ( 'NONE',  ( 0.7954190325252782356, -46.67728753507132922, -11.60747917225568493 ) ) ;
#27204=CARTESIAN_POINT ( 'NONE',  ( 0.8760168074886960365, -47.56749362999708808, -7.161346975773533963 ) ) ;
#27216=ORIENTED_EDGE ( 'NONE', *, *, #25556, .F. ) ;
#27223=CONICAL_SURFACE ( 'NONE', #36234, 42.92674063221959813, 1.485477209440487556 ) ;
#27227=ORIENTED_EDGE ( 'NONE', *, *, #14097, .T. ) ;
#27232=CARTESIAN_POINT ( 'NONE',  ( 0.6254087463353951160, 34.49952850220925882, 33.52637152047093849 ) ) ;
#27236=CARTESIAN_POINT ( 'NONE',  ( 0.1073791018717483448, -16.05399293000841254, 40.02496097243031414 ) ) ;
#27243=ORIENTED_EDGE ( 'NONE', *, *, #55849, .F. ) ;
#27247=CARTESIAN_POINT ( 'NONE',  ( 0.8760168074886960365, -7.161346975774052659, 47.56749362999700992 ) ) ;
#27249=CARTESIAN_POINT ( 'NONE',  ( 0.2230388203127610658, -42.64472907182734929, 6.380812898000848499 ) ) ;
#27264=( BOUNDED_SURFACE ( )  B_SPLINE_SURFACE ( 3, 1, ( 
 ( #31911, #60091 ),
 ( #8092, #42256 ),
 ( #22509, #12503 ),
 ( #41029, #51300 ) ),
 .UNSPECIFIED., .F., .F., .F. ) 
 B_SPLINE_SURFACE_WITH_KNOTS ( ( 4, 4 ),
 ( 2, 2 ),
 ( 0.000000000000000000, 1.000000000000000000 ),
 ( 0.000000000000000000, 1.000000000000000000 ),
 .UNSPECIFIED. ) 
 GEOMETRIC_REPRESENTATION_ITEM ( )  RATIONAL_B_SPLINE_SURFACE ( (
 ( 1.000000000000000000, 1.000000000000000000),
 ( 0.7223157951917480446, 0.9931996967497186413),
 ( 0.7223157951917480446, 0.9931996967497186413),
 ( 1.000000000000000000, 1.000000000000000000) ) ) 
 REPRESENTATION_ITEM ( '' )  SURFACE ( )  );
#27266=CARTESIAN_POINT ( 'NONE',  ( 0.1103310638050661596, -16.42686748615379244, -39.87325896099736156 ) ) ;
#27277=CARTESIAN_POINT ( 'NONE',  ( 0.7954196712028491767, -38.68220069891187762, 28.58653687859100501 ) ) ;
#27279=ORIENTED_EDGE ( 'NONE', *, *, #24150, .T. ) ;
#27288=CARTESIAN_POINT ( 'NONE',  ( 4.549368137175248350, -8.166781970325423856, -42.14271863032831078 ) ) ;
#27294=PRODUCT ( 'straight bevel gear(wobble out)_iso_ISO - Straight bevel gear 2M 48GT 47PT 20PA 5FW ---48O1H50MD20.0S1', 'straight bevel gear(wobble out)_iso_ISO - Straight bevel gear 2M 48GT 47PT 20PA 5FW ---48O1H50MD20.0S1', '', ( #36526 ) ) ;
#27295=ORIENTED_EDGE ( 'NONE', *, *, #36759, .F. ) ;
#27306=CARTESIAN_POINT ( 'NONE',  ( 0.1073791018717578927, -37.10214135362874543, -21.98088480513651888 ) ) ;
#27307=ORIENTED_EDGE ( 'NONE', *, *, #46870, .T. ) ;
#27311=B_SPLINE_CURVE_WITH_KNOTS ( 'NONE', 3,
 ( #61619, #19989, #34388, #23745 ),
 .UNSPECIFIED., .F., .F.,
 ( 4, 4 ),
 ( 0.000000000000000000, 0.005014147105413704723 ),
 .UNSPECIFIED. ) ;
#27313=CARTESIAN_POINT ( 'NONE',  ( -6.017396004339686577, 11.47005965438160402, -14.95000090562869310 ) ) ;
#27314=ORIENTED_EDGE ( 'NONE', *, *, #60812, .F. ) ;
#27315=DIRECTION ( 'NONE',  ( -0.9990097760809875105, 0.000000000000000000, 0.04449120468828680897 ) ) ;
#27321=CARTESIAN_POINT ( 'NONE',  ( 0.3622758884714600280, -40.13994584881793770, 15.73321244754782811 ) ) ;
#27342=CARTESIAN_POINT ( 'NONE',  ( -6.001507490154110336, -4.892199142591176830, -18.19774963328913131 ) ) ;
#27346=ORIENTED_EDGE ( 'NONE', *, *, #61197, .F. ) ;
#27349=CARTESIAN_POINT ( 'NONE',  ( -5.995132425357893702, -13.31880955509717701, -13.33084941932921197 ) ) ;
#27355=EDGE_CURVE ( 'NONE', #49781, #35221, #7345, .T. ) ;
#27356=( BOUNDED_SURFACE ( )  B_SPLINE_SURFACE ( 3, 1, ( 
 ( #30778, #49898 ),
 ( #1957, #6325 ),
 ( #59277, #43685 ),
 ( #58038, #15776 ) ),
 .UNSPECIFIED., .F., .F., .F. ) 
 B_SPLINE_SURFACE_WITH_KNOTS ( ( 4, 4 ),
 ( 2, 2 ),
 ( 0.000000000000000000, 1.000000000000000000 ),
 ( 0.000000000000000000, 1.000000000000000000 ),
 .UNSPECIFIED. ) 
 GEOMETRIC_REPRESENTATION_ITEM ( )  RATIONAL_B_SPLINE_SURFACE ( (
 ( 1.000000000000000000, 1.000000000000000000),
 ( 0.9953040768229005630, 0.8617119497784937465),
 ( 0.9953040768229005630, 0.8617119497784937465),
 ( 1.000000000000000000, 1.000000000000000000) ) ) 
 REPRESENTATION_ITEM ( '' )  SURFACE ( )  );
#27369=ORIENTED_EDGE ( 'NONE', *, *, #4899, .T. ) ;
#27373=ORIENTED_EDGE ( 'NONE', *, *, #7985, .F. ) ;
#27389=ORIENTED_EDGE ( 'NONE', *, *, #40139, .F. ) ;
#27396=CARTESIAN_POINT ( 'NONE',  ( 5.880360259849739535, 39.91356965504111542, 26.61251048557263132 ) ) ;
#27411=DIRECTION ( 'NONE',  ( 1.000000000000000000, 0.000000000000000000, 0.000000000000000000 ) ) ;
#27414=EDGE_CURVE ( 'NONE', #18533, #35404, #24162, .T. ) ;
#27415=CARTESIAN_POINT ( 'NONE',  ( 4.975801465491695552, 40.15204426031497320, 26.14269827151694514 ) ) ;
#27423=CARTESIAN_POINT ( 'NONE',  ( -2.569797478183790229, -4.218948559326347159, 14.01151037928415555 ) ) ;
#27453=CARTESIAN_POINT ( 'NONE',  ( 0.5980894510889457338, 28.72954109785603549, -38.59343625445417558 ) ) ;
#27458=ORIENTED_EDGE ( 'NONE', *, *, #30109, .F. ) ;
#27469=ORIENTED_EDGE ( 'NONE', *, *, #1530, .F. ) ;
#27475=CARTESIAN_POINT ( 'NONE',  ( 0.6017667736363749853, 47.74032759880255128, -5.933018439714829562 ) ) ;
#27476=CARTESIAN_POINT ( 'NONE',  ( 4.691466044806104740, -9.025781474741158661, -43.66525414675639638 ) ) ;
#27494=CARTESIAN_POINT ( 'NONE',  ( 0.2230388203127611768, 31.02270543585787621, 29.94794547692457343 ) ) ;
#27497=EDGE_CURVE ( 'NONE', #30079, #21310, #48795, .T. ) ;
#27501=CARTESIAN_POINT ( 'NONE',  ( 0.5988103564986352323, -41.96244062389634166, -23.52668867203635372 ) ) ;
#27503=ORIENTED_EDGE ( 'NONE', *, *, #55638, .F. ) ;
#27504=CARTESIAN_POINT ( 'NONE',  ( 4.549368137175248350, -13.59764261105780214, 40.71620287708320518 ) ) ;
#27505=ADVANCED_FACE ( 'NONE', ( #19564 ), #10164, .F. ) ;
#27518=ORIENTED_EDGE ( 'NONE', *, *, #55465, .F. ) ;
#27524=CARTESIAN_POINT ( 'NONE',  ( 0.1073791018717578927, 25.86618856530665767, 34.50606437925554815 ) ) ;
#27536=ORIENTED_EDGE ( 'NONE', *, *, #27621, .F. ) ;
#27548=ORIENTED_EDGE ( 'NONE', *, *, #56671, .T. ) ;
#27558=ORIENTED_EDGE ( 'NONE', *, *, #37675, .F. ) ;
#27560=CARTESIAN_POINT ( 'NONE',  ( 3.238931869106853600, -9.350562014686421008, 41.96286875554252305 ) ) ;
#27562=CARTESIAN_POINT ( 'NONE',  ( 0.8751705887134553219, 23.27176129838425922, -42.09020928323351995 ) ) ;
#27564=SURFACE_SIDE_STYLE ('',( #2816 ) ) ;
#27567=CARTESIAN_POINT ( 'NONE',  ( 0.2885700199627515006, 4.828949117911770728, -42.84523253167937185 ) ) ;
#27569=CARTESIAN_POINT ( 'NONE',  ( 0.1092355843206037486, 21.82203846347329090, -37.19569459163113834 ) ) ;
#27570=B_SPLINE_CURVE_WITH_KNOTS ( 'NONE', 3,
 ( #29701, #10612, #34424, #29092 ),
 .UNSPECIFIED., .F., .F.,
 ( 4, 4 ),
 ( 4.670885906470169154E-18, 0.004566006591234647236 ),
 .UNSPECIFIED. ) ;
#27572=CARTESIAN_POINT ( 'NONE',  ( -6.010958268070873523, -7.224487401384171115, -17.40352239307065219 ) ) ;
#27586=DIRECTION ( 'NONE',  ( 0.000000000000000000, 0.000000000000000000, 1.000000000000000000 ) ) ;
#27587=CIRCLE ( 'NONE', #49620, 47.91270532121795611 ) ;
#27594=CARTESIAN_POINT ( 'NONE',  ( 0.5980894510889457338, -47.78766676462071672, -5.583794302585086911 ) ) ;
#27595=CARTESIAN_POINT ( 'NONE',  ( -6.016104459813371719, 2.464823636987443223, 18.68131780085932547 ) ) ;
#27603=ORIENTED_EDGE ( 'NONE', *, *, #41331, .F. ) ;
#27604=CARTESIAN_POINT ( 'NONE',  ( 0.5980894510889457338, -13.12879507229256326, -46.28687279963686763 ) ) ;
#27613=CARTESIAN_POINT ( 'NONE',  ( 0.5988103622719989083, -41.35593060299654411, -24.57719485303623230 ) ) ;
#27614=VERTEX_POINT ( 'NONE', #57423 ) ;
#27616=CARTESIAN_POINT ( 'NONE',  ( 0.5988103622719989083, 29.76496569135161252, -37.79415722405566669 ) ) ;
#27619=ORIENTED_EDGE ( 'NONE', *, *, #48974, .F. ) ;
#27621=EDGE_CURVE ( 'NONE', #5605, #59719, #15122, .T. ) ;
#27622=CARTESIAN_POINT ( 'NONE',  ( 0.1073791018717578927, -41.52698815987159264, -11.62916352156135780 ) ) ;
#27625=CARTESIAN_POINT ( 'NONE',  ( -6.016104459813371719, -4.882138007282621928, -18.19977249352315596 ) ) ;
#27629=VECTOR ( 'NONE', #12922, 1000.000000000000114 ) ;
#27630=ORIENTED_EDGE ( 'NONE', *, *, #50137, .T. ) ;
#27635=B_SPLINE_CURVE_WITH_KNOTS ( 'NONE', 3,
 ( #51282, #23109, #28108, #60992, #18720, #37531 ),
 .UNSPECIFIED., .F., .F.,
 ( 4, 2, 4 ),
 ( 0.000000000000000000, 0.0002450742804987327125, 0.0004901485609974654250 ),
 .UNSPECIFIED. ) ;
#27640=CARTESIAN_POINT ( 'NONE',  ( 4.549368137175248350, -40.58005590356681580, -13.99871866169351442 ) ) ;
#27645=FACE_OUTER_BOUND ( 'NONE', #61096, .T. ) ;
#27647=CARTESIAN_POINT ( 'NONE',  ( -2.708315649062916552, -7.544341609839897878, -12.54007339125012166 ) ) ;
#27651=ADVANCED_FACE ( 'NONE', ( #20788 ), #23840, .F. ) ;
#27652=DIRECTION ( 'NONE',  ( 0.09835009131224553558, 0.9632152266566389454, 0.2500873580884741543 ) ) ;
#27654=CARTESIAN_POINT ( 'NONE',  ( 0.8760168074887076939, 24.81951362746021061, 41.20610493656918294 ) ) ;
#27666=ORIENTED_EDGE ( 'NONE', *, *, #1833, .T. ) ;
#27669=VECTOR ( 'NONE', #60983, 1000.000000000000114 ) ;
#27675=ORIENTED_EDGE ( 'NONE', *, *, #50546, .T. ) ;
#27680=B_SPLINE_CURVE_WITH_KNOTS ( 'NONE', 3,
 ( #13048, #32142, #22115, #55923, #59696, #8011 ),
 .UNSPECIFIED., .F., .F.,
 ( 4, 2, 4 ),
 ( 0.000000000000000000, 0.0002450742804987301646, 0.0004901485609974603292 ),
 .UNSPECIFIED. ) ;
#27681=CARTESIAN_POINT ( 'NONE',  ( 0.8751705887134423323, -19.22545746485690188, 44.08562551107050353 ) ) ;
#27690=CARTESIAN_POINT ( 'NONE',  ( 0.6001305935487422083, 33.64689939321941381, -34.38748867424678224 ) ) ;
#27691=CARTESIAN_POINT ( 'NONE',  ( 0.6031356219577718170, 33.95537057546184911, -34.07882816221585642 ) ) ;
#27694=B_SPLINE_CURVE_WITH_KNOTS ( 'NONE', 3,
 ( #31744, #7285, #46167, #6975 ),
 .UNSPECIFIED., .F., .F.,
 ( 4, 4 ),
 ( 5.818439421673296370E-18, 0.004566006591234646368 ),
 .UNSPECIFIED. ) ;
#27695=VERTEX_POINT ( 'NONE', #25169 ) ;
#27699=CARTESIAN_POINT ( 'NONE',  ( 0.1095718737110178559, 39.93945841550375064, -16.26534146842165995 ) ) ;
#27702=CARTESIAN_POINT ( 'NONE',  ( 0.1095718737110178559, 42.78833451865667570, -5.374020908746496517 ) ) ;
#27703=CARTESIAN_POINT ( 'NONE',  ( 0.8760168074887090262, -34.63873394077464241, -33.37827814204113253 ) ) ;
#27705=CARTESIAN_POINT ( 'NONE',  ( 0.8751705887134553219, 38.69254731947794568, 28.56654290188667034 ) ) ;
#27706=ORIENTED_EDGE ( 'NONE', *, *, #34129, .T. ) ;
#27708=CARTESIAN_POINT ( 'NONE',  ( 0.1098349054025745952, -42.78286259078966935, 5.417317591399088528 ) ) ;
#27717=VECTOR ( 'NONE', #14370, 1000.000000000000114 ) ;
#27719=B_SPLINE_CURVE_WITH_KNOTS ( 'NONE', 3,
 ( #5873, #15015, #34125, #49427 ),
 .UNSPECIFIED., .F., .F.,
 ( 4, 4 ),
 ( 2.061695315165020171E-17, 0.004444306975806114161 ),
 .UNSPECIFIED. ) ;
#27720=CARTESIAN_POINT ( 'NONE',  ( 4.691466044806104740, -37.25818859570289732, -24.49380602310800370 ) ) ;
#27721=ORIENTED_EDGE ( 'NONE', *, *, #24824, .F. ) ;
#27733=CIRCLE ( 'NONE', #6675, 47.91270532121795611 ) ;
#27735=CARTESIAN_POINT ( 'NONE',  ( 0.6028618097248864549, -46.51318640245705183, -12.28244208173044250 ) ) ;
#27741=ORIENTED_EDGE ( 'NONE', *, *, #22354, .T. ) ;
#27744=CARTESIAN_POINT ( 'NONE',  ( 0.1100053167205930493, 5.450899213259504883, -42.77858932361498745 ) ) ;
#27745=EDGE_CURVE ( 'NONE', #42964, #55548, #38325, .T. ) ;
#27746=ORIENTED_EDGE ( 'NONE', *, *, #49791, .F. ) ;
#27754=CARTESIAN_POINT ( 'NONE',  ( -6.015611763856276717, -7.216738110653404981, 17.40650793417841413 ) ) ;
#27758=CARTESIAN_POINT ( 'NONE',  ( 0.7048096507298635682, 48.10291524268443197, -0.8437160066902310573 ) ) ;
#27762=CARTESIAN_POINT ( 'NONE',  ( 0.6023142530420679819, -47.72938419887615424, -6.019593586345132863 ) ) ;
#27772=CARTESIAN_POINT ( 'NONE',  ( -6.017396004339687465, 7.209881890566553153, 17.40926186480781368 ) ) ;
#27782=ADVANCED_FACE ( 'NONE', ( #18255 ), #42209, .F. ) ;
#27784=CARTESIAN_POINT ( 'NONE',  ( 0.5988103622719987973, 47.77151394449997213, -5.677495780220555233 ) ) ;
#27786=CARTESIAN_POINT ( 'NONE',  ( -6.016489644550736315, 17.40716454747938968, -7.215050741357851294 ) ) ;
#27787=CARTESIAN_POINT ( 'NONE',  ( 0.1087620492084205998, 26.53886348603002432, -33.99140154262277491 ) ) ;
#27794=ORIENTED_EDGE ( 'NONE', *, *, #3313, .F. ) ;
#27797=CARTESIAN_POINT ( 'NONE',  ( 3.238931869106854489, 3.793313187126944097, -42.82436385108076138 ) ) ;
#27800=DIRECTION ( 'NONE',  ( 0.1024043820194936449, -0.1428674944016006809, -0.9844298967354730978 ) ) ;
#27806=( BOUNDED_SURFACE ( )  B_SPLINE_SURFACE ( 3, 1, ( 
 ( #61935, #24368 ),
 ( #57858, #19676 ),
 ( #19072, #57228 ),
 ( #14365, #42883 ) ),
 .UNSPECIFIED., .F., .F., .F. ) 
 B_SPLINE_SURFACE_WITH_KNOTS ( ( 4, 4 ),
 ( 2, 2 ),
 ( 0.000000000000000000, 1.000000000000000000 ),
 ( 0.000000000000000000, 1.000000000000000000 ),
 .UNSPECIFIED. ) 
 GEOMETRIC_REPRESENTATION_ITEM ( )  RATIONAL_B_SPLINE_SURFACE ( (
 ( 1.000000000000000000, 1.000000000000000000),
 ( 0.9953040768229013402, 0.8617119497784988535),
 ( 0.9953040768229013402, 0.8617119497784988535),
 ( 1.000000000000000000, 1.000000000000000000) ) ) 
 REPRESENTATION_ITEM ( '' )  SURFACE ( )  );
#27807=CARTESIAN_POINT ( 'NONE',  ( 0.7048096507298635682, 23.32077812596881827, -42.08020459959958970 ) ) ;
#27815=CARTESIAN_POINT ( 'NONE',  ( 0.6031356755773454870, -38.16618524502141696, 29.28597628606482317 ) ) ;
#27821=VECTOR ( 'NONE', #30243, 1000.000000000000000 ) ;
#27824=CARTESIAN_POINT ( 'NONE',  ( 0.7245667037590776127, -46.24390958543283858, 13.24050682223013276 ) ) ;
#27825=EDGE_CURVE ( 'NONE', #4461, #44643, #21107, .T. ) ;
#27827=VERTEX_POINT ( 'NONE', #42082 ) ;
#27844=ORIENTED_EDGE ( 'NONE', *, *, #30725, .T. ) ;
#27847=CARTESIAN_POINT ( 'NONE',  ( 0.6017667736363750963, -34.26315558341214285, 33.76945004754856683 ) ) ;
#27848=CIRCLE ( 'NONE', #7804, 42.92674063221959813 ) ;
#27850=CARTESIAN_POINT ( 'NONE',  ( 0.1073791018717578927, 21.14095454447508615, 37.58707531572213156 ) ) ;
#27852=EDGE_LOOP ( 'NONE', ( #24507, #60268, #11970, #15745 ) ) ;
#27853=FACE_OUTER_BOUND ( 'NONE', #53339, .T. ) ;
#27859=VERTEX_POINT ( 'NONE', #7913 ) ;
#27862=CARTESIAN_POINT ( 'NONE',  ( 0.1073791018717483448, -42.68962945260958008, 6.109314776651994627 ) ) ;
#27865=ADVANCED_FACE ( 'NONE', ( #43306 ), #29004, .F. ) ;
#27882=CARTESIAN_POINT ( 'NONE',  ( 0.1081432562775998391, -16.11101151263798670, -40.00205417854806456 ) ) ;
#27883=B_SPLINE_CURVE_WITH_KNOTS ( 'NONE', 3,
 ( #56063, #7838, #31348, #41386, #22568, #46386 ),
 .UNSPECIFIED., .F., .F.,
 ( 4, 2, 4 ),
 ( 1.764953265579307567E-18, 0.0002450742804987322246, 0.0004901485609974626061 ),
 .UNSPECIFIED. ) ;
#27891=EDGE_LOOP ( 'NONE', ( #27503, #47617, #10656, #44166 ) ) ;
#27897=ORIENTED_EDGE ( 'NONE', *, *, #47368, .F. ) ;
#27905=DIRECTION ( 'NONE',  ( 0.000000000000000000, 0.000000000000000000, 1.000000000000000000 ) ) ;
#27907=CARTESIAN_POINT ( 'NONE',  ( -6.015611763856276717, 13.32857883366833462, 13.31979030221804017 ) ) ;
#27908=CARTESIAN_POINT ( 'NONE',  ( 0.7048096507298579061, -5.442192462019134425, -47.80151517212784285 ) ) ;
#27910=CARTESIAN_POINT ( 'NONE',  ( 0.8751705887134423323, 46.21789262997739201, 13.30665218149378504 ) ) ;
#27923=ORIENTED_EDGE ( 'NONE', *, *, #17072, .F. ) ;
#27931=VERTEX_POINT ( 'NONE', #9448 ) ;
#27932=CARTESIAN_POINT ( 'NONE',  ( 2.301430502907646058, -1.287492012859730028, 48.01619648598871493 ) ) ;
#27935=CARTESIAN_POINT ( 'NONE',  ( 0.7048096507298579061, -46.24547838151358548, -13.26491767067499161 ) ) ;
#27949=CARTESIAN_POINT ( 'NONE',  ( -6.015611763856276717, 7.205255340944849429, -17.41126425312530301 ) ) ;
#27951=CARTESIAN_POINT ( 'NONE',  ( 3.238741278300274029, -7.419593128524375913, 42.34697043723798515 ) ) ;
#27957=DIRECTION ( 'NONE',  ( 0.09835009131224552170, -0.1222230102475082847, 0.9876177374393952935 ) ) ;
#27958=CARTESIAN_POINT ( 'NONE',  ( 0.8760168074887090262, 17.58183840866401226, -44.77533136581864426 ) ) ;
#27965=ORIENTED_EDGE ( 'NONE', *, *, #45481, .F. ) ;
#27973=CARTESIAN_POINT ( 'NONE',  ( 0.6017666602106488405, 6.625262199740437730, 47.64919188470830846 ) ) ;
#27975=ORIENTED_EDGE ( 'NONE', *, *, #18643, .F. ) ;
#27976=VERTEX_POINT ( 'NONE', #38000 ) ;
#27977=EDGE_CURVE ( 'NONE', #60297, #1954, #4114, .T. ) ;
#27978=CARTESIAN_POINT ( 'NONE',  ( 0.6031356219577718170, -38.21934428970593700, -29.21669799774949539 ) ) ;
#27986=LINE ( 'NONE', #5073, #18552 ) ;
#27987=DIRECTION ( 'NONE',  ( -1.000000000000000000, -0.000000000000000000, -0.000000000000000000 ) ) ;
#27988=CARTESIAN_POINT ( 'NONE',  ( -6.010958268070873523, 18.20513189769808804, 4.863021950010711691 ) ) ;
#27989=ORIENTED_EDGE ( 'NONE', *, *, #5917, .F. ) ;
#27992=ORIENTED_EDGE ( 'NONE', *, *, #47889, .T. ) ;
#27998=CARTESIAN_POINT ( 'NONE',  ( -6.016761891674564211, -13.32172022638601128, 13.32657647165350490 ) ) ;
#28004=CARTESIAN_POINT ( 'NONE',  ( -6.016761891674564211, 9.418621820384725396, -16.32039929810246903 ) ) ;
#28005=CARTESIAN_POINT ( 'NONE',  ( 0.1064266418746773885, -10.61815661559970003, -41.79703894102866713 ) ) ;
#28007=CARTESIAN_POINT ( 'NONE',  ( 0.1100247026804066219, 39.90641708963711665, -16.34612806822719122 ) ) ;
#28008=ORIENTED_EDGE ( 'NONE', *, *, #47647, .T. ) ;
#28017=CARTESIAN_POINT ( 'NONE',  ( -6.016489644550737204, 14.95199950534963484, -11.46752133529369821 ) ) ;
#28020=CARTESIAN_POINT ( 'NONE',  ( -2.708315649062910779, 13.41752550814502598, 5.842990691604645015 ) ) ;
#28027=CARTESIAN_POINT ( 'NONE',  ( 0.2224561200757645130, 42.84309024201778726, -4.874377913226053849 ) ) ;
#28029=CARTESIAN_POINT ( 'NONE',  ( 5.880360259849752858, -3.184717612778290796, 47.86623372148044808 ) ) ;
#28035=CARTESIAN_POINT ( 'NONE',  ( 0.6001305935487315502, 29.70149728382437004, -37.84751346122824600 ) ) ;
#28037=CARTESIAN_POINT ( 'NONE',  ( -6.016489644550736315, 14.95199950534948030, 11.46752133529389717 ) ) ;
#28039=CARTESIAN_POINT ( 'NONE',  ( -6.016761891674564211, -17.41015286184797262, -7.207804629151495668 ) ) ;
#28044=ORIENTED_EDGE ( 'NONE', *, *, #53307, .F. ) ;
#28052=CARTESIAN_POINT ( 'NONE',  ( 0.1103310638050662151, 5.710544932888923952, -42.74468893497611788 ) ) ;
#28055=B_SPLINE_CURVE_WITH_KNOTS ( 'NONE', 3,
 ( #1364, #1070, #20206, #11412 ),
 .UNSPECIFIED., .F., .F.,
 ( 4, 4 ),
 ( 6.254634441385501517E-18, 0.004566006591234644633 ),
 .UNSPECIFIED. ) ;
#28068=CARTESIAN_POINT ( 'NONE',  ( 5.880360259849752858, 21.25991003419953174, -43.00389496650593912 ) ) ;
#28070=CARTESIAN_POINT ( 'NONE',  ( 0.8751705887134423323, -47.55935879196466232, -7.160166390004136794 ) ) ;
#28075=ORIENTED_EDGE ( 'NONE', *, *, #26689, .T. ) ;
#28092=CARTESIAN_POINT ( 'NONE',  ( 0.7246131072078539903, 47.79072675905340617, -5.464103862701012559 ) ) ;
#28096=CARTESIAN_POINT ( 'NONE',  ( 0.1104177457020373149, 26.24862037251732616, -34.21590786699014330 ) ) ;
#28097=DIRECTION ( 'NONE',  ( -1.000000000000000000, -0.000000000000000000, -0.000000000000000000 ) ) ;
#28099=LINE ( 'NONE', #23100, #27669 ) ;
#28101=CARTESIAN_POINT ( 'NONE',  ( -2.708315649062910779, -11.44805714186566270, -9.116606751444287227 ) ) ;
#28104=EDGE_CURVE ( 'NONE', #25364, #55454, #12919, .T. ) ;
#28108=CARTESIAN_POINT ( 'NONE',  ( 0.6254087463353913412, -41.31312313681428350, 24.64672211239892974 ) ) ;
#28112=CARTESIAN_POINT ( 'NONE',  ( 4.322998006666165516, -46.85697641700715366, 10.36018990813231788 ) ) ;
#28114=CARTESIAN_POINT ( 'NONE',  ( 0.1097557419366048670, -5.407604117550024903, 42.78407272074148437 ) ) ;
#28132=ADVANCED_FACE ( 'NONE', ( #49518 ), #46890, .F. ) ;
#28144=ORIENTED_EDGE ( 'NONE', *, *, #59411, .F. ) ;
#28147=EDGE_CURVE ( 'NONE', #9403, #20133, #42114, .T. ) ;
#28150=CARTESIAN_POINT ( 'NONE',  ( 0.6023142530420679819, -33.83147280953710379, 34.20176999054650224 ) ) ;
#28155=EDGE_CURVE ( 'NONE', #17050, #39295, #27883, .T. ) ;
#28158=ORIENTED_EDGE ( 'NONE', *, *, #32973, .F. ) ;
#28160=EDGE_CURVE ( 'NONE', #43495, #31225, #18120, .T. ) ;
#28169=ORIENTED_EDGE ( 'NONE', *, *, #36719, .F. ) ;
#28170=DIRECTION ( 'NONE',  ( 0.000000000000000000, 0.000000000000000000, -1.000000000000000000 ) ) ;
#28176=CARTESIAN_POINT ( 'NONE',  ( 0.6031356755825967308, 1.709377914627507658E-05, 48.10744332413644031 ) ) ;
#28178=CARTESIAN_POINT ( 'NONE',  ( 0.1310142868023707330, 34.59629828998416912, -25.74368468368899343 ) ) ;
#28179=CARTESIAN_POINT ( 'NONE',  ( 0.3622758884714730732, 4.808133778521878732, -42.84426538328727219 ) ) ;
#28184=CARTESIAN_POINT ( 'NONE',  ( 4.975801465491694664, -35.64402118370934147, -32.01766832630300286 ) ) ;
#28186=CARTESIAN_POINT ( 'NONE',  ( 4.691466044806102076, 37.25818859570306785, -24.49380602310773725 ) ) ;
#28191=CARTESIAN_POINT ( 'NONE',  ( -6.016104459813374383, -4.871830707672929250, -18.20253432612971523 ) ) ;
#28193=VERTEX_POINT ( 'NONE', #40462 ) ;
#28197=B_SPLINE_CURVE_WITH_KNOTS ( 'NONE', 3,
 ( #43838, #39129, #40068, #11528 ),
 .UNSPECIFIED., .F., .F.,
 ( 4, 4 ),
 ( 0.000000000000000000, 0.005014147105413707325 ),
 .UNSPECIFIED. ) ;
#28198=AXIS2_PLACEMENT_3D ( 'NONE', #31742, #2907, #45248 ) ;
#28210=VERTEX_POINT ( 'NONE', #40781 ) ;
#28212=CARTESIAN_POINT ( 'NONE',  ( -6.001507490154110336, 17.41542759839264320, 7.196845540359233517 ) ) ;
#28229=ORIENTED_EDGE ( 'NONE', *, *, #50482, .F. ) ;
#28231=ADVANCED_FACE ( 'NONE', ( #54827 ), #14571, .F. ) ;
#28243=CARTESIAN_POINT ( 'NONE',  ( -6.015611763856276717, -17.41126425312542736, 7.205255340944552778 ) ) ;
#28246=CIRCLE ( 'NONE', #33280, 47.91270532121795611 ) ;
#28256=CARTESIAN_POINT ( 'NONE',  ( 0.1100247026804066219, -21.70899701554550276, 37.26174279786175703 ) ) ;
#28260=( BOUNDED_SURFACE ( )  B_SPLINE_SURFACE ( 3, 1, ( 
 ( #31587, #50674 ),
 ( #40097, #49450 ),
 ( #7763, #17187 ),
 ( #26888, #58836 ) ),
 .UNSPECIFIED., .F., .F., .F. ) 
 B_SPLINE_SURFACE_WITH_KNOTS ( ( 4, 4 ),
 ( 2, 2 ),
 ( 0.000000000000000000, 1.000000000000000000 ),
 ( 0.000000000000000000, 1.000000000000000000 ),
 .UNSPECIFIED. ) 
 GEOMETRIC_REPRESENTATION_ITEM ( )  RATIONAL_B_SPLINE_SURFACE ( (
 ( 1.000000000000000000, 1.000000000000000000),
 ( 0.7223157951917480446, 0.9931996967497186413),
 ( 0.7223157951917480446, 0.9931996967497186413),
 ( 1.000000000000000000, 1.000000000000000000) ) ) 
 REPRESENTATION_ITEM ( '' )  SURFACE ( )  );
#28273=( BOUNDED_SURFACE ( )  B_SPLINE_SURFACE ( 3, 1, ( 
 ( #35535, #40555 ),
 ( #21110, #60538 ),
 ( #1985, #7932 ),
 ( #11727, #45255 ) ),
 .UNSPECIFIED., .F., .F., .F. ) 
 B_SPLINE_SURFACE_WITH_KNOTS ( ( 4, 4 ),
 ( 2, 2 ),
 ( 0.000000000000000000, 1.000000000000000000 ),
 ( 0.000000000000000000, 1.000000000000000000 ),
 .UNSPECIFIED. ) 
 GEOMETRIC_REPRESENTATION_ITEM ( )  RATIONAL_B_SPLINE_SURFACE ( (
 ( 1.000000000000000000, 1.000000000000000000),
 ( 0.9953040768229013402, 0.8617119497784988535),
 ( 0.9953040768229013402, 0.8617119497784988535),
 ( 1.000000000000000000, 1.000000000000000000) ) ) 
 REPRESENTATION_ITEM ( '' )  SURFACE ( )  );
#28276=CARTESIAN_POINT ( 'NONE',  ( 0.6009453534118439633, -37.89911869481712614, -29.63106322864171105 ) ) ;
#28281=CARTESIAN_POINT ( 'NONE',  ( 4.691466044806103852, -8.371234562542175794, 43.79545162262294156 ) ) ;
#28290=CARTESIAN_POINT ( 'NONE',  ( 0.1098349054025746369, -30.34240357440814861, -30.64407294528938053 ) ) ;
#28293=EDGE_CURVE ( 'NONE', #2081, #26311, #37609, .T. ) ;
#28295=ORIENTED_EDGE ( 'NONE', *, *, #12127, .T. ) ;
#28303=CARTESIAN_POINT ( 'NONE',  ( 1.827119703190780653, 29.55676396270184725, -31.30004882613811290 ) ) ;
#28306=CARTESIAN_POINT ( 'NONE',  ( 0.6001305935487422083, -23.60027211631858179, 41.92422178329128712 ) ) ;
#28310=VECTOR ( 'NONE', #54211, 999.9999999999998863 ) ;
#28316=ORIENTED_EDGE ( 'NONE', *, *, #12552, .T. ) ;
#28321=CARTESIAN_POINT ( 'NONE',  ( 3.680974057930773036, -14.19449211152969781, 45.82782223000849342 ) ) ;
#28339=CARTESIAN_POINT ( 'NONE',  ( 0.1084644655670278651, 42.80575641816240307, 5.234391617064142466 ) ) ;
#28343=CARTESIAN_POINT ( 'NONE',  ( 0.8751705887134423323, 5.393078191592057813, 47.79200036674281904 ) ) ;
#28344=EDGE_LOOP ( 'NONE', ( #34810, #10194, #33021, #48769 ) ) ;
#28352=CARTESIAN_POINT ( 'NONE',  ( 0.1102847568649952675, 5.537466591275668648, -42.76743495471824019 ) ) ;
#28361=EDGE_CURVE ( 'NONE', #16193, #16923, #6093, .T. ) ;
#28363=CARTESIAN_POINT ( 'NONE',  ( 0.5980894510889457338, 19.05812566676443254, 44.17723055703957868 ) ) ;
#28367=CARTESIAN_POINT ( 'NONE',  ( 2.643462169533613793, 22.81120928486495458, -42.27470921730917297 ) ) ;
#28370=ORIENTED_EDGE ( 'NONE', *, *, #36977, .F. ) ;
#28377=EDGE_LOOP ( 'NONE', ( #45750, #41722, #43183, #53633 ) ) ;
#28384=CARTESIAN_POINT ( 'NONE',  ( 0.6041374136657475802, -34.14050483116160706, 33.89363087702989219 ) ) ;
#28385=EDGE_LOOP ( 'NONE', ( #22915, #34849, #60342, #60203 ) ) ;
#28396=CARTESIAN_POINT ( 'NONE',  ( 0.6017666602106490625, 29.00829887116070438, -38.37783452831175879 ) ) ;
#28398=CARTESIAN_POINT ( 'NONE',  ( 0.1103744047535531458, 16.53879706351773393, -39.82693656558416961 ) ) ;
#28400=CARTESIAN_POINT ( 'NONE',  ( 2.643462169533600914, 22.81120928486436483, 42.27470921730947140 ) ) ;
#28402=DIRECTION ( 'NONE',  ( 0.1024043820194936172, 0.4859385467930459335, -0.8679729669084563781 ) ) ;
#28403=CARTESIAN_POINT ( 'NONE',  ( 5.880360259849752858, 26.69116321728570540, -39.86101557989643140 ) ) ;
#28412=CARTESIAN_POINT ( 'NONE',  ( 0.2224561200757591284, 22.21411683958052308, -36.95704201588769422 ) ) ;
#28413=ORIENTED_EDGE ( 'NONE', *, *, #55853, .F. ) ;
#28414=DIRECTION ( 'NONE',  ( 0.1024043820194936311, -0.9139094329506659564, 0.3927886084231538288 ) ) ;
#28424=DIRECTION ( 'NONE',  ( -1.000000000000000000, -0.000000000000000000, -0.000000000000000000 ) ) ;
#28426=ORIENTED_EDGE ( 'NONE', *, *, #55433, .F. ) ;
#28431=B_SPLINE_CURVE_WITH_KNOTS ( 'NONE', 3,
 ( #39109, #1770, #35323, #39726, #6765, #20899 ),
 .UNSPECIFIED., .F., .F.,
 ( 4, 2, 4 ),
 ( 1.870693080156664505E-17, 0.0002293319059085104962, 0.0004586638118170022899 ),
 .UNSPECIFIED. ) ;
#28445=B_SPLINE_CURVE_WITH_KNOTS ( 'NONE', 3,
 ( #48387, #39315, #29890, #24269, #34298, #34002, #53986, #1671, #11112, #44632, #29582, #5448, #29272, #25193, #20812, #15499, #48692, #6358, #10178 ),
 .UNSPECIFIED., .F., .F.,
 ( 4, 3, 3, 3, 3, 3, 4 ),
 ( 1.144439277862597989E-16, 0.0002618519381806278684, 0.0003927759815485985773, 0.0005237000248299448395, 0.0006546240681325003188, 0.0007855481115631340102, 0.0009699050456655093156 ),
 .UNSPECIFIED. ) ;
#28457=CARTESIAN_POINT ( 'NONE',  ( 4.975801465491694664, 3.702618843597456522, -47.76942479135481534 ) ) ;
#28458=ORIENTED_EDGE ( 'NONE', *, *, #42254, .F. ) ;
#28464=CARTESIAN_POINT ( 'NONE',  ( 0.1102847568649952675, -21.64199720113217040, -37.30068345220683312 ) ) ;
#28467=EDGE_CURVE ( 'NONE', #20535, #5623, #50934, .T. ) ;
#28468=CARTESIAN_POINT ( 'NONE',  ( 0.2885697896453110478, -42.63514065501010464, -6.424755442172452646 ) ) ;
#28469=CARTESIAN_POINT ( 'NONE',  ( -6.015611763856276717, -16.31561949997069405, -9.427003116184344833 ) ) ;
#28475=CARTESIAN_POINT ( 'NONE',  ( -6.016104459813371719, -14.95258000663124243, -11.46679299034596156 ) ) ;
#28479=VERTEX_POINT ( 'NONE', #7130 ) ;
#28481=CARTESIAN_POINT ( 'NONE',  ( 0.1073791018717483448, 26.63563652260123149, 33.91564619577815165 ) ) ;
#28482=DIRECTION ( 'NONE',  ( 0.09835009131224552170, -0.9592125346408738595, 0.2650256080583596185 ) ) ;
#28485=CARTESIAN_POINT ( 'NONE',  ( -2.708315649062910779, -0.2635547933244546392, 14.63219292706382468 ) ) ;
#28489=CARTESIAN_POINT ( 'NONE',  ( 4.549368137175248350, -42.84816078363928682, 2.596185425821780246 ) ) ;
#28490=ORIENTED_EDGE ( 'NONE', *, *, #55071, .F. ) ;
#28491=CARTESIAN_POINT ( 'NONE',  ( 0.1103878639767399555, 37.37111717125843313, 21.52017980327911317 ) ) ;
#28513=LINE ( 'NONE', #5002, #57468 ) ;
#28515=CARTESIAN_POINT ( 'NONE',  ( 0.8760168074887076939, -13.30888447662048968, -46.22580377597780910 ) ) ;
#28517=AXIS2_PLACEMENT_3D ( 'NONE', #35575, #39982, #45287 ) ;
#28518=B_SPLINE_CURVE_WITH_KNOTS ( 'NONE', 3,
 ( #12361, #2933, #2303, #55544 ),
 .UNSPECIFIED., .F., .F.,
 ( 4, 4 ),
 ( 0.000000000000000000, 0.005014147105413691713 ),
 .UNSPECIFIED. ) ;
#28527=ORIENTED_EDGE ( 'NONE', *, *, #6086, .F. ) ;
#28529=CARTESIAN_POINT ( 'NONE',  ( 2.643462169533600914, -42.27470921730956377, 22.81120928486421917 ) ) ;
#28532=VERTEX_POINT ( 'NONE', #2125 ) ;
#28536=CARTESIAN_POINT ( 'NONE',  ( 3.680974057930773480, 14.19449211152937806, -45.82782223000860711 ) ) ;
#28545=CARTESIAN_POINT ( 'NONE',  ( 4.322998006666165516, -20.30542865297677935, 43.48102276965666135 ) ) ;
#28546=CARTESIAN_POINT ( 'NONE',  ( -6.016489644550736315, -18.84320342686341121, 0.004404229197709936920 ) ) ;
#28552=B_SPLINE_CURVE_WITH_KNOTS ( 'NONE', 3,
 ( #22725, #36848, #46238, #55595 ),
 .UNSPECIFIED., .F., .F.,
 ( 4, 4 ),
 ( 2.318323674163820247E-17, 0.004564976165746189446 ),
 .UNSPECIFIED. ) ;
#28556=CARTESIAN_POINT ( 'NONE',  ( 0.8760168074887076939, 7.161346975773065893, 47.56749362999715913 ) ) ;
#28559=DIRECTION ( 'NONE',  ( -0.1024043820194934645, -0.8548216096550925736, -0.5087173657443611052 ) ) ;
#28560=CARTESIAN_POINT ( 'NONE',  ( 0.5998501479064708430, 48.10473956285918717, 0.5236536531316605680 ) ) ;
#28562=CARTESIAN_POINT ( 'NONE',  ( -4.908599999999998964, 0.000000000000000000, 0.000000000000000000 ) ) ;
#28566=CARTESIAN_POINT ( 'NONE',  ( 50.00005079999999680, 0.000000000000000000, 10.00000000000000000 ) ) ;
#28567=EDGE_CURVE ( 'NONE', #44340, #22451, #4816, .T. ) ;
#28575=CARTESIAN_POINT ( 'NONE',  ( -2.708315649062910779, -14.54141329178163389, 1.648584381066805049 ) ) ;
#28581=CARTESIAN_POINT ( 'NONE',  ( 0.5998501479064699549, 18.89267974119604077, 44.24259072156093708 ) ) ;
#28582=EDGE_LOOP ( 'NONE', ( #32473, #43037, #45024, #38045 ) ) ;
#28589=CARTESIAN_POINT ( 'NONE',  ( 0.3622758884714730732, 15.73321244754854753, -40.13994584881767480 ) ) ;
#28592=B_SPLINE_CURVE_WITH_KNOTS ( 'NONE', 3,
 ( #21865, #16241, #2426, #16547 ),
 .UNSPECIFIED., .F., .F.,
 ( 4, 4 ),
 ( 0.000000000000000000, 0.005014147105413713397 ),
 .UNSPECIFIED. ) ;
#28616=VERTEX_POINT ( 'NONE', #24256 ) ;
#28622=DIRECTION ( 'NONE',  ( 0.09835009131224564660, 0.3736726418952187601, 0.9223318362920801539 ) ) ;
#28625=( BOUNDED_SURFACE ( )  B_SPLINE_SURFACE ( 3, 1, ( 
 ( #25799, #60843 ),
 ( #7282, #12962 ),
 ( #27342, #22649 ),
 ( #8223, #45862 ) ),
 .UNSPECIFIED., .F., .F., .F. ) 
 B_SPLINE_SURFACE_WITH_KNOTS ( ( 4, 4 ),
 ( 2, 2 ),
 ( 0.000000000000000000, 1.000000000000000000 ),
 ( 0.000000000000000000, 1.000000000000000000 ),
 .UNSPECIFIED. ) 
 GEOMETRIC_REPRESENTATION_ITEM ( )  RATIONAL_B_SPLINE_SURFACE ( (
 ( 1.000000000000000000, 1.000000000000000000),
 ( 0.7223157951917480446, 0.9931996967497186413),
 ( 0.7223157951917480446, 0.9931996967497186413),
 ( 1.000000000000000000, 1.000000000000000000) ) ) 
 REPRESENTATION_ITEM ( '' )  SURFACE ( )  );
#28630=EDGE_CURVE ( 'NONE', #37726, #46057, #44987, .T. ) ;
#28634=VERTEX_POINT ( 'NONE', #14157 ) ;
#28640=CARTESIAN_POINT ( 'NONE',  ( 0.5998501479064708430, -34.38546660123321175, 33.64490850298784608 ) ) ;
#28643=CARTESIAN_POINT ( 'NONE',  ( -6.015611763856276717, 18.84324252354755203, -0.006214430185207123029 ) ) ;
#28647=AXIS2_PLACEMENT_3D ( 'NONE', #41068, #31632, #16935 ) ;
#28649=CARTESIAN_POINT ( 'NONE',  ( 4.975801465491695552, 0.000000000000000000, 0.000000000000000000 ) ) ;
#28656=CARTESIAN_POINT ( 'NONE',  ( 0.1102847568649952675, 39.87696813145905850, 16.41780866919057047 ) ) ;
#28662=CARTESIAN_POINT ( 'NONE',  ( -6.016761891674565099, 17.40752468084782834, 7.214149619366422961 ) ) ;
#28665=CARTESIAN_POINT ( 'NONE',  ( -5.995132425357893702, 11.46484027925389348, -14.95525565067262797 ) ) ;
#28670=EDGE_CURVE ( 'NONE', #42065, #35170, #32213, .T. ) ;
#28678=DIRECTION ( 'NONE',  ( -0.1024043820194934368, 0.4859385467930398272, 0.8679729669084597088 ) ) ;
#28685=ORIENTED_EDGE ( 'NONE', *, *, #47655, .T. ) ;
#28688=CARTESIAN_POINT ( 'NONE',  ( -6.017396004339687465, 17.40836349643167580, 7.212050743684241816 ) ) ;
#28692=FACE_OUTER_BOUND ( 'NONE', #11208, .T. ) ;
#28693=CIRCLE ( 'NONE', #58670, 42.92674063221959813 ) ;
#28695=CARTESIAN_POINT ( 'NONE',  ( 5.880360259849739535, 45.44137230084860590, 15.37531919565251748 ) ) ;
#28699=B_SPLINE_CURVE_WITH_KNOTS ( 'NONE', 3,
 ( #5233, #5837, #34392, #5534 ),
 .UNSPECIFIED., .F., .F.,
 ( 4, 4 ),
 ( 2.061695315165020171E-17, 0.004444306975806115029 ),
 .UNSPECIFIED. ) ;
#28708=CARTESIAN_POINT ( 'NONE',  ( 4.833616638992205949, 46.11947910922903304, 3.476827473558036008 ) ) ;
#28711=CARTESIAN_POINT ( 'NONE',  ( 0.8760168074887090262, 7.161346975773060564, 47.56749362999715913 ) ) ;
#28713=CIRCLE ( 'NONE', #5689, 47.91270532121795611 ) ;
#28719=EDGE_CURVE ( 'NONE', #39423, #43333, #9777, .T. ) ;
#28721=CARTESIAN_POINT ( 'NONE',  ( 0.3622758884714600280, 29.89648521331588071, 31.06363466427737663 ) ) ;
#28730=CARTESIAN_POINT ( 'NONE',  ( 0.8760168074886960365, -46.68716261866184425, 11.58706983520244904 ) ) ;
#28743=AXIS2_PLACEMENT_3D ( 'NONE', #15390, #30080, #11610 ) ;
#28745=CARTESIAN_POINT ( 'NONE',  ( 50.00005079999999680, 9.539392014169456147, 3.000000000000000000 ) ) ;
#28746=ORIENTED_EDGE ( 'NONE', *, *, #53017, .F. ) ;
#28753=ADVANCED_FACE ( 'NONE', ( #953 ), #61007, .F. ) ;
#28757=CARTESIAN_POINT ( 'NONE',  ( 0.6001305935487315502, -18.89378601236093758, 44.24520387813796418 ) ) ;
#28761=CARTESIAN_POINT ( 'NONE',  ( 1.827119703190779321, 27.17434071502558268, 33.38937793923695807 ) ) ;
#28762=DIRECTION ( 'NONE',  ( 0.09835009131224567436, 0.9223318362920787106, -0.3736726418952223683 ) ) ;
#28767=ORIENTED_EDGE ( 'NONE', *, *, #35153, .T. ) ;
#28783=CARTESIAN_POINT ( 'NONE',  ( 0.1092355843206037486, -34.39511076960621239, 26.01340835034354271 ) ) ;
#28784=CARTESIAN_POINT ( 'NONE',  ( 0.7048096507298635682, 42.08020459959950443, 23.32077812596896393 ) ) ;
#28787=ORIENTED_EDGE ( 'NONE', *, *, #53430, .T. ) ;
#28788=CIRCLE ( 'NONE', #7760, 47.91270532121795611 ) ;
#28790=EDGE_CURVE ( 'NONE', #31225, #51844, #53918, .T. ) ;
#28796=DIRECTION ( 'NONE',  ( 0.09835009131224567436, -0.3736726418952255879, -0.9223318362920773783 ) ) ;
#28807=( BOUNDED_SURFACE ( )  B_SPLINE_SURFACE ( 3, 1, ( 
 ( #41651, #17221 ),
 ( #55712, #59810 ),
 ( #7165, #31619 ),
 ( #36039, #22534 ) ),
 .UNSPECIFIED., .F., .F., .F. ) 
 B_SPLINE_SURFACE_WITH_KNOTS ( ( 4, 4 ),
 ( 2, 2 ),
 ( 0.000000000000000000, 1.000000000000000000 ),
 ( 0.000000000000000000, 1.000000000000000000 ),
 .UNSPECIFIED. ) 
 GEOMETRIC_REPRESENTATION_ITEM ( )  RATIONAL_B_SPLINE_SURFACE ( (
 ( 1.000000000000000000, 1.000000000000000000),
 ( 0.7223157951917476005, 0.9931996967497186413),
 ( 0.7223157951917476005, 0.9931996967497186413),
 ( 1.000000000000000000, 1.000000000000000000) ) ) 
 REPRESENTATION_ITEM ( '' )  SURFACE ( )  );
#28809=CONICAL_SURFACE ( 'NONE', #44855, 42.92674063221959813, 1.485477209440487556 ) ;
#28814=CARTESIAN_POINT ( 'NONE',  ( 0.8751705887134553219, -23.27176129838455054, 42.09020928323333521 ) ) ;
#28819=( BOUNDED_SURFACE ( )  B_SPLINE_SURFACE ( 3, 1, ( 
 ( #58200, #54418 ),
 ( #20628, #58815 ),
 ( #54109, #15324 ),
 ( #20030, #58500 ) ),
 .UNSPECIFIED., .F., .F., .F. ) 
 B_SPLINE_SURFACE_WITH_KNOTS ( ( 4, 4 ),
 ( 2, 2 ),
 ( 0.000000000000000000, 1.000000000000000000 ),
 ( 0.000000000000000000, 1.000000000000000000 ),
 .UNSPECIFIED. ) 
 GEOMETRIC_REPRESENTATION_ITEM ( )  RATIONAL_B_SPLINE_SURFACE ( (
 ( 1.000000000000000000, 1.000000000000000000),
 ( 0.9751682680413298332, 0.9999560080971552356),
 ( 0.9751682680413298332, 0.9999560080971552356),
 ( 1.000000000000000000, 1.000000000000000000) ) ) 
 REPRESENTATION_ITEM ( '' )  SURFACE ( )  );
#28828=EDGE_LOOP ( 'NONE', ( #42173, #21731, #42711, #43202 ) ) ;
#28832=VERTEX_POINT ( 'NONE', #21309 ) ;
#28848=DIRECTION ( 'NONE',  ( 0.09835009131224552170, -0.9876177374393967368, -0.1222230102474975155 ) ) ;
#28856=CARTESIAN_POINT ( 'NONE',  ( 0.6001305935487422083, 47.76436356026960084, 5.760103278698182727 ) ) ;
#28857=CARTESIAN_POINT ( 'NONE',  ( 0.1310142868023672913, -40.08041389954892253, 15.91230901232153627 ) ) ;
#28860=CARTESIAN_POINT ( 'NONE',  ( 0.6017666602106489515, 18.08695057064592859, -44.57804174182703605 ) ) ;
#28871=LINE ( 'NONE', #47996, #13416 ) ;
#28874=CARTESIAN_POINT ( 'NONE',  ( 0.1092355843206037486, -21.82203846347354670, 37.19569459163097491 ) ) ;
#28881=ORIENTED_EDGE ( 'NONE', *, *, #54993, .T. ) ;
#28884=CARTESIAN_POINT ( 'NONE',  ( 4.691466044806103852, -40.13652286047880580, -19.42108863068366631 ) ) ;
#28885=FACE_OUTER_BOUND ( 'NONE', #48639, .T. ) ;
#28893=( BOUNDED_SURFACE ( )  B_SPLINE_SURFACE ( 3, 1, ( 
 ( #24646, #52834 ),
 ( #29333, #38455 ),
 ( #43785, #15558 ),
 ( #24958, #44095 ) ),
 .UNSPECIFIED., .F., .F., .F. ) 
 B_SPLINE_SURFACE_WITH_KNOTS ( ( 4, 4 ),
 ( 2, 2 ),
 ( 0.000000000000000000, 1.000000000000000000 ),
 ( 0.000000000000000000, 1.000000000000000000 ),
 .UNSPECIFIED. ) 
 GEOMETRIC_REPRESENTATION_ITEM ( )  RATIONAL_B_SPLINE_SURFACE ( (
 ( 1.000000000000000000, 1.000000000000000000),
 ( 0.9953040768229005630, 0.8617119497784937465),
 ( 0.9953040768229005630, 0.8617119497784937465),
 ( 1.000000000000000000, 1.000000000000000000) ) ) 
 REPRESENTATION_ITEM ( '' )  SURFACE ( )  );
#28895=CARTESIAN_POINT ( 'NONE',  ( -6.016104459813371719, -9.416989654584419611, 16.32137543786079803 ) ) ;
#28904=CARTESIAN_POINT ( 'NONE',  ( 0.1103878639767399417, -30.52789484587433222, -30.45925431905102698 ) ) ;
#28907=B_SPLINE_CURVE_WITH_KNOTS ( 'NONE', 3,
 ( #38403, #47790, #4835, #57449 ),
 .UNSPECIFIED., .F., .F.,
 ( 4, 4 ),
 ( 2.365306999241824718E-17, 0.004564976165746187711 ),
 .UNSPECIFIED. ) ;
#28912=( BOUNDED_SURFACE ( )  B_SPLINE_SURFACE ( 3, 1, ( 
 ( #5888, #40096 ),
 ( #907, #54125 ),
 ( #10949, #20043 ),
 ( #59144, #45095 ) ),
 .UNSPECIFIED., .F., .F., .F. ) 
 B_SPLINE_SURFACE_WITH_KNOTS ( ( 4, 4 ),
 ( 2, 2 ),
 ( 0.000000000000000000, 1.000000000000000000 ),
 ( 0.000000000000000000, 1.000000000000000000 ),
 .UNSPECIFIED. ) 
 GEOMETRIC_REPRESENTATION_ITEM ( )  RATIONAL_B_SPLINE_SURFACE ( (
 ( 1.000000000000000000, 1.000000000000000000),
 ( 0.9953040768229005630, 0.8617119497784937465),
 ( 0.9953040768229005630, 0.8617119497784937465),
 ( 1.000000000000000000, 1.000000000000000000) ) ) 
 REPRESENTATION_ITEM ( '' )  SURFACE ( )  );
#28913=CARTESIAN_POINT ( 'NONE',  ( -2.708315649062916552, -5.356004933109549171, 13.61924161399624822 ) ) ;
#28915=VERTEX_POINT ( 'NONE', #14477 ) ;
#28920=( BOUNDED_SURFACE ( )  B_SPLINE_SURFACE ( 3, 1, ( 
 ( #27754, #45964 ),
 ( #60947, #18370 ),
 ( #8026, #41259 ),
 ( #3008, #12751 ) ),
 .UNSPECIFIED., .F., .F., .F. ) 
 B_SPLINE_SURFACE_WITH_KNOTS ( ( 4, 4 ),
 ( 2, 2 ),
 ( 0.000000000000000000, 1.000000000000000000 ),
 ( 0.000000000000000000, 1.000000000000000000 ),
 .UNSPECIFIED. ) 
 GEOMETRIC_REPRESENTATION_ITEM ( )  RATIONAL_B_SPLINE_SURFACE ( (
 ( 1.000000000000000000, 1.000000000000000000),
 ( 0.9953040768229005630, 0.8617119497784937465),
 ( 0.9953040768229005630, 0.8617119497784937465),
 ( 1.000000000000000000, 1.000000000000000000) ) ) 
 REPRESENTATION_ITEM ( '' )  SURFACE ( )  );
#28922=CARTESIAN_POINT ( 'NONE',  ( 0.6027935024548037868, -12.61964268015589141, 46.42277558035020490 ) ) ;
#28933=DIRECTION ( 'NONE',  ( 0.000000000000000000, 0.000000000000000000, -1.000000000000000000 ) ) ;
#28934=DIRECTION ( 'NONE',  ( 0.000000000000000000, 0.000000000000000000, -1.000000000000000000 ) ) ;
#28939=CARTESIAN_POINT ( 'NONE',  ( 4.549368137175248350, 0.000000000000000000, 0.000000000000000000 ) ) ;
#28940=EDGE_CURVE ( 'NONE', #22273, #5676, #25092, .T. ) ;
#28951=CARTESIAN_POINT ( 'NONE',  ( 0.1103878639767399694, -34.24245495763003788, -26.21398130517505365 ) ) ;
#28953=FACE_OUTER_BOUND ( 'NONE', #31882, .T. ) ;
#28954=ADVANCED_FACE ( 'NONE', ( #11874 ), #44927, .F. ) ;
#28955=CARTESIAN_POINT ( 'NONE',  ( 4.322998006666179727, -16.38761975793238790, 45.10383234877005521 ) ) ;
#28956=CARTESIAN_POINT ( 'NONE',  ( 0.6023143664670691511, -46.53533348215000132, 12.19804739160180951 ) ) ;
#28958=FACE_OUTER_BOUND ( 'NONE', #35752, .T. ) ;
#28963=CARTESIAN_POINT ( 'NONE',  ( 4.549368137175248350, -42.14271863032827525, -8.166781970325585505 ) ) ;
#28964=CARTESIAN_POINT ( 'NONE',  ( 0.8751705887134553219, -19.22545746485630502, -44.08562551107074512 ) ) ;
#28968=CARTESIAN_POINT ( 'NONE',  ( 0.1087620492084205998, -43.12302841504342155, -0.3620418170785275058 ) ) ;
#28970=CARTESIAN_POINT ( 'NONE',  ( 0.1073791018717483448, -11.62916352156123168, -41.52698815987163528 ) ) ;
#28971=B_SPLINE_CURVE_WITH_KNOTS ( 'NONE', 3,
 ( #13490, #37302, #28186, #23188 ),
 .UNSPECIFIED., .F., .F.,
 ( 4, 4 ),
 ( 0.000000000000000000, 0.005014147105413699519 ),
 .UNSPECIFIED. ) ;
#28972=ORIENTED_EDGE ( 'NONE', *, *, #50146, .F. ) ;
#28976=ORIENTED_EDGE ( 'NONE', *, *, #29594, .F. ) ;
#28984=ADVANCED_FACE ( 'NONE', ( #45384 ), #7768, .F. ) ;
#28996=DIRECTION ( 'NONE',  ( 0.09835009131224553558, 0.5996571005210405980, -0.7941905447268757801 ) ) ;
#28997=CARTESIAN_POINT ( 'NONE',  ( 0.6025881611877911270, 46.41131722377291169, 12.66175293297418492 ) ) ;
#29003=CARTESIAN_POINT ( 'NONE',  ( 0.3622758884714730732, 41.85013935980087751, 10.35929834645937397 ) ) ;
#29004=( BOUNDED_SURFACE ( )  B_SPLINE_SURFACE ( 3, 1, ( 
 ( #23869, #28556 ),
 ( #19185, #29177 ),
 ( #10080, #4414 ),
 ( #42999, #341 ) ),
 .UNSPECIFIED., .F., .F., .F. ) 
 B_SPLINE_SURFACE_WITH_KNOTS ( ( 4, 4 ),
 ( 2, 2 ),
 ( 0.000000000000000000, 1.000000000000000000 ),
 ( 0.000000000000000000, 1.000000000000000000 ),
 .UNSPECIFIED. ) 
 GEOMETRIC_REPRESENTATION_ITEM ( )  RATIONAL_B_SPLINE_SURFACE ( (
 ( 1.000000000000000000, 1.000000000000000000),
 ( 0.9953040768229005630, 0.8617119497784937465),
 ( 0.9953040768229005630, 0.8617119497784937465),
 ( 1.000000000000000000, 1.000000000000000000) ) ) 
 REPRESENTATION_ITEM ( '' )  SURFACE ( )  );
#29008=ORIENTED_EDGE ( 'NONE', *, *, #60609, .F. ) ;
#29017=CARTESIAN_POINT ( 'NONE',  ( 4.833616638992205949, -25.31740731790869248, -38.70560126501854370 ) ) ;
#29018=ORIENTED_EDGE ( 'NONE', *, *, #56798, .T. ) ;
#29020=CARTESIAN_POINT ( 'NONE',  ( 0.8751705887134423323, 47.79200036674280483, -5.393078191592203474 ) ) ;
#29021=CARTESIAN_POINT ( 'NONE',  ( 0.1313383488274133815, 26.75504982351763061, 33.82021892231554716 ) ) ;
#29023=CARTESIAN_POINT ( 'NONE',  ( 2.301529144917015213, 11.18385659262678189, -46.71331407887427645 ) ) ;
#29024=ORIENTED_EDGE ( 'NONE', *, *, #687, .T. ) ;
#29032=DIRECTION ( 'NONE',  ( -1.000000000000000000, 0.000000000000000000, 0.000000000000000000 ) ) ;
#29038=CARTESIAN_POINT ( 'NONE',  ( 0.7048096507298635682, -11.63498350884368904, 46.68221792389220326 ) ) ;
#29041=ADVANCED_FACE ( 'NONE', ( #8068 ), #12176, .F. ) ;
#29043=CARTESIAN_POINT ( 'NONE',  ( 0.1064266418746778187, -26.69589626339737265, 33.86837517279499821 ) ) ;
#29044=CARTESIAN_POINT ( 'NONE',  ( 3.238931869106854045, 19.89273896137483533, -38.11291514434422822 ) ) ;
#29045=EDGE_LOOP ( 'NONE', ( #24443, #20726, #59866, #18309 ) ) ;
#29053=CARTESIAN_POINT ( 'NONE',  ( -6.010958268070873523, 11.48268200989218890, -14.94067681728537522 ) ) ;
#29055=VERTEX_POINT ( 'NONE', #36914 ) ;
#29070=CARTESIAN_POINT ( 'NONE',  ( -6.001507490154111224, -16.32705935667514296, 9.408444979392264429 ) ) ;
#29078=CARTESIAN_POINT ( 'NONE',  ( 0.3622758884714730732, -36.91764744403337062, 22.26738722580103413 ) ) ;
#29080=VERTEX_POINT ( 'NONE', #8993 ) ;
#29088=B_SPLINE_CURVE_WITH_KNOTS ( 'NONE', 3,
 ( #43391, #10162, #429, #38689, #53657, #29257 ),
 .UNSPECIFIED., .F., .F.,
 ( 4, 2, 4 ),
 ( 3.496446946337351263E-18, 0.0002450742804987349893, 0.0004901485609974665092 ),
 .UNSPECIFIED. ) ;
#29090=B_SPLINE_CURVE_WITH_KNOTS ( 'NONE', 3,
 ( #13876, #41460, #50826, #61138, #4119, #17955, #56137, #47081, #32984, #60523, #32357, #52058, #28256, #33594, #5046, #28874, #38004, #34210, #48297 ),
 .UNSPECIFIED., .F., .F.,
 ( 4, 3, 3, 3, 3, 3, 4 ),
 ( 1.149162571898268292E-16, 0.0002618519381806242905, 0.0003927759815485965715, 0.0005237000248299455984, 0.0006546240681324996683, 0.0007855481115631327092, 0.0009699050456655110503 ),
 .UNSPECIFIED. ) ;
#29091=ORIENTED_EDGE ( 'NONE', *, *, #5349, .T. ) ;
#29092=CARTESIAN_POINT ( 'NONE',  ( 0.3622758884714730732, 10.35929834645922831, -41.85013935980092015 ) ) ;
#29097=VERTEX_POINT ( 'NONE', #4888 ) ;
#29098=CARTESIAN_POINT ( 'NONE',  ( 0.5998501479064708430, 11.94461217097404493, 46.60114184914321811 ) ) ;
#29105=CARTESIAN_POINT ( 'NONE',  ( 4.549368137175248350, -32.13400537129904677, -28.46244473166662559 ) ) ;
#29111=CARTESIAN_POINT ( 'NONE',  ( 0.1100247026804066219, -16.34612806822732978, -39.90641708963705980 ) ) ;
#29118=CARTESIAN_POINT ( 'NONE',  ( 0.1103744047535531458, 37.32746539760790228, 21.59576373962429940 ) ) ;
#29124=B_SPLINE_CURVE_WITH_KNOTS ( 'NONE', 3,
 ( #15220, #1091, #5473, #15834 ),
 .UNSPECIFIED., .F., .F.,
 ( 4, 4 ),
 ( 0.000000000000000000, 0.005014147105413706458 ),
 .UNSPECIFIED. ) ;
#29131=CARTESIAN_POINT ( 'NONE',  ( -6.015611763856276717, -18.68122482568278286, -2.465697960551244350 ) ) ;
#29132=EDGE_CURVE ( 'NONE', #46173, #15504, #10936, .T. ) ;
#29136=CARTESIAN_POINT ( 'NONE',  ( 0.3622758884714600280, -17.25816669465019615, 39.50828911766968332 ) ) ;
#29141=CARTESIAN_POINT ( 'NONE',  ( 0.3622758884714730732, 36.91764744403321430, -22.26738722580129348 ) ) ;
#29157=CARTESIAN_POINT ( 'NONE',  ( 1.827326673878743479, -39.28486782721054738, -17.60663982372524217 ) ) ;
#29166=CARTESIAN_POINT ( 'NONE',  ( -6.016761891674564211, -18.68243340030201338, -2.456125503350905959 ) ) ;
#29170=CARTESIAN_POINT ( 'NONE',  ( 0.8751705887134553219, 13.30665218149297857, 46.21789262997761938 ) ) ;
#29173=DIRECTION ( 'NONE',  ( 1.000000000000000000, 0.000000000000000000, 0.000000000000000000 ) ) ;
#29175=EDGE_CURVE ( 'NONE', #31234, #20011, #9296, .T. ) ;
#29177=CARTESIAN_POINT ( 'NONE',  ( 0.7048096507298635682, 7.115188260603208192, 47.58126109679103877 ) ) ;
#29182=CARTESIAN_POINT ( 'NONE',  ( -6.017396004339686577, -17.40926186480773907, -7.209881890566737006 ) ) ;
#29183=VECTOR ( 'NONE', #29805, 1000.000000000000114 ) ;
#29185=( BOUNDED_SURFACE ( )  B_SPLINE_SURFACE ( 3, 1, ( 
 ( #3242, #56487 ),
 ( #36803, #17674 ),
 ( #50867, #17068 ),
 ( #46196, #4164 ) ),
 .UNSPECIFIED., .F., .F., .F. ) 
 B_SPLINE_SURFACE_WITH_KNOTS ( ( 4, 4 ),
 ( 2, 2 ),
 ( 0.000000000000000000, 1.000000000000000000 ),
 ( 0.000000000000000000, 1.000000000000000000 ),
 .UNSPECIFIED. ) 
 GEOMETRIC_REPRESENTATION_ITEM ( )  RATIONAL_B_SPLINE_SURFACE ( (
 ( 1.000000000000000000, 1.000000000000000000),
 ( 0.7223157951917480446, 0.9931996967497186413),
 ( 0.7223157951917480446, 0.9931996967497186413),
 ( 1.000000000000000000, 1.000000000000000000) ) ) 
 REPRESENTATION_ITEM ( '' )  SURFACE ( )  );
#29192=CARTESIAN_POINT ( 'NONE',  ( -6.015611763856276717, 9.416239407363534042, -16.32183393015586503 ) ) ;
#29196=B_SPLINE_CURVE_WITH_KNOTS ( 'NONE', 3,
 ( #22423, #8014, #4521, #41552, #27744, #31832, #28352, #60614, #47473, #23661, #28052, #60305, #50918, #22735, #41867, #17731, #32448, #46875, #27125 ),
 .UNSPECIFIED., .F., .F.,
 ( 4, 3, 3, 3, 3, 3, 4 ),
 ( 1.153344816771540786E-16, 0.0002618519381806256457, 0.0003927759815485972221, 0.0005237000248299425627, 0.0006546240681324985841, 0.0007855481115631309744, 0.0009699050456655101829 ),
 .UNSPECIFIED. ) ;
#29200=EDGE_CURVE ( 'NONE', #10336, #23991, #33436, .T. ) ;
#29213=B_SPLINE_CURVE_WITH_KNOTS ( 'NONE', 3,
 ( #17356, #59320, #49617, #21431 ),
 .UNSPECIFIED., .F., .F.,
 ( 4, 4 ),
 ( 0.000000000000000000, 0.004445488388166993383 ),
 .UNSPECIFIED. ) ;
#29214=CARTESIAN_POINT ( 'NONE',  ( 0.6017666602106489515, -48.10631669010027878, 0.3491145841137135442 ) ) ;
#29221=CARTESIAN_POINT ( 'NONE',  ( 0.1081432562775998946, 5.208748643066120287, 42.80885385101083784 ) ) ;
#29224=CARTESIAN_POINT ( 'NONE',  ( 3.238741278300275805, 19.89284324544641436, 38.11287256318068728 ) ) ;
#29229=CARTESIAN_POINT ( 'NONE',  ( -6.016761891674564211, -2.456125503350841566, 18.68243340030202049 ) ) ;
#29230=EDGE_LOOP ( 'NONE', ( #45617, #2795, #53077, #25023 ) ) ;
#29231=CARTESIAN_POINT ( 'NONE',  ( 4.975801465491695552, -47.84403947906842092, -2.564218696447329027 ) ) ;
#29238=CARTESIAN_POINT ( 'NONE',  ( 0.7048096507298579061, -34.61049487267082014, 33.41730025321693631 ) ) ;
#29247=CARTESIAN_POINT ( 'NONE',  ( -6.010958268070873523, -13.33459572764767032, 13.31406649671957787 ) ) ;
#29255=CARTESIAN_POINT ( 'NONE',  ( 0.6031356219577719280, -46.44562759437263111, 12.53544563195218764 ) ) ;
#29257=CARTESIAN_POINT ( 'NONE',  ( 0.8751705887134553219, 23.27176129838425922, -42.09020928323351995 ) ) ;
#29261=EDGE_CURVE ( 'NONE', #45029, #9871, #33723, .T. ) ;
#29265=CARTESIAN_POINT ( 'NONE',  ( 4.975801465491695552, 0.000000000000000000, 0.000000000000000000 ) ) ;
#29267=ORIENTED_EDGE ( 'NONE', *, *, #7985, .T. ) ;
#29268=CARTESIAN_POINT ( 'NONE',  ( 0.1313383488274125765, -33.82021892231565374, 26.75504982351751693 ) ) ;
#29271=EDGE_LOOP ( 'NONE', ( #37842, #28976, #22305, #59227 ) ) ;
#29272=CARTESIAN_POINT ( 'NONE',  ( 0.1100247026804066219, -11.32523219034937156, 41.61078157869232541 ) ) ;
#29274=CARTESIAN_POINT ( 'NONE',  ( 0.5980894510889457338, -44.71414919659894593, -17.76188940524932747 ) ) ;
#29279=CARTESIAN_POINT ( 'NONE',  ( 0.6027935024548037868, -23.90242449907784916, -41.74929432965609521 ) ) ;
#29289=EDGE_CURVE ( 'NONE', #5948, #38470, #25482, .T. ) ;
#29294=CARTESIAN_POINT ( 'NONE',  ( -2.708315649062910779, -1.648584381066950488, -14.54141329178161612 ) ) ;
#29295=EDGE_LOOP ( 'NONE', ( #51101, #52084, #54597, #51298 ) ) ;
#29298=CARTESIAN_POINT ( 'NONE',  ( 0.3622758884714730732, -34.70015533914812522, -25.58609868863756276 ) ) ;
#29303=ORIENTED_EDGE ( 'NONE', *, *, #6430, .T. ) ;
#29308=ORIENTED_EDGE ( 'NONE', *, *, #33550, .T. ) ;
#29311=CARTESIAN_POINT ( 'NONE',  ( 4.549368137175248350, -35.80950303116117794, 23.67244292351576718 ) ) ;
#29315=DIRECTION ( 'NONE',  ( 0.1024043820194936449, -0.8548216096551033427, 0.5087173657443432306 ) ) ;
#29333=CARTESIAN_POINT ( 'NONE',  ( -6.016104459813374383, -17.40682403289243396, -7.215917642689251288 ) ) ;
#29334=CARTESIAN_POINT ( 'NONE',  ( 0.6009453534118439633, 38.43042294376915180, -28.93865405070907926 ) ) ;
#29338=B_SPLINE_CURVE_WITH_KNOTS ( 'NONE', 3,
 ( #46936, #42851, #47229, #4582, #61297, #42539, #60995, #9940, #56912, #18415, #37534, #19046, #13721, #8682, #52521, #9305 ),
 .UNSPECIFIED., .F., .F.,
 ( 4, 3, 3, 3, 3, 4 ),
 ( 2.081781105835003463E-17, 0.0002618515315864420310, 0.0003927756766341996717, 0.0005236998216950579984, 0.0007855159896329915251, 0.001047349442285929171 ),
 .UNSPECIFIED. ) ;
#29340=EDGE_CURVE ( 'NONE', #44468, #34503, #52898, .T. ) ;
#29344=ORIENTED_EDGE ( 'NONE', *, *, #49698, .F. ) ;
#29345=CARTESIAN_POINT ( 'NONE',  ( 3.680882792899936362, -35.20667105325194512, -32.59085259319675743 ) ) ;
#29347=CARTESIAN_POINT ( 'NONE',  ( 0.3622758884714600280, -29.89648521331609743, -31.06363466427717412 ) ) ;
#29349=CARTESIAN_POINT ( 'NONE',  ( 0.2885700199627502793, 17.24062365614539516, 39.51953436244181006 ) ) ;
#29351=VERTEX_POINT ( 'NONE', #22399 ) ;
#29355=DIRECTION ( 'NONE',  ( 1.000000000000000000, -0.000000000000000000, -0.000000000000000000 ) ) ;
#29365=LINE ( 'NONE', #24675, #41872 ) ;
#29373=ADVANCED_FACE ( 'NONE', ( #17099 ), #15839, .F. ) ;
#29379=CARTESIAN_POINT ( 'NONE',  ( 1.827119703190781097, -36.65069040194725147, 22.58367210012827186 ) ) ;
#29389=FACE_OUTER_BOUND ( 'NONE', #24093, .T. ) ;
#29395=PRODUCT_DEFINITION_SHAPE ( 'NONE', 'NONE',  #744 ) ;
#29401=ADVANCED_FACE ( 'NONE', ( #32429 ), #24238, .F. ) ;
#29402=CARTESIAN_POINT ( 'NONE',  ( 4.549368137175248350, 0.000000000000000000, 0.000000000000000000 ) ) ;
#29407=CARTESIAN_POINT ( 'NONE',  ( -6.016761891674564211, 16.31696541414285306, -9.424569481870079812 ) ) ;
#29410=CARTESIAN_POINT ( 'NONE',  ( 0.7048096507298579061, -7.115188260604195847, 47.58126109679088245 ) ) ;
#29413=CARTESIAN_POINT ( 'NONE',  ( 2.301529144917014325, 19.56451384728982035, 43.86846428170467505 ) ) ;
#29426=CARTESIAN_POINT ( 'NONE',  ( 0.1064266379913941102, -30.09411261783711922, 30.88821943652560265 ) ) ;
#29435=ORIENTED_EDGE ( 'NONE', *, *, #52324, .F. ) ;
#29436=CARTESIAN_POINT ( 'NONE',  ( 0.1073791018717578927, -16.95003405440338895, 39.65380858626186722 ) ) ;
#29440=CARTESIAN_POINT ( 'NONE',  ( 0.5998501479064708430, -41.92175333043635987, 23.59887241503281174 ) ) ;
#29442=ORIENTED_EDGE ( 'NONE', *, *, #46972, .F. ) ;
#29443=CARTESIAN_POINT ( 'NONE',  ( 0.8751705887134423323, -46.21789262997747727, -13.30665218149346529 ) ) ;
#29452=ORIENTED_EDGE ( 'NONE', *, *, #31851, .T. ) ;
#29456=CARTESIAN_POINT ( 'NONE',  ( 0.3622758884714730732, 34.70015533914794759, 25.58609868863780434 ) ) ;
#29459=CARTESIAN_POINT ( 'NONE',  ( 4.691466044806103852, -14.01607102724572584, 42.32811009116530698 ) ) ;
#29465=CARTESIAN_POINT ( 'NONE',  ( 4.322998006666165516, -32.40067585697774888, -35.39923696759002070 ) ) ;
#29466=ORIENTED_EDGE ( 'NONE', *, *, #52231, .T. ) ;
#29467=CARTESIAN_POINT ( 'NONE',  ( -6.016489644550736315, -4.872725758886318204, 18.20227673842142480 ) ) ;
#29471=ORIENTED_EDGE ( 'NONE', *, *, #1538, .F. ) ;
#29472=DIRECTION ( 'NONE',  ( 0.000000000000000000, 0.000000000000000000, 1.000000000000000000 ) ) ;
#29485=EDGE_CURVE ( 'NONE', #226, #3592, #48679, .T. ) ;
#29490=CARTESIAN_POINT ( 'NONE',  ( 0.6041374136657475802, 44.37863742124641675, 18.57118264377553629 ) ) ;
#29497=B_SPLINE_CURVE_WITH_KNOTS ( 'NONE', 3,
 ( #8324, #46574, #35951, #32466, #21832, #31226, #26835, #41569, #60953, #46892, #18063, #8637, #27762, #7393, #3928, #50623 ),
 .UNSPECIFIED., .F., .F.,
 ( 4, 3, 3, 3, 3, 4 ),
 ( 1.995049841954898532E-17, 0.0002618515315864418684, 0.0003927756766341984791, 0.0005236998216950566973, 0.0007855159896329908745, 0.001047349442285928304 ),
 .UNSPECIFIED. ) ;
#29501=CARTESIAN_POINT ( 'NONE',  ( 0.5988103622719990193, 28.80261254779987112, 38.53259676306930714 ) ) ;
#29506=ORIENTED_EDGE ( 'NONE', *, *, #24479, .T. ) ;
#29511=ORIENTED_EDGE ( 'NONE', *, *, #23807, .T. ) ;
#29512=ORIENTED_EDGE ( 'NONE', *, *, #31371, .F. ) ;
#29518=ORIENTED_EDGE ( 'NONE', *, *, #2713, .T. ) ;
#29523=VERTEX_POINT ( 'NONE', #54265 ) ;
#29524=CARTESIAN_POINT ( 'NONE',  ( 0.6027935024548037868, -18.57106801640327731, 44.37842839362943437 ) ) ;
#29525=CARTESIAN_POINT ( 'NONE',  ( 2.643462169533613793, 44.89050350746127549, 17.09809940585677168 ) ) ;
#29527=CARTESIAN_POINT ( 'NONE',  ( 0.1310142868023692897, 0.6370537502136495167, -43.11885108606331585 ) ) ;
#29530=CARTESIAN_POINT ( 'NONE',  ( 0.5998501479064708430, -33.64490850298820845, -34.38546660123286358 ) ) ;
#29531=CARTESIAN_POINT ( 'NONE',  ( 0.8760168074886960365, 0.8912768426706220160, -48.09529047980637273 ) ) ;
#29544=CARTESIAN_POINT ( 'NONE',  ( 0.5998501479064699549, 44.24259072156085182, -18.89267974119621485 ) ) ;
#29547=DIRECTION ( 'NONE',  ( 0.000000000000000000, 0.000000000000000000, 1.000000000000000000 ) ) ;
#29548=CARTESIAN_POINT ( 'NONE',  ( 0.6001305935487422083, 29.70149728382435228, -37.84751346122826021 ) ) ;
#29556=CARTESIAN_POINT ( 'NONE',  ( 0.1084644655670280733, 30.21121552070997751, -30.77359411724695093 ) ) ;
#29557=CARTESIAN_POINT ( 'NONE',  ( 0.7954196712028460681, 38.68220069891169999, -28.58653687859125725 ) ) ;
#29563=FACE_OUTER_BOUND ( 'NONE', #58028, .T. ) ;
#29564=B_SPLINE_CURVE_WITH_KNOTS ( 'NONE', 3,
 ( #37612, #13804, #29345, #28184 ),
 .UNSPECIFIED., .F., .F.,
 ( 4, 4 ),
 ( 2.165040709395311930E-17, 0.004444306975806114161 ),
 .UNSPECIFIED. ) ;
#29571=CARTESIAN_POINT ( 'NONE',  ( 0.8751705887134423323, 46.21789262997739201, 13.30665218149378504 ) ) ;
#29579=CARTESIAN_POINT ( 'NONE',  ( 1.827326673878742813, -34.89023127623437404, 25.21837361081529849 ) ) ;
#29581=ORIENTED_EDGE ( 'NONE', *, *, #25063, .F. ) ;
#29582=CARTESIAN_POINT ( 'NONE',  ( 0.1103310638050662013, -11.24099191367028183, 41.63362651001246206 ) ) ;
#29587=CARTESIAN_POINT ( 'NONE',  ( 0.6030672727741701600, -23.97812608463503992, -41.70584815505880272 ) ) ;
#29589=CARTESIAN_POINT ( 'NONE',  ( 4.549368137175248350, -13.99871866169391765, 40.58005590356665948 ) ) ;
#29591=AXIS2_PLACEMENT_3D ( 'NONE', #13559, #37372, #13254 ) ;
#29594=EDGE_CURVE ( 'NONE', #4682, #3337, #23281, .T. ) ;
#29611=B_SPLINE_CURVE_WITH_KNOTS ( 'NONE', 3,
 ( #18485, #19418, #38850, #24411 ),
 .UNSPECIFIED., .F., .F.,
 ( 4, 4 ),
 ( 0.000000000000000000, 0.004445488388166991649 ),
 .UNSPECIFIED. ) ;
#29618=CARTESIAN_POINT ( 'NONE',  ( 0.6001305935487422083, 12.95698906763808900, -46.33281397023051795 ) ) ;
#29626=ORIENTED_EDGE ( 'NONE', *, *, #27414, .F. ) ;
#29629=CARTESIAN_POINT ( 'NONE',  ( 4.549368137175248350, -40.58005590356681580, -13.99871866169351442 ) ) ;
#29635=CARTESIAN_POINT ( 'NONE',  ( 0.8751705887134553219, 34.63284514348538323, 33.37254303619566542 ) ) ;
#29636=CARTESIAN_POINT ( 'NONE',  ( 2.643462169533613793, 28.13401304854720308, -38.93558293168510431 ) ) ;
#29644=CARTESIAN_POINT ( 'NONE',  ( 0.3622758884714730732, -41.85013935980095567, -10.35929834645908265 ) ) ;
#29654=CARTESIAN_POINT ( 'NONE',  ( 0.1100247026804066219, 16.34612806822703490, 39.90641708963718060 ) ) ;
#29655=EDGE_CURVE ( 'NONE', #6741, #58555, #43950, .T. ) ;
#29662=CARTESIAN_POINT ( 'NONE',  ( 0.3622758884714730732, -10.35929834645951964, 41.85013935980084199 ) ) ;
#29664=VERTEX_POINT ( 'NONE', #36141 ) ;
#29676=CARTESIAN_POINT ( 'NONE',  ( 3.680882792899936362, -27.71664061799177503, 39.15943299201938999 ) ) ;
#29677=CARTESIAN_POINT ( 'NONE',  ( 4.975801465491695552, -45.18341283946470099, 15.94009207552969620 ) ) ;
#29680=ORIENTED_EDGE ( 'NONE', *, *, #61302, .T. ) ;
#29684=CARTESIAN_POINT ( 'NONE',  ( 4.975801465491695552, -47.84403947906842092, -2.564218696447329027 ) ) ;
#29694=CARTESIAN_POINT ( 'NONE',  ( 0.6001305935487422083, -17.92615948558569272, 44.64600790884025372 ) ) ;
#29697=ORIENTED_EDGE ( 'NONE', *, *, #23432, .T. ) ;
#29701=CARTESIAN_POINT ( 'NONE',  ( 4.549368137175248350, 8.582197505784431968, -42.06008734272388239 ) ) ;
#29702=DIRECTION ( 'NONE',  ( 0.09835009131224552170, -0.9164135549743811504, 0.3879606369183475900 ) ) ;
#29703=CARTESIAN_POINT ( 'NONE',  ( 1.827326673878743701, -27.17438009792357434, 33.38933471001428899 ) ) ;
#29705=ORIENTED_EDGE ( 'NONE', *, *, #15648, .T. ) ;
#29710=CARTESIAN_POINT ( 'NONE',  ( 0.3622758884714600280, -25.58609868863743841, -34.70015533914819628 ) ) ;
#29714=CARTESIAN_POINT ( 'NONE',  ( -6.017396004339686577, 16.31807101179383679, -9.422598049764452810 ) ) ;
#29719=AXIS2_PLACEMENT_3D ( 'NONE', #11282, #30369, #25373 ) ;
#29721=FACE_OUTER_BOUND ( 'NONE', #50848, .T. ) ;
#29724=DIRECTION ( 'NONE',  ( 0.09835009131224564660, -0.6119264800004838856, 0.7847759187265433978 ) ) ;
#29736=ORIENTED_EDGE ( 'NONE', *, *, #34146, .T. ) ;
#29737=DIRECTION ( 'NONE',  ( 0.1024043820194936449, 0.9641676559171069583, 0.2447326578667362307 ) ) ;
#29741=CARTESIAN_POINT ( 'NONE',  ( 0.1073791018717483448, -30.83464511437118816, -30.14884492832378626 ) ) ;
#29754=EDGE_LOOP ( 'NONE', ( #16296, #46730, #31149, #20492 ) ) ;
#29756=CARTESIAN_POINT ( 'NONE',  ( 0.3622758884714600280, 4.808133778521302304, 42.84426538328732903 ) ) ;
#29757=B_SPLINE_CURVE_WITH_KNOTS ( 'NONE', 3,
 ( #56634, #36951, #23138, #46646, #32234, #51313 ),
 .UNSPECIFIED., .F., .F.,
 ( 4, 2, 4 ),
 ( 8.541065402288459803E-17, 0.0002293366620881456082, 0.0004586733241762058354 ),
 .UNSPECIFIED. ) ;
#29760=EDGE_CURVE ( 'NONE', #45115, #55224, #24721, .T. ) ;
#29770=CARTESIAN_POINT ( 'NONE',  ( 0.5988103564986361205, 6.880138274944319399, 47.61318305157298170 ) ) ;
#29772=B_SPLINE_CURVE_WITH_KNOTS ( 'NONE', 3,
 ( #56386, #13501, #18502, #37627 ),
 .UNSPECIFIED., .F., .F.,
 ( 4, 4 ),
 ( 0.000000000000000000, 0.005014147105413715132 ),
 .UNSPECIFIED. ) ;
#29780=ORIENTED_EDGE ( 'NONE', *, *, #39792, .F. ) ;
#29782=CARTESIAN_POINT ( 'NONE',  ( 0.8751705887134553219, 37.60752970653828697, -29.98056538504921065 ) ) ;
#29789=CARTESIAN_POINT ( 'NONE',  ( -2.708315649062916552, 5.842990691604414977, 13.41752550814512546 ) ) ;
#29796=CARTESIAN_POINT ( 'NONE',  ( 0.5998501479064708430, -41.92175333043635987, 23.59887241503281174 ) ) ;
#29797=CARTESIAN_POINT ( 'NONE',  ( 4.975801465491694664, -43.22084481528235500, 20.67815041659062913 ) ) ;
#29805=DIRECTION ( 'NONE',  ( 0.09835009131224552170, 0.9164135549743782638, -0.3879606369183544179 ) ) ;
#29807=AXIS2_PLACEMENT_3D ( 'NONE', #38765, #44395, #43462 ) ;
#29809=CARTESIAN_POINT ( 'NONE',  ( 4.833616638992208614, -41.67905425467692737, -20.04871863793795228 ) ) ;
#29811=VERTEX_POINT ( 'NONE', #18880 ) ;
#29813=CARTESIAN_POINT ( 'NONE',  ( 4.691466044806102076, 14.01607102724483056, 42.32811009116559831 ) ) ;
#29816=CARTESIAN_POINT ( 'NONE',  ( -6.015611763856276717, 4.870987357968176390, 18.20278301740938431 ) ) ;
#29822=CARTESIAN_POINT ( 'NONE',  ( 0.1103744047535531458, 11.12399292196378831, 41.66501489234567401 ) ) ;
#29832=VERTEX_POINT ( 'NONE', #18555 ) ;
#29835=ORIENTED_EDGE ( 'NONE', *, *, #6269, .F. ) ;
#29837=CARTESIAN_POINT ( 'NONE',  ( 0.6031357023905875581, -18.45021748202310974, 44.42879114414625974 ) ) ;
#29849=CARTESIAN_POINT ( 'NONE',  ( 0.3622758884714600280, 42.62881903538200845, 6.444611261694737081 ) ) ;
#29850=CARTESIAN_POINT ( 'NONE',  ( -6.016761891674564211, 18.20023637398605842, -4.880293656734773222 ) ) ;
#29855=CARTESIAN_POINT ( 'NONE',  ( 4.549368137175248350, 0.000000000000000000, 0.000000000000000000 ) ) ;
#29857=CARTESIAN_POINT ( 'NONE',  ( 0.1102847568649952675, -39.80641842112257933, 16.58813073670638261 ) ) ;
#29862=CARTESIAN_POINT ( 'NONE',  ( -2.569797478183783568, 1.464172661884163285, -14.55946937464482360 ) ) ;
#29865=CARTESIAN_POINT ( 'NONE',  ( 0.1098349054025746785, 30.64407294528948356, -30.34240357440803848 ) ) ;
#29872=CARTESIAN_POINT ( 'NONE',  ( 0.6009452777970413218, -23.67489783211123111, 41.87890062805995228 ) ) ;
#29882=CARTESIAN_POINT ( 'NONE',  ( 0.7954190325252785687, -7.138712176115113550, -47.56618055754173469 ) ) ;
#29884=EDGE_LOOP ( 'NONE', ( #60492, #29835, #39391, #27721 ) ) ;
#29885=CARTESIAN_POINT ( 'NONE',  ( 0.1103878639767399694, -43.12442673975421314, 0.04853618198105230652 ) ) ;
#29890=CARTESIAN_POINT ( 'NONE',  ( 0.1092565886968783623, -10.86136484717998663, 41.73439049602432505 ) ) ;
#29893=ORIENTED_EDGE ( 'NONE', *, *, #37473, .T. ) ;
#29901=CARTESIAN_POINT ( 'NONE',  ( 0.5998501479064699549, 18.89267974119604077, 44.24259072156093708 ) ) ;
#29903=( BOUNDED_SURFACE ( )  B_SPLINE_SURFACE ( 3, 1, ( 
 ( #51816, #28029 ),
 ( #47148, #9220 ),
 ( #23633, #4190 ),
 ( #18954, #13631 ) ),
 .UNSPECIFIED., .F., .F., .F. ) 
 B_SPLINE_SURFACE_WITH_KNOTS ( ( 4, 4 ),
 ( 2, 2 ),
 ( 0.000000000000000000, 1.000000000000000000 ),
 ( 0.000000000000000000, 1.000000000000000000 ),
 .UNSPECIFIED. ) 
 GEOMETRIC_REPRESENTATION_ITEM ( )  RATIONAL_B_SPLINE_SURFACE ( (
 ( 1.000000000000000000, 1.000000000000000000),
 ( 0.7223157951917476005, 0.9931996967497186413),
 ( 0.7223157951917476005, 0.9931996967497186413),
 ( 1.000000000000000000, 1.000000000000000000) ) ) 
 REPRESENTATION_ITEM ( '' )  SURFACE ( )  );
#29904=VECTOR ( 'NONE', #58803, 1000.000000000000000 ) ;
#29909=EDGE_CURVE ( 'NONE', #16942, #10591, #663, .T. ) ;
#29911=CARTESIAN_POINT ( 'NONE',  ( -6.010958268070873523, 9.434296419346436480, -16.31164801516932528 ) ) ;
#29912=VECTOR ( 'NONE', #5951, 1000.000000000000114 ) ;
#29913=VERTEX_POINT ( 'NONE', #15098 ) ;
#29914=CARTESIAN_POINT ( 'NONE',  ( 0.5998501479064708430, 46.60114184914316837, -11.94461217097420658 ) ) ;
#29924=( BOUNDED_SURFACE ( )  B_SPLINE_SURFACE ( 3, 1, ( 
 ( #9193, #10436 ),
 ( #14532, #33944 ),
 ( #42729, #61789 ),
 ( #9497, #38964 ) ),
 .UNSPECIFIED., .F., .F., .F. ) 
 B_SPLINE_SURFACE_WITH_KNOTS ( ( 4, 4 ),
 ( 2, 2 ),
 ( 0.000000000000000000, 1.000000000000000000 ),
 ( 0.000000000000000000, 1.000000000000000000 ),
 .UNSPECIFIED. ) 
 GEOMETRIC_REPRESENTATION_ITEM ( )  RATIONAL_B_SPLINE_SURFACE ( (
 ( 1.000000000000000000, 1.000000000000000000),
 ( 0.9953040768229005630, 0.8617119497784937465),
 ( 0.9953040768229005630, 0.8617119497784937465),
 ( 1.000000000000000000, 1.000000000000000000) ) ) 
 REPRESENTATION_ITEM ( '' )  SURFACE ( )  );
#29931=CARTESIAN_POINT ( 'NONE',  ( 4.833616638992205949, -38.70560126501880660, 25.31740731790829102 ) ) ;
#29932=CARTESIAN_POINT ( 'NONE',  ( 4.691466044806103852, 14.64802401911168062, 42.11359095667496177 ) ) ;
#29934=EDGE_LOOP ( 'NONE', ( #22311, #30587, #58708, #19376 ) ) ;
#29936=CARTESIAN_POINT ( 'NONE',  ( 2.643462169533600914, -40.89244134039093836, -25.20536747735765104 ) ) ;
#29938=CARTESIAN_POINT ( 'NONE',  ( 0.1073791018717483448, -21.98088480513640874, -37.10214135362880228 ) ) ;
#29950=CARTESIAN_POINT ( 'NONE',  ( 3.680882792899936362, 35.20667105325171775, 32.59085259319700612 ) ) ;
#29953=CARTESIAN_POINT ( 'NONE',  ( -6.016761891674564211, -7.214149619366230226, -17.40752468084790650 ) ) ;
#29958=EDGE_CURVE ( 'NONE', #60202, #7602, #3136, .T. ) ;
#29959=CARTESIAN_POINT ( 'NONE',  ( 0.6254087463353934506, 46.64065386173398053, 11.78492518233826125 ) ) ;
#29960=CARTESIAN_POINT ( 'NONE',  ( 4.549368137175248350, 38.40568845698250300, 19.17571786012337753 ) ) ;
#29961=CARTESIAN_POINT ( 'NONE',  ( 4.975801465491695552, -39.51822597168514051, 27.09127437476313816 ) ) ;
#29962=ORIENTED_EDGE ( 'NONE', *, *, #52182, .T. ) ;
#29965=VECTOR ( 'NONE', #24089, 1000.000000000000114 ) ;
#29967=CARTESIAN_POINT ( 'NONE',  ( 0.1097557419366048670, 16.70891382096314004, 39.75589591229793029 ) ) ;
#29975=CARTESIAN_POINT ( 'NONE',  ( -5.995132425357893702, 11.47834865841117491, -14.94489030678139230 ) ) ;
#29980=B_SPLINE_CURVE_WITH_KNOTS ( 'NONE', 3,
 ( #3294, #3601, #36542, #3913, #18047, #17419 ),
 .UNSPECIFIED., .F., .F.,
 ( 4, 2, 4 ),
 ( 1.250788275041438294E-16, 0.0002450741128632354863, 0.0004901482257263459642 ),
 .UNSPECIFIED. ) ;
#29996=CARTESIAN_POINT ( 'NONE',  ( 0.6028618097248862329, -0.1745704727162494252, -48.10721794025128162 ) ) ;
#29997=ORIENTED_EDGE ( 'NONE', *, *, #26320, .T. ) ;
#29999=VERTEX_POINT ( 'NONE', #31041 ) ;
#30020=VERTEX_POINT ( 'NONE', #2517 ) ;
#30031=FACE_OUTER_BOUND ( 'NONE', #31096, .T. ) ;
#30041=ORIENTED_EDGE ( 'NONE', *, *, #28293, .F. ) ;
#30044=CARTESIAN_POINT ( 'NONE',  ( 0.1092355843206037486, 37.19569459163105307, 21.82203846347341525 ) ) ;
#30045=CARTESIAN_POINT ( 'NONE',  ( 0.6001305935487422083, 12.95698906763746194, 46.33281397023068138 ) ) ;
#30046=CARTESIAN_POINT ( 'NONE',  ( 0.1073791018717483448, -30.14884492832410601, 30.83464511437086841 ) ) ;
#30061=VERTEX_POINT ( 'NONE', #18806 ) ;
#30063=CARTESIAN_POINT ( 'NONE',  ( 4.975801465491694664, 31.15993731089074359, 36.39623109580477234 ) ) ;
#30069=CARTESIAN_POINT ( 'NONE',  ( 0.1313383488274145194, 33.82021892231549032, -26.75504982351774075 ) ) ;
#30073=CARTESIAN_POINT ( 'NONE',  ( 0.5998501479064699549, 24.50586714782546593, 41.39809967730496254 ) ) ;
#30074=CARTESIAN_POINT ( 'NONE',  ( -6.016489644550736315, -13.32104266208108534, 13.32727118274432954 ) ) ;
#30079=VERTEX_POINT ( 'NONE', #58214 ) ;
#30080=DIRECTION ( 'NONE',  ( -1.000000000000000000, -0.000000000000000000, -0.000000000000000000 ) ) ;
#30081=EDGE_LOOP ( 'NONE', ( #36569, #22652, #12349, #58624 ) ) ;
#30084=ORIENTED_EDGE ( 'NONE', *, *, #26976, .T. ) ;
#30086=CARTESIAN_POINT ( 'NONE',  ( 4.975801465491695552, -45.55012473237743365, -14.85979367497158599 ) ) ;
#30090=CARTESIAN_POINT ( 'NONE',  ( 0.6031356755773454870, 18.40989784469860524, -44.44549206087163640 ) ) ;
#30094=FILL_AREA_STYLE_COLOUR ( '', #14830 ) ;
#30098=ADVANCED_FACE ( 'NONE', ( #9695 ), #27223, .F. ) ;
#30102=CARTESIAN_POINT ( 'NONE',  ( 4.975801465491695552, 35.64402118370958306, -32.01766832630274706 ) ) ;
#30104=CARTESIAN_POINT ( 'NONE',  ( 4.975801465491695552, -42.71626295676279028, 21.70134120755125906 ) ) ;
#30106=EDGE_CURVE ( 'NONE', #48896, #41987, #15033, .T. ) ;
#30108=B_SPLINE_CURVE_WITH_KNOTS ( 'NONE', 3,
 ( #46776, #3505, #22642, #41771, #7274, #17953 ),
 .UNSPECIFIED., .F., .F.,
 ( 4, 2, 4 ),
 ( 8.609910155989501895E-17, 0.0002293366620881447408, 0.0004586733241762033959 ),
 .UNSPECIFIED. ) ;
#30109=EDGE_CURVE ( 'NONE', #35637, #27976, #57281, .T. ) ;
#30112=VERTEX_POINT ( 'NONE', #34445 ) ;
#30119=CIRCLE ( 'NONE', #17133, 47.91270532121795611 ) ;
#30126=ORIENTED_EDGE ( 'NONE', *, *, #23844, .T. ) ;
#30127=VERTEX_POINT ( 'NONE', #48524 ) ;
#30132=CARTESIAN_POINT ( 'NONE',  ( 0.5998501479064699549, 24.50586714782546593, 41.39809967730496254 ) ) ;
#30133=EDGE_CURVE ( 'NONE', #46497, #61502, #47147, .T. ) ;
#30135=CARTESIAN_POINT ( 'NONE',  ( -2.569797478183783568, -11.33042594333554298, 9.259773107242873280 ) ) ;
#30142=ORIENTED_EDGE ( 'NONE', *, *, #26409, .T. ) ;
#30147=B_SPLINE_CURVE_WITH_KNOTS ( 'NONE', 3,
 ( #23678, #9571, #47808, #52792, #28997, #24295, #43429, #469, #58706, #59962, #40581, #21137, #49326, #35567, #59644, #45278 ),
 .UNSPECIFIED., .F., .F.,
 ( 4, 3, 3, 3, 3, 4 ),
 ( 1.868480190406682863E-17, 0.0002618515315864420852, 0.0003927756766342001596, 0.0005236998216950582152, 0.0007855159896329938019, 0.001047349442285931773 ),
 .UNSPECIFIED. ) ;
#30148=CARTESIAN_POINT ( 'NONE',  ( -6.017396004339687465, -2.460690056887917532, 18.68180398134249387 ) ) ;
#30149=ORIENTED_EDGE ( 'NONE', *, *, #30691, .T. ) ;
#30152=CARTESIAN_POINT ( 'NONE',  ( 0.8751705887134553219, 38.69254731947794568, 28.56654290188667034 ) ) ;
#30158=CARTESIAN_POINT ( 'NONE',  ( 0.1104177457020372594, 34.21590786699005093, 26.24862037251744340 ) ) ;
#30162=CARTESIAN_POINT ( 'NONE',  ( 0.1097557419366048670, 34.07666148910645632, -26.42915440612296152 ) ) ;
#30165=CARTESIAN_POINT ( 'NONE',  ( 4.975801465491695552, 27.09127437476327671, 39.51822597168504814 ) ) ;
#30167=CARTESIAN_POINT ( 'NONE',  ( 0.1102847568649952675, 30.42833243501150520, -30.55869130182077598 ) ) ;
#30168=( BOUNDED_SURFACE ( )  B_SPLINE_SURFACE ( 3, 1, ( 
 ( #9566, #28068 ),
 ( #34019, #42495 ),
 ( #61556, #28367 ),
 ( #56862, #33094 ) ),
 .UNSPECIFIED., .F., .F., .F. ) 
 B_SPLINE_SURFACE_WITH_KNOTS ( ( 4, 4 ),
 ( 2, 2 ),
 ( 0.000000000000000000, 1.000000000000000000 ),
 ( 0.000000000000000000, 1.000000000000000000 ),
 .UNSPECIFIED. ) 
 GEOMETRIC_REPRESENTATION_ITEM ( )  RATIONAL_B_SPLINE_SURFACE ( (
 ( 1.000000000000000000, 1.000000000000000000),
 ( 0.7223157951917476005, 0.9931996967497186413),
 ( 0.7223157951917476005, 0.9931996967497186413),
 ( 1.000000000000000000, 1.000000000000000000) ) ) 
 REPRESENTATION_ITEM ( '' )  SURFACE ( )  );
#30170=CARTESIAN_POINT ( 'NONE',  ( 4.975801465491694664, -15.94009207553080643, 45.18341283946430309 ) ) ;
#30172=CARTESIAN_POINT ( 'NONE',  ( 0.8760168074887076939, 44.09317760313751933, -19.22870327415258274 ) ) ;
#30173=B_SPLINE_CURVE_WITH_KNOTS ( 'NONE', 3,
 ( #56392, #4067, #55777, #22904 ),
 .UNSPECIFIED., .F., .F.,
 ( 4, 4 ),
 ( 0.000000000000000000, 0.005014147105413690846 ),
 .UNSPECIFIED. ) ;
#30176=CARTESIAN_POINT ( 'NONE',  ( -2.569797478183783568, 8.547745408040794857, -11.87678401312186161 ) ) ;
#30178=CARTESIAN_POINT ( 'NONE',  ( 4.975801465491694664, -46.87746200127448049, -9.906103548668065528 ) ) ;
#30180=B_SPLINE_CURVE_WITH_KNOTS ( 'NONE', 3,
 ( #27681, #59950, #54930, #31449, #3850, #22059 ),
 .UNSPECIFIED., .F., .F.,
 ( 4, 2, 4 ),
 ( 1.283058336952897540E-16, 0.0002450741128632341853, 0.0004901482257263400011 ),
 .UNSPECIFIED. ) ;
#30183=CARTESIAN_POINT ( 'NONE',  ( 0.8751705887134423323, -47.55935879196466232, -7.160166390004136794 ) ) ;
#30185=EDGE_CURVE ( 'NONE', #9792, #25496, #4215, .T. ) ;
#30189=CARTESIAN_POINT ( 'NONE',  ( 0.2230388203127599833, -33.74101226470682491, 26.84831060237785749 ) ) ;
#30194=ORIENTED_EDGE ( 'NONE', *, *, #38755, .T. ) ;
#30196=CARTESIAN_POINT ( 'NONE',  ( -6.016104459813374383, 11.47525878590937864, -14.94608397322072157 ) ) ;
#30201=FACE_OUTER_BOUND ( 'NONE', #12986, .T. ) ;
#30209=CARTESIAN_POINT ( 'NONE',  ( 0.5980894510889457338, -48.10766805928368939, 0.7015180096003246213 ) ) ;
#30211=VERTEX_POINT ( 'NONE', #3064 ) ;
#30215=ORIENTED_EDGE ( 'NONE', *, *, #60760, .T. ) ;
#30216=DIRECTION ( 'NONE',  ( 0.09835009131224564660, 0.5996571005210301619, 0.7941905447268835516 ) ) ;
#30217=CARTESIAN_POINT ( 'NONE',  ( 0.5988103564986356764, 44.67429521517308189, 17.84821699813498341 ) ) ;
#30222=B_SPLINE_CURVE_WITH_KNOTS ( 'NONE', 3,
 ( #40759, #16939, #55117, #31018, #31953, #12546 ),
 .UNSPECIFIED., .F., .F.,
 ( 4, 2, 4 ),
 ( 2.224174099750402646E-17, 0.0002293319059085101167, 0.0004586638118169979531 ),
 .UNSPECIFIED. ) ;
#30224=EDGE_CURVE ( 'NONE', #5867, #54484, #58980, .T. ) ;
#30229=ORIENTED_EDGE ( 'NONE', *, *, #51178, .F. ) ;
#30230=CARTESIAN_POINT ( 'NONE',  ( 0.5988103564986357874, 41.96244062389618534, 23.52668867203664860 ) ) ;
#30232=EDGE_LOOP ( 'NONE', ( #16311, #9507, #38062, #25293 ) ) ;
#30234=CARTESIAN_POINT ( 'NONE',  ( -2.569797478183783568, -12.44213550320658612, 7.701637110048465296 ) ) ;
#30239=CARTESIAN_POINT ( 'NONE',  ( 2.643462169533600914, 7.637863311827604029, -47.42536612906420856 ) ) ;
#30243=DIRECTION ( 'NONE',  ( 0.1024043820194936449, 0.5087173657443462282, 0.8548216096551014553 ) ) ;
#30245=B_SPLINE_CURVE_WITH_KNOTS ( 'NONE', 3,
 ( #12212, #50692, #26908, #21285 ),
 .UNSPECIFIED., .F., .F.,
 ( 4, 4 ),
 ( 6.254634441385501517E-18, 0.004566006591234648103 ),
 .UNSPECIFIED. ) ;
#30255=CARTESIAN_POINT ( 'NONE',  ( 4.549368137175248350, -28.46244473166650479, -32.13400537129916046 ) ) ;
#30257=VECTOR ( 'NONE', #16294, 1000.000000000000000 ) ;
#30259=EDGE_CURVE ( 'NONE', #17098, #21985, #61240, .T. ) ;
#30260=CARTESIAN_POINT ( 'NONE',  ( 0.6023143664670691511, 0.2618215695307587465, -48.10676742339276046 ) ) ;
#30261=ADVANCED_FACE ( 'NONE', ( #60084 ), #28260, .F. ) ;
#30262=CARTESIAN_POINT ( 'NONE',  ( 4.549368137175248350, -38.40568845698262379, -19.17571786012310753 ) ) ;
#30265=CARTESIAN_POINT ( 'NONE',  ( 2.301430502907645614, 1.287492012859394963, -48.01619648598872203 ) ) ;
#30269=CARTESIAN_POINT ( 'NONE',  ( -6.016761891674564211, -16.31696541414278911, 9.424569481870193499 ) ) ;
#30270=CARTESIAN_POINT ( 'NONE',  ( 0.5998501479064699549, 0.5236536531308225717, 48.10473956285920138 ) ) ;
#30271=CARTESIAN_POINT ( 'NONE',  ( 0.6254311100348659558, 41.31309618784381854, 24.64676532715809643 ) ) ;
#30278=CARTESIAN_POINT ( 'NONE',  ( 4.549368137175248350, -3.018832571116246477, -42.82045902618772004 ) ) ;
#30279=ORIENTED_EDGE ( 'NONE', *, *, #23218, .T. ) ;
#30281=CARTESIAN_POINT ( 'NONE',  ( 0.1073791018717578927, -0.4849339620936172768, 43.12183934961190346 ) ) ;
#30288=CARTESIAN_POINT ( 'NONE',  ( 0.1073791018717483448, 41.77800844988500018, 10.69234304550068337 ) ) ;
#30293=CARTESIAN_POINT ( 'NONE',  ( 0.2885697896453111588, 43.10898998017122352, 0.8047882042608043296 ) ) ;
#30299=CARTESIAN_POINT ( 'NONE',  ( 3.680882792899937250, 47.77138407787916918, 4.423598386734563626 ) ) ;
#30319=CARTESIAN_POINT ( 'NONE',  ( 1.827119703190780653, -41.88501940447986982, -9.946884032290961741 ) ) ;
#30322=ORIENTED_EDGE ( 'NONE', *, *, #27745, .F. ) ;
#30332=CARTESIAN_POINT ( 'NONE',  ( 0.3622758884714730732, -43.10531414739105571, 0.8252992914326598983 ) ) ;
#30333=CARTESIAN_POINT ( 'NONE',  ( 0.8760168074887076939, -46.22580377597795120, 13.30888447662000473 ) ) ;
#30337=CARTESIAN_POINT ( 'NONE',  ( 4.549368137175248350, 0.000000000000000000, 0.000000000000000000 ) ) ;
#30341=VECTOR ( 'NONE', #57500, 1000.000000000000114 ) ;
#30345=CARTESIAN_POINT ( 'NONE',  ( 0.3622758884714600280, -39.50828911766986096, -17.25816669464980890 ) ) ;
#30346=EDGE_CURVE ( 'NONE', #22109, #39562, #21605, .T. ) ;
#30347=CARTESIAN_POINT ( 'NONE',  ( 0.1073791018717578927, 37.10214135362858912, 21.98088480513677823 ) ) ;
#30351=ORIENTED_EDGE ( 'NONE', *, *, #61535, .F. ) ;
#30359=ORIENTED_EDGE ( 'NONE', *, *, #24821, .F. ) ;
#30360=FACE_OUTER_BOUND ( 'NONE', #45877, .T. ) ;
#30361=ORIENTED_EDGE ( 'NONE', *, *, #13814, .T. ) ;
#30363=ORIENTED_EDGE ( 'NONE', *, *, #34146, .F. ) ;
#30369=DIRECTION ( 'NONE',  ( 1.000000000000000000, 0.000000000000000000, 0.000000000000000000 ) ) ;
#30373=DIRECTION ( 'NONE',  ( -0.1024043820194934645, 0.8548216096550962373, 0.5087173657443551100 ) ) ;
#30375=CARTESIAN_POINT ( 'NONE',  ( 0.6030672727741701600, 23.97812608463474859, 41.70584815505896614 ) ) ;
#30377=CARTESIAN_POINT ( 'NONE',  ( 0.6001305935487422083, -46.33281397023054637, -12.95698906763792557 ) ) ;
#30380=AXIS2_PLACEMENT_3D ( 'NONE', #1729, #40004, #54343 ) ;
#30385=CARTESIAN_POINT ( 'NONE',  ( 4.975801465491695552, -2.564218696447830403, 47.84403947906839250 ) ) ;
#30393=CARTESIAN_POINT ( 'NONE',  ( 0.8751705887134553219, -38.69254731947813752, -28.56654290188640033 ) ) ;
#30395=CARTESIAN_POINT ( 'NONE',  ( 0.6254311100348639574, 44.17670535157486000, 19.04346769887709101 ) ) ;
#30405=CARTESIAN_POINT ( 'NONE',  ( 0.6254311100348624031, -42.00127298835437983, 23.45480814408353254 ) ) ;
#30406=CARTESIAN_POINT ( 'NONE',  ( 4.549368137175248350, 32.13400537129925283, -28.46244473166639111 ) ) ;
#30407=CARTESIAN_POINT ( 'NONE',  ( 0.3622758884714730732, 41.42293301073625855, -11.95365414648454205 ) ) ;
#30408=CARTESIAN_POINT ( 'NONE',  ( -6.015611763856276717, -11.47596948473801248, -14.94556629257436953 ) ) ;
#30418=EDGE_CURVE ( 'NONE', #5544, #29351, #22193, .T. ) ;
#30422=CARTESIAN_POINT ( 'NONE',  ( -2.708315649062910779, -2.171184472130790244, 14.47261168455365876 ) ) ;
#30431=VERTEX_POINT ( 'NONE', #33678 ) ;
#30432=CARTESIAN_POINT ( 'NONE',  ( 0.1073791018717578927, 10.69234304549997105, 41.77800844988518492 ) ) ;
#30433=ORIENTED_EDGE ( 'NONE', *, *, #9688, .T. ) ;
#30442=CARTESIAN_POINT ( 'NONE',  ( 0.8760168074887090262, 44.77533136581856610, 17.58183840866416503 ) ) ;
#30446=EDGE_LOOP ( 'NONE', ( #13391, #8308, #44267, #18709 ) ) ;
#30451=CARTESIAN_POINT ( 'NONE',  ( 4.975801465491694664, 31.15993731089074359, 36.39623109580477234 ) ) ;
#30458=ORIENTED_EDGE ( 'NONE', *, *, #46455, .T. ) ;
#30459=ORIENTED_EDGE ( 'NONE', *, *, #29958, .F. ) ;
#30460=CARTESIAN_POINT ( 'NONE',  ( 0.1073791018717578927, 16.05399293000759542, 40.02496097243063389 ) ) ;
#30461=CARTESIAN_POINT ( 'NONE',  ( 0.1102144999581333162, 34.13606714958013555, 26.35238362727852035 ) ) ;
#30463=DIRECTION ( 'NONE',  ( 0.09835009131224549395, 0.2500873580884707681, -0.9632152266566397225 ) ) ;
#30469=CARTESIAN_POINT ( 'NONE',  ( 0.1064266379913938187, -6.185137063632724974, -42.67882137217588934 ) ) ;
#30474=CARTESIAN_POINT ( 'NONE',  ( 0.5988103564986355654, 5.677495323490723500, -47.77151399983770830 ) ) ;
#30480=EDGE_CURVE ( 'NONE', #59613, #6804, #47797, .T. ) ;
#30489=CARTESIAN_POINT ( 'NONE',  ( -2.569797478183783568, 10.65947181927825582, 10.02484965418644869 ) ) ;
#30492=VERTEX_POINT ( 'NONE', #40247 ) ;
#30493=CARTESIAN_POINT ( 'NONE',  ( -2.569797478183783568, 12.89088113963426352, 6.924386868080891766 ) ) ;
#30494=CARTESIAN_POINT ( 'NONE',  ( 0.8760168074887076939, 33.37827814204125332, -34.63873394077453582 ) ) ;
#30496=ORIENTED_EDGE ( 'NONE', *, *, #45068, .F. ) ;
#30507=CARTESIAN_POINT ( 'NONE',  ( 0.7245667037590743931, -24.75815201345817584, -41.24129124474288233 ) ) ;
#30508=ORIENTED_EDGE ( 'NONE', *, *, #9688, .F. ) ;
#30509=EDGE_LOOP ( 'NONE', ( #21736, #16545, #28158, #14155 ) ) ;
#30511=CARTESIAN_POINT ( 'NONE',  ( 4.322998006666165516, -35.39923696759034044, 32.40067585697738650 ) ) ;
#30514=LINE ( 'NONE', #49324, #51494 ) ;
#30515=CARTESIAN_POINT ( 'NONE',  ( 1.827119703190779765, -42.82501615430328457, -4.394694966566333960 ) ) ;
#30518=EDGE_CURVE ( 'NONE', #2003, #44145, #30579, .T. ) ;
#30524=ADVANCED_FACE ( 'NONE', ( #20195 ), #21878, .F. ) ;
#30528=CARTESIAN_POINT ( 'NONE',  ( 0.8751705887134423323, -37.60752970653809513, -29.98056538504947710 ) ) ;
#30533=( BOUNDED_SURFACE ( )  B_SPLINE_SURFACE ( 3, 1, ( 
 ( #4538, #10198 ),
 ( #18678, #9260 ),
 ( #23674, #30511 ),
 ( #40278, #34942 ) ),
 .UNSPECIFIED., .F., .F., .F. ) 
 B_SPLINE_SURFACE_WITH_KNOTS ( ( 4, 4 ),
 ( 2, 2 ),
 ( 0.000000000000000000, 1.000000000000000000 ),
 ( 0.000000000000000000, 1.000000000000000000 ),
 .UNSPECIFIED. ) 
 GEOMETRIC_REPRESENTATION_ITEM ( )  RATIONAL_B_SPLINE_SURFACE ( (
 ( 1.000000000000000000, 1.000000000000000000),
 ( 0.7223157951917480446, 0.9931996967497186413),
 ( 0.7223157951917480446, 0.9931996967497186413),
 ( 1.000000000000000000, 1.000000000000000000) ) ) 
 REPRESENTATION_ITEM ( '' )  SURFACE ( )  );
#30534=EDGE_CURVE ( 'NONE', #19553, #2469, #5154, .T. ) ;
#30540=CARTESIAN_POINT ( 'NONE',  ( 0.6041374136657475802, 18.57118264377538353, -44.37863742124648780 ) ) ;
#30547=ADVANCED_FACE ( 'NONE', ( #16104 ), #28625, .F. ) ;
#30548=DIRECTION ( 'NONE',  ( 0.000000000000000000, 0.000000000000000000, 1.000000000000000000 ) ) ;
#30552=B_SPLINE_CURVE_WITH_KNOTS ( 'NONE', 3,
 ( #50054, #2103, #35667, #45076 ),
 .UNSPECIFIED., .F., .F.,
 ( 4, 4 ),
 ( 0.000000000000000000, 0.005014147105413693448 ),
 .UNSPECIFIED. ) ;
#30554=CARTESIAN_POINT ( 'NONE',  ( 4.975801465491694664, 35.64402118370912120, 32.01766832630325155 ) ) ;
#30555=CARTESIAN_POINT ( 'NONE',  ( -5.995132425357893702, 4.885449473615586236, -18.19985213254566858 ) ) ;
#30562=CARTESIAN_POINT ( 'NONE',  ( 0.6023143664670691511, 41.79259346737322289, -23.82663958122392955 ) ) ;
#30563=CARTESIAN_POINT ( 'NONE',  ( 0.5988103564986355654, -29.76496605343820434, -37.79415694022848271 ) ) ;
#30569=CARTESIAN_POINT ( 'NONE',  ( -6.016489644550737204, 0.004404229198039697445, -18.84320342686341121 ) ) ;
#30575=CARTESIAN_POINT ( 'NONE',  ( -6.017396004339686577, -14.94857180792001117, 11.47192209077581460 ) ) ;
#30576=VERTEX_POINT ( 'NONE', #27038 ) ;
#30577=ADVANCED_FACE ( 'NONE', ( #16718 ), #58607, .F. ) ;
#30579=B_SPLINE_CURVE_WITH_KNOTS ( 'NONE', 3,
 ( #24575, #756, #11101, #20800 ),
 .UNSPECIFIED., .F., .F.,
 ( 4, 4 ),
 ( 5.553824967135426632E-18, 0.004566006591234646368 ),
 .UNSPECIFIED. ) ;
#30587=ORIENTED_EDGE ( 'NONE', *, *, #19699, .T. ) ;
#30600=CARTESIAN_POINT ( 'NONE',  ( 0.6041374136657476912, 44.37863742124666544, -18.57118264377493588 ) ) ;
#30602=EDGE_CURVE ( 'NONE', #61648, #25122, #26229, .T. ) ;
#30613=CARTESIAN_POINT ( 'NONE',  ( 0.3622758884714730732, 15.73321244754854753, -40.13994584881767480 ) ) ;
#30619=CARTESIAN_POINT ( 'NONE',  ( 4.549368137175248350, 42.14271863032833920, -8.166781970325278195 ) ) ;
#30622=CARTESIAN_POINT ( 'NONE',  ( 0.1081432562775997697, 30.19275717928080738, 30.79166192943855407 ) ) ;
#30624=DIRECTION ( 'NONE',  ( 0.09835009131224567436, -0.8656670924898649533, 0.4908642831975215115 ) ) ;
#30637=( BOUNDED_SURFACE ( )  B_SPLINE_SURFACE ( 3, 1, ( 
 ( #21249, #44770 ),
 ( #49436, #21558 ),
 ( #6491, #25632 ),
 ( #40381, #1812 ) ),
 .UNSPECIFIED., .F., .F., .F. ) 
 B_SPLINE_SURFACE_WITH_KNOTS ( ( 4, 4 ),
 ( 2, 2 ),
 ( 0.000000000000000000, 1.000000000000000000 ),
 ( 0.000000000000000000, 1.000000000000000000 ),
 .UNSPECIFIED. ) 
 GEOMETRIC_REPRESENTATION_ITEM ( )  RATIONAL_B_SPLINE_SURFACE ( (
 ( 1.000000000000000000, 1.000000000000000000),
 ( 0.9953040768229013402, 0.8617119497784988535),
 ( 0.9953040768229013402, 0.8617119497784988535),
 ( 1.000000000000000000, 1.000000000000000000) ) ) 
 REPRESENTATION_ITEM ( '' )  SURFACE ( )  );
#30653=CARTESIAN_POINT ( 'NONE',  ( 0.1084644655670281843, 43.12277244437005663, -0.3976617192053908401 ) ) ;
#30657=CARTESIAN_POINT ( 'NONE',  ( 0.1104177457020373287, -41.65375561851293185, 11.16615714989236707 ) ) ;
#30658=CONICAL_SURFACE ( 'NONE', #17662, 42.92674063221959813, 1.485477209440487556 ) ;
#30672=CARTESIAN_POINT ( 'NONE',  ( 0.8751705887134553219, -47.79200036674276220, -5.393078191592532988 ) ) ;
#30673=EDGE_LOOP ( 'NONE', ( #23296, #15475, #47401, #27746 ) ) ;
#30675=CARTESIAN_POINT ( 'NONE',  ( 0.1100247026804066219, -26.11768802553221391, -34.31594964380173707 ) ) ;
#30682=EDGE_LOOP ( 'NONE', ( #1242, #54464, #49416, #47409 ) ) ;
#30685=CARTESIAN_POINT ( 'NONE',  ( 0.8751705887134553219, 34.63284514348538323, 33.37254303619566542 ) ) ;
#30687=LINE ( 'NONE', #39198, #21452 ) ;
#30690=EDGE_LOOP ( 'NONE', ( #16276, #47912, #17927, #34954 ) ) ;
#30691=EDGE_CURVE ( 'NONE', #7624, #22663, #46784, .T. ) ;
#30692=CARTESIAN_POINT ( 'NONE',  ( -6.016761891674565099, 18.20023637398599092, 4.880293656735028129 ) ) ;
#30697=DIRECTION ( 'NONE',  ( 0.09835009131224567436, -0.8579344853044309493, -0.5042575517176655087 ) ) ;
#30704=CARTESIAN_POINT ( 'NONE',  ( 0.6017667736363750963, -29.00830848931600769, -38.37782726569680847 ) ) ;
#30708=ORIENTED_EDGE ( 'NONE', *, *, #45481, .T. ) ;
#30709=CARTESIAN_POINT ( 'NONE',  ( -6.015611763856276717, -18.68284711750056815, -2.453375430804263235 ) ) ;
#30712=EDGE_CURVE ( 'NONE', #6250, #42579, #43260, .T. ) ;
#30713=CARTESIAN_POINT ( 'NONE',  ( 0.7246131072078545454, 44.12003537001153575, 19.16331062551101994 ) ) ;
#30724=CARTESIAN_POINT ( 'NONE',  ( 0.1073791018717578927, -0.4849339620936172768, 43.12183934961190346 ) ) ;
#30725=EDGE_CURVE ( 'NONE', #57516, #27042, #4126, .T. ) ;
#30732=FACE_OUTER_BOUND ( 'NONE', #40179, .T. ) ;
#30740=CIRCLE ( 'NONE', #43803, 47.91270532121795611 ) ;
#30749=CARTESIAN_POINT ( 'NONE',  ( 4.549368137175248350, -35.57418903283131328, 24.02461520945210793 ) ) ;
#30759=CARTESIAN_POINT ( 'NONE',  ( 0.1073791018717578927, 43.12183934961191056, 0.4849339620934667305 ) ) ;
#30765=CARTESIAN_POINT ( 'NONE',  ( 0.1097557419366048670, 41.71221507312532850, 10.94578341459284765 ) ) ;
#30767=B_SPLINE_CURVE_WITH_KNOTS ( 'NONE', 3,
 ( #24340, #29043, #53139, #52524, #513, #57206 ),
 .UNSPECIFIED., .F., .F.,
 ( 4, 2, 4 ),
 ( 2.224174099750402646E-17, 0.0002293319059085110925, 0.0004586638118169999046 ),
 .UNSPECIFIED. ) ;
#30769=EDGE_LOOP ( 'NONE', ( #47831, #12446, #27965, #7603 ) ) ;
#30776=CARTESIAN_POINT ( 'NONE',  ( 0.2224561200757568247, 15.79689521915808648, 40.12166550582818303 ) ) ;
#30777=CARTESIAN_POINT ( 'NONE',  ( 0.7954190325252786797, 28.58653703871157248, -38.68220061605139648 ) ) ;
#30778=CARTESIAN_POINT ( 'NONE',  ( -6.015611763856276717, 7.205255340944613174, 17.41126425312540249 ) ) ;
#30785=CARTESIAN_POINT ( 'NONE',  ( 0.6009453534118439633, 12.87216801774545338, -46.35353704332099767 ) ) ;
#30790=CARTESIAN_POINT ( 'NONE',  ( 0.8751705887134553219, 5.393078191592700854, -47.79200036674274088 ) ) ;
#30793=LINE ( 'NONE', #49914, #61643 ) ;
#30798=CARTESIAN_POINT ( 'NONE',  ( -6.015611763856276717, -18.68284711750060367, 2.453375430804002111 ) ) ;
#30802=CARTESIAN_POINT ( 'NONE',  ( -6.016104459813374383, -18.19977249352307425, -4.882138007282940784 ) ) ;
#30804=CARTESIAN_POINT ( 'NONE',  ( 4.975801465491695552, 43.22084481528192157, 20.67815041659156705 ) ) ;
#30809=CARTESIAN_POINT ( 'NONE',  ( -6.016489644550737204, -13.32727118274447342, 13.32104266208094678 ) ) ;
#30810=CARTESIAN_POINT ( 'NONE',  ( 0.6031357023905875581, 6.236038527293414013, 47.70157053127531555 ) ) ;
#30814=ORIENTED_EDGE ( 'NONE', *, *, #25454, .F. ) ;
#30819=CARTESIAN_POINT ( 'NONE',  ( 4.975801465491694664, -39.51822597168476392, -27.09127437476367106 ) ) ;
#30821=ORIENTED_EDGE ( 'NONE', *, *, #55723, .F. ) ;
#30827=EDGE_CURVE ( 'NONE', #868, #22443, #57402, .T. ) ;
#30834=CARTESIAN_POINT ( 'NONE',  ( 4.322998006666179727, 45.75942687572297984, -14.45630056002892161 ) ) ;
#30845=LINE ( 'NONE', #20536, #11498 ) ;
#30847=DIRECTION ( 'NONE',  ( 0.000000000000000000, 0.000000000000000000, -1.000000000000000000 ) ) ;
#30848=FACE_OUTER_BOUND ( 'NONE', #14510, .T. ) ;
#30852=CARTESIAN_POINT ( 'NONE',  ( 0.1097557419366048670, -42.72583172879057400, 5.849988371690356459 ) ) ;
#30853=CARTESIAN_POINT ( 'NONE',  ( 0.1313383488274134925, -22.11173226734867470, -37.02311703718843461 ) ) ;
#30860=CARTESIAN_POINT ( 'NONE',  ( 0.1081432562775997835, -41.54352569227153680, -11.56998286599521286 ) ) ;
#30871=CARTESIAN_POINT ( 'NONE',  ( 0.5998501479064699549, -28.86886762351154090, 38.48283596221978797 ) ) ;
#30883=CARTESIAN_POINT ( 'NONE',  ( 0.8751705887134423323, -7.160166390004656378, 47.55935879196458416 ) ) ;
#30889=CARTESIAN_POINT ( 'NONE',  ( 0.1095718737110177449, 41.72082389913616396, -10.91304379105019073 ) ) ;
#30898=CARTESIAN_POINT ( 'NONE',  ( 0.1087620492084204749, -39.70193592734194254, -16.83695155255820097 ) ) ;
#30902=CARTESIAN_POINT ( 'NONE',  ( 0.1103936448916694457, -6.269440624735986453E-17, 43.12443171339902648 ) ) ;
#30924=EDGE_CURVE ( 'NONE', #55224, #6250, #28246, .T. ) ;
#30925=CARTESIAN_POINT ( 'NONE',  ( 0.1310142868023686513, -30.94009702668495265, 30.03916697317163198 ) ) ;
#30927=ORIENTED_EDGE ( 'NONE', *, *, #7132, .F. ) ;
#30928=CARTESIAN_POINT ( 'NONE',  ( 3.680974057930773036, 40.59247216052818885, 25.57193971028174673 ) ) ;
#30931=CARTESIAN_POINT ( 'NONE',  ( -6.015611763856276717, 7.216738110653516891, -17.40650793417836439 ) ) ;
#30934=CARTESIAN_POINT ( 'NONE',  ( 0.2224561200757586565, -20.89867881469742628, -37.71651051365620333 ) ) ;
#30939=EDGE_CURVE ( 'NONE', #26668, #1954, #47674, .T. ) ;
#30943=CARTESIAN_POINT ( 'NONE',  ( 0.8751705887134553219, -37.60752970653848593, 29.98056538504896906 ) ) ;
#30952=CARTESIAN_POINT ( 'NONE',  ( 0.3622758884714600280, 42.62881903538200845, 6.444611261694737081 ) ) ;
#30960=DIRECTION ( 'NONE',  ( 0.09835009131224566048, -0.3879606369183696279, 0.9164135549743717135 ) ) ;
#30964=CARTESIAN_POINT ( 'NONE',  ( 0.2885700199627519447, -40.13549263616314988, -15.75356883787140028 ) ) ;
#30978=CARTESIAN_POINT ( 'NONE',  ( 0.1092565886968783900, 43.12345370280014833, -0.3103822814775415995 ) ) ;
#30983=ORIENTED_EDGE ( 'NONE', *, *, #11710, .T. ) ;
#30984=CARTESIAN_POINT ( 'NONE',  ( 2.301430502907646947, 30.25184447737433402, -37.31003439265377608 ) ) ;
#30992=CIRCLE ( 'NONE', #25984, 42.92674063221959813 ) ;
#30993=CARTESIAN_POINT ( 'NONE',  ( 0.6001305935487422083, 33.64689939321895196, 34.38748867424724409 ) ) ;
#30997=CARTESIAN_POINT ( 'NONE',  ( 4.549368137175248350, 0.000000000000000000, 0.000000000000000000 ) ) ;
#31002=VERTEX_POINT ( 'NONE', #13812 ) ;
#31009=CARTESIAN_POINT ( 'NONE',  ( 0.1104177457020373010, -16.49849172082188886, 39.84367193872649437 ) ) ;
#31011=ORIENTED_EDGE ( 'NONE', *, *, #28155, .T. ) ;
#31015=ORIENTED_EDGE ( 'NONE', *, *, #61142, .T. ) ;
#31018=CARTESIAN_POINT ( 'NONE',  ( 0.2224561200757660395, -33.74134531362616229, -26.84793396060971205 ) ) ;
#31032=( NAMED_UNIT ( * ) PLANE_ANGLE_UNIT ( ) SI_UNIT ( $, .RADIAN. ) );
#31033=CARTESIAN_POINT ( 'NONE',  ( 4.549368137175248350, -42.82045902618770583, -3.018832571116409014 ) ) ;
#31038=CARTESIAN_POINT ( 'NONE',  ( 0.3622758884714600280, -39.50828911766986096, -17.25816669464980890 ) ) ;
#31039=VECTOR ( 'NONE', #2567, 1000.000000000000114 ) ;
#31040=CARTESIAN_POINT ( 'NONE',  ( 0.1097557419366048670, 21.36873056345894284, -37.45792859959205856 ) ) ;
#31041=CARTESIAN_POINT ( 'NONE',  ( 4.975801465491694664, 15.94009207553051510, -45.18341283946441678 ) ) ;
#31046=B_SPLINE_CURVE_WITH_KNOTS ( 'NONE', 3,
 ( #55157, #16340, #2844, #16041 ),
 .UNSPECIFIED., .F., .F.,
 ( 4, 4 ),
 ( 2.302551629917872730E-17, 0.004564976165746188579 ),
 .UNSPECIFIED. ) ;
#31051=ORIENTED_EDGE ( 'NONE', *, *, #27497, .T. ) ;
#31053=CARTESIAN_POINT ( 'NONE',  ( 1.827326673878743923, -41.24690799101799854, -12.32830836993806578 ) ) ;
#31058=CARTESIAN_POINT ( 'NONE',  ( 0.5988103564986356764, 47.77151399983768698, 5.677495323490888701 ) ) ;
#31059=CARTESIAN_POINT ( 'NONE',  ( 4.833616638992205949, 14.43699082351650809, 43.93936707042104928 ) ) ;
#31060=CARTESIAN_POINT ( 'NONE',  ( 0.6029303876144825880, -12.32464004947847336, -46.50193792184020936 ) ) ;
#31063=B_SPLINE_CURVE_WITH_KNOTS ( 'NONE', 3,
 ( #58054, #38379, #5119, #24876 ),
 .UNSPECIFIED., .F., .F.,
 ( 4, 4 ),
 ( 0.000000000000000000, 0.005014147105413698652 ),
 .UNSPECIFIED. ) ;
#31064=CARTESIAN_POINT ( 'NONE',  ( -6.016104459813371719, 13.32794178584997624, 13.32039631884689257 ) ) ;
#31066=B_SPLINE_CURVE_WITH_KNOTS ( 'NONE', 3,
 ( #25543, #44679, #54331, #24942, #20854, #25237, #11456, #49653, #50575, #60274, #31168, #41521, #7030, #26783, #41214, #17388 ),
 .UNSPECIFIED., .F., .F.,
 ( 4, 3, 3, 3, 3, 4 ),
 ( 1.868480190406682863E-17, 0.0002618515315864419226, 0.0003927756766341999428, 0.0005236998216950559384, 0.0007855159896329862125, 0.001047349442285928738 ),
 .UNSPECIFIED. ) ;
#31067=ADVANCED_FACE ( 'NONE', ( #17885 ), #3006, .F. ) ;
#31072=EDGE_CURVE ( 'NONE', #14733, #46644, #14118, .T. ) ;
#31073=VERTEX_POINT ( 'NONE', #28489 ) ;
#31083=DIRECTION ( 'NONE',  ( -1.000000000000000000, -0.000000000000000000, -0.000000000000000000 ) ) ;
#31087=CARTESIAN_POINT ( 'NONE',  ( 0.1101816497532063233, 41.68997876247031797, 11.03018586750508945 ) ) ;
#31090=CARTESIAN_POINT ( 'NONE',  ( 0.7954196712028474003, -47.79303691884135219, 5.415566793624525310 ) ) ;
#31096=EDGE_LOOP ( 'NONE', ( #36030, #13830, #30041, #1690 ) ) ;
#31104=CARTESIAN_POINT ( 'NONE',  ( 0.8760168074887090262, 46.68716261866160266, 11.58706983520342426 ) ) ;
#31109=CARTESIAN_POINT ( 'NONE',  ( 0.5998501479064699549, -17.92509395669137362, 44.64337787626217846 ) ) ;
#31130=( BOUNDED_SURFACE ( )  B_SPLINE_SURFACE ( 3, 1, ( 
 ( #15366, #47637 ),
 ( #24127, #53542 ),
 ( #10660, #61698 ),
 ( #33862, #52937 ) ),
 .UNSPECIFIED., .F., .F., .F. ) 
 B_SPLINE_SURFACE_WITH_KNOTS ( ( 4, 4 ),
 ( 2, 2 ),
 ( 0.000000000000000000, 1.000000000000000000 ),
 ( 0.000000000000000000, 1.000000000000000000 ),
 .UNSPECIFIED. ) 
 GEOMETRIC_REPRESENTATION_ITEM ( )  RATIONAL_B_SPLINE_SURFACE ( (
 ( 1.000000000000000000, 1.000000000000000000),
 ( 0.7223157951917476005, 0.9931996967497186413),
 ( 0.7223157951917476005, 0.9931996967497186413),
 ( 1.000000000000000000, 1.000000000000000000) ) ) 
 REPRESENTATION_ITEM ( '' )  SURFACE ( )  );
#31131=B_SPLINE_CURVE_WITH_KNOTS ( 'NONE', 3,
 ( #33699, #52775, #9878, #48094, #24278, #43413 ),
 .UNSPECIFIED., .F., .F.,
 ( 4, 2, 4 ),
 ( 1.870559545977334001E-17, 0.0002293319059085097643, 0.0004586638118170008262 ),
 .UNSPECIFIED. ) ;
#31135=ORIENTED_EDGE ( 'NONE', *, *, #55572, .F. ) ;
#31149=ORIENTED_EDGE ( 'NONE', *, *, #13474, .T. ) ;
#31151=VECTOR ( 'NONE', #61637, 1000.000000000000114 ) ;
#31152=CARTESIAN_POINT ( 'NONE',  ( 0.6028618097248863439, 18.57111736963386051, 44.37846879336940731 ) ) ;
#31157=VERTEX_POINT ( 'NONE', #34452 ) ;
#31158=CARTESIAN_POINT ( 'NONE',  ( 0.1102144999581332607, 42.77179372778542898, -5.503895401229541129 ) ) ;
#31159=CARTESIAN_POINT ( 'NONE',  ( 0.2230388203127594560, -4.873876086128563934, 42.84312106681672816 ) ) ;
#31165=CARTESIAN_POINT ( 'NONE',  ( -6.016761891674565099, -0.003433883959915969616, 18.84319130225482297 ) ) ;
#31168=CARTESIAN_POINT ( 'NONE',  ( 0.6031356219577718170, -41.61861914321228539, 24.12932366310793952 ) ) ;
#31174=CARTESIAN_POINT ( 'NONE',  ( 0.6001305935487422083, -6.798494447611897584, -47.62765676940940551 ) ) ;
#31179=CARTESIAN_POINT ( 'NONE',  ( 2.643462169533613793, -11.09243630552565563, 46.73820883660187775 ) ) ;
#31180=DIRECTION ( 'NONE',  ( 0.000000000000000000, 0.000000000000000000, 1.000000000000000000 ) ) ;
#31185=DIRECTION ( 'NONE',  ( 0.09835009131224567436, 0.7941905447268818863, -0.5996571005210326044 ) ) ;
#31186=( BOUNDED_SURFACE ( )  B_SPLINE_SURFACE ( 3, 1, ( 
 ( #55959, #51559 ),
 ( #13077, #32173 ),
 ( #38744, #34338 ),
 ( #57799, #28695 ) ),
 .UNSPECIFIED., .F., .F., .F. ) 
 B_SPLINE_SURFACE_WITH_KNOTS ( ( 4, 4 ),
 ( 2, 2 ),
 ( 0.000000000000000000, 1.000000000000000000 ),
 ( 0.000000000000000000, 1.000000000000000000 ),
 .UNSPECIFIED. ) 
 GEOMETRIC_REPRESENTATION_ITEM ( )  RATIONAL_B_SPLINE_SURFACE ( (
 ( 1.000000000000000000, 1.000000000000000000),
 ( 0.7223157951917480446, 0.9931996967497186413),
 ( 0.7223157951917480446, 0.9931996967497186413),
 ( 1.000000000000000000, 1.000000000000000000) ) ) 
 REPRESENTATION_ITEM ( '' )  SURFACE ( )  );
#31187=CARTESIAN_POINT ( 'NONE',  ( 0.6028618097248863439, 41.57478760529404838, -24.20479143424847379 ) ) ;
#31189=CARTESIAN_POINT ( 'NONE',  ( 0.5998501479064708430, 0.5236536531314925913, -48.10473956285919428 ) ) ;
#31195=DIRECTION ( 'NONE',  ( -0.1024043820194934368, -0.9573600124648721232, -0.2701391291102888115 ) ) ;
#31197=ORIENTED_EDGE ( 'NONE', *, *, #37925, .T. ) ;
#31201=CARTESIAN_POINT ( 'NONE',  ( 0.1102144999581332607, 41.68747259405349581, -11.03964818279730586 ) ) ;
#31206=AXIS2_PLACEMENT_3D ( 'NONE', #46329, #28424, #8704 ) ;
#31207=ORIENTED_EDGE ( 'NONE', *, *, #30534, .T. ) ;
#31209=CARTESIAN_POINT ( 'NONE',  ( -6.016761891674564211, 7.214149619366359900, 17.40752468084784965 ) ) ;
#31217=CARTESIAN_POINT ( 'NONE',  ( 0.6254311100348644015, 0.6881768005102522068, -48.10157347124182792 ) ) ;
#31225=VERTEX_POINT ( 'NONE', #30345 ) ;
#31226=CARTESIAN_POINT ( 'NONE',  ( 0.6027935024548038978, -47.67281620606627968, -6.452291758824557633 ) ) ;
#31231=CARTESIAN_POINT ( 'NONE',  ( 0.1064266418746774578, -42.82540703015436634, 5.071708474752518292 ) ) ;
#31234=VERTEX_POINT ( 'NONE', #49458 ) ;
#31236=ORIENTED_EDGE ( 'NONE', *, *, #21019, .T. ) ;
#31238=CARTESIAN_POINT ( 'NONE',  ( 0.6254311100348637353, -17.77188277739589140, -44.70341307176148860 ) ) ;
#31250=EDGE_LOOP ( 'NONE', ( #15773, #59734, #13380, #26988 ) ) ;
#31255=CARTESIAN_POINT ( 'NONE',  ( 0.1095718737110177865, -5.374020908746645731, -42.78833451865665438 ) ) ;
#31257=CARTESIAN_POINT ( 'NONE',  ( 0.1064266379913938326, 41.79703901861803672, 10.61815631313376329 ) ) ;
#31265=CARTESIAN_POINT ( 'NONE',  ( -6.016761891674565099, -14.94721834528406923, -11.47373234755518823 ) ) ;
#31266=CARTESIAN_POINT ( 'NONE',  ( -6.016761891674564211, 18.68153697670645030, -2.462934516563616949 ) ) ;
#31267=CARTESIAN_POINT ( 'NONE',  ( 0.7245667037590759474, -47.57651946688182676, 7.091191019330059575 ) ) ;
#31271=CARTESIAN_POINT ( 'NONE',  ( 0.6001305935487422083, 48.10757715638247589, 0.5236757026890891398 ) ) ;
#31275=CARTESIAN_POINT ( 'NONE',  ( -6.010958268070873523, -17.40352239307062021, 7.224487401384238616 ) ) ;
#31277=EDGE_CURVE ( 'NONE', #25998, #35346, #14842, .T. ) ;
#31283=EDGE_LOOP ( 'NONE', ( #35148, #43916, #50789, #11814 ) ) ;
#31284=CARTESIAN_POINT ( 'NONE',  ( 0.1104177457020373010, 11.15670205480004640, -41.65628910360727843 ) ) ;
#31285=( BOUNDED_SURFACE ( )  B_SPLINE_SURFACE ( 3, 1, ( 
 ( #42481, #60937 ),
 ( #46248, #13349 ),
 ( #55925, #56847 ),
 ( #56234, #37471 ) ),
 .UNSPECIFIED., .F., .F., .F. ) 
 B_SPLINE_SURFACE_WITH_KNOTS ( ( 4, 4 ),
 ( 2, 2 ),
 ( 0.000000000000000000, 1.000000000000000000 ),
 ( 0.000000000000000000, 1.000000000000000000 ),
 .UNSPECIFIED. ) 
 GEOMETRIC_REPRESENTATION_ITEM ( )  RATIONAL_B_SPLINE_SURFACE ( (
 ( 1.000000000000000000, 1.000000000000000000),
 ( 0.7223157951917480446, 0.9931996967497186413),
 ( 0.7223157951917480446, 0.9931996967497186413),
 ( 1.000000000000000000, 1.000000000000000000) ) ) 
 REPRESENTATION_ITEM ( '' )  SURFACE ( )  );
#31289=ORIENTED_EDGE ( 'NONE', *, *, #56671, .F. ) ;
#31299=CARTESIAN_POINT ( 'NONE',  ( -6.017396004339686577, -13.32495836419615287, -13.32329839588568987 ) ) ;
#31312=CARTESIAN_POINT ( 'NONE',  ( -6.017396004339687465, 13.32329839588554954, 13.32495836419629320 ) ) ;
#31325=ORIENTED_EDGE ( 'NONE', *, *, #61732, .T. ) ;
#31328=EDGE_LOOP ( 'NONE', ( #44524, #30322, #35975, #20863 ) ) ;
#31329=CARTESIAN_POINT ( 'NONE',  ( 0.1103310638050662013, -42.74468893497613919, -5.710544932888772962 ) ) ;
#31348=CARTESIAN_POINT ( 'NONE',  ( 0.6254087463353915632, 46.28445368454755027, -13.11428234126315573 ) ) ;
#31349=CARTESIAN_POINT ( 'NONE',  ( 0.1092565886968785011, 21.29292791075586777, -37.50119754628587998 ) ) ;
#31353=B_SPLINE_CURVE_WITH_KNOTS ( 'NONE', 3,
 ( #39733, #58782, #9974, #11206, #30293, #6456 ),
 .UNSPECIFIED., .F., .F.,
 ( 4, 2, 4 ),
 ( 1.807478856737577690E-17, 0.0002293319059085095204, 0.0004586638118170009346 ),
 .UNSPECIFIED. ) ;
#31356=CIRCLE ( 'NONE', #60346, 47.91270532121795611 ) ;
#31364=EDGE_LOOP ( 'NONE', ( #43851, #59823, #40556, #52844 ) ) ;
#31368=CARTESIAN_POINT ( 'NONE',  ( 0.6025881611877910160, -12.24025891548890854, -46.52425620537265161 ) ) ;
#31371=EDGE_CURVE ( 'NONE', #32449, #55625, #59635, .T. ) ;
#31395=EDGE_LOOP ( 'NONE', ( #20309, #21200, #59075, #46417 ) ) ;
#31399=CARTESIAN_POINT ( 'NONE',  ( 0.5988103622719985752, -47.77151394450001476, 5.677495780220241706 ) ) ;
#31409=LINE ( 'NONE', #49573, #1897 ) ;
#31414=CARTESIAN_POINT ( 'NONE',  ( -6.016104459813374383, -14.95258000663140407, 11.46679299034574839 ) ) ;
#31417=CARTESIAN_POINT ( 'NONE',  ( 5.880360259849739535, -3.184717612777607787, -47.86623372148049071 ) ) ;
#31422=VECTOR ( 'NONE', #52668, 1000.000000000000114 ) ;
#31423=CARTESIAN_POINT ( 'NONE',  ( 0.6009453534118440743, -33.70725662590634641, -34.32439302680955961 ) ) ;
#31429=CARTESIAN_POINT ( 'NONE',  ( -6.017396004339686577, -18.68180398134251874, 2.460690056887720800 ) ) ;
#31434=LINE ( 'NONE', #59933, #48803 ) ;
#31437=CARTESIAN_POINT ( 'NONE',  ( 4.975801465491695552, 0.000000000000000000, 0.000000000000000000 ) ) ;
#31442=EDGE_LOOP ( 'NONE', ( #25428, #22835, #4018, #42279 ) ) ;
#31445=FACE_OUTER_BOUND ( 'NONE', #2147, .T. ) ;
#31449=CARTESIAN_POINT ( 'NONE',  ( 0.6254311100348637353, -19.04346769887721535, 44.17670535157478184 ) ) ;
#31451=CARTESIAN_POINT ( 'NONE',  ( 0.1100053167205930771, 21.71746606919056077, 37.25683392728340948 ) ) ;
#31456=ORIENTED_EDGE ( 'NONE', *, *, #4112, .T. ) ;
#31460=CARTESIAN_POINT ( 'NONE',  ( 0.5980894510889457338, -29.84264441023752212, -37.73932204245508615 ) ) ;
#31464=CARTESIAN_POINT ( 'NONE',  ( 0.6031356755773454870, 18.40994522247695286, 44.44547243635328471 ) ) ;
#31466=CARTESIAN_POINT ( 'NONE',  ( 0.8751705887134423323, 37.60752970653787486, 29.98056538504974000 ) ) ;
#31471=FACE_OUTER_BOUND ( 'NONE', #25668, .T. ) ;
#31473=CARTESIAN_POINT ( 'NONE',  ( -6.016489644550737204, -4.881234076340502881, 18.19999694163062642 ) ) ;
#31478=FACE_OUTER_BOUND ( 'NONE', #26663, .T. ) ;
#31493=CARTESIAN_POINT ( 'NONE',  ( 5.880360259849752858, 3.090325311464201530, 47.87242051977166568 ) ) ;
#31503=ORIENTED_EDGE ( 'NONE', *, *, #24821, .T. ) ;
#31509=CARTESIAN_POINT ( 'NONE',  ( 4.975801465491694664, 36.39623109580467997, -31.15993731089085017 ) ) ;
#31514=EDGE_CURVE ( 'NONE', #13235, #52485, #57286, .T. ) ;
#31518=CARTESIAN_POINT ( 'NONE',  ( 0.1081432562775999084, -39.67792926340389670, -16.89351827868208744 ) ) ;
#31528=ORIENTED_EDGE ( 'NONE', *, *, #13115, .F. ) ;
#31535=CARTESIAN_POINT ( 'NONE',  ( -6.015611763856276717, 7.205255340944613174, 17.41126425312540249 ) ) ;
#31537=ORIENTED_EDGE ( 'NONE', *, *, #16275, .F. ) ;
#31548=CARTESIAN_POINT ( 'NONE',  ( 0.1310142868023671248, -21.00772081177052897, -37.66054729763584419 ) ) ;
#31557=ORIENTED_EDGE ( 'NONE', *, *, #47041, .T. ) ;
#31558=CARTESIAN_POINT ( 'NONE',  ( 0.5998501479064708430, 33.64490850298796687, 34.38546660123309096 ) ) ;
#31561=B_SPLINE_CURVE_WITH_KNOTS ( 'NONE', 3,
 ( #54054, #30563, #15876, #2048, #7360, #50295 ),
 .UNSPECIFIED., .F., .F.,
 ( 4, 2, 4 ),
 ( 3.496446946337351263E-18, 0.0002450742804987350977, 0.0004901485609974667260 ),
 .UNSPECIFIED. ) ;
#31562=CARTESIAN_POINT ( 'NONE',  ( 0.3622758884714600280, -36.91764744403305087, -22.26738722580154217 ) ) ;
#31563=CARTESIAN_POINT ( 'NONE',  ( 0.8751705887134423323, -37.60752970653809513, -29.98056538504947710 ) ) ;
#31565=VERTEX_POINT ( 'NONE', #1147 ) ;
#31566=CARTESIAN_POINT ( 'NONE',  ( 4.549368137175248350, 13.59764261105693350, 40.71620287708348940 ) ) ;
#31576=CARTESIAN_POINT ( 'NONE',  ( 0.6001305935487315502, -47.76436356026972163, 5.760103278697207507 ) ) ;
#31578=CARTESIAN_POINT ( 'NONE',  ( -2.708315649062910779, -5.842990691604685871, 13.41752550814500822 ) ) ;
#31580=( BOUNDED_SURFACE ( )  B_SPLINE_SURFACE ( 3, 1, ( 
 ( #29975, #33462 ),
 ( #19666, #9957 ),
 ( #29053, #15583 ),
 ( #53456, #24355 ) ),
 .UNSPECIFIED., .F., .F., .F. ) 
 B_SPLINE_SURFACE_WITH_KNOTS ( ( 4, 4 ),
 ( 2, 2 ),
 ( 0.000000000000000000, 1.000000000000000000 ),
 ( 0.000000000000000000, 1.000000000000000000 ),
 .UNSPECIFIED. ) 
 GEOMETRIC_REPRESENTATION_ITEM ( )  RATIONAL_B_SPLINE_SURFACE ( (
 ( 1.000000000000000000, 1.000000000000000000),
 ( 0.7223157951917476005, 0.9931996967497186413),
 ( 0.7223157951917476005, 0.9931996967497186413),
 ( 1.000000000000000000, 1.000000000000000000) ) ) 
 REPRESENTATION_ITEM ( '' )  SURFACE ( )  );
#31584=CARTESIAN_POINT ( 'NONE',  ( 0.8760168074886960365, 44.77533136581880768, -17.58183840866353975 ) ) ;
#31585=B_SPLINE_CURVE_WITH_KNOTS ( 'NONE', 3,
 ( #42047, #12916, #26995, #32012 ),
 .UNSPECIFIED., .F., .F.,
 ( 4, 4 ),
 ( 0.000000000000000000, 0.005014147105413698652 ),
 .UNSPECIFIED. ) ;
#31587=CARTESIAN_POINT ( 'NONE',  ( -6.015611763856276717, -14.94556629257433578, 11.47596948473805689 ) ) ;
#31592=CARTESIAN_POINT ( 'NONE',  ( 0.1102847568649952675, 11.07236323260753252, -41.67876919128912050 ) ) ;
#31607=CARTESIAN_POINT ( 'NONE',  ( -6.001507490154111224, -18.84387066167321478, -0.01557731607573140456 ) ) ;
#31619=CARTESIAN_POINT ( 'NONE',  ( 2.643462169533613793, -1.382267876918128469, -48.01657676222237114 ) ) ;
#31631=ADVANCED_FACE ( 'NONE', ( #54067, #45031 ), #55305, .F. ) ;
#31632=DIRECTION ( 'NONE',  ( -1.000000000000000000, -0.000000000000000000, -0.000000000000000000 ) ) ;
#31635=EDGE_CURVE ( 'NONE', #58429, #22109, #56529, .T. ) ;
#31636=ORIENTED_EDGE ( 'NONE', *, *, #45193, .F. ) ;
#31638=CARTESIAN_POINT ( 'NONE',  ( 0.1100053167205930632, -21.71746606919081657, -37.25683392728325316 ) ) ;
#31642=CARTESIAN_POINT ( 'NONE',  ( 0.1100247026804066219, -42.73303500775683972, -5.797046384219709303 ) ) ;
#31643=LINE ( 'NONE', #22249, #14737 ) ;
#31647=CARTESIAN_POINT ( 'NONE',  ( -6.010958268070873523, -11.45964880703816746, -14.95835081545485679 ) ) ;
#31654=CARTESIAN_POINT ( 'NONE',  ( 0.1313383488274146305, 4.995828979989462404, -42.83318330237621296 ) ) ;
#31668=ORIENTED_EDGE ( 'NONE', *, *, #32904, .T. ) ;
#31672=EDGE_LOOP ( 'NONE', ( #18585, #12845, #26187, #1234 ) ) ;
#31673=ADVANCED_FACE ( 'NONE', ( #7695 ), #41107, .F. ) ;
#31674=( BOUNDED_SURFACE ( )  B_SPLINE_SURFACE ( 3, 1, ( 
 ( #58412, #15230 ),
 ( #14932, #24001 ),
 ( #57478, #1101 ),
 ( #20239, #165 ) ),
 .UNSPECIFIED., .F., .F., .F. ) 
 B_SPLINE_SURFACE_WITH_KNOTS ( ( 4, 4 ),
 ( 2, 2 ),
 ( 0.000000000000000000, 1.000000000000000000 ),
 ( 0.000000000000000000, 1.000000000000000000 ),
 .UNSPECIFIED. ) 
 GEOMETRIC_REPRESENTATION_ITEM ( )  RATIONAL_B_SPLINE_SURFACE ( (
 ( 1.000000000000000000, 1.000000000000000000),
 ( 0.7223157951917480446, 0.9931996967497186413),
 ( 0.7223157951917480446, 0.9931996967497186413),
 ( 1.000000000000000000, 1.000000000000000000) ) ) 
 REPRESENTATION_ITEM ( '' )  SURFACE ( )  );
#31680=VERTEX_POINT ( 'NONE', #7066 ) ;
#31683=CARTESIAN_POINT ( 'NONE',  ( 0.6001305935487315502, 34.38748867424666855, 33.64689939321954171 ) ) ;
#31688=CARTESIAN_POINT ( 'NONE',  ( 0.6030672727741701600, 29.21669544497198245, 38.21927534816993699 ) ) ;
#31689=EDGE_LOOP ( 'NONE', ( #48137, #52473, #23710, #23635 ) ) ;
#31710=VERTEX_POINT ( 'NONE', #50009 ) ;
#31711=CARTESIAN_POINT ( 'NONE',  ( 3.238931869106855377, -7.419701784410841938, -42.34694073502587486 ) ) ;
#31712=CARTESIAN_POINT ( 'NONE',  ( 0.1064266418746777076, -41.79703894102878081, 10.61815661559926660 ) ) ;
#31715=CARTESIAN_POINT ( 'NONE',  ( -6.016489644550736315, -4.881234076340246197, -18.19999694163069037 ) ) ;
#31717=CARTESIAN_POINT ( 'NONE',  ( 0.6031357023905874470, -41.64046004335399687, -24.09149424676601470 ) ) ;
#31720=B_SPLINE_CURVE_WITH_KNOTS ( 'NONE', 3,
 ( #58656, #43691, #733, #19872 ),
 .UNSPECIFIED., .F., .F.,
 ( 4, 4 ),
 ( 2.303004670188525934E-17, 0.004564976165746189446 ),
 .UNSPECIFIED. ) ;
#31726=CONICAL_SURFACE ( 'NONE', #51693, 42.92674063221959813, 1.485477209440487556 ) ;
#31742=CARTESIAN_POINT ( 'NONE',  ( 4.975801465491695552, 0.000000000000000000, 0.000000000000000000 ) ) ;
#31743=CARTESIAN_POINT ( 'NONE',  ( 0.6027935024548037868, 46.51312430684505728, -12.28245664247797819 ) ) ;
#31744=CARTESIAN_POINT ( 'NONE',  ( 4.549368137175248350, 42.84816078363930814, -2.596185425821480930 ) ) ;
#31757=B_SPLINE_CURVE_WITH_KNOTS ( 'NONE', 3,
 ( #61198, #56494, #46206, #31466 ),
 .UNSPECIFIED., .F., .F.,
 ( 4, 4 ),
 ( 0.000000000000000000, 0.004445488388166994251 ),
 .UNSPECIFIED. ) ;
#31764=EDGE_CURVE ( 'NONE', #61173, #22462, #23362, .T. ) ;
#31774=CARTESIAN_POINT ( 'NONE',  ( 0.1103872315293168010, 0.02583155086974350811, -43.12442619660166088 ) ) ;
#31775=ORIENTED_EDGE ( 'NONE', *, *, #20383, .F. ) ;
#31778=B_SPLINE_CURVE_WITH_KNOTS ( 'NONE', 3,
 ( #11706, #30785, #36139, #49905, #12326, #21398, #35826, #59913, #41149, #59598, #16707, #50513, #45532, #12029, #21707, #40848 ),
 .UNSPECIFIED., .F., .F.,
 ( 4, 3, 3, 3, 3, 4 ),
 ( 2.030557555191247372E-17, 0.0002618515315864389952, 0.0003927756766341964734, 0.0005236998216950555047, 0.0007855159896329897903, 0.001047349442285926569 ),
 .UNSPECIFIED. ) ;
#31782=CARTESIAN_POINT ( 'NONE',  ( 0.6030672727741701600, 34.07876014368860496, -33.95535904584750853 ) ) ;
#31784=CARTESIAN_POINT ( 'NONE',  ( -6.001507490154111224, 2.444174634178140071, 18.68469198366097572 ) ) ;
#31788=CARTESIAN_POINT ( 'NONE',  ( 0.1098349054025746507, 39.92296693299707044, -16.30574661324329711 ) ) ;
#31795=ORIENTED_EDGE ( 'NONE', *, *, #13247, .F. ) ;
#31809=CARTESIAN_POINT ( 'NONE',  ( 4.549368137175248350, -42.84816078363928682, -2.596185425821792236 ) ) ;
#31816=CARTESIAN_POINT ( 'NONE',  ( 0.8760168074887090262, 0.8912768426699538837, 48.09529047980637984 ) ) ;
#31817=CIRCLE ( 'NONE', #25812, 48.35291015139245019 ) ;
#31820=CARTESIAN_POINT ( 'NONE',  ( 4.975801465491694664, 2.564218696446817880, 47.84403947906844223 ) ) ;
#31832=CARTESIAN_POINT ( 'NONE',  ( 0.1101816497532063094, 5.494186916735715798, -42.77304337559937153 ) ) ;
#31833=ADVANCED_FACE ( 'NONE', ( #43100 ), #54213, .F. ) ;
#31836=EDGE_CURVE ( 'NONE', #59097, #23973, #28907, .T. ) ;
#31842=CARTESIAN_POINT ( 'NONE',  ( 0.6028618097248863439, 41.74935807801012544, 23.90242650600291086 ) ) ;
#31851=EDGE_CURVE ( 'NONE', #27614, #34543, #31131, .T. ) ;
#31871=CARTESIAN_POINT ( 'NONE',  ( 0.1103878639767399000, -26.21398130517543024, 34.24245495762976077 ) ) ;
#31876=ORIENTED_EDGE ( 'NONE', *, *, #3098, .T. ) ;
#31882=EDGE_LOOP ( 'NONE', ( #44744, #43492, #45418, #25015 ) ) ;
#31883=CARTESIAN_POINT ( 'NONE',  ( 0.1092355843206037486, 37.49628696754459867, -21.30139719602332349 ) ) ;
#31890=EDGE_CURVE ( 'NONE', #37253, #30061, #20299, .T. ) ;
#31893=CARTESIAN_POINT ( 'NONE',  ( 4.549368137175248350, 0.000000000000000000, 0.000000000000000000 ) ) ;
#31896=LINE ( 'NONE', #31578, #57602 ) ;
#31907=CARTESIAN_POINT ( 'NONE',  ( 0.1073791018717578927, 26.63563652260167203, -33.91564619577780348 ) ) ;
#31910=CARTESIAN_POINT ( 'NONE',  ( 0.1101816497532062955, 11.03018586750494556, -41.68997876247036771 ) ) ;
#31911=CARTESIAN_POINT ( 'NONE',  ( -6.015611763856276717, -11.46610900684733281, 14.95313250337425970 ) ) ;
#31934=VERTEX_POINT ( 'NONE', #57048 ) ;
#31940=DIRECTION ( 'NONE',  ( 0.09835009131224552170, -0.8579344853044379438, 0.5042575517176537403 ) ) ;
#31953=CARTESIAN_POINT ( 'NONE',  ( 0.2885697896453123246, -33.71073718007520625, -26.88157175352875683 ) ) ;
#31954=CARTESIAN_POINT ( 'NONE',  ( -6.015611763856276717, 2.453375430804336954, -18.68284711750055749 ) ) ;
#31962=CARTESIAN_POINT ( 'NONE',  ( 0.1073791018717578927, 40.02496097243057704, -16.05399293000775529 ) ) ;
#31963=FACE_OUTER_BOUND ( 'NONE', #51625, .T. ) ;
#31967=EDGE_CURVE ( 'NONE', #5629, #25496, #9490, .T. ) ;
#31968=CARTESIAN_POINT ( 'NONE',  ( 0.1313383488274141586, 39.59253935480796827, -17.09007684155463735 ) ) ;
#31970=ORIENTED_EDGE ( 'NONE', *, *, #2227, .T. ) ;
#31975=CARTESIAN_POINT ( 'NONE',  ( 0.1098349054025746507, 21.74670956129760668, -37.23978094195829414 ) ) ;
#31992=CARTESIAN_POINT ( 'NONE',  ( 2.643462169533600914, -11.09243630552500903, -46.73820883660201986 ) ) ;
#31997=ORIENTED_EDGE ( 'NONE', *, *, #1896, .T. ) ;
#32002=ORIENTED_EDGE ( 'NONE', *, *, #3684, .T. ) ;
#32009=B_SPLINE_CURVE_WITH_KNOTS ( 'NONE', 3,
 ( #59498, #48566, #11287, #53864, #44215, #39826, #44522, #30375, #53556, #49490, #6544, #34794, #58879, #10990, #15997, #30073 ),
 .UNSPECIFIED., .F., .F.,
 ( 4, 3, 3, 3, 3, 4 ),
 ( 1.868480190406682863E-17, 0.0002618515315864419226, 0.0003927756766341999970, 0.0005236998216950594079, 0.0007855159896329896819, 0.001047349442285925702 ),
 .UNSPECIFIED. ) ;
#32011=CARTESIAN_POINT ( 'NONE',  ( 2.301529144917016101, 28.20894756932140979, -38.87759814529788827 ) ) ;
#32012=CARTESIAN_POINT ( 'NONE',  ( 4.549368137175248350, 42.84816078363930814, -2.596185425821480930 ) ) ;
#32025=CARTESIAN_POINT ( 'NONE',  ( 0.2224561200757598778, -41.44719785461225570, -11.89200283918776435 ) ) ;
#32031=( BOUNDED_SURFACE ( )  B_SPLINE_SURFACE ( 3, 1, ( 
 ( #29131, #52618 ),
 ( #47942, #15671 ),
 ( #10969, #4991 ),
 ( #48855, #25053 ) ),
 .UNSPECIFIED., .F., .F., .F. ) 
 B_SPLINE_SURFACE_WITH_KNOTS ( ( 4, 4 ),
 ( 2, 2 ),
 ( 0.000000000000000000, 1.000000000000000000 ),
 ( 0.000000000000000000, 1.000000000000000000 ),
 .UNSPECIFIED. ) 
 GEOMETRIC_REPRESENTATION_ITEM ( )  RATIONAL_B_SPLINE_SURFACE ( (
 ( 1.000000000000000000, 1.000000000000000000),
 ( 0.9953040768229005630, 0.8617119497784937465),
 ( 0.9953040768229005630, 0.8617119497784937465),
 ( 1.000000000000000000, 1.000000000000000000) ) ) 
 REPRESENTATION_ITEM ( '' )  SURFACE ( )  );
#32033=CONICAL_SURFACE ( 'NONE', #22013, 42.92674063221959813, 1.485477209440487556 ) ;
#32047=EDGE_CURVE ( 'NONE', #35054, #19605, #57284, .T. ) ;
#32048=CARTESIAN_POINT ( 'NONE',  ( 4.833616638992205949, -43.64812679991108979, -15.29495699393711838 ) ) ;
#32054=CARTESIAN_POINT ( 'NONE',  ( 0.5980894510889457338, -38.59343625445427506, -28.72954109785590049 ) ) ;
#32066=CARTESIAN_POINT ( 'NONE',  ( 0.1073791018717578927, -0.4849339620936172768, 43.12183934961190346 ) ) ;
#32069=ORIENTED_EDGE ( 'NONE', *, *, #15091, .T. ) ;
#32071=CARTESIAN_POINT ( 'NONE',  ( 0.5998501479064699549, 6.798102206413494386, 47.62484632993690781 ) ) ;
#32082=ADVANCED_FACE ( 'NONE', ( #12705 ), #32671, .F. ) ;
#32089=ORIENTED_EDGE ( 'NONE', *, *, #59624, .T. ) ;
#32094=DIRECTION ( 'NONE',  ( 0.09835009131224564660, -0.6981896185982674474, -0.7091251765524044792 ) ) ;
#32099=CARTESIAN_POINT ( 'NONE',  ( 0.1102847568649952675, 39.80641842112245143, -16.58813073670667748 ) ) ;
#32102=CARTESIAN_POINT ( 'NONE',  ( -6.010958268070873523, 13.31406649671962761, 13.33459572764762591 ) ) ;
#32105=ORIENTED_EDGE ( 'NONE', *, *, #52324, .T. ) ;
#32107=DIRECTION ( 'NONE',  ( -1.000000000000000000, -0.000000000000000000, -0.000000000000000000 ) ) ;
#32112=AXIS2_PLACEMENT_3D ( 'NONE', #61817, #38372, #58043 ) ;
#32118=EDGE_CURVE ( 'NONE', #39207, #33948, #50430, .T. ) ;
#32125=CARTESIAN_POINT ( 'NONE',  ( 0.5980894510889448457, -37.73932204245498667, -29.84264441023765002 ) ) ;
#32128=CARTESIAN_POINT ( 'NONE',  ( -2.708315649062910779, 11.76894112707812212, -8.698422600177005748 ) ) ;
#32134=ORIENTED_EDGE ( 'NONE', *, *, #44014, .F. ) ;
#32138=CARTESIAN_POINT ( 'NONE',  ( 0.8760168074886960365, -17.58183840866369607, -44.77533136581875084 ) ) ;
#32139=CARTESIAN_POINT ( 'NONE',  ( 4.549368137175248350, 0.000000000000000000, 0.000000000000000000 ) ) ;
#32142=CARTESIAN_POINT ( 'NONE',  ( 0.5988103564986360094, -38.53259703935813718, -28.80261217992908129 ) ) ;
#32144=CARTESIAN_POINT ( 'NONE',  ( 0.6023143664670691511, -44.34466302085811407, -18.65155446683236562 ) ) ;
#32145=EDGE_LOOP ( 'NONE', ( #1291, #36107, #16531, #51414 ) ) ;
#32155=EDGE_CURVE ( 'NONE', #42216, #52728, #38675, .T. ) ;
#32160=ORIENTED_EDGE ( 'NONE', *, *, #32549, .F. ) ;
#32168=ORIENTED_EDGE ( 'NONE', *, *, #20841, .T. ) ;
#32169=CARTESIAN_POINT ( 'NONE',  ( -6.017396004339687465, -2.458362590802666947, -18.68211039806566376 ) ) ;
#32173=CARTESIAN_POINT ( 'NONE',  ( 2.643462169533600914, 46.02269433264213205, 13.76277278785576463 ) ) ;
#32176=ORIENTED_EDGE ( 'NONE', *, *, #56949, .T. ) ;
#32181=EDGE_CURVE ( 'NONE', #33708, #6988, #40040, .T. ) ;
#32182=ORIENTED_EDGE ( 'NONE', *, *, #35153, .F. ) ;
#32185=CARTESIAN_POINT ( 'NONE',  ( 0.6254311100348635133, -24.64676532715822077, 41.31309618784372617 ) ) ;
#32187=CARTESIAN_POINT ( 'NONE',  ( 4.975801465491695552, -9.906103548667894998, -46.87746200127453022 ) ) ;
#32189=EDGE_CURVE ( 'NONE', #32408, #46644, #40818, .T. ) ;
#32190=CARTESIAN_POINT ( 'NONE',  ( 0.1095718737110177865, 37.47471772507220322, -21.33933464366381116 ) ) ;
#32193=ORIENTED_EDGE ( 'NONE', *, *, #3170, .T. ) ;
#32202=CIRCLE ( 'NONE', #58150, 42.92674063221959813 ) ;
#32205=CARTESIAN_POINT ( 'NONE',  ( 0.6028618097248862329, 38.27229381545012643, 29.14732267129586418 ) ) ;
#32209=( BOUNDED_SURFACE ( )  B_SPLINE_SURFACE ( 3, 1, ( 
 ( #48618, #38032 ),
 ( #23898, #10419 ),
 ( #28895, #15121 ),
 ( #34539, #4751 ) ),
 .UNSPECIFIED., .F., .F., .F. ) 
 B_SPLINE_SURFACE_WITH_KNOTS ( ( 4, 4 ),
 ( 2, 2 ),
 ( 0.000000000000000000, 1.000000000000000000 ),
 ( 0.000000000000000000, 1.000000000000000000 ),
 .UNSPECIFIED. ) 
 GEOMETRIC_REPRESENTATION_ITEM ( )  RATIONAL_B_SPLINE_SURFACE ( (
 ( 1.000000000000000000, 1.000000000000000000),
 ( 0.9953040768229013402, 0.8617119497784988535),
 ( 0.9953040768229013402, 0.8617119497784988535),
 ( 1.000000000000000000, 1.000000000000000000) ) ) 
 REPRESENTATION_ITEM ( '' )  SURFACE ( )  );
#32213=B_SPLINE_CURVE_WITH_KNOTS ( 'NONE', 3,
 ( #40902, #4090, #59967, #55253, #27616, #37340 ),
 .UNSPECIFIED., .F., .F.,
 ( 4, 2, 4 ),
 ( 1.241905198432914574E-16, 0.0002450741128632342395, 0.0004901482257263442294 ),
 .UNSPECIFIED. ) ;
#32215=DIRECTION ( 'NONE',  ( 0.09835009131224552170, -0.007732607185423958154, -0.9951218349151971232 ) ) ;
#32220=CARTESIAN_POINT ( 'NONE',  ( 0.6031356219577718170, -38.11305734842083126, 29.35521383643393634 ) ) ;
#32223=CARTESIAN_POINT ( 'NONE',  ( 2.643462169533600914, 47.42536612906418725, 7.637863311827770119 ) ) ;
#32234=CARTESIAN_POINT ( 'NONE',  ( 0.1064266379913939853, 22.04679939086782525, 37.06314005629921127 ) ) ;
#32237=CARTESIAN_POINT ( 'NONE',  ( 0.1103310638050662290, 26.18709435931479845, 34.26302445194755109 ) ) ;
#32243=CARTESIAN_POINT ( 'NONE',  ( 3.680882792899938138, -42.44216617524801194, -22.36818923730755415 ) ) ;
#32246=VECTOR ( 'NONE', #3075, 1000.000000000000000 ) ;
#32250=CARTESIAN_POINT ( 'NONE',  ( -2.708315649062916552, -12.54007339125019982, 7.544341609839765539 ) ) ;
#32253=CARTESIAN_POINT ( 'NONE',  ( 0.1097557419366048670, -16.29667732266778302, 39.92664986079706324 ) ) ;
#32255=ORIENTED_EDGE ( 'NONE', *, *, #49707, .T. ) ;
#32260=VERTEX_POINT ( 'NONE', #54188 ) ;
#32269=EDGE_CURVE ( 'NONE', #27827, #4313, #49768, .T. ) ;
#32270=CARTESIAN_POINT ( 'NONE',  ( 4.322998006666179727, 30.86725474310310702, 36.74401119231420410 ) ) ;
#32276=CARTESIAN_POINT ( 'NONE',  ( 0.5998501479064708430, 37.84527566984816360, 29.69975237324626605 ) ) ;
#32278=CARTESIAN_POINT ( 'NONE',  ( 0.2885697896453117139, -39.51953439758099051, -17.24062360132701954 ) ) ;
#32280=CARTESIAN_POINT ( 'NONE',  ( 0.1100247026804066219, 21.70899701554524341, -37.26174279786191335 ) ) ;
#32292=CARTESIAN_POINT ( 'NONE',  ( 0.6001305935487315502, -41.40054608060309960, 24.50730504006385502 ) ) ;
#32293=ORIENTED_EDGE ( 'NONE', *, *, #7479, .F. ) ;
#32303=EDGE_CURVE ( 'NONE', #29097, #11449, #23580, .T. ) ;
#32306=CARTESIAN_POINT ( 'NONE',  ( 0.3622758884714730732, 0.8252992914322084816, 43.10531414739106282 ) ) ;
#32315=( BOUNDED_SURFACE ( )  B_SPLINE_SURFACE ( 3, 1, ( 
 ( #59824, #26940 ),
 ( #26313, #8130 ),
 ( #26621, #56042 ),
 ( #17542, #16617 ) ),
 .UNSPECIFIED., .F., .F., .F. ) 
 B_SPLINE_SURFACE_WITH_KNOTS ( ( 4, 4 ),
 ( 2, 2 ),
 ( 0.000000000000000000, 1.000000000000000000 ),
 ( 0.000000000000000000, 1.000000000000000000 ),
 .UNSPECIFIED. ) 
 GEOMETRIC_REPRESENTATION_ITEM ( )  RATIONAL_B_SPLINE_SURFACE ( (
 ( 1.000000000000000000, 1.000000000000000000),
 ( 0.9751682680413298332, 0.9999560080971552356),
 ( 0.9751682680413298332, 0.9999560080971552356),
 ( 1.000000000000000000, 1.000000000000000000) ) ) 
 REPRESENTATION_ITEM ( '' )  SURFACE ( )  );
#32320=CARTESIAN_POINT ( 'NONE',  ( 0.09136607875274982415, 0.000000000000000000, 43.12527911185304674 ) ) ;
#32326=B_SPLINE_CURVE_WITH_KNOTS ( 'NONE', 3,
 ( #54126, #7133, #11247, #48001 ),
 .UNSPECIFIED., .F., .F.,
 ( 4, 4 ),
 ( 0.000000000000000000, 0.005014147105413698652 ),
 .UNSPECIFIED. ) ;
#32330=VERTEX_POINT ( 'NONE', #1572 ) ;
#32343=CARTESIAN_POINT ( 'NONE',  ( -6.017396004339686577, 18.68180398134253650, -2.460690056887598232 ) ) ;
#32345=B_SPLINE_CURVE_WITH_KNOTS ( 'NONE', 3,
 ( #45589, #21151, #44670, #36195 ),
 .UNSPECIFIED., .F., .F.,
 ( 4, 4 ),
 ( 2.250920953359534068E-17, 0.004564976165746189446 ),
 .UNSPECIFIED. ) ;
#32352=CARTESIAN_POINT ( 'NONE',  ( -5.995132425357893702, 2.468096378288119563, 18.68182899165012500 ) ) ;
#32357=CARTESIAN_POINT ( 'NONE',  ( 0.1103310638050661874, -21.63353985999714624, 37.30561229499292608 ) ) ;
#32361=CARTESIAN_POINT ( 'NONE',  ( 3.680882792899937250, 46.78529781139673105, 10.62117075007664369 ) ) ;
#32363=CARTESIAN_POINT ( 'NONE',  ( 0.6009452777970410997, 46.35353542372322977, -12.87217382175445479 ) ) ;
#32367=CARTESIAN_POINT ( 'NONE',  ( 4.549368137175248350, -19.17571786012296187, -38.40568845698270195 ) ) ;
#32374=VECTOR ( 'NONE', #26560, 999.9999999999998863 ) ;
#32376=ORIENTED_EDGE ( 'NONE', *, *, #6664, .T. ) ;
#32382=EDGE_LOOP ( 'NONE', ( #19999, #41948, #58609, #16535, #369, #50387 ) ) ;
#32384=ORIENTED_EDGE ( 'NONE', *, *, #33394, .T. ) ;
#32385=CARTESIAN_POINT ( 'NONE',  ( -6.001507490154110336, 11.48377994779700728, 14.94036486426017341 ) ) ;
#32388=ADVANCED_FACE ( 'NONE', ( #44543 ), #4630, .F. ) ;
#32390=VERTEX_POINT ( 'NONE', #51351 ) ;
#32392=CARTESIAN_POINT ( 'NONE',  ( 0.1095718737110178420, 21.33933464366368682, 37.47471772507226717 ) ) ;
#32395=VERTEX_POINT ( 'NONE', #47287 ) ;
#32399=FACE_OUTER_BOUND ( 'NONE', #20901, .T. ) ;
#32400=CARTESIAN_POINT ( 'NONE',  ( 4.833616638992205949, 15.29495699393727293, -43.64812679991103295 ) ) ;
#32407=CARTESIAN_POINT ( 'NONE',  ( 0.8760168074887076939, 47.56749362999713782, -7.161346975773211554 ) ) ;
#32408=VERTEX_POINT ( 'NONE', #31962 ) ;
#32413=EDGE_CURVE ( 'NONE', #9792, #59574, #39248, .T. ) ;
#32421=FACE_OUTER_BOUND ( 'NONE', #46974, .T. ) ;
#32422=CARTESIAN_POINT ( 'NONE',  ( 0.1313383488274147970, -34.59671037481856359, -25.74310646082139442 ) ) ;
#32423=CARTESIAN_POINT ( 'NONE',  ( 0.3622758884714600280, 15.73321244754796666, 40.13994584881788086 ) ) ;
#32429=FACE_OUTER_BOUND ( 'NONE', #4522, .T. ) ;
#32435=CARTESIAN_POINT ( 'NONE',  ( 0.1100053167205930216, 42.77858932361496613, 5.450899213259652321 ) ) ;
#32439=CARTESIAN_POINT ( 'NONE',  ( 0.5998501479064699549, -46.60114184914309021, -11.94461217097453343 ) ) ;
#32443=CARTESIAN_POINT ( 'NONE',  ( 0.1103310638050662290, 39.81020119244058009, 16.57910240621655262 ) ) ;
#32448=CARTESIAN_POINT ( 'NONE',  ( 0.1087620492084206830, 5.987629195157810003, -42.70684898916390893 ) ) ;
#32449=VERTEX_POINT ( 'NONE', #4032 ) ;
#32465=ORIENTED_EDGE ( 'NONE', *, *, #60948, .T. ) ;
#32466=CARTESIAN_POINT ( 'NONE',  ( 0.6023143664670691511, -47.66103278671586452, -6.538774821499023560 ) ) ;
#32467=ADVANCED_FACE ( 'NONE', ( #42300 ), #50379, .F. ) ;
#32473=ORIENTED_EDGE ( 'NONE', *, *, #53168, .T. ) ;
#32478=ORIENTED_EDGE ( 'NONE', *, *, #35446, .T. ) ;
#32483=EDGE_CURVE ( 'NONE', #44510, #34393, #364, .T. ) ;
#32486=B_SPLINE_CURVE_WITH_KNOTS ( 'NONE', 3,
 ( #6843, #25981, #2142, #59477 ),
 .UNSPECIFIED., .F., .F.,
 ( 4, 4 ),
 ( 6.254634441385501517E-18, 0.004566006591234645501 ),
 .UNSPECIFIED. ) ;
#32495=CARTESIAN_POINT ( 'NONE',  ( 0.5998501479064708430, -24.50586714782633280, 41.39809967730445095 ) ) ;
#32496=VECTOR ( 'NONE', #57521, 1000.000000000000114 ) ;
#32498=B_SPLINE_CURVE_WITH_KNOTS ( 'NONE', 3,
 ( #18818, #27277, #46400, #60772, #17893, #37017 ),
 .UNSPECIFIED., .F., .F.,
 ( 4, 2, 4 ),
 ( 1.285010118223292934E-16, 0.0002450741128632324506, 0.0004901482257263364232 ),
 .UNSPECIFIED. ) ;
#32504=DIRECTION ( 'NONE',  ( -1.000000000000000000, 0.000000000000000000, 0.000000000000000000 ) ) ;
#32505=LINE ( 'NONE', #50663, #41380 ) ;
#32506=CARTESIAN_POINT ( 'NONE',  ( 4.975801465491695552, 45.55012473237732706, 14.85979367497190040 ) ) ;
#32516=CARTESIAN_POINT ( 'NONE',  ( 0.7246131072078548785, -44.12003537001164233, -19.16331062551070730 ) ) ;
#32519=ORIENTED_EDGE ( 'NONE', *, *, #44370, .F. ) ;
#32525=CARTESIAN_POINT ( 'NONE',  ( 0.7246131072078569879, -48.09507913767667020, -0.8205838906001429178 ) ) ;
#32530=CARTESIAN_POINT ( 'NONE',  ( -6.001507490154110336, -18.68469198366095085, -2.444174634178336358 ) ) ;
#32538=CARTESIAN_POINT ( 'NONE',  ( 0.5998501479064699549, 23.59887241503354716, -41.92175333043595487 ) ) ;
#32539=ORIENTED_EDGE ( 'NONE', *, *, #32483, .F. ) ;
#32540=B_SPLINE_CURVE_WITH_KNOTS ( 'NONE', 3,
 ( #60699, #36624, #55693, #46639, #41952, #56315, #17819, #12824, #3992, #46335, #23132, #36944, #18127, #37247, #13429, #32538 ),
 .UNSPECIFIED., .F., .F.,
 ( 4, 3, 3, 3, 3, 4 ),
 ( 1.868480190406682863E-17, 0.0002618515315864432236, 0.0003927756766342012438, 0.0005236998216950575647, 0.0007855159896329922840, 0.001047349442285927003 ),
 .UNSPECIFIED. ) ;
#32549=EDGE_CURVE ( 'NONE', #17351, #21388, #34808, .T. ) ;
#32558=VECTOR ( 'NONE', #54079, 1000.000000000000227 ) ;
#32559=ORIENTED_EDGE ( 'NONE', *, *, #10261, .F. ) ;
#32561=CARTESIAN_POINT ( 'NONE',  ( 4.975801465491694664, 46.87746200127440943, 9.906103548668390602 ) ) ;
#32565=CARTESIAN_POINT ( 'NONE',  ( 0.1087620492084205720, -16.83695155255859177, 39.70193592734176491 ) ) ;
#32571=AXIS2_PLACEMENT_3D ( 'NONE', #34499, #53567, #49504 ) ;
#32573=ORIENTED_EDGE ( 'NONE', *, *, #36719, .T. ) ;
#32574=CARTESIAN_POINT ( 'NONE',  ( 0.1092355843206037486, -21.30139719602345494, -37.49628696754451340 ) ) ;
#32575=CARTESIAN_POINT ( 'NONE',  ( -2.708315649062910779, 14.54141329178162323, -1.648584381066900306 ) ) ;
#32577=CARTESIAN_POINT ( 'NONE',  ( 0.1097557419366048670, -34.07666148910663395, 26.42915440612274125 ) ) ;
#32580=VERTEX_POINT ( 'NONE', #29710 ) ;
#32586=CARTESIAN_POINT ( 'NONE',  ( 0.5988103622719987973, -5.677495780220720434, -47.77151394449995792 ) ) ;
#32588=ORIENTED_EDGE ( 'NONE', *, *, #22149, .T. ) ;
#32590=CARTESIAN_POINT ( 'NONE',  ( 0.2230388203127614266, 4.873876086128248630, -42.84312106681679921 ) ) ;
#32592=CARTESIAN_POINT ( 'NONE',  ( 0.1098349054025746369, -16.30574661324343566, -39.92296693299701360 ) ) ;
#32598=ORIENTED_EDGE ( 'NONE', *, *, #56084, .T. ) ;
#32608=ADVANCED_FACE ( 'NONE', ( #47598 ), #24360, .F. ) ;
#32618=EDGE_CURVE ( 'NONE', #56342, #43333, #54423, .T. ) ;
#32619=VERTEX_POINT ( 'NONE', #20633 ) ;
#32626=CARTESIAN_POINT ( 'NONE',  ( 0.7954196712028469562, 48.09103417491925114, 0.8690072546827309896 ) ) ;
#32630=EDGE_CURVE ( 'NONE', #60778, #23902, #11552, .T. ) ;
#32639=CARTESIAN_POINT ( 'NONE',  ( 4.549368137175248350, 32.41327393324141326, -28.14399996863463116 ) ) ;
#32640=VERTEX_POINT ( 'NONE', #40085 ) ;
#32641=CARTESIAN_POINT ( 'NONE',  ( 0.8751705887134553219, -7.160166390003972481, -47.55935879196468363 ) ) ;
#32648=VECTOR ( 'NONE', #41192, 1000.000000000000000 ) ;
#32653=CARTESIAN_POINT ( 'NONE',  ( -5.995132425357893702, -17.41298668506975744, 7.203480333239017597 ) ) ;
#32668=CARTESIAN_POINT ( 'NONE',  ( 0.6001305935487422083, 29.70149728382386556, 37.84751346122865101 ) ) ;
#32669=CARTESIAN_POINT ( 'NONE',  ( -6.016761891674565099, 14.94721834528414917, 11.47373234755508342 ) ) ;
#32670=LINE ( 'NONE', #27647, #19750 ) ;
#32671=( BOUNDED_SURFACE ( )  B_SPLINE_SURFACE ( 3, 1, ( 
 ( #7653, #41522 ),
 ( #22702, #60584 ),
 ( #36827, #59982 ),
 ( #21782, #27396 ) ),
 .UNSPECIFIED., .F., .F., .F. ) 
 B_SPLINE_SURFACE_WITH_KNOTS ( ( 4, 4 ),
 ( 2, 2 ),
 ( 0.000000000000000000, 1.000000000000000000 ),
 ( 0.000000000000000000, 1.000000000000000000 ),
 .UNSPECIFIED. ) 
 GEOMETRIC_REPRESENTATION_ITEM ( )  RATIONAL_B_SPLINE_SURFACE ( (
 ( 1.000000000000000000, 1.000000000000000000),
 ( 0.7223157951917480446, 0.9931996967497186413),
 ( 0.7223157951917480446, 0.9931996967497186413),
 ( 1.000000000000000000, 1.000000000000000000) ) ) 
 REPRESENTATION_ITEM ( '' )  SURFACE ( )  );
#32677=CARTESIAN_POINT ( 'NONE',  ( 2.643462169533613793, -46.02269433264243048, 13.76277278785480540 ) ) ;
#32684=ORIENTED_EDGE ( 'NONE', *, *, #15884, .F. ) ;
#32686=CARTESIAN_POINT ( 'NONE',  ( 0.6031356755773454870, -38.16621646312189142, -29.28593560184418365 ) ) ;
#32690=CIRCLE ( 'NONE', #48686, 47.91270532121795611 ) ;
#32691=CARTESIAN_POINT ( 'NONE',  ( 4.833616638992208614, -8.578242093416086789, 45.44786513329582789 ) ) ;
#32695=VERTEX_POINT ( 'NONE', #25948 ) ;
#32697=ORIENTED_EDGE ( 'NONE', *, *, #50202, .T. ) ;
#32700=CARTESIAN_POINT ( 'NONE',  ( 0.1103310638050661874, -30.43528225250919661, -30.55179781597986732 ) ) ;
#32703=CYLINDRICAL_SURFACE ( 'NONE', #45003, 10.00000000000000000 ) ;
#32707=ORIENTED_EDGE ( 'NONE', *, *, #11110, .F. ) ;
#32713=ADVANCED_FACE ( 'NONE', ( #20941 ), #30637, .F. ) ;
#32714=VERTEX_POINT ( 'NONE', #59443 ) ;
#32731=CARTESIAN_POINT ( 'NONE',  ( -6.010958268070873523, -4.891065400978513722, 18.19761767765828608 ) ) ;
#32734=CARTESIAN_POINT ( 'NONE',  ( 4.691466044806102964, -14.01607102724513076, -42.32811009116549883 ) ) ;
#32741=CIRCLE ( 'NONE', #56720, 47.91270532121795611 ) ;
#32742=CARTESIAN_POINT ( 'NONE',  ( 0.6001305935487315502, 23.60027211631770427, 41.92422178329178450 ) ) ;
#32745=FACE_OUTER_BOUND ( 'NONE', #35164, .T. ) ;
#32752=AXIS2_PLACEMENT_3D ( 'NONE', #14197, #55, #13266 ) ;
#32753=CARTESIAN_POINT ( 'NONE',  ( 0.2224561200757612656, 6.380320192201981655, -42.64482917976813070 ) ) ;
#32761=ORIENTED_EDGE ( 'NONE', *, *, #23573, .F. ) ;
#32764=CARTESIAN_POINT ( 'NONE',  ( 0.6028618097248863439, -44.51207924874665167, -18.24855319618731286 ) ) ;
#32767=ORIENTED_EDGE ( 'NONE', *, *, #28790, .F. ) ;
#32775=CARTESIAN_POINT ( 'NONE',  ( 0.5988103564986361205, -17.84821699813511486, 44.67429521517301794 ) ) ;
#32783=VECTOR ( 'NONE', #17075, 1000.000000000000227 ) ;
#32784=ORIENTED_EDGE ( 'NONE', *, *, #21360, .F. ) ;
#32785=AXIS2_PLACEMENT_3D ( 'NONE', #14085, #61344, #14388 ) ;
#32798=EDGE_LOOP ( 'NONE', ( #1098, #15981, #42876, #36736 ) ) ;
#32799=CARTESIAN_POINT ( 'NONE',  ( 0.6041374136657475802, -18.24862627831505435, -44.51224464244992163 ) ) ;
#32811=CARTESIAN_POINT ( 'NONE',  ( 0.6017666602106490625, -29.56224131406243671, -37.95277954208626170 ) ) ;
#32814=CARTESIAN_POINT ( 'NONE',  ( 0.6029303876144825880, 47.71279573267359098, -6.149480157546095782 ) ) ;
#32817=CARTESIAN_POINT ( 'NONE',  ( -6.010958268070873523, -9.434296419346091866, -16.31164801516952068 ) ) ;
#32821=EDGE_CURVE ( 'NONE', #29080, #4682, #32505, .T. ) ;
#32829=CARTESIAN_POINT ( 'NONE',  ( 4.549368137175248350, -24.02461520945246320, -35.57418903283107880 ) ) ;
#32844=CARTESIAN_POINT ( 'NONE',  ( 0.8751705887134423323, -11.58504748649167837, -46.67919521768883584 ) ) ;
#32845=FACE_OUTER_BOUND ( 'NONE', #18790, .T. ) ;
#32855=ADVANCED_FACE ( 'NONE', ( #5503 ), #43482, .F. ) ;
#32858=CARTESIAN_POINT ( 'NONE',  ( 0.8751705887134553219, 7.160166390003662507, 47.55935879196473337 ) ) ;
#32859=AXIS2_PLACEMENT_3D ( 'NONE', #38752, #20250, #5186 ) ;
#32861=CARTESIAN_POINT ( 'NONE',  ( 0.6041374136657476912, -44.37863742124680044, 18.57118264377460903 ) ) ;
#32867=CARTESIAN_POINT ( 'NONE',  ( 0.3622758884714600280, 22.26738722580168073, -36.91764744403298693 ) ) ;
#32869=ORIENTED_EDGE ( 'NONE', *, *, #17688, .T. ) ;
#32871=VERTEX_POINT ( 'NONE', #19037 ) ;
#32873=( BOUNDED_SURFACE ( )  B_SPLINE_SURFACE ( 3, 1, ( 
 ( #19720, #38847 ),
 ( #57901, #15028 ),
 ( #34138, #29410 ),
 ( #34441, #48519 ) ),
 .UNSPECIFIED., .F., .F., .F. ) 
 B_SPLINE_SURFACE_WITH_KNOTS ( ( 4, 4 ),
 ( 2, 2 ),
 ( 0.000000000000000000, 1.000000000000000000 ),
 ( 0.000000000000000000, 1.000000000000000000 ),
 .UNSPECIFIED. ) 
 GEOMETRIC_REPRESENTATION_ITEM ( )  RATIONAL_B_SPLINE_SURFACE ( (
 ( 1.000000000000000000, 1.000000000000000000),
 ( 0.9953040768229013402, 0.8617119497784988535),
 ( 0.9953040768229013402, 0.8617119497784988535),
 ( 1.000000000000000000, 1.000000000000000000) ) ) 
 REPRESENTATION_ITEM ( '' )  SURFACE ( )  );
#32876=ORIENTED_EDGE ( 'NONE', *, *, #43963, .F. ) ;
#32878=CARTESIAN_POINT ( 'NONE',  ( 0.6009453534118439633, -34.32439302680990778, 33.70725662590598404 ) ) ;
#32880=CIRCLE ( 'NONE', #20831, 42.92674063221959813 ) ;
#32890=CARTESIAN_POINT ( 'NONE',  ( 0.1073791018717578927, -21.14095454447534550, -37.58707531572198235 ) ) ;
#32891=CARTESIAN_POINT ( 'NONE',  ( 4.975801465491695552, 15.94009207552985252, 45.18341283946464415 ) ) ;
#32895=EDGE_CURVE ( 'NONE', #7638, #38559, #43690, .T. ) ;
#32896=DIRECTION ( 'NONE',  ( 1.000000000000000000, 0.000000000000000000, 0.000000000000000000 ) ) ;
#32904=EDGE_CURVE ( 'NONE', #60819, #30020, #186, .T. ) ;
#32908=CONICAL_SURFACE ( 'NONE', #59755, 42.92674063221959813, 1.485477209440487556 ) ;
#32929=CARTESIAN_POINT ( 'NONE',  ( -6.015611763856276717, 2.465697960551047618, 18.68122482568280773 ) ) ;
#32930=VERTEX_POINT ( 'NONE', #34061 ) ;
#32933=EDGE_LOOP ( 'NONE', ( #19668, #14378, #57802, #46660 ) ) ;
#32936=CARTESIAN_POINT ( 'NONE',  ( 0.1313383488274144917, 40.08066228784242924, 15.91164383651759806 ) ) ;
#32939=ORIENTED_EDGE ( 'NONE', *, *, #15238, .T. ) ;
#32943=CARTESIAN_POINT ( 'NONE',  ( 0.5988103622719989083, 48.10388392585941375, 0.6065097949915312370 ) ) ;
#32966=( BOUNDED_SURFACE ( )  B_SPLINE_SURFACE ( 3, 1, ( 
 ( #49715, #41269 ),
 ( #21835, #59724 ),
 ( #35330, #2079 ),
 ( #31535, #45972 ) ),
 .UNSPECIFIED., .F., .F., .F. ) 
 B_SPLINE_SURFACE_WITH_KNOTS ( ( 4, 4 ),
 ( 2, 2 ),
 ( 0.000000000000000000, 1.000000000000000000 ),
 ( 0.000000000000000000, 1.000000000000000000 ),
 .UNSPECIFIED. ) 
 GEOMETRIC_REPRESENTATION_ITEM ( )  RATIONAL_B_SPLINE_SURFACE ( (
 ( 1.000000000000000000, 1.000000000000000000),
 ( 0.7223157951917476005, 0.9931996967497186413),
 ( 0.7223157951917476005, 0.9931996967497186413),
 ( 1.000000000000000000, 1.000000000000000000) ) ) 
 REPRESENTATION_ITEM ( '' )  SURFACE ( )  );
#32969=CARTESIAN_POINT ( 'NONE',  ( 1.827326673878743257, -40.22837085190322881, 15.32882202537205707 ) ) ;
#32973=EDGE_CURVE ( 'NONE', #43495, #52417, #16172, .T. ) ;
#32977=ADVANCED_FACE ( 'NONE', ( #25865 ), #21405, .F. ) ;
#32979=ADVANCED_FACE ( 'NONE', ( #11165 ), #34437, .T. ) ;
#32982=CARTESIAN_POINT ( 'NONE',  ( 4.975801465491695552, -36.39623109580445259, -31.15993731089111662 ) ) ;
#32984=CARTESIAN_POINT ( 'NONE',  ( 0.1104177457020373149, -21.55798761925413842, 37.34931850022132238 ) ) ;
#32987=CARTESIAN_POINT ( 'NONE',  ( 4.975801465491695552, 0.000000000000000000, 0.000000000000000000 ) ) ;
#32988=CARTESIAN_POINT ( 'NONE',  ( 0.8760168074886965917, -41.20610493656892714, -24.81951362746064049 ) ) ;
#32995=CARTESIAN_POINT ( 'NONE',  ( -6.010958268070873523, 18.20513189769815554, -4.863021950010456784 ) ) ;
#32997=ORIENTED_EDGE ( 'NONE', *, *, #38549, .F. ) ;
#32998=EDGE_CURVE ( 'NONE', #5623, #21984, #34984, .T. ) ;
#33002=ORIENTED_EDGE ( 'NONE', *, *, #13147, .T. ) ;
#33003=VERTEX_POINT ( 'NONE', #35600 ) ;
#33005=ORIENTED_EDGE ( 'NONE', *, *, #14169, .F. ) ;
#33016=ORIENTED_EDGE ( 'NONE', *, *, #12127, .F. ) ;
#33018=B_SPLINE_CURVE_WITH_KNOTS ( 'NONE', 3,
 ( #25878, #3902, #8294, #32753, #22413, #12727 ),
 .UNSPECIFIED., .F., .F.,
 ( 4, 2, 4 ),
 ( 1.736958732247374613E-17, 0.0002293319059085092493, 0.0004586638118170010972 ),
 .UNSPECIFIED. ) ;
#33019=ADVANCED_FACE ( 'NONE', ( #6413 ), #13838, .F. ) ;
#33021=ORIENTED_EDGE ( 'NONE', *, *, #28147, .F. ) ;
#33023=CARTESIAN_POINT ( 'NONE',  ( 0.7048096507298579061, -29.95256433478753877, 37.64898672361901077 ) ) ;
#33026=CARTESIAN_POINT ( 'NONE',  ( 0.2885700199627507789, 41.43179222486418922, -11.93479339212623636 ) ) ;
#33029=CARTESIAN_POINT ( 'NONE',  ( 0.1104177457020373149, 5.633723015004302503, 42.75487793940126124 ) ) ;
#33043=CARTESIAN_POINT ( 'NONE',  ( -6.016761891674565099, 14.95139917749719949, -11.46828378093544210 ) ) ;
#33059=CARTESIAN_POINT ( 'NONE',  ( -6.016489644550736315, -9.425415887800975057, -16.31649074174286795 ) ) ;
#33067=VECTOR ( 'NONE', #10497, 1000.000000000000227 ) ;
#33069=CARTESIAN_POINT ( 'NONE',  ( 4.549368137175248350, 42.14271863032822552, 8.166781970325878603 ) ) ;
#33071=CARTESIAN_POINT ( 'NONE',  ( 3.680974057930773924, 4.423547572561673746, 47.77138393978997755 ) ) ;
#33074=VECTOR ( 'NONE', #51744, 1000.000000000000114 ) ;
#33093=CIRCLE ( 'NONE', #3900, 47.91270532121795611 ) ;
#33094=CARTESIAN_POINT ( 'NONE',  ( 0.8760168074887090262, 23.27577685234598448, -42.09738177923931346 ) ) ;
#33105=CARTESIAN_POINT ( 'NONE',  ( 0.6041374136657475802, 6.106202762792853456, 47.71861871402591504 ) ) ;
#33107=VERTEX_POINT ( 'NONE', #42163 ) ;
#33122=CARTESIAN_POINT ( 'NONE',  ( 0.3622758884714730732, 10.35929834645922831, -41.85013935980092015 ) ) ;
#33123=CARTESIAN_POINT ( 'NONE',  ( 0.1104177457020372594, 16.49849172082163662, -39.84367193872661517 ) ) ;
#33134=CARTESIAN_POINT ( 'NONE',  ( 4.549368137175248350, 0.000000000000000000, 0.000000000000000000 ) ) ;
#33135=CARTESIAN_POINT ( 'NONE',  ( -6.016489644550737204, 4.881234076340629890, -18.19999694163059090 ) ) ;
#33139=CARTESIAN_POINT ( 'NONE',  ( -6.001507490154110336, 18.19774963328914907, -4.892199142591112881 ) ) ;
#33141=CARTESIAN_POINT ( 'NONE',  ( 0.1073791018717578927, 21.98088480513665388, -37.10214135362866728 ) ) ;
#33163=CARTESIAN_POINT ( 'NONE',  ( -6.016489644550736315, 7.206912786933527215, -17.41053539857192334 ) ) ;
#33175=ORIENTED_EDGE ( 'NONE', *, *, #32181, .T. ) ;
#33177=ORIENTED_EDGE ( 'NONE', *, *, #24991, .F. ) ;
#33182=B_SPLINE_CURVE_WITH_KNOTS ( 'NONE', 3,
 ( #54712, #30928, #34716, #53779 ),
 .UNSPECIFIED., .F., .F.,
 ( 4, 4 ),
 ( 0.000000000000000000, 0.004445488388166993383 ),
 .UNSPECIFIED. ) ;
#33183=CARTESIAN_POINT ( 'NONE',  ( 0.1092355843206037486, -16.78033551728689687, 39.72582785521888837 ) ) ;
#33185=VERTEX_POINT ( 'NONE', #51506 ) ;
#33191=ORIENTED_EDGE ( 'NONE', *, *, #41972, .T. ) ;
#33196=CARTESIAN_POINT ( 'NONE',  ( 0.2224561200757623480, -42.64482917976811649, -6.380320192201828000 ) ) ;
#33201=ADVANCED_FACE ( 'NONE', ( #17710 ), #60262, .F. ) ;
#33203=CARTESIAN_POINT ( 'NONE',  ( -6.015611763856276717, -14.95313250337422062, -11.46610900684738432 ) ) ;
#33213=CARTESIAN_POINT ( 'NONE',  ( -5.995132425357893702, -9.414704407577920264, 16.32377331145317712 ) ) ;
#33214=CARTESIAN_POINT ( 'NONE',  ( 0.1092355843206037486, -16.22491322981600348, -39.95589129953361152 ) ) ;
#33223=B_SPLINE_CURVE_WITH_KNOTS ( 'NONE', 3,
 ( #12838, #51016, #34101, #29677 ),
 .UNSPECIFIED., .F., .F.,
 ( 4, 4 ),
 ( 0.000000000000000000, 0.005014147105413711662 ),
 .UNSPECIFIED. ) ;
#33227=ORIENTED_EDGE ( 'NONE', *, *, #25597, .T. ) ;
#33232=( BOUNDED_SURFACE ( )  B_SPLINE_SURFACE ( 3, 1, ( 
 ( #56117, #50806 ),
 ( #55190, #23240 ),
 ( #3188, #13540 ),
 ( #56424, #41138 ) ),
 .UNSPECIFIED., .F., .F., .F. ) 
 B_SPLINE_SURFACE_WITH_KNOTS ( ( 4, 4 ),
 ( 2, 2 ),
 ( 0.000000000000000000, 1.000000000000000000 ),
 ( 0.000000000000000000, 1.000000000000000000 ),
 .UNSPECIFIED. ) 
 GEOMETRIC_REPRESENTATION_ITEM ( )  RATIONAL_B_SPLINE_SURFACE ( (
 ( 1.000000000000000000, 1.000000000000000000),
 ( 0.9953040768229013402, 0.8617119497784988535),
 ( 0.9953040768229013402, 0.8617119497784988535),
 ( 1.000000000000000000, 1.000000000000000000) ) ) 
 REPRESENTATION_ITEM ( '' )  SURFACE ( )  );
#33240=ORIENTED_EDGE ( 'NONE', *, *, #21171, .F. ) ;
#33244=CARTESIAN_POINT ( 'NONE',  ( 2.643462169533600914, -43.83256147628719646, -19.65219740572174345 ) ) ;
#33245=EDGE_CURVE ( 'NONE', #33948, #31234, #19059, .T. ) ;
#33247=CARTESIAN_POINT ( 'NONE',  ( -6.015611763856276717, 4.870987357968176390, 18.20278301740938431 ) ) ;
#33251=CARTESIAN_POINT ( 'NONE',  ( 0.6029303876144825880, -38.24575311130019628, 29.18200390283984191 ) ) ;
#33260=LINE ( 'NONE', #57628, #4654 ) ;
#33267=CARTESIAN_POINT ( 'NONE',  ( 0.5980894510889448457, -46.28687279963683920, -13.12879507229272136 ) ) ;
#33280=AXIS2_PLACEMENT_3D ( 'NONE', #3440, #17267, #45177 ) ;
#33287=CARTESIAN_POINT ( 'NONE',  ( 4.691466044806103852, -33.74235639413308263, -29.14742760351097672 ) ) ;
#33294=EDGE_CURVE ( 'NONE', #52389, #37253, #18148, .T. ) ;
#33297=CARTESIAN_POINT ( 'NONE',  ( 0.8751705887134423323, 11.58504748649134974, 46.67919521768892110 ) ) ;
#33301=CARTESIAN_POINT ( 'NONE',  ( 0.09136607875274982415, 0.000000000000000000, 0.000000000000000000 ) ) ;
#33302=CARTESIAN_POINT ( 'NONE',  ( 2.301430502907646058, -33.04218380901196639, -34.86297247504463570 ) ) ;
#33308=CARTESIAN_POINT ( 'NONE',  ( 0.6009452777970414328, -38.43042656245054900, -28.93864923253884669 ) ) ;
#33309=( BOUNDED_SURFACE ( )  B_SPLINE_SURFACE ( 3, 1, ( 
 ( #60153, #13805 ),
 ( #27572, #46702 ),
 ( #55449, #56993 ),
 ( #10322, #14116 ) ),
 .UNSPECIFIED., .F., .F., .F. ) 
 B_SPLINE_SURFACE_WITH_KNOTS ( ( 4, 4 ),
 ( 2, 2 ),
 ( 0.000000000000000000, 1.000000000000000000 ),
 ( 0.000000000000000000, 1.000000000000000000 ),
 .UNSPECIFIED. ) 
 GEOMETRIC_REPRESENTATION_ITEM ( )  RATIONAL_B_SPLINE_SURFACE ( (
 ( 1.000000000000000000, 1.000000000000000000),
 ( 0.7223157951917480446, 0.9931996967497186413),
 ( 0.7223157951917480446, 0.9931996967497186413),
 ( 1.000000000000000000, 1.000000000000000000) ) ) 
 REPRESENTATION_ITEM ( '' )  SURFACE ( )  );
#33325=CARTESIAN_POINT ( 'NONE',  ( 0.8751705887134553219, -44.76769609654225235, -17.57879340691528469 ) ) ;
#33331=CARTESIAN_POINT ( 'NONE',  ( 0.8760168074886965917, -38.69913431881842314, 28.57146030081914390 ) ) ;
#33334=FACE_OUTER_BOUND ( 'NONE', #11304, .T. ) ;
#33352=CARTESIAN_POINT ( 'NONE',  ( 0.5980894510889457338, -37.73932204245538458, 29.84264441023714198 ) ) ;
#33354=CARTESIAN_POINT ( 'NONE',  ( 0.7048096507298635682, -24.78213711671570607, -41.23648859290917557 ) ) ;
#33355=LINE ( 'NONE', #42447, #42589 ) ;
#33363=ORIENTED_EDGE ( 'NONE', *, *, #39926, .T. ) ;
#33365=CARTESIAN_POINT ( 'NONE',  ( 0.1073791018717578927, -33.91564619577789585, -26.63563652260155123 ) ) ;
#33366=CARTESIAN_POINT ( 'NONE',  ( 0.5980894510889448457, 29.84264441023778502, -37.73932204245488720 ) ) ;
#33368=AXIS2_PLACEMENT_3D ( 'NONE', #13792, #32896, #28170 ) ;
#33369=CARTESIAN_POINT ( 'NONE',  ( 0.1073791018717578927, 42.68962945260945929, 6.109314776652849943 ) ) ;
#33372=DIRECTION ( 'NONE',  ( 0.1024043820194936449, -0.6159418278945547609, -0.7811075516170102873 ) ) ;
#33378=ORIENTED_EDGE ( 'NONE', *, *, #26320, .F. ) ;
#33380=CARTESIAN_POINT ( 'NONE',  ( 0.1081432562775997003, 39.67792926340376880, 16.89351827868236100 ) ) ;
#33385=CARTESIAN_POINT ( 'NONE',  ( 4.549368137175248350, -3.018832571116875751, 42.82045902618767030 ) ) ;
#33393=CARTESIAN_POINT ( 'NONE',  ( -6.016761891674565099, -7.207804629151182141, -17.41015286184810407 ) ) ;
#33394=EDGE_CURVE ( 'NONE', #40478, #46978, #34561, .T. ) ;
#33397=ORIENTED_EDGE ( 'NONE', *, *, #16994, .T. ) ;
#33398=CARTESIAN_POINT ( 'NONE',  ( 0.8751705887134553219, 23.27176129838425922, -42.09020928323351995 ) ) ;
#33409=CARTESIAN_POINT ( 'NONE',  ( -6.016489644550737204, -11.47450955518498361, 14.94663725562912049 ) ) ;
#33411=CARTESIAN_POINT ( 'NONE',  ( 0.6001305935487422083, 5.760103278697394025, 47.76436356026970032 ) ) ;
#33413=ORIENTED_EDGE ( 'NONE', *, *, #32895, .F. ) ;
#33419=VERTEX_POINT ( 'NONE', #30170 ) ;
#33426=VERTEX_POINT ( 'NONE', #46460 ) ;
#33429=CARTESIAN_POINT ( 'NONE',  ( 4.691466044806102076, 44.46979273209130668, 3.249105306918581348 ) ) ;
#33431=CARTESIAN_POINT ( 'NONE',  ( 0.1098349054025746369, 16.69989664087454884, -39.75970464594248455 ) ) ;
#33433=DIRECTION ( 'NONE',  ( -1.000000000000000000, -0.000000000000000000, -0.000000000000000000 ) ) ;
#33436=LINE ( 'NONE', #37846, #9890 ) ;
#33443=B_SPLINE_CURVE_WITH_KNOTS ( 'NONE', 3,
 ( #34626, #6074, #49950, #53691 ),
 .UNSPECIFIED., .F., .F.,
 ( 4, 4 ),
 ( 2.030441771438897580E-17, 0.004444306975806115896 ),
 .UNSPECIFIED. ) ;
#33448=FACE_OUTER_BOUND ( 'NONE', #54287, .T. ) ;
#33462=CARTESIAN_POINT ( 'NONE',  ( 5.880360259849752858, -26.69116321728600383, 39.86101557989624666 ) ) ;
#33465=B_SPLINE_CURVE_WITH_KNOTS ( 'NONE', 3,
 ( #59973, #22080, #41207, #50882, #41513, #2020 ),
 .UNSPECIFIED., .F., .F.,
 ( 4, 2, 4 ),
 ( 8.672106141451628927E-17, 0.0002293366620881450661, 0.0004586733241762034501 ),
 .UNSPECIFIED. ) ;
#33469=ORIENTED_EDGE ( 'NONE', *, *, #39926, .F. ) ;
#33474=CARTESIAN_POINT ( 'NONE',  ( 0.5998501479064699549, -47.62484632993692912, 6.798102206413326520 ) ) ;
#33480=LINE ( 'NONE', #51319, #50391 ) ;
#33498=EDGE_CURVE ( 'NONE', #22273, #15900, #30108, .T. ) ;
#33500=ORIENTED_EDGE ( 'NONE', *, *, #20742, .F. ) ;
#33504=CARTESIAN_POINT ( 'NONE',  ( 0.1103744047535531458, 30.46616790811179953, 30.52096488484638215 ) ) ;
#33507=ORIENTED_EDGE ( 'NONE', *, *, #61491, .T. ) ;
#33512=CONICAL_SURFACE ( 'NONE', #12498, 42.92674063221959813, 1.485477209440487556 ) ;
#33516=CARTESIAN_POINT ( 'NONE',  ( 0.5998501479064699549, 0.5236536531308225717, 48.10473956285920138 ) ) ;
#33520=CARTESIAN_POINT ( 'NONE',  ( 4.322998006666165516, 25.80712523194275221, -40.45864630878492818 ) ) ;
#33527=VECTOR ( 'NONE', #15575, 1000.000000000000000 ) ;
#33528=( BOUNDED_SURFACE ( )  B_SPLINE_SURFACE ( 3, 1, ( 
 ( #5771, #25518 ),
 ( #53398, #34945 ),
 ( #44060, #54008 ),
 ( #39040, #49025 ) ),
 .UNSPECIFIED., .F., .F., .F. ) 
 B_SPLINE_SURFACE_WITH_KNOTS ( ( 4, 4 ),
 ( 2, 2 ),
 ( 0.000000000000000000, 1.000000000000000000 ),
 ( 0.000000000000000000, 1.000000000000000000 ),
 .UNSPECIFIED. ) 
 GEOMETRIC_REPRESENTATION_ITEM ( )  RATIONAL_B_SPLINE_SURFACE ( (
 ( 1.000000000000000000, 1.000000000000000000),
 ( 0.7223157951917480446, 0.9931996967497186413),
 ( 0.7223157951917480446, 0.9931996967497186413),
 ( 1.000000000000000000, 1.000000000000000000) ) ) 
 REPRESENTATION_ITEM ( '' )  SURFACE ( )  );
#33530=EDGE_CURVE ( 'NONE', #19827, #51524, #59283, .T. ) ;
#33532=CARTESIAN_POINT ( 'NONE',  ( 0.3622758884714600280, 4.808133778521302304, 42.84426538328732903 ) ) ;
#33540=ORIENTED_EDGE ( 'NONE', *, *, #29958, .T. ) ;
#33548=ORIENTED_EDGE ( 'NONE', *, *, #38011, .F. ) ;
#33550=EDGE_CURVE ( 'NONE', #6988, #33784, #21128, .T. ) ;
#33552=CARTESIAN_POINT ( 'NONE',  ( 0.2230388203127596503, -42.84312106681679921, -4.873876086128098528 ) ) ;
#33556=CIRCLE ( 'NONE', #40537, 10.00000000000000000 ) ;
#33563=CARTESIAN_POINT ( 'NONE',  ( 0.7246131072078572100, 5.464103862700868675, 47.79072675905346301 ) ) ;
#33574=ORIENTED_EDGE ( 'NONE', *, *, #31967, .F. ) ;
#33577=FACE_OUTER_BOUND ( 'NONE', #10734, .T. ) ;
#33582=CARTESIAN_POINT ( 'NONE',  ( -6.016761891674564211, -18.84319130225482297, 0.003433883959717882409 ) ) ;
#33583=( BOUNDED_SURFACE ( )  B_SPLINE_SURFACE ( 3, 1, ( 
 ( #38732, #5164 ),
 ( #14920, #43746 ),
 ( #39342, #57786 ),
 ( #61864, #4856 ) ),
 .UNSPECIFIED., .F., .F., .F. ) 
 B_SPLINE_SURFACE_WITH_KNOTS ( ( 4, 4 ),
 ( 2, 2 ),
 ( 0.000000000000000000, 1.000000000000000000 ),
 ( 0.000000000000000000, 1.000000000000000000 ),
 .UNSPECIFIED. ) 
 GEOMETRIC_REPRESENTATION_ITEM ( )  RATIONAL_B_SPLINE_SURFACE ( (
 ( 1.000000000000000000, 1.000000000000000000),
 ( 0.9953040768229013402, 0.8617119497784988535),
 ( 0.9953040768229013402, 0.8617119497784988535),
 ( 1.000000000000000000, 1.000000000000000000) ) ) 
 REPRESENTATION_ITEM ( '' )  SURFACE ( )  );
#33585=CARTESIAN_POINT ( 'NONE',  ( -6.001507490154111224, 14.94036486426013433, 11.48377994779706235 ) ) ;
#33587=EDGE_CURVE ( 'NONE', #43871, #40367, #4416, .T. ) ;
#33590=CARTESIAN_POINT ( 'NONE',  ( 0.3622758884714730732, -36.91764744403337062, 22.26738722580103413 ) ) ;
#33592=CARTESIAN_POINT ( 'NONE',  ( 2.643462169533600914, 42.27470921730940034, -22.81120928486451405 ) ) ;
#33594=CARTESIAN_POINT ( 'NONE',  ( 0.1098349054025746091, -21.74670956129786603, 37.23978094195813782 ) ) ;
#33600=FACE_OUTER_BOUND ( 'NONE', #5079, .T. ) ;
#33601=EDGE_CURVE ( 'NONE', #21910, #1315, #42141, .T. ) ;
#33604=ORIENTED_EDGE ( 'NONE', *, *, #17583, .F. ) ;
#33605=DIRECTION ( 'NONE',  ( 0.09835009131224552170, -0.4908642831975423837, 0.8656670924898530739 ) ) ;
#33608=ORIENTED_EDGE ( 'NONE', *, *, #18601, .T. ) ;
#33612=ORIENTED_EDGE ( 'NONE', *, *, #50202, .F. ) ;
#33613=ADVANCED_FACE ( 'NONE', ( #19489 ), #39453, .F. ) ;
#33615=EDGE_CURVE ( 'NONE', #52459, #59097, #28871, .T. ) ;
#33619=ORIENTED_EDGE ( 'NONE', *, *, #41591, .T. ) ;
#33623=CARTESIAN_POINT ( 'NONE',  ( 4.549368137175248350, -32.41327393324159800, 28.14399996863441800 ) ) ;
#33625=ORIENTED_EDGE ( 'NONE', *, *, #46090, .T. ) ;
#33626=CARTESIAN_POINT ( 'NONE',  ( 0.7954190325252789018, -44.76287681188620837, -17.60078418394979138 ) ) ;
#33627=EDGE_CURVE ( 'NONE', #44423, #43089, #16703, .T. ) ;
#33630=ORIENTED_EDGE ( 'NONE', *, *, #59977, .T. ) ;
#33639=B_SPLINE_CURVE_WITH_KNOTS ( 'NONE', 3,
 ( #35908, #49670, #6725, #54664 ),
 .UNSPECIFIED., .F., .F.,
 ( 4, 4 ),
 ( 2.303004670188525934E-17, 0.004564976165746187711 ),
 .UNSPECIFIED. ) ;
#33646=CARTESIAN_POINT ( 'NONE',  ( 0.3622758884714600280, -41.85013935980108357, 10.35929834645850001 ) ) ;
#33652=CARTESIAN_POINT ( 'NONE',  ( 0.3622758884714600280, 37.74294673546586409, -20.83792692158932525 ) ) ;
#33654=LINE ( 'NONE', #28020, #14803 ) ;
#33657=B_SPLINE_CURVE_WITH_KNOTS ( 'NONE', 3,
 ( #20734, #31059, #29813, #49533 ),
 .UNSPECIFIED., .F., .F.,
 ( 4, 4 ),
 ( 0.000000000000000000, 0.005014147105413699519 ),
 .UNSPECIFIED. ) ;
#33659=CARTESIAN_POINT ( 'NONE',  ( 2.301529144917016101, -30.25186323939247757, -37.31001381748723134 ) ) ;
#33662=CARTESIAN_POINT ( 'NONE',  ( 0.6001305935487315502, -44.24520387813816313, -18.89378601236050059 ) ) ;
#33668=DIRECTION ( 'NONE',  ( 0.000000000000000000, 0.000000000000000000, -1.000000000000000000 ) ) ;
#33669=CARTESIAN_POINT ( 'NONE',  ( 0.6017666602106488405, -23.75081624637651245, 41.83584962818275699 ) ) ;
#33677=EDGE_CURVE ( 'NONE', #4311, #59715, #44348, .T. ) ;
#33678=CARTESIAN_POINT ( 'NONE',  ( 0.3622758884714600280, -36.91764744403305087, -22.26738722580154217 ) ) ;
#33679=( BOUNDED_SURFACE ( )  B_SPLINE_SURFACE ( 3, 1, ( 
 ( #18119, #27204 ),
 ( #17197, #3373 ),
 ( #36317, #61012 ),
 ( #26899, #60383 ) ),
 .UNSPECIFIED., .F., .F., .F. ) 
 B_SPLINE_SURFACE_WITH_KNOTS ( ( 4, 4 ),
 ( 2, 2 ),
 ( 0.000000000000000000, 1.000000000000000000 ),
 ( 0.000000000000000000, 1.000000000000000000 ),
 .UNSPECIFIED. ) 
 GEOMETRIC_REPRESENTATION_ITEM ( )  RATIONAL_B_SPLINE_SURFACE ( (
 ( 1.000000000000000000, 1.000000000000000000),
 ( 0.7223157951917480446, 0.9931996967497186413),
 ( 0.7223157951917480446, 0.9931996967497186413),
 ( 1.000000000000000000, 1.000000000000000000) ) ) 
 REPRESENTATION_ITEM ( '' )  SURFACE ( )  );
#33680=CARTESIAN_POINT ( 'NONE',  ( -6.016761891674565099, 4.873659902332367011, 18.20201388312097279 ) ) ;
#33694=CARTESIAN_POINT ( 'NONE',  ( 0.7048096507298635682, -44.76417498422303964, -17.62869676200394053 ) ) ;
#33699=CARTESIAN_POINT ( 'NONE',  ( 0.1073791018717578927, 16.95003405440313315, -39.65380858626198091 ) ) ;
#33705=CARTESIAN_POINT ( 'NONE',  ( -6.016104459813374383, -7.206059014949953934, -17.41090761020844013 ) ) ;
#33707=ORIENTED_EDGE ( 'NONE', *, *, #39386, .T. ) ;
#33708=VERTEX_POINT ( 'NONE', #10396 ) ;
#33711=ORIENTED_EDGE ( 'NONE', *, *, #55771, .F. ) ;
#33713=LINE ( 'NONE', #9893, #43661 ) ;
#33720=CARTESIAN_POINT ( 'NONE',  ( 0.1103878639767399417, -37.37111717125858235, -21.52017980327885027 ) ) ;
#33723=B_SPLINE_CURVE_WITH_KNOTS ( 'NONE', 3,
 ( #29635, #54342, #29950, #30554 ),
 .UNSPECIFIED., .F., .F.,
 ( 4, 4 ),
 ( 1.898592485710544765E-17, 0.004444306975806117631 ),
 .UNSPECIFIED. ) ;
#33729=CARTESIAN_POINT ( 'NONE',  ( -6.016104459813374383, 16.31603998697569580, 9.426230926598698545 ) ) ;
#33735=CARTESIAN_POINT ( 'NONE',  ( 4.549368137175248350, -24.02461520945246320, -35.57418903283107880 ) ) ;
#33744=CARTESIAN_POINT ( 'NONE',  ( -6.001507490154110336, -9.435425682280705217, -16.31148204059957152 ) ) ;
#33759=CARTESIAN_POINT ( 'NONE',  ( 0.1073791018717483448, -34.50606437925530656, -25.86618856530698451 ) ) ;
#33770=ORIENTED_EDGE ( 'NONE', *, *, #11262, .T. ) ;
#33779=EDGE_CURVE ( 'NONE', #2725, #38521, #10713, .T. ) ;
#33783=B_SPLINE_CURVE_WITH_KNOTS ( 'NONE', 3,
 ( #39950, #59623, #20502, #58685, #11732, #59007, #40258, #35229, #30810, #2294, #54290, #6668, #36781, #27973, #41792, #32071 ),
 .UNSPECIFIED., .F., .F.,
 ( 4, 3, 3, 3, 3, 4 ),
 ( 1.995049841954898532E-17, 0.0002618515315864414347, 0.0003927756766341991296, 0.0005236998216950568058, 0.0007855159896329902240, 0.001047349442285928304 ),
 .UNSPECIFIED. ) ;
#33784=VERTEX_POINT ( 'NONE', #48909 ) ;
#33786=ORIENTED_EDGE ( 'NONE', *, *, #48779, .F. ) ;
#33798=ORIENTED_EDGE ( 'NONE', *, *, #34774, .T. ) ;
#33809=CARTESIAN_POINT ( 'NONE',  ( 4.691466044806102076, -25.04870410140817327, 36.88741755356026175 ) ) ;
#33820=CIRCLE ( 'NONE', #23786, 42.92674063221959813 ) ;
#33833=CARTESIAN_POINT ( 'NONE',  ( 0.1095718737110177865, -16.26534146842179851, -39.93945841550369380 ) ) ;
#33836=CARTESIAN_POINT ( 'NONE',  ( 4.549368137175248350, 35.57418903283081590, 24.02461520945284690 ) ) ;
#33844=B_SPLINE_CURVE_WITH_KNOTS ( 'NONE', 3,
 ( #56423, #28536, #37665, #47660 ),
 .UNSPECIFIED., .F., .F.,
 ( 4, 4 ),
 ( 0.000000000000000000, 0.004445488388166996853 ),
 .UNSPECIFIED. ) ;
#33845=CARTESIAN_POINT ( 'NONE',  ( 0.1097557419366048670, 37.45792859959197330, 21.36873056345907074 ) ) ;
#33855=CARTESIAN_POINT ( 'NONE',  ( 0.5988103622719991304, -44.67429504351072467, 17.84821742497916830 ) ) ;
#33862=CARTESIAN_POINT ( 'NONE',  ( -6.015611763856276717, 17.41126425312547710, -7.205255340944423992 ) ) ;
#33865=CARTESIAN_POINT ( 'NONE',  ( 0.1064266379913940547, 40.05351204369885210, 15.98292486309350124 ) ) ;
#33866=ORIENTED_EDGE ( 'NONE', *, *, #39144, .F. ) ;
#33868=ORIENTED_EDGE ( 'NONE', *, *, #26365, .F. ) ;
#33875=CARTESIAN_POINT ( 'NONE',  ( 0.5998501479064708430, 5.759754759340140140, 47.76154736470759588 ) ) ;
#33877=ORIENTED_EDGE ( 'NONE', *, *, #24309, .F. ) ;
#33883=CARTESIAN_POINT ( 'NONE',  ( 4.549368137175248350, -3.018832571116246477, -42.82045902618772004 ) ) ;
#33889=CARTESIAN_POINT ( 'NONE',  ( -6.017396004339686577, -18.68211039806562113, -2.458362590802985359 ) ) ;
#33894=CARTESIAN_POINT ( 'NONE',  ( -5.995132425357893702, 7.203480333239314248, -17.41298668506963310 ) ) ;
#33896=CARTESIAN_POINT ( 'NONE',  ( 0.6001305935487315502, 0.5236757026889412581, -48.10757715638248300 ) ) ;
#33900=CIRCLE ( 'NONE', #57874, 42.92674063221959813 ) ;
#33911=EDGE_CURVE ( 'NONE', #48869, #47737, #5347, .T. ) ;
#33912=CARTESIAN_POINT ( 'NONE',  ( 3.680974057930773036, 47.94008194857087801, 1.849713332883914818 ) ) ;
#33913=CARTESIAN_POINT ( 'NONE',  ( 0.3622758884714600280, 26.89560658783384994, -33.69533458712316332 ) ) ;
#33918=ORIENTED_EDGE ( 'NONE', *, *, #48583, .F. ) ;
#33923=ORIENTED_EDGE ( 'NONE', *, *, #16969, .T. ) ;
#33928=ORIENTED_EDGE ( 'NONE', *, *, #55433, .T. ) ;
#33931=ORIENTED_EDGE ( 'NONE', *, *, #17919, .T. ) ;
#33934=CARTESIAN_POINT ( 'NONE',  ( 0.1100053167205930632, -30.62023953839061718, -30.36644426605129610 ) ) ;
#33943=CARTESIAN_POINT ( 'NONE',  ( -5.995132425357893702, 17.40647075750126760, -7.219211173946302296 ) ) ;
#33944=CARTESIAN_POINT ( 'NONE',  ( 0.7048096507298635682, 5.442192462019463051, -47.80151517212782153 ) ) ;
#33948=VERTEX_POINT ( 'NONE', #33759 ) ;
#33963=ORIENTED_EDGE ( 'NONE', *, *, #26689, .F. ) ;
#33965=CARTESIAN_POINT ( 'NONE',  ( -2.708315649062910779, 4.041664582652797044, -14.06540004355478857 ) ) ;
#33970=CARTESIAN_POINT ( 'NONE',  ( 0.1310142868023690677, -43.11885108606330164, -0.6370537502134987484 ) ) ;
#33971=( BOUNDED_SURFACE ( )  B_SPLINE_SURFACE ( 3, 1, ( 
 ( #46096, #2830 ),
 ( #3140, #22269 ),
 ( #6577, #58917 ),
 ( #30408, #49524 ) ),
 .UNSPECIFIED., .F., .F., .F. ) 
 B_SPLINE_SURFACE_WITH_KNOTS ( ( 4, 4 ),
 ( 2, 2 ),
 ( 0.000000000000000000, 1.000000000000000000 ),
 ( 0.000000000000000000, 1.000000000000000000 ),
 .UNSPECIFIED. ) 
 GEOMETRIC_REPRESENTATION_ITEM ( )  RATIONAL_B_SPLINE_SURFACE ( (
 ( 1.000000000000000000, 1.000000000000000000),
 ( 0.9953040768229013402, 0.8617119497784988535),
 ( 0.9953040768229013402, 0.8617119497784988535),
 ( 1.000000000000000000, 1.000000000000000000) ) ) 
 REPRESENTATION_ITEM ( '' )  SURFACE ( )  );
#33972=CARTESIAN_POINT ( 'NONE',  ( 4.975801465491694664, -31.15993731089097452, -36.39623109580456628 ) ) ;
#33975=EDGE_CURVE ( 'NONE', #48896, #58618, #30767, .T. ) ;
#33976=CARTESIAN_POINT ( 'NONE',  ( 0.6025881611877910160, -18.20817581200385504, -44.52856035602900420 ) ) ;
#33983=CARTESIAN_POINT ( 'NONE',  ( 0.5988103622719992414, -34.44344971428051139, 33.58571533649100616 ) ) ;
#33984=CARTESIAN_POINT ( 'NONE',  ( 0.6031356755773454870, -46.46821530722348115, 12.45114731045949519 ) ) ;
#33986=DIRECTION ( 'NONE',  ( 1.000000000000000000, 0.000000000000000000, 0.000000000000000000 ) ) ;
#33992=CARTESIAN_POINT ( 'NONE',  ( 4.975801465491694664, -47.10002938642148251, 8.787181743659342459 ) ) ;
#33993=CARTESIAN_POINT ( 'NONE',  ( 0.5988103564986352323, -6.880138274944628485, -47.61318305157292485 ) ) ;
#34002=CARTESIAN_POINT ( 'NONE',  ( 0.1101816497532063233, -11.03018586750523689, 41.68997876247028245 ) ) ;
#34006=EDGE_CURVE ( 'NONE', #31680, #32580, #3142, .T. ) ;
#34007=ORIENTED_EDGE ( 'NONE', *, *, #60310, .F. ) ;
#34010=AXIS2_PLACEMENT_3D ( 'NONE', #38527, #10624, #14711 ) ;
#34017=ORIENTED_EDGE ( 'NONE', *, *, #52556, .F. ) ;
#34018=ORIENTED_EDGE ( 'NONE', *, *, #286, .F. ) ;
#34019=CARTESIAN_POINT ( 'NONE',  ( -6.001507490154111224, -9.435425682280932591, 16.31148204059944007 ) ) ;
#34020=LINE ( 'NONE', #29294, #16544 ) ;
#34022=CARTESIAN_POINT ( 'NONE',  ( 3.680974057930773924, -47.28851186371002768, -8.091325130366254115 ) ) ;
#34037=EDGE_CURVE ( 'NONE', #59362, #22451, #31561, .T. ) ;
#34038=ORIENTED_EDGE ( 'NONE', *, *, #19813, .T. ) ;
#34041=EDGE_CURVE ( 'NONE', #14890, #56157, #56175, .T. ) ;
#34045=CARTESIAN_POINT ( 'NONE',  ( 0.6028618097248862329, -47.67286800277447867, 6.452328974162811370 ) ) ;
#34046=CARTESIAN_POINT ( 'NONE',  ( 4.833616638992208614, -26.07076047129108787, -38.20222678111930037 ) ) ;
#34047=CARTESIAN_POINT ( 'NONE',  ( 0.6001305935487422083, 17.92615948558540495, -44.64600790884038162 ) ) ;
#34049=AXIS2_PLACEMENT_3D ( 'NONE', #4064, #42333, #27905 ) ;
#34050=EDGE_CURVE ( 'NONE', #19158, #5629, #55392, .T. ) ;
#34051=CARTESIAN_POINT ( 'NONE',  ( 0.6028618097248862329, 29.14732267129573273, -38.27229381545022591 ) ) ;
#34052=CARTESIAN_POINT ( 'NONE',  ( -6.015611763856276717, -2.453375430804198398, 18.68284711750057525 ) ) ;
#34055=FACE_OUTER_BOUND ( 'NONE', #13512, .T. ) ;
#34061=CARTESIAN_POINT ( 'NONE',  ( -4.908599999999998964, 5.921523664636232727E-15, -48.35291015139245019 ) ) ;
#34063=DIRECTION ( 'NONE',  ( 1.000000000000000000, 0.000000000000000000, 0.000000000000000000 ) ) ;
#34064=CARTESIAN_POINT ( 'NONE',  ( -2.708315649062916552, -2.171184472130592624, -14.47261168455368896 ) ) ;
#34072=CARTESIAN_POINT ( 'NONE',  ( 0.3622758884714730732, 22.26738722580116558, 36.91764744403329246 ) ) ;
#34074=EDGE_LOOP ( 'NONE', ( #53776, #11821, #53108, #35160 ) ) ;
#34078=EDGE_CURVE ( 'NONE', #24199, #31934, #10593, .T. ) ;
#34080=CARTESIAN_POINT ( 'NONE',  ( 0.1064266379913940824, 17.02047542254793555, 39.62374453032503396 ) ) ;
#34083=EDGE_CURVE ( 'NONE', #11994, #41909, #137, .T. ) ;
#34087=CARTESIAN_POINT ( 'NONE',  ( 0.1073791018717483448, -10.69234304550083081, 41.77800844988496465 ) ) ;
#34095=VERTEX_POINT ( 'NONE', #40318 ) ;
#34097=CARTESIAN_POINT ( 'NONE',  ( 0.6023142530420679819, 34.20176999054661593, 33.83147280953699010 ) ) ;
#34101=CARTESIAN_POINT ( 'NONE',  ( 4.833616638992208614, -43.64812679991131716, 15.29495699393648067 ) ) ;
#34104=FACE_OUTER_BOUND ( 'NONE', #34120, .T. ) ;
#34110=ORIENTED_EDGE ( 'NONE', *, *, #9277, .F. ) ;
#34116=CARTESIAN_POINT ( 'NONE',  ( 4.322998006666179727, 20.30542865297587340, 43.48102276965709478 ) ) ;
#34120=EDGE_LOOP ( 'NONE', ( #3492, #58481, #53931, #20235 ) ) ;
#34125=CARTESIAN_POINT ( 'NONE',  ( 3.680882792899937694, -14.19444521819999139, -45.82784180332832591 ) ) ;
#34129=EDGE_CURVE ( 'NONE', #1954, #56408, #28552, .T. ) ;
#34131=CARTESIAN_POINT ( 'NONE',  ( 0.6031356755773454870, 12.45114731045965684, 46.46821530722343851 ) ) ;
#34135=CARTESIAN_POINT ( 'NONE',  ( 4.549368137175248350, 32.41327393324141326, -28.14399996863463116 ) ) ;
#34138=CARTESIAN_POINT ( 'NONE',  ( -6.016104459813371719, 2.454244026261361178, -18.68271063303492241 ) ) ;
#34141=CARTESIAN_POINT ( 'NONE',  ( 0.5998501479064708430, -48.10473956285919428, -0.5236536531313246146 ) ) ;
#34146=EDGE_CURVE ( 'NONE', #4009, #52432, #33018, .T. ) ;
#34155=CARTESIAN_POINT ( 'NONE',  ( 0.8751705887134423323, -44.76769609654249393, 17.57879340691464165 ) ) ;
#34162=ORIENTED_EDGE ( 'NONE', *, *, #16204, .T. ) ;
#34168=CARTESIAN_POINT ( 'NONE',  ( 0.8751705887134423323, -19.22545746485690188, 44.08562551107050353 ) ) ;
#34174=FACE_OUTER_BOUND ( 'NONE', #9209, .T. ) ;
#34176=ORIENTED_EDGE ( 'NONE', *, *, #57751, .F. ) ;
#34180=CARTESIAN_POINT ( 'NONE',  ( 0.8760168074886965917, 34.63873394077487688, -33.37827814204089094 ) ) ;
#34182=EDGE_CURVE ( 'NONE', #19553, #44510, #50906, .T. ) ;
#34184=CARTESIAN_POINT ( 'NONE',  ( 4.549368137175248350, -38.59302160394740611, -18.79584381673521065 ) ) ;
#34185=B_SPLINE_CURVE_WITH_KNOTS ( 'NONE', 3,
 ( #15051, #53234, #5909, #1227, #48541, #29741 ),
 .UNSPECIFIED., .F., .F.,
 ( 4, 2, 4 ),
 ( 8.651749916829332779E-17, 0.0002293366620881423013, 0.0004586733241761980833 ),
 .UNSPECIFIED. ) ;
#34194=CARTESIAN_POINT ( 'NONE',  ( 4.549368137175248350, 13.99871866169365653, -40.58005590356676606 ) ) ;
#34203=CARTESIAN_POINT ( 'NONE',  ( 0.7048096507298579061, 0.8437160066907277711, -48.10291524268441066 ) ) ;
#34204=CARTESIAN_POINT ( 'NONE',  ( 0.8760168074887076939, 41.20610493656909057, -24.81951362746035628 ) ) ;
#34210=CARTESIAN_POINT ( 'NONE',  ( 0.1081432562775999084, -21.92800090985295824, 37.13343246403887576 ) ) ;
#34214=B_SPLINE_CURVE_WITH_KNOTS ( 'NONE', 3,
 ( #14148, #38572, #5319, #24446, #39195, #43583, #33251, #47646, #8695, #27815, #32220, #19056, #41939, #23425, #46324, #46948 ),
 .UNSPECIFIED., .F., .F.,
 ( 4, 3, 3, 3, 3, 4 ),
 ( 2.221635811791082109E-17, 0.0002618515315864455005, 0.0003927756766341994007, 0.0005236998216950557216, 0.0007855159896329911998, 0.001047349442285927870 ),
 .UNSPECIFIED. ) ;
#34216=CARTESIAN_POINT ( 'NONE',  ( 2.301430502907645170, 48.01619648598871493, 1.287492012859562163 ) ) ;
#34218=CARTESIAN_POINT ( 'NONE',  ( 0.3622758884714600280, 17.25816669464994746, -39.50828911766980411 ) ) ;
#34220=LINE ( 'NONE', #15731, #7850 ) ;
#34224=CARTESIAN_POINT ( 'NONE',  ( 0.3622758884714600280, 39.50828911766974016, 17.25816669465007891 ) ) ;
#34228=ORIENTED_EDGE ( 'NONE', *, *, #24059, .F. ) ;
#34230=CARTESIAN_POINT ( 'NONE',  ( 2.643462169533613793, -13.76277278785528857, -46.02269433264228127 ) ) ;
#34233=CARTESIAN_POINT ( 'NONE',  ( 0.1073791018717483448, -40.02496097243048467, -16.05399293000801819 ) ) ;
#34239=CARTESIAN_POINT ( 'NONE',  ( 0.1073791018717578927, -30.14884492832369745, -30.83464511437127697 ) ) ;
#34244=EDGE_CURVE ( 'NONE', #43756, #32260, #38465, .T. ) ;
#34246=CARTESIAN_POINT ( 'NONE',  ( 0.5998501479064708430, -18.89267974119696447, 44.24259072156053918 ) ) ;
#34255=EDGE_CURVE ( 'NONE', #27042, #4984, #18812, .T. ) ;
#34257=CARTESIAN_POINT ( 'NONE',  ( 0.5998501479064708430, -38.48283596222049141, 28.86886762351059588 ) ) ;
#34270=CARTESIAN_POINT ( 'NONE',  ( -6.015611763856276717, 9.416239407363303116, 16.32183393015600004 ) ) ;
#34274=CARTESIAN_POINT ( 'NONE',  ( 4.975801465491695552, 36.39623109580423943, 31.15993731089136887 ) ) ;
#34282=CARTESIAN_POINT ( 'NONE',  ( 0.6001305935487315502, 38.48510059944048578, -28.87057754790896880 ) ) ;
#34283=CARTESIAN_POINT ( 'NONE',  ( -6.010958268070873523, 7.224487401384534380, -17.40352239307050297 ) ) ;
#34288=CARTESIAN_POINT ( 'NONE',  ( 0.6001305935487315502, -12.95698906763843006, 46.33281397023041848 ) ) ;
#34289=CARTESIAN_POINT ( 'NONE',  ( 4.975801465491695552, -43.22084481528207078, -20.67815041659126862 ) ) ;
#34292=VERTEX_POINT ( 'NONE', #23649 ) ;
#34298=CARTESIAN_POINT ( 'NONE',  ( 0.1100053167205931187, -10.98799238780980225, 41.70112744323650134 ) ) ;
#34299=CARTESIAN_POINT ( 'NONE',  ( 0.3622758884714730732, -4.808133778522197588, 42.84426538328723666 ) ) ;
#34302=VECTOR ( 'NONE', #27652, 1000.000000000000000 ) ;
#34303=EDGE_CURVE ( 'NONE', #10899, #9817, #46440, .T. ) ;
#34308=ADVANCED_FACE ( 'NONE', ( #10478 ), #38722, .F. ) ;
#34315=VECTOR ( 'NONE', #29737, 999.9999999999998863 ) ;
#34317=VERTEX_POINT ( 'NONE', #24886 ) ;
#34326=CARTESIAN_POINT ( 'NONE',  ( 0.1073791018717578927, -42.81622261970997556, 5.147744207006151207 ) ) ;
#34338=CARTESIAN_POINT ( 'NONE',  ( 4.322998006666165516, 45.75942687572278800, 14.45630056002956110 ) ) ;
#34341=CARTESIAN_POINT ( 'NONE',  ( 0.1310142868023699003, 39.59283406808307149, 17.08943085418600916 ) ) ;
#34344=EDGE_CURVE ( 'NONE', #14306, #43794, #44472, .T. ) ;
#34349=CARTESIAN_POINT ( 'NONE',  ( 0.3622758884714730732, -20.83792692158999316, 37.74294673546550172 ) ) ;
#34356=B_SPLINE_CURVE_WITH_KNOTS ( 'NONE', 3,
 ( #3721, #56660, #52579, #9673, #61054, #56968 ),
 .UNSPECIFIED., .F., .F.,
 ( 4, 2, 4 ),
 ( 1.265936389305167544E-16, 0.0002450741128632346190, 0.0004901482257263427116 ),
 .UNSPECIFIED. ) ;
#34360=CARTESIAN_POINT ( 'NONE',  ( 0.8760168074886965917, 17.58183840866335856, 44.77533136581888584 ) ) ;
#34363=CARTESIAN_POINT ( 'NONE',  ( 0.6031357023905875581, 38.19275261685275069, -29.25135304925241186 ) ) ;
#34365=CARTESIAN_POINT ( 'NONE',  ( 0.6254311100348624031, 17.77188277739556455, 44.70341307176162360 ) ) ;
#34366=DIRECTION ( 'NONE',  ( 0.000000000000000000, 0.000000000000000000, -1.000000000000000000 ) ) ;
#34368=CARTESIAN_POINT ( 'NONE',  ( 0.3622758884714730732, -33.69533458712361806, 26.89560658783328861 ) ) ;
#34369=ORIENTED_EDGE ( 'NONE', *, *, #57354, .F. ) ;
#34372=CARTESIAN_POINT ( 'NONE',  ( 0.6001305935487315502, 0.5236757026882711274, 48.10757715638249010 ) ) ;
#34375=LINE ( 'NONE', #6431, #33527 ) ;
#34377=CARTESIAN_POINT ( 'NONE',  ( 0.7954190325252784577, 11.60747917225584835, -46.67728753507131501 ) ) ;
#34378=EDGE_CURVE ( 'NONE', #34651, #23287, #23306, .T. ) ;
#34379=ORIENTED_EDGE ( 'NONE', *, *, #20742, .T. ) ;
#34388=CARTESIAN_POINT ( 'NONE',  ( 4.833616638992208614, 25.31740731790898735, -38.70560126501837317 ) ) ;
#34392=CARTESIAN_POINT ( 'NONE',  ( 3.680882792899938138, 45.82784180332838275, -14.19444521819982796 ) ) ;
#34393=VERTEX_POINT ( 'NONE', #28963 ) ;
#34396=CARTESIAN_POINT ( 'NONE',  ( 0.7048096507298579061, -19.18768066167151432, 44.11842270945940214 ) ) ;
#34400=CARTESIAN_POINT ( 'NONE',  ( 0.8751705887134423323, 17.57879340691479797, 44.76769609654243709 ) ) ;
#34406=CARTESIAN_POINT ( 'NONE',  ( 0.6031356755852232965, 5.421189728766411748E-15, -48.10744332413860747 ) ) ;
#34408=CARTESIAN_POINT ( 'NONE',  ( 4.549368137175248350, -24.02461520945246320, -35.57418903283107880 ) ) ;
#34414=CARTESIAN_POINT ( 'NONE',  ( 0.8751705887134553219, -42.09020928323357680, -23.27176129838411001 ) ) ;
#34415=EDGE_LOOP ( 'NONE', ( #61404, #52155, #57403, #37503 ) ) ;
#34424=CARTESIAN_POINT ( 'NONE',  ( 1.827119703190779321, 9.946884032291105626, -41.88501940447984850 ) ) ;
#34427=CARTESIAN_POINT ( 'NONE',  ( 4.549368137175248350, 0.000000000000000000, 0.000000000000000000 ) ) ;
#34433=CARTESIAN_POINT ( 'NONE',  ( 0.6031357023905875581, 12.40899271757774081, 46.47951061918815441 ) ) ;
#34435=CARTESIAN_POINT ( 'NONE',  ( -6.001507490154110336, -17.41542759839258991, -7.196845540359352533 ) ) ;
#34437=CONICAL_SURFACE ( 'NONE', #30380, 47.91270532121795611, 0.04450589592585343229 ) ;
#34441=CARTESIAN_POINT ( 'NONE',  ( -6.015611763856276717, 2.453375430804336954, -18.68284711750055749 ) ) ;
#34445=CARTESIAN_POINT ( 'NONE',  ( 4.975801465491694664, -39.51822597168476392, -27.09127437476367106 ) ) ;
#34448=AXIS2_PLACEMENT_3D ( 'NONE', #18867, #13234, #61423 ) ;
#34452=CARTESIAN_POINT ( 'NONE',  ( 4.549368137175248350, -42.82045902618774136, 3.018832571115817487 ) ) ;
#34454=EDGE_CURVE ( 'NONE', #15076, #57080, #4628, .T. ) ;
#34457=CARTESIAN_POINT ( 'NONE',  ( 0.3622758884714730732, -29.89648521331652731, 31.06363466427676201 ) ) ;
#34459=EDGE_CURVE ( 'NONE', #54112, #17050, #26291, .T. ) ;
#34460=ORIENTED_EDGE ( 'NONE', *, *, #18696, .F. ) ;
#34475=CARTESIAN_POINT ( 'NONE',  ( 0.6001305935487315502, 24.50730504006400068, 41.40054608060301433 ) ) ;
#34476=VERTEX_POINT ( 'NONE', #22650 ) ;
#34481=ORIENTED_EDGE ( 'NONE', *, *, #19225, .F. ) ;
#34486=CARTESIAN_POINT ( 'NONE',  ( 0.6001305935487315502, 34.38748867424713751, -33.64689939321905854 ) ) ;
#34489=CARTESIAN_POINT ( 'NONE',  ( -6.015611763856276717, 16.31561949997088945, -9.427003116184000220 ) ) ;
#34499=CARTESIAN_POINT ( 'NONE',  ( 4.549368137175248350, 0.000000000000000000, 0.000000000000000000 ) ) ;
#34503=VERTEX_POINT ( 'NONE', #60222 ) ;
#34505=LINE ( 'NONE', #29789, #39824 ) ;
#34515=DIRECTION ( 'NONE',  ( 0.000000000000000000, 0.000000000000000000, 1.000000000000000000 ) ) ;
#34517=CARTESIAN_POINT ( 'NONE',  ( -6.016761891674565099, -17.40752468084777504, -7.214149619366543753 ) ) ;
#34534=ORIENTED_EDGE ( 'NONE', *, *, #56431, .F. ) ;
#34539=CARTESIAN_POINT ( 'NONE',  ( -6.015611763856276717, -9.416239407363420355, 16.32183393015593609 ) ) ;
#34541=ORIENTED_EDGE ( 'NONE', *, *, #39849, .F. ) ;
#34543=VERTEX_POINT ( 'NONE', #34218 ) ;
#34549=CARTESIAN_POINT ( 'NONE',  ( 0.3622758884714730732, 41.42293301073625855, -11.95365414648454205 ) ) ;
#34550=ORIENTED_EDGE ( 'NONE', *, *, #2227, .F. ) ;
#34554=CARTESIAN_POINT ( 'NONE',  ( 0.1081432562775997974, -30.79166192943866420, 30.19275717928070080 ) ) ;
#34557=CARTESIAN_POINT ( 'NONE',  ( 0.6009452777970414328, -12.02913818029345272, 46.57942614304337070 ) ) ;
#34558=CARTESIAN_POINT ( 'NONE',  ( 0.1100247026804066219, 41.61078157869235383, 11.32523219034922590 ) ) ;
#34561=B_SPLINE_CURVE_WITH_KNOTS ( 'NONE', 3,
 ( #26099, #34904, #24875, #6964 ),
 .UNSPECIFIED., .F., .F.,
 ( 4, 4 ),
 ( 2.297383214701472214E-17, 0.004564976165746188579 ),
 .UNSPECIFIED. ) ;
#34576=VECTOR ( 'NONE', #17546, 1000.000000000000341 ) ;
#34581=CARTESIAN_POINT ( 'NONE',  ( 0.8751705887134423323, 19.22545746485661766, -44.08562551107063143 ) ) ;
#34584=CARTESIAN_POINT ( 'NONE',  ( 0.6031357023905875581, -6.322524267548935484, 47.69018446756497553 ) ) ;
#34590=CARTESIAN_POINT ( 'NONE',  ( 0.6031356755773454870, -24.05369945659562703, 41.66228085015284677 ) ) ;
#34598=CARTESIAN_POINT ( 'NONE',  ( 0.6254087463353912302, -6.960754339421479031, -47.60024110474246584 ) ) ;
#34607=CARTESIAN_POINT ( 'NONE',  ( 4.975801465491694664, -32.01766832630337944, 35.64402118370901462 ) ) ;
#34608=CARTESIAN_POINT ( 'NONE',  ( 3.238741278300274029, 1.828728677531826108, -42.95313747363662316 ) ) ;
#34611=ORIENTED_EDGE ( 'NONE', *, *, #46265, .T. ) ;
#34615=CARTESIAN_POINT ( 'NONE',  ( 0.8751705887134553219, -46.21789262997766201, 13.30665218149281870 ) ) ;
#34624=ORIENTED_EDGE ( 'NONE', *, *, #13002, .T. ) ;
#34626=CARTESIAN_POINT ( 'NONE',  ( 0.8751705887134553219, 44.76769609654211735, 17.57879340691559378 ) ) ;
#34645=ADVANCED_FACE ( 'NONE', ( #8852 ), #51117, .F. ) ;
#34650=DIRECTION ( 'NONE',  ( 0.09835009131224552170, -0.3879606369183575265, -0.9164135549743768205 ) ) ;
#34651=VERTEX_POINT ( 'NONE', #33913 ) ;
#34665=B_SPLINE_CURVE_WITH_KNOTS ( 'NONE', 3,
 ( #30178, #58059, #10789, #52754 ),
 .UNSPECIFIED., .F., .F.,
 ( 4, 4 ),
 ( 1.734723475976807094E-18, 0.005014147105413696050 ),
 .UNSPECIFIED. ) ;
#34670=CARTESIAN_POINT ( 'NONE',  ( 0.6029303876144825880, -0.1308990448399069417, 48.10727438003475953 ) ) ;
#34673=CARTESIAN_POINT ( 'NONE',  ( 0.6031356755852232965, 5.421189728766411748E-15, -48.10744332413860747 ) ) ;
#34683=CARTESIAN_POINT ( 'NONE',  ( 2.643462169533600914, -47.78621045426879022, 4.896978544601340744 ) ) ;
#34703=ORIENTED_EDGE ( 'NONE', *, *, #41540, .T. ) ;
#34716=CARTESIAN_POINT ( 'NONE',  ( 2.301430502907646058, 40.93949994354150590, 25.12309903330034544 ) ) ;
#34727=CARTESIAN_POINT ( 'NONE',  ( -5.995132425357893702, 17.40647075750116457, 7.219211173946554538 ) ) ;
#34731=EDGE_CURVE ( 'NONE', #43474, #43585, #6903, .T. ) ;
#34743=CARTESIAN_POINT ( 'NONE',  ( 0.8760168074886960365, 44.09317760313724932, 19.22870327415319380 ) ) ;
#34744=CARTESIAN_POINT ( 'NONE',  ( 4.975801465491694664, -31.15993731089097452, -36.39623109580456628 ) ) ;
#34745=CARTESIAN_POINT ( 'NONE',  ( 2.301430502907645614, -37.31003439265388266, -30.25184447737420967 ) ) ;
#34747=CARTESIAN_POINT ( 'NONE',  ( 0.7048096507298579061, 44.76417498422313912, -17.62869676200362790 ) ) ;
#34749=EDGE_CURVE ( 'NONE', #58534, #17351, #16033, .T. ) ;
#34755=DIRECTION ( 'NONE',  ( 1.000000000000000000, 0.000000000000000000, 0.000000000000000000 ) ) ;
#34757=CARTESIAN_POINT ( 'NONE',  ( 0.7246131072078559887, 11.65529928397572590, 46.66866179549017346 ) ) ;
#34768=CARTESIAN_POINT ( 'NONE',  ( -2.569797478183783568, -6.011723966604058944, -13.34095667500602644 ) ) ;
#34771=CARTESIAN_POINT ( 'NONE',  ( 4.549368137175248350, 38.59302160394752690, -18.79584381673492288 ) ) ;
#34774=EDGE_CURVE ( 'NONE', #29832, #59804, #35200, .T. ) ;
#34777=ORIENTED_EDGE ( 'NONE', *, *, #43766, .F. ) ;
#34790=VERTEX_POINT ( 'NONE', #46396 ) ;
#34794=CARTESIAN_POINT ( 'NONE',  ( 0.6028618097248863439, 24.20479143424832813, 41.57478760529411943 ) ) ;
#34796=CARTESIAN_POINT ( 'NONE',  ( 0.6023143664670691511, 44.34466302085797196, 18.65155446683267115 ) ) ;
#34797=ORIENTED_EDGE ( 'NONE', *, *, #39713, .F. ) ;
#34798=EDGE_CURVE ( 'NONE', #39339, #9846, #59119, .T. ) ;
#34799=CARTESIAN_POINT ( 'NONE',  ( -6.017396004339686577, 18.20140164570668873, 4.875835690939244849 ) ) ;
#34801=B_SPLINE_CURVE_WITH_KNOTS ( 'NONE', 3,
 ( #10874, #42314, #61373, #53143 ),
 .UNSPECIFIED., .F., .F.,
 ( 4, 4 ),
 ( 2.183987964099526702E-17, 0.004444306975806114161 ),
 .UNSPECIFIED. ) ;
#34808=B_SPLINE_CURVE_WITH_KNOTS ( 'NONE', 3,
 ( #29098, #48216, #577, #53204, #4963, #44167, #43853, #896, #34433, #34131, #5269, #20331, #10309, #5879, #57573, #1199 ),
 .UNSPECIFIED., .F., .F.,
 ( 4, 3, 3, 3, 3, 4 ),
 ( 2.030557555191247372E-17, 0.0002618515315864412721, 0.0003927756766341967986, 0.0005236998216950550710, 0.0007855159896329879472, 0.001047349442285926569 ),
 .UNSPECIFIED. ) ;
#34810=ORIENTED_EDGE ( 'NONE', *, *, #24819, .F. ) ;
#34813=CARTESIAN_POINT ( 'NONE',  ( 0.5998501479064699549, -0.5236536531311584142, -48.10473956285919428 ) ) ;
#34819=CARTESIAN_POINT ( 'NONE',  ( 4.549368137175248350, 0.000000000000000000, 0.000000000000000000 ) ) ;
#34822=CARTESIAN_POINT ( 'NONE',  ( 0.8751705887134423323, 24.81530984069208401, -41.19904111682483716 ) ) ;
#34823=CIRCLE ( 'NONE', #7781, 47.91270532121795611 ) ;
#34836=VECTOR ( 'NONE', #2626, 1000.000000000000114 ) ;
#34839=CARTESIAN_POINT ( 'NONE',  ( 4.549368137175248350, -2.596185425822241211, 42.84816078363925840 ) ) ;
#34849=ORIENTED_EDGE ( 'NONE', *, *, #6664, .F. ) ;
#34861=LINE ( 'NONE', #30135, #37042 ) ;
#34862=VECTOR ( 'NONE', #53210, 1000.000000000000114 ) ;
#34865=FACE_OUTER_BOUND ( 'NONE', #4281, .T. ) ;
#34871=CARTESIAN_POINT ( 'NONE',  ( 0.1092355843206037486, 41.57624119012373143, 11.45151637801141931 ) ) ;
#34873=EDGE_CURVE ( 'NONE', #4009, #27049, #20322, .T. ) ;
#34874=( BOUNDED_SURFACE ( )  B_SPLINE_SURFACE ( 3, 1, ( 
 ( #14032, #24333 ),
 ( #38453, #14644 ),
 ( #47529, #9300 ),
 ( #52517, #61899 ) ),
 .UNSPECIFIED., .F., .F., .F. ) 
 B_SPLINE_SURFACE_WITH_KNOTS ( ( 4, 4 ),
 ( 2, 2 ),
 ( 0.000000000000000000, 1.000000000000000000 ),
 ( 0.000000000000000000, 1.000000000000000000 ),
 .UNSPECIFIED. ) 
 GEOMETRIC_REPRESENTATION_ITEM ( )  RATIONAL_B_SPLINE_SURFACE ( (
 ( 1.000000000000000000, 1.000000000000000000),
 ( 0.7223157951917476005, 0.9931996967497186413),
 ( 0.7223157951917476005, 0.9931996967497186413),
 ( 1.000000000000000000, 1.000000000000000000) ) ) 
 REPRESENTATION_ITEM ( '' )  SURFACE ( )  );
#34876=CARTESIAN_POINT ( 'NONE',  ( 4.549368137175248350, 13.99871866169305434, 40.58005590356696501 ) ) ;
#34884=CONICAL_SURFACE ( 'NONE', #60875, 42.92674063221959813, 1.485477209440487556 ) ;
#34899=CARTESIAN_POINT ( 'NONE',  ( 0.6029303876144825880, -6.409038528276480129, 47.67862422489722007 ) ) ;
#34903=CARTESIAN_POINT ( 'NONE',  ( 0.8751705887134553219, 37.60752970653828697, -29.98056538504921065 ) ) ;
#34904=CARTESIAN_POINT ( 'NONE',  ( 1.827326673878743923, -41.88502433275010617, 9.946825761453776948 ) ) ;
#34907=CARTESIAN_POINT ( 'NONE',  ( 0.7246131072078570989, -34.58859703353100201, 33.42811616637859373 ) ) ;
#34908=CARTESIAN_POINT ( 'NONE',  ( 0.6025881611877911270, -46.52425620537277950, 12.24025891548842360 ) ) ;
#34914=CARTESIAN_POINT ( 'NONE',  ( -6.016489644550736315, 4.872725758886445213, -18.20227673842138927 ) ) ;
#34917=ORIENTED_EDGE ( 'NONE', *, *, #46265, .F. ) ;
#34919=CARTESIAN_POINT ( 'NONE',  ( 0.3622758884714730732, -33.69533458712361806, 26.89560658783328861 ) ) ;
#34923=VERTEX_POINT ( 'NONE', #7737 ) ;
#34935=CARTESIAN_POINT ( 'NONE',  ( 0.7245667037590772797, 19.16327388244000218, 44.12005358974313651 ) ) ;
#34936=CARTESIAN_POINT ( 'NONE',  ( -6.015611763856276717, 18.84324252354755203, 0.006214430185208092740 ) ) ;
#34939=ORIENTED_EDGE ( 'NONE', *, *, #28719, .F. ) ;
#34941=CARTESIAN_POINT ( 'NONE',  ( 4.833616638992208614, 41.27831852777643462, -20.86133030530247012 ) ) ;
#34942=CARTESIAN_POINT ( 'NONE',  ( 5.880360259849739535, -36.03610316515405287, 31.66572319753499443 ) ) ;
#34945=CARTESIAN_POINT ( 'NONE',  ( 2.643462169533600914, 34.93025802711726158, -32.97543604874639556 ) ) ;
#34946=CARTESIAN_POINT ( 'NONE',  ( 0.3622758884714730732, -42.84426538328728640, -4.808133778521729518 ) ) ;
#34954=ORIENTED_EDGE ( 'NONE', *, *, #30133, .F. ) ;
#34960=CARTESIAN_POINT ( 'NONE',  ( 0.7048096507298635682, -42.08020459959966075, -23.32077812596866551 ) ) ;
#34964=EDGE_CURVE ( 'NONE', #6050, #25842, #7521, .T. ) ;
#34968=CARTESIAN_POINT ( 'NONE',  ( 0.8760168074887090262, -48.09529047980637273, 0.8912768426704575919 ) ) ;
#34974=CARTESIAN_POINT ( 'NONE',  ( 0.1092355843206037486, -41.57624119012380959, -11.45151637801112976 ) ) ;
#34977=( BOUNDED_SURFACE ( )  B_SPLINE_SURFACE ( 3, 1, ( 
 ( #42732, #4466 ),
 ( #31784, #629 ),
 ( #46199, #41816 ),
 ( #23304, #19769 ) ),
 .UNSPECIFIED., .F., .F., .F. ) 
 B_SPLINE_SURFACE_WITH_KNOTS ( ( 4, 4 ),
 ( 2, 2 ),
 ( 0.000000000000000000, 1.000000000000000000 ),
 ( 0.000000000000000000, 1.000000000000000000 ),
 .UNSPECIFIED. ) 
 GEOMETRIC_REPRESENTATION_ITEM ( )  RATIONAL_B_SPLINE_SURFACE ( (
 ( 1.000000000000000000, 1.000000000000000000),
 ( 0.7223157951917476005, 0.9931996967497186413),
 ( 0.7223157951917476005, 0.9931996967497186413),
 ( 1.000000000000000000, 1.000000000000000000) ) ) 
 REPRESENTATION_ITEM ( '' )  SURFACE ( )  );
#34979=B_SPLINE_CURVE_WITH_KNOTS ( 'NONE', 3,
 ( #35435, #11619, #30704, #26019, #40450, #2184, #59513, #45454, #2503, #57488, #61277, #18703, #37837, #32811, #51568, #18396 ),
 .UNSPECIFIED., .F., .F.,
 ( 4, 3, 3, 3, 3, 4 ),
 ( 2.221635811791082109E-17, 0.0002618515315864343332, 0.0003927756766341896429, 0.0005236998216950500837, 0.0007855159896329812251, 0.001047349442285922232 ),
 .UNSPECIFIED. ) ;
#34984=LINE ( 'NONE', #11470, #43431 ) ;
#34986=ADVANCED_FACE ( 'NONE', ( #51570 ), #61541, .F. ) ;
#34991=CARTESIAN_POINT ( 'NONE',  ( 0.5998501479064708430, 17.92509395669044636, 44.64337787626254794 ) ) ;
#34992=CARTESIAN_POINT ( 'NONE',  ( 0.6017667736363750963, -0.3491025323183876150, 48.10631678344240925 ) ) ;
#34993=CARTESIAN_POINT ( 'NONE',  ( 0.8751705887134423323, -29.98056538504989277, 37.60752970653777538 ) ) ;
#34996=ORIENTED_EDGE ( 'NONE', *, *, #41663, .F. ) ;
#35003=CARTESIAN_POINT ( 'NONE',  ( 0.1103744047535531458, 41.66501489234563849, -11.12399292196393397 ) ) ;
#35009=CARTESIAN_POINT ( 'NONE',  ( 0.1101816497532063510, -11.29256821151185086, -41.61967362528552883 ) ) ;
#35022=CARTESIAN_POINT ( 'NONE',  ( 4.975801465491694664, -26.14269827151650816, -40.15204426031524321 ) ) ;
#35029=CARTESIAN_POINT ( 'NONE',  ( 0.6017667736363750963, 44.57803721604151548, -18.08696174077343954 ) ) ;
#35043=CARTESIAN_POINT ( 'NONE',  ( 5.880360259849752858, 39.86101557989634614, 26.69116321728584751 ) ) ;
#35050=CARTESIAN_POINT ( 'NONE',  ( 0.3622758884714730732, 25.58609868863768355, -34.70015533914803285 ) ) ;
#35051=CARTESIAN_POINT ( 'NONE',  ( 0.1100247026804066219, 30.37337782329848679, 30.61332956994592536 ) ) ;
#35054=VERTEX_POINT ( 'NONE', #26549 ) ;
#35069=CARTESIAN_POINT ( 'NONE',  ( 0.1064266379913941102, 0.5615183164811746730, 43.12102052820964104 ) ) ;
#35075=ORIENTED_EDGE ( 'NONE', *, *, #45100, .T. ) ;
#35078=CARTESIAN_POINT ( 'NONE',  ( 0.1073791018717483448, 43.12183934961191056, -0.4849339620928847516 ) ) ;
#35081=CARTESIAN_POINT ( 'NONE',  ( 0.1092565886968784317, -41.57372480460693254, 11.46097737058291344 ) ) ;
#35082=ORIENTED_EDGE ( 'NONE', *, *, #32155, .F. ) ;
#35084=CARTESIAN_POINT ( 'NONE',  ( 4.975801465491695552, -47.10002938642136883, -8.787181743659990829 ) ) ;
#35086=EDGE_CURVE ( 'NONE', #2003, #35399, #32202, .T. ) ;
#35091=CARTESIAN_POINT ( 'NONE',  ( 0.8751705887134423323, -33.37254303619531726, -34.63284514348573850 ) ) ;
#35092=ORIENTED_EDGE ( 'NONE', *, *, #25662, .T. ) ;
#35098=CARTESIAN_POINT ( 'NONE',  ( 0.7954190325252809002, 41.21355377862698788, -24.79809930825941677 ) ) ;
#35100=EDGE_LOOP ( 'NONE', ( #61109, #54555, #13906, #1856 ) ) ;
#35104=ORIENTED_EDGE ( 'NONE', *, *, #60290, .F. ) ;
#35105=EDGE_CURVE ( 'NONE', #11373, #17098, #9756, .T. ) ;
#35118=EDGE_CURVE ( 'NONE', #35637, #13776, #46392, .T. ) ;
#35119=ORIENTED_EDGE ( 'NONE', *, *, #42025, .T. ) ;
#35121=CARTESIAN_POINT ( 'NONE',  ( 0.8751705887134423323, 23.27176129838367302, 42.09020928323383259 ) ) ;
#35125=CARTESIAN_POINT ( 'NONE',  ( 0.5988103564986354543, 37.79415694022860350, -29.76496605343807289 ) ) ;
#35129=CARTESIAN_POINT ( 'NONE',  ( 0.5980894510889457338, 38.59343625445407611, 28.72954109785617405 ) ) ;
#35130=CARTESIAN_POINT ( 'NONE',  ( 0.8751705887134423323, 44.08562551107055327, 19.22545746485676688 ) ) ;
#35140=DIRECTION ( 'NONE',  ( 0.09835009131224552170, 0.6981896185982721104, -0.7091251765523998163 ) ) ;
#35148=ORIENTED_EDGE ( 'NONE', *, *, #9474, .T. ) ;
#35153=EDGE_CURVE ( 'NONE', #58534, #6671, #16536, .T. ) ;
#35154=CARTESIAN_POINT ( 'NONE',  ( 0.5998501479064708430, -11.94461217097437000, -46.60114184914313995 ) ) ;
#35156=ORIENTED_EDGE ( 'NONE', *, *, #134, .T. ) ;
#35157=CARTESIAN_POINT ( 'NONE',  ( 0.3622758884714600280, 37.74294673546586409, -20.83792692158932525 ) ) ;
#35160=ORIENTED_EDGE ( 'NONE', *, *, #45023, .F. ) ;
#35164=EDGE_LOOP ( 'NONE', ( #9652, #36948, #41343, #55531 ) ) ;
#35168=FACE_OUTER_BOUND ( 'NONE', #35475, .T. ) ;
#35170=VERTEX_POINT ( 'NONE', #8410 ) ;
#35173=EDGE_CURVE ( 'NONE', #42065, #34651, #23151, .T. ) ;
#35189=CARTESIAN_POINT ( 'NONE',  ( 4.975801465491694664, 8.787181743659507660, 47.10002938642145409 ) ) ;
#35192=CARTESIAN_POINT ( 'NONE',  ( 0.3622758884714600280, 6.444611261694588755, -42.62881903538203687 ) ) ;
#35196=CARTESIAN_POINT ( 'NONE',  ( 0.1073791018717578927, 26.63563652260167203, -33.91564619577780348 ) ) ;
#35200=CIRCLE ( 'NONE', #8167, 10.00000000000000000 ) ;
#35201=CARTESIAN_POINT ( 'NONE',  ( 0.1313383488274132704, -43.11882601516400371, 0.6377633466099100756 ) ) ;
#35207=CARTESIAN_POINT ( 'NONE',  ( 2.643462169533613793, 46.73820883660191328, 11.09243630552549398 ) ) ;
#35212=CARTESIAN_POINT ( 'NONE',  ( -6.010958268070873523, -14.95835081545466139, -11.45964880703842326 ) ) ;
#35213=CARTESIAN_POINT ( 'NONE',  ( 4.975801465491695552, -47.76942479135487929, 3.702618843596635401 ) ) ;
#35221=VERTEX_POINT ( 'NONE', #13445 ) ;
#35229=CARTESIAN_POINT ( 'NONE',  ( 0.6030672727741701600, 6.192762795893809624, 47.70721108823350676 ) ) ;
#35232=( BOUNDED_SURFACE ( )  B_SPLINE_SURFACE ( 3, 1, ( 
 ( #35516, #6640 ),
 ( #16091, #7272 ),
 ( #54895, #35207 ),
 ( #45236, #31104 ) ),
 .UNSPECIFIED., .F., .F., .F. ) 
 B_SPLINE_SURFACE_WITH_KNOTS ( ( 4, 4 ),
 ( 2, 2 ),
 ( 0.000000000000000000, 1.000000000000000000 ),
 ( 0.000000000000000000, 1.000000000000000000 ),
 .UNSPECIFIED. ) 
 GEOMETRIC_REPRESENTATION_ITEM ( )  RATIONAL_B_SPLINE_SURFACE ( (
 ( 1.000000000000000000, 1.000000000000000000),
 ( 0.7223157951917476005, 0.9931996967497186413),
 ( 0.7223157951917476005, 0.9931996967497186413),
 ( 1.000000000000000000, 1.000000000000000000) ) ) 
 REPRESENTATION_ITEM ( '' )  SURFACE ( )  );
#35235=CARTESIAN_POINT ( 'NONE',  ( -6.017396004339686577, -18.20079405513553183, 4.878103249821005072 ) ) ;
#35238=CARTESIAN_POINT ( 'NONE',  ( 0.7048096507298635682, -7.115188260603519055, -47.58126109679101035 ) ) ;
#35245=( BOUNDED_SURFACE ( )  B_SPLINE_SURFACE ( 3, 1, ( 
 ( #34052, #39066 ),
 ( #53424, #30239 ),
 ( #49352, #1720 ),
 ( #20857, #54336 ) ),
 .UNSPECIFIED., .F., .F., .F. ) 
 B_SPLINE_SURFACE_WITH_KNOTS ( ( 4, 4 ),
 ( 2, 2 ),
 ( 0.000000000000000000, 1.000000000000000000 ),
 ( 0.000000000000000000, 1.000000000000000000 ),
 .UNSPECIFIED. ) 
 GEOMETRIC_REPRESENTATION_ITEM ( )  RATIONAL_B_SPLINE_SURFACE ( (
 ( 1.000000000000000000, 1.000000000000000000),
 ( 0.7223157951917480446, 0.9931996967497186413),
 ( 0.7223157951917480446, 0.9931996967497186413),
 ( 1.000000000000000000, 1.000000000000000000) ) ) 
 REPRESENTATION_ITEM ( '' )  SURFACE ( )  );
#35247=CARTESIAN_POINT ( 'NONE',  ( -6.015611763856276717, -7.205255340944737519, 17.41126425312535275 ) ) ;
#35253=ORIENTED_EDGE ( 'NONE', *, *, #24899, .F. ) ;
#35258=ORIENTED_EDGE ( 'NONE', *, *, #9615, .T. ) ;
#35259=CARTESIAN_POINT ( 'NONE',  ( 0.8751705887134423323, 11.58504748649134974, 46.67919521768892110 ) ) ;
#35266=CARTESIAN_POINT ( 'NONE',  ( 0.6254087463353908971, 42.00124903776036689, 23.45485308995613849 ) ) ;
#35277=CARTESIAN_POINT ( 'NONE',  ( 0.1103310638050661874, -41.63362651001257575, -11.24099191366984662 ) ) ;
#35282=ORIENTED_EDGE ( 'NONE', *, *, #27078, .T. ) ;
#35285=CARTESIAN_POINT ( 'NONE',  ( 4.549368137175248350, 2.596185425821941894, -42.84816078363927971 ) ) ;
#35303=CARTESIAN_POINT ( 'NONE',  ( 0.6041374136657476912, 38.05989626241430557, -29.42442150067158835 ) ) ;
#35307=VERTEX_POINT ( 'NONE', #48194 ) ;
#35308=AXIS2_PLACEMENT_3D ( 'NONE', #20056, #5594, #43879 ) ;
#35309=EDGE_CURVE ( 'NONE', #45423, #21910, #54548, .T. ) ;
#35310=CARTESIAN_POINT ( 'NONE',  ( -6.016104459813371719, 7.215917642689068323, 17.40682403289250857 ) ) ;
#35311=CARTESIAN_POINT ( 'NONE',  ( 0.1095718737110179114, -39.74279513315663337, -16.74012863188490741 ) ) ;
#35312=CARTESIAN_POINT ( 'NONE',  ( 4.549368137175248350, 0.000000000000000000, 0.000000000000000000 ) ) ;
#35313=ORIENTED_EDGE ( 'NONE', *, *, #1861, .F. ) ;
#35314=EDGE_CURVE ( 'NONE', #10336, #45553, #768, .T. ) ;
#35316=CARTESIAN_POINT ( 'NONE',  ( 0.1087620492084206275, -0.3620418170789792556, 43.12302841504342155 ) ) ;
#35323=CARTESIAN_POINT ( 'NONE',  ( 0.1310142868023712048, -37.02349354742227661, -22.11113027429274425 ) ) ;
#35326=ORIENTED_EDGE ( 'NONE', *, *, #860, .F. ) ;
#35330=CARTESIAN_POINT ( 'NONE',  ( -6.010958268070873523, 7.197664668556443601, 17.41463273278780832 ) ) ;
#35332=B_SPLINE_CURVE_WITH_KNOTS ( 'NONE', 3,
 ( #16401, #40542, #26104, #22335 ),
 .UNSPECIFIED., .F., .F.,
 ( 4, 4 ),
 ( 0.000000000000000000, 0.005014147105413701254 ),
 .UNSPECIFIED. ) ;
#35335=CARTESIAN_POINT ( 'NONE',  ( -6.016761891674565099, -17.41015286184807209, 7.207804629151251419 ) ) ;
#35337=EDGE_LOOP ( 'NONE', ( #21943, #12698, #8424, #52371 ) ) ;
#35346=VERTEX_POINT ( 'NONE', #48483 ) ;
#35349=( BOUNDED_SURFACE ( )  B_SPLINE_SURFACE ( 3, 1, ( 
 ( #25011, #29694 ),
 ( #21229, #39436 ),
 ( #10921, #1481 ),
 ( #20315, #25931 ) ),
 .UNSPECIFIED., .F., .F., .F. ) 
 B_SPLINE_SURFACE_WITH_KNOTS ( ( 4, 4 ),
 ( 2, 2 ),
 ( 0.000000000000000000, 1.000000000000000000 ),
 ( 0.000000000000000000, 1.000000000000000000 ),
 .UNSPECIFIED. ) 
 GEOMETRIC_REPRESENTATION_ITEM ( )  RATIONAL_B_SPLINE_SURFACE ( (
 ( 1.000000000000000000, 1.000000000000000000),
 ( 0.9751682680413298332, 0.9999560080971552356),
 ( 0.9751682680413298332, 0.9999560080971552356),
 ( 1.000000000000000000, 1.000000000000000000) ) ) 
 REPRESENTATION_ITEM ( '' )  SURFACE ( )  );
#35354=B_SPLINE_CURVE_WITH_KNOTS ( 'NONE', 3,
 ( #3735, #8439, #36373, #31968, #50743, #18177 ),
 .UNSPECIFIED., .F., .F.,
 ( 4, 2, 4 ),
 ( 8.558167549966217657E-17, 0.0002293366620881433855, 0.0004586733241762012275 ),
 .UNSPECIFIED. ) ;
#35359=CARTESIAN_POINT ( 'NONE',  ( 0.1073791018717483448, -6.109314776652422729, -42.68962945260951614 ) ) ;
#35362=CARTESIAN_POINT ( 'NONE',  ( 5.880360259849739535, 3.184717612777296036, 47.86623372148050493 ) ) ;
#35371=CARTESIAN_POINT ( 'NONE',  ( 0.6001305935487422083, -41.92422178329185556, 23.60027211631757638 ) ) ;
#35375=CARTESIAN_POINT ( 'NONE',  ( -6.016761891674565099, 18.20201388312102253, -4.873659902332176053 ) ) ;
#35381=CARTESIAN_POINT ( 'NONE',  ( 0.5980894510889448457, 47.78766676462075935, -5.583794302584760061 ) ) ;
#35389=CARTESIAN_POINT ( 'NONE',  ( 0.1103310638050661735, -41.67627416617921199, 11.08182869403221815 ) ) ;
#35399=VERTEX_POINT ( 'NONE', #34408 ) ;
#35404=VERTEX_POINT ( 'NONE', #29684 ) ;
#35405=FACE_OUTER_BOUND ( 'NONE', #38044, .T. ) ;
#35432=CARTESIAN_POINT ( 'NONE',  ( 3.680882792899937250, 4.423598386734397536, -47.77138407787918339 ) ) ;
#35435=CARTESIAN_POINT ( 'NONE',  ( 0.5998501479064708430, -28.86886762351098312, -38.48283596222019298 ) ) ;
#35439=EDGE_CURVE ( 'NONE', #12663, #39207, #38191, .T. ) ;
#35446=EDGE_CURVE ( 'NONE', #15365, #11373, #12783, .T. ) ;
#35465=B_SPLINE_CURVE_WITH_KNOTS ( 'NONE', 3,
 ( #6165, #4946, #9984, #20611 ),
 .UNSPECIFIED., .F., .F.,
 ( 4, 4 ),
 ( 2.602085213965210642E-18, 0.004566006591234643766 ),
 .UNSPECIFIED. ) ;
#35466=EDGE_CURVE ( 'NONE', #59804, #6825, #25922, .T. ) ;
#35467=CARTESIAN_POINT ( 'NONE',  ( 0.5998501479064699549, -12.95623334615470057, -46.33007877220734372 ) ) ;
#35475=EDGE_LOOP ( 'NONE', ( #644, #17128, #30279, #37030 ) ) ;
#35477=VERTEX_POINT ( 'NONE', #59105 ) ;
#35481=CARTESIAN_POINT ( 'NONE',  ( 0.6041374136657475802, -41.57494627055128689, -24.20487816031505801 ) ) ;
#35483=CARTESIAN_POINT ( 'NONE',  ( 0.1101816497532063233, 0.1358190954549551299, 43.12424935764384060 ) ) ;
#35484=CARTESIAN_POINT ( 'NONE',  ( 4.549368137175248350, 40.71620287708344677, -13.59764261105707739 ) ) ;
#35487=CARTESIAN_POINT ( 'NONE',  ( 0.1073791018717483448, 0.4849339620927342054, 43.12183934961191767 ) ) ;
#35489=CARTESIAN_POINT ( 'NONE',  ( 0.7954190325252790128, 13.28627193046304278, 46.22745637125046159 ) ) ;
#35491=ORIENTED_EDGE ( 'NONE', *, *, #5318, .F. ) ;
#35492=CARTESIAN_POINT ( 'NONE',  ( 0.1073791018717483448, 41.77800844988500018, 10.69234304550068337 ) ) ;
#35502=EDGE_CURVE ( 'NONE', #23847, #24034, #26175, .T. ) ;
#35503=ORIENTED_EDGE ( 'NONE', *, *, #23880, .T. ) ;
#35506=CARTESIAN_POINT ( 'NONE',  ( 0.5988103564986355654, 28.80261217992921985, -38.53259703935803060 ) ) ;
#35508=CARTESIAN_POINT ( 'NONE',  ( 0.1103744047535531458, -39.85659247569272168, 16.46720136312911364 ) ) ;
#35516=CARTESIAN_POINT ( 'NONE',  ( -5.995132425357893702, -18.19985213254568635, -4.885449473615521399 ) ) ;
#35521=CARTESIAN_POINT ( 'NONE',  ( 0.2230388203127593172, -11.89247826311245682, -41.44703429209680223 ) ) ;
#35528=EDGE_CURVE ( 'NONE', #55047, #57783, #19539, .T. ) ;
#35529=CARTESIAN_POINT ( 'NONE',  ( 4.975801465491695552, 45.55012473237732706, 14.85979367497190040 ) ) ;
#35531=ORIENTED_EDGE ( 'NONE', *, *, #4331, .T. ) ;
#35532=EDGE_LOOP ( 'NONE', ( #2489, #11374, #20198, #47327 ) ) ;
#35535=CARTESIAN_POINT ( 'NONE',  ( -6.016761891674564211, 18.68243340030203115, 2.456125503350775841 ) ) ;
#35543=ORIENTED_EDGE ( 'NONE', *, *, #21042, .F. ) ;
#35551=CARTESIAN_POINT ( 'NONE',  ( 4.549368137175248350, -40.71620287708353914, 13.59764261105679317 ) ) ;
#35554=CARTESIAN_POINT ( 'NONE',  ( 0.6001305935487315502, -48.10757715638248300, 0.5236757026887750577 ) ) ;
#35557=CARTESIAN_POINT ( 'NONE',  ( 0.7048096507298579061, 19.18768066167122655, -44.11842270945954425 ) ) ;
#35561=CARTESIAN_POINT ( 'NONE',  ( -6.010958268070873523, -9.409153349053472226, -16.32616437357121697 ) ) ;
#35566=CARTESIAN_POINT ( 'NONE',  ( 0.1073791018717483448, 37.58707531572176919, 21.14095454447572564 ) ) ;
#35567=CARTESIAN_POINT ( 'NONE',  ( 0.6017666602106489515, 46.55749120190029799, 12.11361215600196140 ) ) ;
#35570=EDGE_LOOP ( 'NONE', ( #58187, #36625, #54719, #43488 ) ) ;
#35575=CARTESIAN_POINT ( 'NONE',  ( 50.00005079999999680, 12.80000000000000071, 3.000000000000000000 ) ) ;
#35586=EDGE_CURVE ( 'NONE', #55407, #58295, #18644, .T. ) ;
#35592=DIRECTION ( 'NONE',  ( 0.000000000000000000, 0.000000000000000000, 1.000000000000000000 ) ) ;
#35593=ADVANCED_FACE ( 'NONE', ( #19010 ), #55141, .F. ) ;
#35597=ORIENTED_EDGE ( 'NONE', *, *, #25592, .T. ) ;
#35600=CARTESIAN_POINT ( 'NONE',  ( 0.5998501479064708430, 44.64337787626247689, -17.92509395669061689 ) ) ;
#35602=CARTESIAN_POINT ( 'NONE',  ( 4.549368137175248350, -38.59302160394766901, 18.79584381673463866 ) ) ;
#35603=CARTESIAN_POINT ( 'NONE',  ( 0.8751705887134553219, -28.56654290188682666, 38.69254731947783199 ) ) ;
#35606=CARTESIAN_POINT ( 'NONE',  ( 0.6027935024548038978, -44.51201578381240864, 18.24855952726150932 ) ) ;
#35609=CARTESIAN_POINT ( 'NONE',  ( 0.6031356755773454870, 41.66225520948404437, -24.05374386753673122 ) ) ;
#35612=CARTESIAN_POINT ( 'NONE',  ( 0.8751705887134423323, 7.160166390004303771, -47.55935879196464100 ) ) ;
#35613=ORIENTED_EDGE ( 'NONE', *, *, #44743, .F. ) ;
#35616=FACE_OUTER_BOUND ( 'NONE', #53478, .T. ) ;
#35622=CARTESIAN_POINT ( 'NONE',  ( 0.1073791018717578927, -10.69234304550026593, -41.77800844988510676 ) ) ;
#35627=CARTESIAN_POINT ( 'NONE',  ( 0.1098349054025745952, -10.95525583467247266, -41.70974743324811129 ) ) ;
#35632=CARTESIAN_POINT ( 'NONE',  ( 0.5998501479064699549, -11.94461217097501837, 46.60114184914296942 ) ) ;
#35636=FACE_OUTER_BOUND ( 'NONE', #38037, .T. ) ;
#35637=VERTEX_POINT ( 'NONE', #60641 ) ;
#35649=DIRECTION ( 'NONE',  ( -1.000000000000000000, 0.000000000000000000, 0.000000000000000000 ) ) ;
#35656=CARTESIAN_POINT ( 'NONE',  ( 4.833616638992208614, 38.20222678111939274, -26.07076047129095642 ) ) ;
#35657=ORIENTED_EDGE ( 'NONE', *, *, #45096, .T. ) ;
#35661=ORIENTED_EDGE ( 'NONE', *, *, #22156, .T. ) ;
#35667=CARTESIAN_POINT ( 'NONE',  ( 4.691466044806102076, 24.49380602310761290, 37.25818859570315311 ) ) ;
#35668=CARTESIAN_POINT ( 'NONE',  ( 0.1087620492084206414, -5.269740196867624071, -42.80136086877931945 ) ) ;
#35673=CARTESIAN_POINT ( 'NONE',  ( 0.1073791018717578927, 37.58707531572206051, -21.14095454447521405 ) ) ;
#35676=ORIENTED_EDGE ( 'NONE', *, *, #51400, .T. ) ;
#35678=DIRECTION ( 'NONE',  ( 0.000000000000000000, 0.000000000000000000, -1.000000000000000000 ) ) ;
#35679=DIRECTION ( 'NONE',  ( 0.09835009131224567436, -0.2650256080583827112, 0.9592125346408675313 ) ) ;
#35684=LINE ( 'NONE', #25952, #55072 ) ;
#35690=DIRECTION ( 'NONE',  ( 0.000000000000000000, 0.000000000000000000, -1.000000000000000000 ) ) ;
#35692=CARTESIAN_POINT ( 'NONE',  ( 0.2885700199627513340, 0.8047882683532806558, 43.10898996868493782 ) ) ;
#35695=CARTESIAN_POINT ( 'NONE',  ( 0.6254311100348646235, 11.78487556908942224, 46.64066536338341251 ) ) ;
#35698=CARTESIAN_POINT ( 'NONE',  ( 0.1103744047535531458, 11.19884698423366842, -41.64495780681027526 ) ) ;
#35700=DIRECTION ( 'NONE',  ( -1.000000000000000000, 0.000000000000000000, -0.000000000000000000 ) ) ;
#35706=ORIENTED_EDGE ( 'NONE', *, *, #51837, .T. ) ;
#35707=CARTESIAN_POINT ( 'NONE',  ( 4.833616638992208614, 14.43699082351714225, -43.93936707042086454 ) ) ;
#35722=CARTESIAN_POINT ( 'NONE',  ( 0.1102847568649952675, -26.32556309315093301, -34.15672344772079327 ) ) ;
#35724=ORIENTED_EDGE ( 'NONE', *, *, #38138, .F. ) ;
#35726=VERTEX_POINT ( 'NONE', #29003 ) ;
#35727=CARTESIAN_POINT ( 'NONE',  ( 0.1084644655670281010, 11.54510651093203144, 41.55047717876508528 ) ) ;
#35741=CARTESIAN_POINT ( 'NONE',  ( 1.827326673878742147, -22.58371678864607901, 36.65065268305619384 ) ) ;
#35746=DIRECTION ( 'NONE',  ( 1.000000000000000000, 0.000000000000000000, 0.000000000000000000 ) ) ;
#35749=( GEOMETRIC_REPRESENTATION_CONTEXT ( 3 ) GLOBAL_UNCERTAINTY_ASSIGNED_CONTEXT ( ( #17350 ) ) GLOBAL_UNIT_ASSIGNED_CONTEXT ( ( #20710, #31032, #21328 ) ) REPRESENTATION_CONTEXT ( 'NONE', 'WORKASPACE' ) );
#35752=EDGE_LOOP ( 'NONE', ( #3076, #12992, #40447, #5010 ) ) ;
#35760=CARTESIAN_POINT ( 'NONE',  ( 4.833616638992208614, -3.476827473557542625, -46.11947910922908989 ) ) ;
#35763=CARTESIAN_POINT ( 'NONE',  ( 4.691466044806102964, -40.13652286047907580, 19.42108863068307301 ) ) ;
#35771=EDGE_LOOP ( 'NONE', ( #12729, #46064, #57687, #28426 ) ) ;
#35773=CARTESIAN_POINT ( 'NONE',  ( 4.975801465491695552, 14.85979367497174408, -45.55012473237738391 ) ) ;
#35779=B_SPLINE_CURVE_WITH_KNOTS ( 'NONE', 3,
 ( #54675, #11804, #60005, #30883 ),
 .UNSPECIFIED., .F., .F.,
 ( 4, 4 ),
 ( 0.000000000000000000, 0.004445488388166994251 ),
 .UNSPECIFIED. ) ;
#35785=VECTOR ( 'NONE', #28848, 1000.000000000000114 ) ;
#35791=CARTESIAN_POINT ( 'NONE',  ( 0.5988103622719987973, 41.96244039798791903, -23.52668907282300736 ) ) ;
#35793=ORIENTED_EDGE ( 'NONE', *, *, #49707, .F. ) ;
#35796=CARTESIAN_POINT ( 'NONE',  ( 0.8760168074887076939, -5.394043284319854692, 47.80016357497240165 ) ) ;
#35801=CARTESIAN_POINT ( 'NONE',  ( 0.1102144999581333024, -30.58258619461942729, 30.40435207217175773 ) ) ;
#35805=CIRCLE ( 'NONE', #49778, 47.91270532121795611 ) ;
#35813=CARTESIAN_POINT ( 'NONE',  ( -6.015611763856276717, -11.47596948473801248, -14.94556629257436953 ) ) ;
#35814=EDGE_CURVE ( 'NONE', #40338, #2450, #52230, .T. ) ;
#35826=CARTESIAN_POINT ( 'NONE',  ( 0.6029303876144825880, 12.57751758557269994, -46.43417959025978803 ) ) ;
#35845=CARTESIAN_POINT ( 'NONE',  ( 0.8751705887134553219, -48.08707113907594533, 0.8911681664086766874 ) ) ;
#35852=ORIENTED_EDGE ( 'NONE', *, *, #59974, .F. ) ;
#35856=EDGE_CURVE ( 'NONE', #19448, #31565, #50031, .T. ) ;
#35857=ORIENTED_EDGE ( 'NONE', *, *, #27497, .F. ) ;
#35858=CARTESIAN_POINT ( 'NONE',  ( 0.6001305935487315502, 6.798494447612227098, -47.62765676940936999 ) ) ;
#35860=CARTESIAN_POINT ( 'NONE',  ( 4.549368137175248350, 24.02461520945223228, 35.57418903283122802 ) ) ;
#35864=VECTOR ( 'NONE', #19996, 1000.000000000000000 ) ;
#35867=CARTESIAN_POINT ( 'NONE',  ( -2.569797478183790229, -7.701637110048767276, 12.44213550320639783 ) ) ;
#35881=CARTESIAN_POINT ( 'NONE',  ( 4.549368137175248350, 0.000000000000000000, 0.000000000000000000 ) ) ;
#35886=EDGE_CURVE ( 'NONE', #10420, #23287, #55639, .T. ) ;
#35887=CARTESIAN_POINT ( 'NONE',  ( 0.1103878639767399555, -42.74915604780183997, 5.676988162227942780 ) ) ;
#35903=CARTESIAN_POINT ( 'NONE',  ( 5.880360259849752858, -9.405269135695570881, 47.04104239318750302 ) ) ;
#35904=CARTESIAN_POINT ( 'NONE',  ( 0.8751705887134553219, 0.8911681664081729792, 48.08707113907595243 ) ) ;
#35905=CARTESIAN_POINT ( 'NONE',  ( 0.3622758884714600280, 31.06363466427727360, -29.89648521331598729 ) ) ;
#35908=CARTESIAN_POINT ( 'NONE',  ( 0.3622758884714600280, -31.06363466427748321, 29.89648521331577058 ) ) ;
#35911=( BOUNDED_SURFACE ( )  B_SPLINE_SURFACE ( 3, 1, ( 
 ( #15239, #34047 ),
 ( #14939, #58727 ),
 ( #38751, #30540 ),
 ( #15542, #39673 ) ),
 .UNSPECIFIED., .F., .F., .F. ) 
 B_SPLINE_SURFACE_WITH_KNOTS ( ( 4, 4 ),
 ( 2, 2 ),
 ( 0.000000000000000000, 1.000000000000000000 ),
 ( 0.000000000000000000, 1.000000000000000000 ),
 .UNSPECIFIED. ) 
 GEOMETRIC_REPRESENTATION_ITEM ( )  RATIONAL_B_SPLINE_SURFACE ( (
 ( 1.000000000000000000, 1.000000000000000000),
 ( 0.9751682680413298332, 0.9999560080971552356),
 ( 0.9751682680413298332, 0.9999560080971552356),
 ( 1.000000000000000000, 1.000000000000000000) ) ) 
 REPRESENTATION_ITEM ( '' )  SURFACE ( )  );
#35921=CARTESIAN_POINT ( 'NONE',  ( 4.549368137175248350, -2.596185425821630588, -42.84816078363929392 ) ) ;
#35926=CARTESIAN_POINT ( 'NONE',  ( 0.1100053167205930910, 41.60823192620008371, -11.33468317718512530 ) ) ;
#35929=CARTESIAN_POINT ( 'NONE',  ( 0.8760168074886965917, -17.58183840866369252, -44.77533136581875084 ) ) ;
#35939=CARTESIAN_POINT ( 'NONE',  ( 0.5998501479064699549, -28.86886762351154090, 38.48283596221978797 ) ) ;
#35951=CARTESIAN_POINT ( 'NONE',  ( 0.6017667736363750963, -47.64919355032684223, -6.625250263233462888 ) ) ;
#35952=ADVANCED_FACE ( 'NONE', ( #56414 ), #21127, .F. ) ;
#35956=ORIENTED_EDGE ( 'NONE', *, *, #20697, .T. ) ;
#35959=ORIENTED_EDGE ( 'NONE', *, *, #33245, .T. ) ;
#35961=EDGE_CURVE ( 'NONE', #13656, #6553, #42356, .T. ) ;
#35967=CARTESIAN_POINT ( 'NONE',  ( 4.691466044806103852, 36.88741755356070229, -25.04870410140750181 ) ) ;
#35975=ORIENTED_EDGE ( 'NONE', *, *, #41331, .T. ) ;
#35983=CARTESIAN_POINT ( 'NONE',  ( 0.1102144999581333024, 37.40973521037463456, -21.45299314243954925 ) ) ;
#35985=CONICAL_SURFACE ( 'NONE', #43996, 42.92674063221959813, 1.485477209440487556 ) ;
#35986=ORIENTED_EDGE ( 'NONE', *, *, #1330, .F. ) ;
#35996=( BOUNDED_SURFACE ( )  B_SPLINE_SURFACE ( 3, 1, ( 
 ( #54289, #30494 ),
 ( #12892, #11731 ),
 ( #30809, #49929 ),
 ( #25194, #53987 ) ),
 .UNSPECIFIED., .F., .F., .F. ) 
 B_SPLINE_SURFACE_WITH_KNOTS ( ( 4, 4 ),
 ( 2, 2 ),
 ( 0.000000000000000000, 1.000000000000000000 ),
 ( 0.000000000000000000, 1.000000000000000000 ),
 .UNSPECIFIED. ) 
 GEOMETRIC_REPRESENTATION_ITEM ( )  RATIONAL_B_SPLINE_SURFACE ( (
 ( 1.000000000000000000, 1.000000000000000000),
 ( 0.9953040768229005630, 0.8617119497784937465),
 ( 0.9953040768229005630, 0.8617119497784937465),
 ( 1.000000000000000000, 1.000000000000000000) ) ) 
 REPRESENTATION_ITEM ( '' )  SURFACE ( )  );
#36024=CARTESIAN_POINT ( 'NONE',  ( 3.238931869106853600, 41.96286875554255147, 9.350562014686273571 ) ) ;
#36027=CARTESIAN_POINT ( 'NONE',  ( -6.010958268070873523, 4.863021950010902650, -18.20513189769803120 ) ) ;
#36029=CARTESIAN_POINT ( 'NONE',  ( 0.1073791018717483448, 25.86618856530710531, -34.50606437925521419 ) ) ;
#36030=ORIENTED_EDGE ( 'NONE', *, *, #61021, .T. ) ;
#36031=CARTESIAN_POINT ( 'NONE',  ( 0.7246131072078574320, -46.66866179549023741, 11.65529928397556780 ) ) ;
#36035=CARTESIAN_POINT ( 'NONE',  ( 0.1081432562775998113, -25.91533557232866869, -34.46918062033742558 ) ) ;
#36039=CARTESIAN_POINT ( 'NONE',  ( -6.015611763856276717, -0.006214430185273883862, 18.84324252354755203 ) ) ;
#36042=CARTESIAN_POINT ( 'NONE',  ( -6.016761891674565099, 13.32172022638591713, 13.32657647165359904 ) ) ;
#36047=ORIENTED_EDGE ( 'NONE', *, *, #36899, .T. ) ;
#36055=CARTESIAN_POINT ( 'NONE',  ( 4.691466044806103852, -2.583163953528794021, 44.51344083442434396 ) ) ;
#36057=CARTESIAN_POINT ( 'NONE',  ( 0.1103744047535531458, -42.75042227379824311, -5.667281528142243729 ) ) ;
#36061=CARTESIAN_POINT ( 'NONE',  ( -6.016489644550737204, -14.94663725562907963, -11.47450955518503335 ) ) ;
#36071=ORIENTED_EDGE ( 'NONE', *, *, #49227, .F. ) ;
#36076=CARTESIAN_POINT ( 'NONE',  ( 0.1084644655670282121, -16.86976209534753224, -39.68806829486941012 ) ) ;
#36084=ORIENTED_EDGE ( 'NONE', *, *, #45813, .T. ) ;
#36093=ORIENTED_EDGE ( 'NONE', *, *, #54001, .F. ) ;
#36097=ADVANCED_FACE ( 'NONE', ( #49188 ), #25142, .F. ) ;
#36101=ORIENTED_EDGE ( 'NONE', *, *, #32303, .F. ) ;
#36107=ORIENTED_EDGE ( 'NONE', *, *, #12697, .F. ) ;
#36108=LINE ( 'NONE', #42045, #59720 ) ;
#36109=CIRCLE ( 'NONE', #52073, 42.92674063221959813 ) ;
#36111=ORIENTED_EDGE ( 'NONE', *, *, #61228, .T. ) ;
#36122=B_SPLINE_CURVE_WITH_KNOTS ( 'NONE', 3,
 ( #44559, #31053, #6907, #36393 ),
 .UNSPECIFIED., .F., .F.,
 ( 4, 4 ),
 ( 2.256078575551061230E-17, 0.004564976165746191181 ),
 .UNSPECIFIED. ) ;
#36133=CARTESIAN_POINT ( 'NONE',  ( 0.1101816497532063371, 34.29544870207477913, 26.14462713083307221 ) ) ;
#36139=CARTESIAN_POINT ( 'NONE',  ( 0.6017667736363749853, 12.78803812527888262, -46.37677940471285609 ) ) ;
#36141=CARTESIAN_POINT ( 'NONE',  ( 0.1073791018717483448, 34.50606437925512182, 25.86618856530722610 ) ) ;
#36149=CARTESIAN_POINT ( 'NONE',  ( 0.1097557419366048670, -0.2231007852156707827, -43.12388302211984126 ) ) ;
#36151=CARTESIAN_POINT ( 'NONE',  ( -6.001507490154111224, -18.68469198366098283, 2.444174634178074790 ) ) ;
#36157=ORIENTED_EDGE ( 'NONE', *, *, #46922, .F. ) ;
#36160=CARTESIAN_POINT ( 'NONE',  ( 0.1103744047535531458, -37.36621271144552026, 21.52865142340072424 ) ) ;
#36167=CARTESIAN_POINT ( 'NONE',  ( 0.8760168074887076939, -33.37827814204148780, 34.63873394077430135 ) ) ;
#36168=EDGE_CURVE ( 'NONE', #55625, #32395, #56010, .T. ) ;
#36169=ORIENTED_EDGE ( 'NONE', *, *, #51977, .T. ) ;
#36173=EDGE_CURVE ( 'NONE', #47659, #45115, #5182, .T. ) ;
#36174=CARTESIAN_POINT ( 'NONE',  ( 0.1087620492084205720, 21.24797679669908135, 37.52665900408526056 ) ) ;
#36185=ORIENTED_EDGE ( 'NONE', *, *, #46483, .F. ) ;
#36191=CARTESIAN_POINT ( 'NONE',  ( 0.5980894510889457338, 47.60453381548693130, -6.974827154143607544 ) ) ;
#36192=ORIENTED_EDGE ( 'NONE', *, *, #48810, .T. ) ;
#36193=CARTESIAN_POINT ( 'NONE',  ( 0.1100053167205930632, 42.73174076921944220, -5.806749312984677225 ) ) ;
#36195=CARTESIAN_POINT ( 'NONE',  ( 4.549368137175248350, 24.02461520945223228, 35.57418903283122802 ) ) ;
#36199=CARTESIAN_POINT ( 'NONE',  ( 1.827119703190779765, -20.44859290426063936, 37.88337895042260328 ) ) ;
#36202=CARTESIAN_POINT ( 'NONE',  ( 0.1064266379913943739, -34.55203636557793345, -25.80493164505191217 ) ) ;
#36217=EDGE_CURVE ( 'NONE', #16197, #22082, #12809, .T. ) ;
#36219=CARTESIAN_POINT ( 'NONE',  ( 0.6009453534118439633, -44.61081284455544704, 18.00606795643196989 ) ) ;
#36225=ORIENTED_EDGE ( 'NONE', *, *, #36924, .T. ) ;
#36234=AXIS2_PLACEMENT_3D ( 'NONE', #15651, #34755, #53821 ) ;
#36235=ORIENTED_EDGE ( 'NONE', *, *, #60765, .T. ) ;
#36239=CARTESIAN_POINT ( 'NONE',  ( 0.1092355843206037486, -39.72582785521905890, -16.78033551728650608 ) ) ;
#36266=ORIENTED_EDGE ( 'NONE', *, *, #19067, .T. ) ;
#36269=CARTESIAN_POINT ( 'NONE',  ( 0.1098349054025746507, -26.42143025180014604, 34.08267426123914134 ) ) ;
#36280=CARTESIAN_POINT ( 'NONE',  ( 0.8751705887134553219, -44.08562551107095828, 19.22545746485582185 ) ) ;
#36281=CARTESIAN_POINT ( 'NONE',  ( 0.1064266418746776799, 41.79703894102872397, -10.61815661559954904 ) ) ;
#36284=CARTESIAN_POINT ( 'NONE',  ( 0.1084644655670282398, 37.14658555883732305, -21.90577137312953582 ) ) ;
#36287=B_SPLINE_CURVE_WITH_KNOTS ( 'NONE', 3,
 ( #55973, #41002, #12789, #12471, #8058, #22471 ),
 .UNSPECIFIED., .F., .F.,
 ( 4, 2, 4 ),
 ( 1.266823315017301927E-16, 0.0002450741128632358116, 0.0004901482257263448800 ),
 .UNSPECIFIED. ) ;
#36288=ADVANCED_FACE ( 'NONE', ( #42906 ), #55783, .F. ) ;
#36293=CARTESIAN_POINT ( 'NONE',  ( 0.5980894510889448457, -47.78766676462080909, 5.583794302584446534 ) ) ;
#36298=CARTESIAN_POINT ( 'NONE',  ( 0.6009453534118439633, 37.89911869481691298, 29.63106322864197750 ) ) ;
#36315=CARTESIAN_POINT ( 'NONE',  ( 0.1095718737110177865, 11.40943879390648696, -41.58781525899398446 ) ) ;
#36316=EDGE_CURVE ( 'NONE', #22472, #45586, #11092, .T. ) ;
#36317=CARTESIAN_POINT ( 'NONE',  ( -6.001507490154110336, 18.68469198366097217, 2.444174634178205796 ) ) ;
#36323=B_SPLINE_CURVE_WITH_KNOTS ( 'NONE', 3,
 ( #12433, #7703, #53756, #10889 ),
 .UNSPECIFIED., .F., .F.,
 ( 4, 4 ),
 ( 7.152448122690996019E-18, 0.005014147105413695182 ),
 .UNSPECIFIED. ) ;
#36329=CARTESIAN_POINT ( 'NONE',  ( 4.549368137175248350, 42.06008734272383975, 8.582197505784577629 ) ) ;
#36330=ORIENTED_EDGE ( 'NONE', *, *, #57282, .T. ) ;
#36343=FACE_OUTER_BOUND ( 'NONE', #8655, .T. ) ;
#36345=VECTOR ( 'NONE', #17652, 1000.000000000000114 ) ;
#36346=ORIENTED_EDGE ( 'NONE', *, *, #21657, .T. ) ;
#36355=CARTESIAN_POINT ( 'NONE',  ( 0.6254087463353916743, 6.960754339421171721, 47.60024110474255110 ) ) ;
#36358=ORIENTED_EDGE ( 'NONE', *, *, #29175, .F. ) ;
#36360=CARTESIAN_POINT ( 'NONE',  ( 0.1097557419366048670, -21.75515245866099079, -37.23482781437637357 ) ) ;
#36364=CARTESIAN_POINT ( 'NONE',  ( 0.1084644655670283508, -42.80575641816244570, -5.234391617063844926 ) ) ;
#36370=CARTESIAN_POINT ( 'NONE',  ( 0.8751705887134553219, -5.393078191593054349, 47.79200036674269825 ) ) ;
#36372=ADVANCED_FACE ( 'NONE', ( #29389 ), #53136, .F. ) ;
#36373=CARTESIAN_POINT ( 'NONE',  ( 0.2230388203127633140, 39.54016926433973111, -17.20066002792375670 ) ) ;
#36380=EDGE_CURVE ( 'NONE', #51524, #4311, #53654, .T. ) ;
#36381=CARTESIAN_POINT ( 'NONE',  ( 4.549368137175248350, -19.17571786012351254, 38.40568845698243194 ) ) ;
#36383=CARTESIAN_POINT ( 'NONE',  ( -2.708315649062916552, -14.47261168455371028, 2.171184472130447851 ) ) ;
#36388=CARTESIAN_POINT ( 'NONE',  ( 0.2224561200757615154, -0.7594684977688249683, 43.11279565427788185 ) ) ;
#36393=CARTESIAN_POINT ( 'NONE',  ( 4.549368137175248350, -40.71620287708334018, -13.59764261105737404 ) ) ;
#36405=CARTESIAN_POINT ( 'NONE',  ( 0.6023143664670691511, 29.07782746490703474, 38.32505149877522399 ) ) ;
#36435=CARTESIAN_POINT ( 'NONE',  ( 0.5998501479064708430, 23.59887241503295741, 41.92175333043627461 ) ) ;
#36437=FACE_OUTER_BOUND ( 'NONE', #13598, .T. ) ;
#36451=CARTESIAN_POINT ( 'NONE',  ( 0.6023142530420679819, -34.20176999054685041, -33.83147280953675562 ) ) ;
#36455=CARTESIAN_POINT ( 'NONE',  ( 0.2885700199627512785, 43.10898996868493072, -0.8047882683534313131 ) ) ;
#36464=CARTESIAN_POINT ( 'NONE',  ( 0.7954190325252782356, -48.09103420665682194, 0.8690070772087629125 ) ) ;
#36472=ORIENTED_EDGE ( 'NONE', *, *, #16994, .F. ) ;
#36483=ORIENTED_EDGE ( 'NONE', *, *, #53235, .F. ) ;
#36495=CARTESIAN_POINT ( 'NONE',  ( 0.1084644655670281427, 39.68806829486948118, -16.86976209534739723 ) ) ;
#36501=CARTESIAN_POINT ( 'NONE',  ( 0.5980894510889457338, 11.77356634613317787, -46.65000524237075297 ) ) ;
#36506=CARTESIAN_POINT ( 'NONE',  ( -6.016104459813374383, -0.005335450885198452994, 18.84322058118302223 ) ) ;
#36508=B_SPLINE_CURVE_WITH_KNOTS ( 'NONE', 3,
 ( #2025, #21156, #11773, #30852, #7027, #59659, #26158, #35887, #56506, #9514, #47137, #57112, #4481, #27708, #9211, #37130, #61504, #13941, #3879 ),
 .UNSPECIFIED., .F., .F.,
 ( 4, 3, 3, 3, 3, 3, 4 ),
 ( 1.153344816771540786E-16, 0.0002618519381806248326, 0.0003927759815485966800, 0.0005237000248299420206, 0.0006546240681324977167, 0.0007855481115631320586, 0.0009699050456655102914 ),
 .UNSPECIFIED. ) ;
#36516=CARTESIAN_POINT ( 'NONE',  ( 4.833616638992208614, -38.70560126501845843, -25.31740731790884524 ) ) ;
#36517=ORIENTED_EDGE ( 'NONE', *, *, #7132, .T. ) ;
#36519=CARTESIAN_POINT ( 'NONE',  ( 0.6041374136657476912, -6.106202762793827787, 47.71861871402578714 ) ) ;
#36524=CARTESIAN_POINT ( 'NONE',  ( -6.015611763856276717, 0.006214430185405465240, -18.84324252354755203 ) ) ;
#36526=PRODUCT_CONTEXT ( 'NONE', #39569, 'mechanical' ) ;
#36533=ORIENTED_EDGE ( 'NONE', *, *, #56564, .F. ) ;
#36536=CARTESIAN_POINT ( 'NONE',  ( -6.010958268070873523, 7.224487401384299012, 17.40352239307059534 ) ) ;
#36539=EDGE_LOOP ( 'NONE', ( #48652, #2550, #37029, #51317 ) ) ;
#36542=CARTESIAN_POINT ( 'NONE',  ( 0.7246131072078538793, -29.92944207473678375, 37.65685186358339109 ) ) ;
#36543=VERTEX_POINT ( 'NONE', #59741 ) ;
#36550=ORIENTED_EDGE ( 'NONE', *, *, #37941, .T. ) ;
#36556=CARTESIAN_POINT ( 'NONE',  ( 0.1310142868023682905, 11.77532653407838836, -41.48473022063170390 ) ) ;
#36565=ORIENTED_EDGE ( 'NONE', *, *, #6086, .T. ) ;
#36569=ORIENTED_EDGE ( 'NONE', *, *, #38914, .T. ) ;
#36574=CARTESIAN_POINT ( 'NONE',  ( 0.6254087463353902310, 44.17672642933501237, -19.04342133627998379 ) ) ;
#36575=CARTESIAN_POINT ( 'NONE',  ( 4.975801465491695552, 0.000000000000000000, 0.000000000000000000 ) ) ;
#36584=CARTESIAN_POINT ( 'NONE',  ( 0.5998501479064708430, 47.76154736470757456, -5.759754759340284913 ) ) ;
#36585=CARTESIAN_POINT ( 'NONE',  ( 4.549368137175248350, -42.84816078363928682, -2.596185425821792236 ) ) ;
#36588=EDGE_CURVE ( 'NONE', #29999, #58167, #20651, .T. ) ;
#36589=CARTESIAN_POINT ( 'NONE',  ( 1.827119703190779765, 12.32825544177779165, 41.24693285842933221 ) ) ;
#36599=B_SPLINE_CURVE_WITH_KNOTS ( 'NONE', 3,
 ( #37840, #56891, #41595, #41913 ),
 .UNSPECIFIED., .F., .F.,
 ( 4, 4 ),
 ( 2.091695478256946045E-17, 0.004444306975806114161 ),
 .UNSPECIFIED. ) ;
#36608=( BOUNDED_SURFACE ( )  B_SPLINE_SURFACE ( 3, 1, ( 
 ( #2617, #26127 ),
 ( #49939, #35238 ),
 ( #1996, #26428 ),
 ( #6994, #44641 ) ),
 .UNSPECIFIED., .F., .F., .F. ) 
 B_SPLINE_SURFACE_WITH_KNOTS ( ( 4, 4 ),
 ( 2, 2 ),
 ( 0.000000000000000000, 1.000000000000000000 ),
 ( 0.000000000000000000, 1.000000000000000000 ),
 .UNSPECIFIED. ) 
 GEOMETRIC_REPRESENTATION_ITEM ( )  RATIONAL_B_SPLINE_SURFACE ( (
 ( 1.000000000000000000, 1.000000000000000000),
 ( 0.9953040768229005630, 0.8617119497784937465),
 ( 0.9953040768229005630, 0.8617119497784937465),
 ( 1.000000000000000000, 1.000000000000000000) ) ) 
 REPRESENTATION_ITEM ( '' )  SURFACE ( )  );
#36609=CARTESIAN_POINT ( 'NONE',  ( 0.1073791018717483448, -40.02496097243048467, -16.05399293000801819 ) ) ;
#36624=CARTESIAN_POINT ( 'NONE',  ( 0.6009453534118439633, 24.43073772334918203, -41.44251633523867184 ) ) ;
#36625=ORIENTED_EDGE ( 'NONE', *, *, #37883, .F. ) ;
#36629=CARTESIAN_POINT ( 'NONE',  ( -6.015611763856276717, -11.46610900684713030, -14.95313250337441424 ) ) ;
#36634=CARTESIAN_POINT ( 'NONE',  ( 0.1073791018717483448, 26.63563652260123149, 33.91564619577815165 ) ) ;
#36641=EDGE_CURVE ( 'NONE', #39264, #12159, #47828, .T. ) ;
#36647=ORIENTED_EDGE ( 'NONE', *, *, #2746, .F. ) ;
#36653=CARTESIAN_POINT ( 'NONE',  ( 4.691466044806102076, -44.51344083442437238, 2.583163953528321066 ) ) ;
#36655=CARTESIAN_POINT ( 'NONE',  ( 4.549368137175248350, 0.000000000000000000, 0.000000000000000000 ) ) ;
#36661=CARTESIAN_POINT ( 'NONE',  ( 4.549368137175248350, 19.17571786012269541, 38.40568845698284406 ) ) ;
#36662=CARTESIAN_POINT ( 'NONE',  ( 0.1313383488274128541, -42.66669366003527841, 6.260443365526650261 ) ) ;
#36678=LINE ( 'NONE', #55749, #2685 ) ;
#36682=CARTESIAN_POINT ( 'NONE',  ( 0.1103878639767399278, 21.52017980327898528, -37.37111717125851840 ) ) ;
#36688=EDGE_CURVE ( 'NONE', #37892, #7602, #59661, .T. ) ;
#36699=CARTESIAN_POINT ( 'NONE',  ( -6.016489644550737204, 11.47450955518509552, -14.94663725562903878 ) ) ;
#36703=FACE_OUTER_BOUND ( 'NONE', #57340, .T. ) ;
#36710=ORIENTED_EDGE ( 'NONE', *, *, #44374, .T. ) ;
#36711=CARTESIAN_POINT ( 'NONE',  ( 0.5998501479064708430, 46.33007877220720871, 12.95623334615518374 ) ) ;
#36718=VERTEX_POINT ( 'NONE', #19945 ) ;
#36719=EDGE_CURVE ( 'NONE', #21910, #29055, #6096, .T. ) ;
#36720=CARTESIAN_POINT ( 'NONE',  ( 2.643462169533613793, -42.27470921730922981, -22.81120928486480892 ) ) ;
#36724=ADVANCED_FACE ( 'NONE', ( #58416 ), #6270, .F. ) ;
#36733=ORIENTED_EDGE ( 'NONE', *, *, #11057, .F. ) ;
#36736=ORIENTED_EDGE ( 'NONE', *, *, #33394, .F. ) ;
#36739=ADVANCED_FACE ( 'NONE', ( #5790 ), #15105, .F. ) ;
#36743=CARTESIAN_POINT ( 'NONE',  ( 3.680882792899938138, 47.94008871805919370, -1.849662971457720850 ) ) ;
#36747=ORIENTED_EDGE ( 'NONE', *, *, #36688, .T. ) ;
#36751=CARTESIAN_POINT ( 'NONE',  ( 0.6041374136657475802, 41.57494627055111636, 24.20487816031535289 ) ) ;
#36759=EDGE_CURVE ( 'NONE', #42953, #52918, #51449, .T. ) ;
#36762=CARTESIAN_POINT ( 'NONE',  ( 0.8760168074887076939, -38.69913431881803945, -28.57146030081966259 ) ) ;
#36764=EDGE_CURVE ( 'NONE', #50490, #42276, #22085, .T. ) ;
#36765=CARTESIAN_POINT ( 'NONE',  ( -6.015611763856276717, 16.32183393015596451, 9.416239407363361735 ) ) ;
#36769=CARTESIAN_POINT ( 'NONE',  ( 3.680974057930773924, 25.57193971028160107, -40.59247216052828122 ) ) ;
#36770=ORIENTED_EDGE ( 'NONE', *, *, #16275, .T. ) ;
#36777=DIRECTION ( 'NONE',  ( 0.09835009131224552170, -0.8656670924898581809, -0.4908642831975333354 ) ) ;
#36778=ORIENTED_EDGE ( 'NONE', *, *, #22208, .T. ) ;
#36781=CARTESIAN_POINT ( 'NONE',  ( 0.6023142530420679819, 6.538792732869218582, 47.66103033449100934 ) ) ;
#36783=B_SPLINE_CURVE_WITH_KNOTS ( 'NONE', 3,
 ( #59312, #49303, #44634, #45556, #6361, #2610, #21115, #16117, #21733, #36160, #40873, #53988, #16419, #16732, #44336, #45259, #40559, #44950, #7294 ),
 .UNSPECIFIED., .F., .F.,
 ( 4, 3, 3, 3, 3, 3, 4 ),
 ( 1.149162571898268292E-16, 0.0002618519381806262963, 0.0003927759815485967884, 0.0005237000248299434300, 0.0006546240681324954399, 0.0007855481115631328176, 0.0009699050456655098577 ),
 .UNSPECIFIED. ) ;
#36789=CARTESIAN_POINT ( 'NONE',  ( 0.1073791018717483448, -0.4849339620930353534, -43.12183934961191056 ) ) ;
#36792=CARTESIAN_POINT ( 'NONE',  ( 2.301529144917015657, -47.77346141661147527, -4.990866136406468812 ) ) ;
#36794=B_SPLINE_CURVE_WITH_KNOTS ( 'NONE', 3,
 ( #27910, #47032, #51383, #23209, #3460, #36711 ),
 .UNSPECIFIED., .F., .F.,
 ( 4, 2, 4 ),
 ( 1.266794085606387986E-16, 0.0002450741128632358658, 0.0004901482257263449884 ),
 .UNSPECIFIED. ) ;
#36795=CARTESIAN_POINT ( 'NONE',  ( 0.1104177457020372732, 21.56646482560080003, 37.34442418285510001 ) ) ;
#36796=EDGE_CURVE ( 'NONE', #9480, #49434, #11451, .T. ) ;
#36801=ORIENTED_EDGE ( 'NONE', *, *, #34964, .F. ) ;
#36802=CARTESIAN_POINT ( 'NONE',  ( 0.6041374136657475802, -12.61972904329631540, 46.42299778158134416 ) ) ;
#36803=CARTESIAN_POINT ( 'NONE',  ( -6.010958268070873523, -0.01451635840150067996, -18.84344976839986785 ) ) ;
#36804=CARTESIAN_POINT ( 'NONE',  ( 0.6017666602106490625, 33.76944145963975075, -34.26316403931524235 ) ) ;
#36811=FACE_OUTER_BOUND ( 'NONE', #44054, .T. ) ;
#36814=CARTESIAN_POINT ( 'NONE',  ( -6.015611763856276717, 13.31979030221799398, 13.32857883366838081 ) ) ;
#36818=VECTOR ( 'NONE', #30463, 1000.000000000000114 ) ;
#36822=FACE_OUTER_BOUND ( 'NONE', #13143, .T. ) ;
#36824=CARTESIAN_POINT ( 'NONE',  ( 4.691466044806103852, -43.79545162262303393, -8.371234562541701507 ) ) ;
#36827=CARTESIAN_POINT ( 'NONE',  ( -6.001507490154110336, -16.32705935667500796, -9.408444979392495355 ) ) ;
#36836=B_SPLINE_CURVE_WITH_KNOTS ( 'NONE', 3,
 ( #903, #53513, #40092, #30332 ),
 .UNSPECIFIED., .F., .F.,
 ( 4, 4 ),
 ( 5.818439421673297140E-18, 0.004566006591234648103 ),
 .UNSPECIFIED. ) ;
#36844=SHAPE_DEFINITION_REPRESENTATION ( #29395, #8803 ) ;
#36848=CARTESIAN_POINT ( 'NONE',  ( 1.827326673878742813, 33.38933471001438846, 27.17438009792344289 ) ) ;
#36852=LINE ( 'NONE', #8007, #53151 ) ;
#36855=ORIENTED_EDGE ( 'NONE', *, *, #5865, .F. ) ;
#36871=ORIENTED_EDGE ( 'NONE', *, *, #55087, .F. ) ;
#36881=VERTEX_POINT ( 'NONE', #7650 ) ;
#36882=ORIENTED_EDGE ( 'NONE', *, *, #5242, .T. ) ;
#36888=FACE_OUTER_BOUND ( 'NONE', #21192, .T. ) ;
#36891=CARTESIAN_POINT ( 'NONE',  ( -6.016489644550737204, 7.215050741358277619, -17.40716454747921915 ) ) ;
#36894=CARTESIAN_POINT ( 'NONE',  ( 0.1092355843206037486, -26.49036028133807363, 34.02913268098544819 ) ) ;
#36895=VERTEX_POINT ( 'NONE', #44990 ) ;
#36898=DIRECTION ( 'NONE',  ( 0.000000000000000000, 0.000000000000000000, 1.000000000000000000 ) ) ;
#36899=EDGE_CURVE ( 'NONE', #60202, #51250, #36508, .T. ) ;
#36907=CARTESIAN_POINT ( 'NONE',  ( 0.1102144999581333024, 26.35238362727840311, -34.13606714958023503 ) ) ;
#36909=ORIENTED_EDGE ( 'NONE', *, *, #28940, .F. ) ;
#36910=CARTESIAN_POINT ( 'NONE',  ( 0.1100247026804066219, 37.43141430507372291, -21.41511734445759529 ) ) ;
#36912=EDGE_LOOP ( 'NONE', ( #2, #7469, #28169, #23139 ) ) ;
#36913=CIRCLE ( 'NONE', #22890, 42.92674063221959813 ) ;
#36914=CARTESIAN_POINT ( 'NONE',  ( 0.8751705887134553219, -41.19904111682524928, 24.81530984069135570 ) ) ;
#36919=CARTESIAN_POINT ( 'NONE',  ( -6.001507490154110336, -18.84387066167321478, 0.01557731607546725128 ) ) ;
#36922=CARTESIAN_POINT ( 'NONE',  ( 0.6009452777970412107, 38.43042656245034294, 28.93864923253911314 ) ) ;
#36924=EDGE_CURVE ( 'NONE', #45586, #15076, #28693, .T. ) ;
#36926=CARTESIAN_POINT ( 'NONE',  ( 0.8751705887134423323, -44.08562551107069538, -19.22545746485646490 ) ) ;
#36930=CARTESIAN_POINT ( 'NONE',  ( 0.2885700199627522777, 31.05173037893199606, 29.91358789498793058 ) ) ;
#36939=CARTESIAN_POINT ( 'NONE',  ( -5.995132425357893702, -18.68405145320022243, -2.451215106828539714 ) ) ;
#36942=ORIENTED_EDGE ( 'NONE', *, *, #53350, .F. ) ;
#36944=CARTESIAN_POINT ( 'NONE',  ( 0.6028618097248863439, 23.90242650600276519, -41.74935807801021781 ) ) ;
#36947=ADVANCED_FACE ( 'NONE', ( #36822 ), #23149, .F. ) ;
#36948=ORIENTED_EDGE ( 'NONE', *, *, #18601, .F. ) ;
#36951=CARTESIAN_POINT ( 'NONE',  ( 0.2885700199627497242, 22.25146206940414118, 36.93108631019301669 ) ) ;
#36953=CARTESIAN_POINT ( 'NONE',  ( 0.5998501479064708430, -28.86886762351098312, -38.48283596222019298 ) ) ;
#36958=CARTESIAN_POINT ( 'NONE',  ( 0.1073791018717483448, -26.63563652260144821, -33.91564619577798823 ) ) ;
#36960=B_SPLINE_CURVE_WITH_KNOTS ( 'NONE', 3,
 ( #18945, #14856, #9515, #16383, #6021, #19866, #29857, #48972, #48657, #35508, #44604, #10770, #20465, #54566, #11697, #1642, #49269, #6956, #11077 ),
 .UNSPECIFIED., .F., .F.,
 ( 4, 3, 3, 3, 3, 3, 4 ),
 ( 1.153344816771540786E-16, 0.0002618519381806232063, 0.0003927759815485975473, 0.0005237000248299442974, 0.0006546240681324945725, 0.0007855481115631333597, 0.0009699050456655120261 ),
 .UNSPECIFIED. ) ;
#36963=VERTEX_POINT ( 'NONE', #18322 ) ;
#36966=B_SPLINE_CURVE_WITH_KNOTS ( 'NONE', 3,
 ( #3795, #31711, #22935, #26382 ),
 .UNSPECIFIED., .F., .F.,
 ( 4, 4 ),
 ( 6.992893892674702526E-18, 0.004566006591234645501 ),
 .UNSPECIFIED. ) ;
#36967=ORIENTED_EDGE ( 'NONE', *, *, #18167, .F. ) ;
#36970=CARTESIAN_POINT ( 'NONE',  ( 4.975801465491695552, -26.14269827151708370, 40.15204426031488794 ) ) ;
#36977=EDGE_CURVE ( 'NONE', #55224, #20551, #26715, .T. ) ;
#36985=CARTESIAN_POINT ( 'NONE',  ( 0.1073791018717578927, -42.68962945260949482, -6.109314776652552403 ) ) ;
#36987=( BOUNDED_SURFACE ( )  B_SPLINE_SURFACE ( 3, 1, ( 
 ( #6688, #59640 ),
 ( #10820, #26137 ),
 ( #29911, #20222 ),
 ( #49631, #2005 ) ),
 .UNSPECIFIED., .F., .F., .F. ) 
 B_SPLINE_SURFACE_WITH_KNOTS ( ( 4, 4 ),
 ( 2, 2 ),
 ( 0.000000000000000000, 1.000000000000000000 ),
 ( 0.000000000000000000, 1.000000000000000000 ),
 .UNSPECIFIED. ) 
 GEOMETRIC_REPRESENTATION_ITEM ( )  RATIONAL_B_SPLINE_SURFACE ( (
 ( 1.000000000000000000, 1.000000000000000000),
 ( 0.7223157951917476005, 0.9931996967497186413),
 ( 0.7223157951917476005, 0.9931996967497186413),
 ( 1.000000000000000000, 1.000000000000000000) ) ) 
 REPRESENTATION_ITEM ( '' )  SURFACE ( )  );
#36998=CARTESIAN_POINT ( 'NONE',  ( 0.5988103622719984642, 37.79415722405556721, 29.76496569135174752 ) ) ;
#37004=ADVANCED_FACE ( 'NONE', ( #8582 ), #8306, .F. ) ;
#37013=VERTEX_POINT ( 'NONE', #46517 ) ;
#37017=CARTESIAN_POINT ( 'NONE',  ( 0.5998501479064708430, -38.48283596222049141, 28.86886762351059588 ) ) ;
#37024=FACE_OUTER_BOUND ( 'NONE', #30081, .T. ) ;
#37029=ORIENTED_EDGE ( 'NONE', *, *, #34731, .F. ) ;
#37030=ORIENTED_EDGE ( 'NONE', *, *, #18837, .T. ) ;
#37034=ORIENTED_EDGE ( 'NONE', *, *, #7416, .F. ) ;
#37036=ADVANCED_FACE ( 'NONE', ( #41832 ), #51491, .T. ) ;
#37042=VECTOR ( 'NONE', #49247, 1000.000000000000000 ) ;
#37044=CARTESIAN_POINT ( 'NONE',  ( 0.3622758884714730732, -11.95365414648468594, -41.42293301073622303 ) ) ;
#37045=ORIENTED_EDGE ( 'NONE', *, *, #5508, .T. ) ;
#37048=ORIENTED_EDGE ( 'NONE', *, *, #3170, .F. ) ;
#37052=CARTESIAN_POINT ( 'NONE',  ( 0.1313383488274123267, 11.77600546273712290, 41.48452234694100582 ) ) ;
#37053=EDGE_LOOP ( 'NONE', ( #36778, #25678, #57378, #46339 ) ) ;
#37056=EDGE_LOOP ( 'NONE', ( #21484, #37096, #42160, #60952 ) ) ;
#37060=CARTESIAN_POINT ( 'NONE',  ( -6.016761891674565099, 18.68243340030205957, -2.456125503350522710 ) ) ;
#37068=EDGE_CURVE ( 'NONE', #29664, #40762, #5711, .T. ) ;
#37070=CARTESIAN_POINT ( 'NONE',  ( -6.001507490154111224, -7.225628667346702727, 17.40350523682693051 ) ) ;
#37078=CARTESIAN_POINT ( 'NONE',  ( 0.6001305935487422083, -47.62765676940938420, -6.798494447612039693 ) ) ;
#37082=ORIENTED_EDGE ( 'NONE', *, *, #24309, .T. ) ;
#37084=ORIENTED_EDGE ( 'NONE', *, *, #49698, .T. ) ;
#37089=VERTEX_POINT ( 'NONE', #48354 ) ;
#37095=ORIENTED_EDGE ( 'NONE', *, *, #61142, .F. ) ;
#37096=ORIENTED_EDGE ( 'NONE', *, *, #17771, .T. ) ;
#37097=ADVANCED_FACE ( 'NONE', ( #47745 ), #18692, .F. ) ;
#37099=EDGE_CURVE ( 'NONE', #25364, #45115, #10141, .T. ) ;
#37100=FACE_OUTER_BOUND ( 'NONE', #17364, .T. ) ;
#37106=CARTESIAN_POINT ( 'NONE',  ( 0.8751705887134553219, -47.79200036674276220, -5.393078191592532988 ) ) ;
#37108=CARTESIAN_POINT ( 'NONE',  ( 0.6025881611877910160, -48.10699274197334319, -0.2181813582436762100 ) ) ;
#37110=EDGE_LOOP ( 'NONE', ( #5482, #34550, #39012, #26813 ) ) ;
#37114=CARTESIAN_POINT ( 'NONE',  ( 0.5998501479064699549, 33.64490850298844293, -34.38546660123262200 ) ) ;
#37117=B_SPLINE_CURVE_WITH_KNOTS ( 'NONE', 3,
 ( #27236, #41659, #13153, #32253, #46666, #3709, #22845, #54798, #31009, #50118, #26305, #2487, #21611, #40751, #236, #33183, #32565, #14080, #13453 ),
 .UNSPECIFIED., .F., .F.,
 ( 4, 3, 3, 3, 3, 3, 4 ),
 ( 1.185767046459373819E-16, 0.0002618519381806248868, 0.0003927759815485954331, 0.0005237000248299434300, 0.0006546240681324973915, 0.0007855481115631293481, 0.0009699050456655103998 ),
 .UNSPECIFIED. ) ;
#37122=ADVANCED_FACE ( 'NONE', ( #14854 ), #42737, .F. ) ;
#37123=CARTESIAN_POINT ( 'NONE',  ( 0.1097557419366048670, 39.75589591229785924, -16.70891382096329281 ) ) ;
#37125=CARTESIAN_POINT ( 'NONE',  ( 0.1073791018717578927, 42.81622261970994003, -5.147744207006430983 ) ) ;
#37130=CARTESIAN_POINT ( 'NONE',  ( 0.1092355843206037486, -42.79374386763049642, 5.330717085612596939 ) ) ;
#37135=CARTESIAN_POINT ( 'NONE',  ( 0.2230388203127650903, -34.66629317821153222, -25.64246103889284356 ) ) ;
#37137=CARTESIAN_POINT ( 'NONE',  ( 0.1064266379913941934, 42.67882137217590355, -6.185137063632576648 ) ) ;
#37147=DIRECTION ( 'NONE',  ( -0.1024043820194934229, 0.6159418278945659742, -0.7811075516170014055 ) ) ;
#37148=CARTESIAN_POINT ( 'NONE',  ( 0.1104177457020373287, 42.75615561261993491, 5.624018123398786706 ) ) ;
#37151=EDGE_CURVE ( 'NONE', #21383, #31710, #37172, .T. ) ;
#37152=CARTESIAN_POINT ( 'NONE',  ( 4.975801465491695552, -35.64402118370979622, 32.01766832630250548 ) ) ;
#37162=VERTEX_POINT ( 'NONE', #35196 ) ;
#37165=CARTESIAN_POINT ( 'NONE',  ( 4.975801465491695552, 42.71626295676264817, -21.70134120755155394 ) ) ;
#37167=ORIENTED_EDGE ( 'NONE', *, *, #48749, .F. ) ;
#37170=CARTESIAN_POINT ( 'NONE',  ( -2.569797478183790229, 12.89088113963436122, -6.924386868080713242 ) ) ;
#37172=B_SPLINE_CURVE_WITH_KNOTS ( 'NONE', 3,
 ( #25153, #43060, #98, #57411, #14549, #33652 ),
 .UNSPECIFIED., .F., .F.,
 ( 4, 2, 4 ),
 ( 1.870559545977334001E-17, 0.0002293319059085101167, 0.0004586638118170015309 ),
 .UNSPECIFIED. ) ;
#37174=VECTOR ( 'NONE', #18983, 1000.000000000000227 ) ;
#37177=VERTEX_POINT ( 'NONE', #58974 ) ;
#37179=CARTESIAN_POINT ( 'NONE',  ( -6.016489644550737204, -18.84320342686341121, -0.004404229197973906322 ) ) ;
#37185=VERTEX_POINT ( 'NONE', #36435 ) ;
#37186=EDGE_LOOP ( 'NONE', ( #50539, #15814, #44164, #29780 ) ) ;
#37187=CARTESIAN_POINT ( 'NONE',  ( 4.549368137175248350, 35.57418903283115696, -24.02461520945233531 ) ) ;
#37192=EDGE_LOOP ( 'NONE', ( #53692, #41045, #36565, #48691 ) ) ;
#37199=ORIENTED_EDGE ( 'NONE', *, *, #54052, .T. ) ;
#37200=CARTESIAN_POINT ( 'NONE',  ( 0.5998501479064699549, -33.64490850298868452, 34.38546660123239462 ) ) ;
#37203=B_SPLINE_CURVE_WITH_KNOTS ( 'NONE', 3,
 ( #30724, #54510, #50455, #36388, #59220, #7522 ),
 .UNSPECIFIED., .F., .F.,
 ( 4, 2, 4 ),
 ( 1.807478856737577690E-17, 0.0002293319059085094391, 0.0004586638118170007720 ),
 .UNSPECIFIED. ) ;
#37210=VERTEX_POINT ( 'NONE', #16699 ) ;
#37212=CARTESIAN_POINT ( 'NONE',  ( 4.833616638992208614, 38.70560126501828080, 25.31740731790911880 ) ) ;
#37214=CARTESIAN_POINT ( 'NONE',  ( 50.00005079999999680, 0.000000000000000000, 0.000000000000000000 ) ) ;
#37216=CARTESIAN_POINT ( 'NONE',  ( 4.833616638992208614, 43.93936707042080059, 14.43699082351728968 ) ) ;
#37223=EDGE_CURVE ( 'NONE', #29664, #26668, #23731, .T. ) ;
#37228=EDGE_CURVE ( 'NONE', #1703, #20061, #20735, .T. ) ;
#37229=CARTESIAN_POINT ( 'NONE',  ( 0.1100247026804066219, -5.797046384220175597, 42.73303500775676866 ) ) ;
#37241=FACE_OUTER_BOUND ( 'NONE', #22231, .T. ) ;
#37246=DIRECTION ( 'NONE',  ( -1.000000000000000000, -0.000000000000000000, -0.000000000000000000 ) ) ;
#37247=CARTESIAN_POINT ( 'NONE',  ( 0.6017666602106489515, 23.75081624637622113, -41.83584962818292752 ) ) ;
#37253=VERTEX_POINT ( 'NONE', #56430 ) ;
#37258=B_SPLINE_CURVE_WITH_KNOTS ( 'NONE', 3,
 ( #35602, #44693, #6415, #39690 ),
 .UNSPECIFIED., .F., .F.,
 ( 4, 4 ),
 ( 6.254634441385501517E-18, 0.004566006591234648970 ),
 .UNSPECIFIED. ) ;
#37260=ORIENTED_EDGE ( 'NONE', *, *, #34873, .F. ) ;
#37270=CARTESIAN_POINT ( 'NONE',  ( 0.6023143664670691511, -34.20175727332151894, 33.83148565876871317 ) ) ;
#37278=VERTEX_POINT ( 'NONE', #12940 ) ;
#37280=CARTESIAN_POINT ( 'NONE',  ( 0.1103310638050662290, -21.49083802119874775, -37.38800124003704184 ) ) ;
#37283=CARTESIAN_POINT ( 'NONE',  ( 0.1104177457020373010, -34.20994892372227270, 26.25638621857933686 ) ) ;
#37293=CARTESIAN_POINT ( 'NONE',  ( 0.3622758884714600280, -15.73321244754826509, -40.13994584881776007 ) ) ;
#37302=CARTESIAN_POINT ( 'NONE',  ( 4.833616638992205949, 38.70560126501862896, -25.31740731790855747 ) ) ;
#37310=ORIENTED_EDGE ( 'NONE', *, *, #37571, .F. ) ;
#37312=DIRECTION ( 'NONE',  ( -1.000000000000000000, -0.000000000000000000, -0.000000000000000000 ) ) ;
#37314=B_SPLINE_CURVE_WITH_KNOTS ( 'NONE', 3,
 ( #3666, #22799, #41930, #56298 ),
 .UNSPECIFIED., .F., .F.,
 ( 4, 4 ),
 ( 0.000000000000000000, 0.005014147105413703856 ),
 .UNSPECIFIED. ) ;
#37318=CARTESIAN_POINT ( 'NONE',  ( -6.016104459813374383, 18.68131780085931837, 2.464823636987509392 ) ) ;
#37321=CARTESIAN_POINT ( 'NONE',  ( 0.6027935024548037868, 29.14731236071017051, 38.27223087442856553 ) ) ;
#37338=VERTEX_POINT ( 'NONE', #15633 ) ;
#37340=CARTESIAN_POINT ( 'NONE',  ( 0.5998501479064708430, 29.69975237324613460, -37.84527566984826308 ) ) ;
#37343=CARTESIAN_POINT ( 'NONE',  ( 4.975801465491695552, -2.564218696447830403, 47.84403947906839250 ) ) ;
#37354=( BOUNDED_SURFACE ( )  B_SPLINE_SURFACE ( 3, 1, ( 
 ( #17037, #54908 ),
 ( #36151, #60223 ),
 ( #21104, #26109 ),
 ( #30798, #49920 ) ),
 .UNSPECIFIED., .F., .F., .F. ) 
 B_SPLINE_SURFACE_WITH_KNOTS ( ( 4, 4 ),
 ( 2, 2 ),
 ( 0.000000000000000000, 1.000000000000000000 ),
 ( 0.000000000000000000, 1.000000000000000000 ),
 .UNSPECIFIED. ) 
 GEOMETRIC_REPRESENTATION_ITEM ( )  RATIONAL_B_SPLINE_SURFACE ( (
 ( 1.000000000000000000, 1.000000000000000000),
 ( 0.7223157951917476005, 0.9931996967497186413),
 ( 0.7223157951917476005, 0.9931996967497186413),
 ( 1.000000000000000000, 1.000000000000000000) ) ) 
 REPRESENTATION_ITEM ( '' )  SURFACE ( )  );
#37358=( BOUNDED_SURFACE ( )  B_SPLINE_SURFACE ( 3, 1, ( 
 ( #59834, #45457 ),
 ( #16948, #50735 ),
 ( #36061, #35129 ),
 ( #55125, #2810 ) ),
 .UNSPECIFIED., .F., .F., .F. ) 
 B_SPLINE_SURFACE_WITH_KNOTS ( ( 4, 4 ),
 ( 2, 2 ),
 ( 0.000000000000000000, 1.000000000000000000 ),
 ( 0.000000000000000000, 1.000000000000000000 ),
 .UNSPECIFIED. ) 
 GEOMETRIC_REPRESENTATION_ITEM ( )  RATIONAL_B_SPLINE_SURFACE ( (
 ( 1.000000000000000000, 1.000000000000000000),
 ( 0.9953040768229005630, 0.8617119497784937465),
 ( 0.9953040768229005630, 0.8617119497784937465),
 ( 1.000000000000000000, 1.000000000000000000) ) ) 
 REPRESENTATION_ITEM ( '' )  SURFACE ( )  );
#37362=CARTESIAN_POINT ( 'NONE',  ( 4.549368137175248350, 0.000000000000000000, 0.000000000000000000 ) ) ;
#37372=DIRECTION ( 'NONE',  ( -1.000000000000000000, -0.000000000000000000, -0.000000000000000000 ) ) ;
#37405=CARTESIAN_POINT ( 'NONE',  ( 0.1104177457020373149, -30.49705356371285347, -30.49013195371445306 ) ) ;
#37407=CARTESIAN_POINT ( 'NONE',  ( 0.1081432562775998391, 0.4234896101211546027, -43.12249629849792854 ) ) ;
#37415=CARTESIAN_POINT ( 'NONE',  ( 0.6023142530420679819, 33.83147280953687641, -34.20176999054672962 ) ) ;
#37417=LINE ( 'NONE', #46501, #20402 ) ;
#37419=ORIENTED_EDGE ( 'NONE', *, *, #55351, .F. ) ;
#37421=CARTESIAN_POINT ( 'NONE',  ( -2.569797478183783568, 14.44232325624826707, -2.353985772484601835 ) ) ;
#37423=CARTESIAN_POINT ( 'NONE',  ( 0.1104177457020373287, 39.83992599038884919, -16.50753524010258033 ) ) ;
#37425=CARTESIAN_POINT ( 'NONE',  ( 0.8751705887134423323, -7.160166390004656378, 47.55935879196458416 ) ) ;
#37429=CARTESIAN_POINT ( 'NONE',  ( 0.5998501479064708430, 46.60114184914316837, -11.94461217097420658 ) ) ;
#37434=CARTESIAN_POINT ( 'NONE',  ( 0.8760168074887076939, -37.61398439004553751, 29.98565522133283068 ) ) ;
#37455=CARTESIAN_POINT ( 'NONE',  ( 4.975801465491695552, 0.000000000000000000, 0.000000000000000000 ) ) ;
#37457=CARTESIAN_POINT ( 'NONE',  ( 0.8760168074886960365, -48.09529047980637273, -0.8912768426704541502 ) ) ;
#37464=ORIENTED_EDGE ( 'NONE', *, *, #33677, .T. ) ;
#37467=EDGE_CURVE ( 'NONE', #61214, #61173, #57266, .T. ) ;
#37471=CARTESIAN_POINT ( 'NONE',  ( 5.880360259849739535, 31.66572319753511877, 36.03610316515393919 ) ) ;
#37473=EDGE_CURVE ( 'NONE', #24987, #37338, #60269, .T. ) ;
#37474=VERTEX_POINT ( 'NONE', #11869 ) ;
#37483=ORIENTED_EDGE ( 'NONE', *, *, #2279, .T. ) ;
#37490=CARTESIAN_POINT ( 'NONE',  ( 4.691466044806103852, 43.79545162262296998, 8.371234562542003488 ) ) ;
#37491=EDGE_CURVE ( 'NONE', #50490, #21383, #17693, .T. ) ;
#37492=VECTOR ( 'NONE', #6713, 1000.000000000000000 ) ;
#37503=ORIENTED_EDGE ( 'NONE', *, *, #59435, .T. ) ;
#37506=B_SPLINE_CURVE_WITH_KNOTS ( 'NONE', 3,
 ( #21624, #40763, #59828, #51656, #56351, #253 ),
 .UNSPECIFIED., .F., .F.,
 ( 4, 2, 4 ),
 ( 0.000000000000000000, 0.0002450742804987317367, 0.0004901485609974634734 ),
 .UNSPECIFIED. ) ;
#37507=ADVANCED_FACE ( 'NONE', ( #13710 ), #8683, .F. ) ;
#37510=CARTESIAN_POINT ( 'NONE',  ( 0.7954190325252786797, -33.39101560460825624, 34.61997719899426329 ) ) ;
#37511=EDGE_CURVE ( 'NONE', #21617, #56576, #28099, .T. ) ;
#37521=CARTESIAN_POINT ( 'NONE',  ( 0.8751705887134553219, 44.08562551107081617, -19.22545746485614870 ) ) ;
#37523=CARTESIAN_POINT ( 'NONE',  ( -6.010958268070873523, 14.95835081545473955, 11.45964880703832023 ) ) ;
#37530=CARTESIAN_POINT ( 'NONE',  ( 0.7954196712028475114, 37.62416450255248179, 29.96539649507097991 ) ) ;
#37531=CARTESIAN_POINT ( 'NONE',  ( 0.8751705887134553219, -41.19904111682524928, 24.81530984069135570 ) ) ;
#37534=CARTESIAN_POINT ( 'NONE',  ( 0.6031356219577719280, 47.70727206974377310, 6.192730535896314059 ) ) ;
#37538=CARTESIAN_POINT ( 'NONE',  ( 0.1102847568649952675, -5.537466591275985728, 42.76743495471819756 ) ) ;
#37548=B_SPLINE_CURVE_WITH_KNOTS ( 'NONE', 3,
 ( #35551, #48398, #44645, #19919 ),
 .UNSPECIFIED., .F., .F.,
 ( 4, 4 ),
 ( 5.485677294651094893E-18, 0.004566006591234647236 ),
 .UNSPECIFIED. ) ;
#37555=DIRECTION ( 'NONE',  ( 0.000000000000000000, 0.000000000000000000, 1.000000000000000000 ) ) ;
#37556=B_SPLINE_CURVE_WITH_KNOTS ( 'NONE', 3,
 ( #50301, #50914, #55920, #35921 ),
 .UNSPECIFIED., .F., .F.,
 ( 4, 4 ),
 ( 0.000000000000000000, 0.005014147105413698652 ),
 .UNSPECIFIED. ) ;
#37568=EDGE_CURVE ( 'NONE', #44145, #60939, #14326, .T. ) ;
#37571=EDGE_CURVE ( 'NONE', #26859, #26613, #51670, .T. ) ;
#37576=ADVANCED_FACE ( 'NONE', ( #19327 ), #19138, .F. ) ;
#37590=ORIENTED_EDGE ( 'NONE', *, *, #51197, .T. ) ;
#37592=CARTESIAN_POINT ( 'NONE',  ( 0.1104177457020372732, -21.56646482560105937, -37.34442418285495791 ) ) ;
#37607=FACE_OUTER_BOUND ( 'NONE', #37056, .T. ) ;
#37609=LINE ( 'NONE', #46694, #14870 ) ;
#37612=CARTESIAN_POINT ( 'NONE',  ( 0.8751705887134553219, -34.63284514348562482, -33.37254303619542384 ) ) ;
#37627=CARTESIAN_POINT ( 'NONE',  ( 4.975801465491695552, 9.906103548667566372, 46.87746200127460128 ) ) ;
#37631=( BOUNDED_SURFACE ( )  B_SPLINE_SURFACE ( 3, 1, ( 
 ( #4125, #47375 ),
 ( #3825, #42090 ),
 ( #4423, #27037 ),
 ( #36765, #32988 ) ),
 .UNSPECIFIED., .F., .F., .F. ) 
 B_SPLINE_SURFACE_WITH_KNOTS ( ( 4, 4 ),
 ( 2, 2 ),
 ( 0.000000000000000000, 1.000000000000000000 ),
 ( 0.000000000000000000, 1.000000000000000000 ),
 .UNSPECIFIED. ) 
 GEOMETRIC_REPRESENTATION_ITEM ( )  RATIONAL_B_SPLINE_SURFACE ( (
 ( 1.000000000000000000, 1.000000000000000000),
 ( 0.9953040768229013402, 0.8617119497784988535),
 ( 0.9953040768229013402, 0.8617119497784988535),
 ( 1.000000000000000000, 1.000000000000000000) ) ) 
 REPRESENTATION_ITEM ( '' )  SURFACE ( )  );
#37642=LINE ( 'NONE', #3772, #40497 ) ;
#37645=ORIENTED_EDGE ( 'NONE', *, *, #58031, .T. ) ;
#37650=VERTEX_POINT ( 'NONE', #49356 ) ;
#37655=ORIENTED_EDGE ( 'NONE', *, *, #3367, .F. ) ;
#37657=CARTESIAN_POINT ( 'NONE',  ( -6.017396004339686577, 9.422598049764623340, 16.31807101179373731 ) ) ;
#37658=CARTESIAN_POINT ( 'NONE',  ( 4.975801465491695552, -35.64402118370979622, 32.01766832630250548 ) ) ;
#37662=FACE_OUTER_BOUND ( 'NONE', #17214, .T. ) ;
#37665=CARTESIAN_POINT ( 'NONE',  ( 2.301430502907646947, 13.67112791032043084, -46.04685681264152208 ) ) ;
#37672=CIRCLE ( 'NONE', #8657, 42.92674063221959813 ) ;
#37674=CARTESIAN_POINT ( 'NONE',  ( 2.643462169533600914, -19.65219740572217688, 43.83256147628700461 ) ) ;
#37675=EDGE_CURVE ( 'NONE', #26391, #47393, #53660, .T. ) ;
#37682=VECTOR ( 'NONE', #6267, 1000.000000000000000 ) ;
#37685=CARTESIAN_POINT ( 'NONE',  ( 0.1310142868023688179, -22.11113027429312083, 37.02349354742202792 ) ) ;
#37687=CARTESIAN_POINT ( 'NONE',  ( 0.6041374136657475802, 29.14743607025033967, 38.27243465845350556 ) ) ;
#37696=ORIENTED_EDGE ( 'NONE', *, *, #5917, .T. ) ;
#37703=DIRECTION ( 'NONE',  ( -1.000000000000000000, -0.000000000000000000, -0.000000000000000000 ) ) ;
#37708=EDGE_CURVE ( 'NONE', #44643, #20535, #22122, .T. ) ;
#37718=DIRECTION ( 'NONE',  ( 1.000000000000000000, 0.000000000000000000, 0.000000000000000000 ) ) ;
#37724=B_SPLINE_CURVE_WITH_KNOTS ( 'NONE', 3,
 ( #20501, #49608, #34608, #17577 ),
 .UNSPECIFIED., .F., .F.,
 ( 4, 4 ),
 ( 2.294131830766625192E-17, 0.004564976165746188579 ),
 .UNSPECIFIED. ) ;
#37726=VERTEX_POINT ( 'NONE', #20258 ) ;
#37729=ORIENTED_EDGE ( 'NONE', *, *, #24565, .F. ) ;
#37733=CARTESIAN_POINT ( 'NONE',  ( 0.3622758884714730732, 41.42293301073625855, -11.95365414648454205 ) ) ;
#37736=CARTESIAN_POINT ( 'NONE',  ( 0.1101816497532062678, 5.763501205266542193, 42.73758747687831772 ) ) ;
#37738=ADVANCED_FACE ( 'NONE', ( #34055 ), #10712, .F. ) ;
#37741=CARTESIAN_POINT ( 'NONE',  ( -6.001507490154110336, -4.862106078788054120, 18.20581304543296142 ) ) ;
#37743=CARTESIAN_POINT ( 'NONE',  ( 0.6254311100348639574, 24.64676532715794011, -41.31309618784389670 ) ) ;
#37754=CARTESIAN_POINT ( 'NONE',  ( 0.7048096507298635682, -37.64898672361973553, 29.95256433478663283 ) ) ;
#37759=CARTESIAN_POINT ( 'NONE',  ( 4.322998006666179727, 10.36018990813312968, -46.85697641700698313 ) ) ;
#37760=CARTESIAN_POINT ( 'NONE',  ( 0.3622758884714600280, 40.13994584881781691, -15.73321244754812298 ) ) ;
#37763=CARTESIAN_POINT ( 'NONE',  ( 0.7954190325252777916, 29.96539637359164843, 37.62416463577120140 ) ) ;
#37772=CARTESIAN_POINT ( 'NONE',  ( 0.7246131072078569879, -33.42811616637893479, -34.58859703353066806 ) ) ;
#37774=CARTESIAN_POINT ( 'NONE',  ( 2.301430502907645614, 44.85388302506905234, -17.18551536142205194 ) ) ;
#37775=CARTESIAN_POINT ( 'NONE',  ( 0.1092355843206037486, 42.71527351115371829, 5.926758618548121582 ) ) ;
#37778=CARTESIAN_POINT ( 'NONE',  ( -6.001507490154110336, 18.84387066167321478, -0.01557731607559883699 ) ) ;
#37780=CARTESIAN_POINT ( 'NONE',  ( 3.680974057930773036, -35.20670187740681456, 32.59081219553969078 ) ) ;
#37793=CARTESIAN_POINT ( 'NONE',  ( 4.975801465491694664, -45.18341283946446651, -15.94009207553035523 ) ) ;
#37800=CARTESIAN_POINT ( 'NONE',  ( 0.8751705887134423323, 48.08707113907594533, 0.8911681664090089772 ) ) ;
#37803=CARTESIAN_POINT ( 'NONE',  ( 0.6001305935487315502, -34.38748867424691014, -33.64689939321930012 ) ) ;
#37806=ORIENTED_EDGE ( 'NONE', *, *, #21576, .T. ) ;
#37817=CARTESIAN_POINT ( 'NONE',  ( 0.6254311100348652896, -6.960804577577174967, 47.60023274471267740 ) ) ;
#37818=B_SPLINE_CURVE_WITH_KNOTS ( 'NONE', 3,
 ( #7570, #26694, #2874, #22006 ),
 .UNSPECIFIED., .F., .F.,
 ( 4, 4 ),
 ( 2.142911263092167033E-17, 0.004564976165746191181 ),
 .UNSPECIFIED. ) ;
#37821=DIRECTION ( 'NONE',  ( 0.000000000000000000, 0.000000000000000000, 1.000000000000000000 ) ) ;
#37823=ADVANCED_FACE ( 'NONE', ( #56208 ), #29903, .F. ) ;
#37826=EDGE_LOOP ( 'NONE', ( #57788, #49486, #24994, #33711 ) ) ;
#37832=CARTESIAN_POINT ( 'NONE',  ( 0.6254087463353915632, -33.52637152047104507, 34.49952850220913803 ) ) ;
#37836=EDGE_LOOP ( 'NONE', ( #49320, #20979, #20281, #33786 ) ) ;
#37837=CARTESIAN_POINT ( 'NONE',  ( 0.6023142530420679819, -29.49327578399161354, -38.00626667377512291 ) ) ;
#37840=CARTESIAN_POINT ( 'NONE',  ( 0.8751705887134553219, 42.09020928323342758, 23.27176129838440488 ) ) ;
#37841=CARTESIAN_POINT ( 'NONE',  ( 0.1097557419366048670, 16.29667732266752722, -39.92664986079716982 ) ) ;
#37842=ORIENTED_EDGE ( 'NONE', *, *, #21394, .F. ) ;
#37846=CARTESIAN_POINT ( 'NONE',  ( -2.569797478183783568, 6.924386868080847357, -12.89088113963429194 ) ) ;
#37857=CARTESIAN_POINT ( 'NONE',  ( 0.1100053167205930771, -5.450899213259822851, 42.77858932361494482 ) ) ;
#37866=ORIENTED_EDGE ( 'NONE', *, *, #52677, .F. ) ;
#37870=VECTOR ( 'NONE', #38915, 1000.000000000000114 ) ;
#37879=EDGE_CURVE ( 'NONE', #38025, #58675, #50515, .T. ) ;
#37882=ORIENTED_EDGE ( 'NONE', *, *, #42111, .T. ) ;
#37883=EDGE_CURVE ( 'NONE', #37650, #42525, #61696, .T. ) ;
#37884=CARTESIAN_POINT ( 'NONE',  ( -6.017396004339687465, 17.40926186480789539, -7.209881890566363971 ) ) ;
#37885=CARTESIAN_POINT ( 'NONE',  ( 4.549368137175248350, 0.000000000000000000, 0.000000000000000000 ) ) ;
#37887=CARTESIAN_POINT ( 'NONE',  ( 2.643462169533613793, 40.89244134039111600, -25.20536747735737038 ) ) ;
#37888=CARTESIAN_POINT ( 'NONE',  ( 0.8751705887134423323, 37.60752970653787486, 29.98056538504974000 ) ) ;
#37892=VERTEX_POINT ( 'NONE', #19563 ) ;
#37900=CARTESIAN_POINT ( 'NONE',  ( 0.6031356219577718170, -33.95537057546208359, 34.07882816221562905 ) ) ;
#37908=ADVANCED_FACE ( 'NONE', ( #6331 ), #50731, .F. ) ;
#37913=ADVANCED_FACE ( 'NONE', ( #20787 ), #25508, .F. ) ;
#37923=CARTESIAN_POINT ( 'NONE',  ( 0.1073791018717483448, -10.69234304550083081, 41.77800844988496465 ) ) ;
#37925=EDGE_CURVE ( 'NONE', #2051, #44917, #11639, .T. ) ;
#37929=CARTESIAN_POINT ( 'NONE',  ( 5.880360259849739535, 26.61251048557248922, -39.91356965504121490 ) ) ;
#37938=CARTESIAN_POINT ( 'NONE',  ( 4.322998006666179727, -36.74401119231429647, 30.86725474310297557 ) ) ;
#37940=ORIENTED_EDGE ( 'NONE', *, *, #31072, .F. ) ;
#37941=EDGE_CURVE ( 'NONE', #50136, #36718, #40020, .T. ) ;
#37947=EDGE_CURVE ( 'NONE', #7184, #940, #25776, .T. ) ;
#37948=ORIENTED_EDGE ( 'NONE', *, *, #44978, .T. ) ;
#37950=CARTESIAN_POINT ( 'NONE',  ( 4.549368137175248350, 42.14271863032822552, 8.166781970325878603 ) ) ;
#37954=AXIS2_PLACEMENT_3D ( 'NONE', #40677, #15926, #40070 ) ;
#37957=CARTESIAN_POINT ( 'NONE',  ( 0.6001305935487422083, -38.48510059944028683, -28.87057754790923525 ) ) ;
#37962=CARTESIAN_POINT ( 'NONE',  ( 0.2885700199627515561, -42.84523253167937895, -4.828949117911622402 ) ) ;
#37963=CARTESIAN_POINT ( 'NONE',  ( 0.8760168074886960365, -44.09317760313739853, -19.22870327415288827 ) ) ;
#37978=ORIENTED_EDGE ( 'NONE', *, *, #6777, .F. ) ;
#37982=CARTESIAN_POINT ( 'NONE',  ( -6.016761891674564211, 18.20201388312095503, 4.873659902332430960 ) ) ;
#37983=ADVANCED_FACE ( 'NONE', ( #26095 ), #35232, .F. ) ;
#37984=CARTESIAN_POINT ( 'NONE',  ( 0.1064266418746774301, -41.50637583369812944, -11.70292610004310419 ) ) ;
#37985=ORIENTED_EDGE ( 'NONE', *, *, #41327, .F. ) ;
#37988=CARTESIAN_POINT ( 'NONE',  ( 4.975801465491695552, -45.18341283946470099, 15.94009207552969620 ) ) ;
#37994=CARTESIAN_POINT ( 'NONE',  ( 0.6001305935487315502, 48.10757715638247589, 0.5236757026891092348 ) ) ;
#37996=DIRECTION ( 'NONE',  ( -1.000000000000000000, -0.000000000000000000, -0.000000000000000000 ) ) ;
#38000=CARTESIAN_POINT ( 'NONE',  ( 0.8751705887134553219, 29.98056538504910051, 37.60752970653838645 ) ) ;
#38004=CARTESIAN_POINT ( 'NONE',  ( 0.1087620492084204610, -21.87505161834442902, 37.16461718700628580 ) ) ;
#38011=EDGE_CURVE ( 'NONE', #4544, #15054, #31778, .T. ) ;
#38012=CARTESIAN_POINT ( 'NONE',  ( 2.301430502907644726, 11.18388433759652578, 46.71331171933237414 ) ) ;
#38015=DIRECTION ( 'NONE',  ( 0.000000000000000000, 0.000000000000000000, 1.000000000000000000 ) ) ;
#38023=VERTEX_POINT ( 'NONE', #55203 ) ;
#38025=VERTEX_POINT ( 'NONE', #48559 ) ;
#38028=EDGE_CURVE ( 'NONE', #29080, #32390, #51167, .T. ) ;
#38032=CARTESIAN_POINT ( 'NONE',  ( 0.6001305935487315502, 24.50730504006458332, -41.40054608060268038 ) ) ;
#38037=EDGE_LOOP ( 'NONE', ( #12163, #29024, #22523, #8387 ) ) ;
#38040=CARTESIAN_POINT ( 'NONE',  ( -6.001507490154110336, 18.20581304543297918, 4.862106078787989283 ) ) ;
#38042=CARTESIAN_POINT ( 'NONE',  ( 0.5998501479064699549, -44.64337787626236320, -17.92509395669093308 ) ) ;
#38044=EDGE_LOOP ( 'NONE', ( #8894, #33507, #4912, #956 ) ) ;
#38045=ORIENTED_EDGE ( 'NONE', *, *, #7265, .F. ) ;
#38052=CARTESIAN_POINT ( 'NONE',  ( 0.1092355843206037486, 5.330717085612747042, 42.79374386763048221 ) ) ;
#38054=CARTESIAN_POINT ( 'NONE',  ( -6.015611763856276717, -4.870987357968304288, 18.20278301740935234 ) ) ;
#38057=EDGE_CURVE ( 'NONE', #45571, #29832, #41780, .T. ) ;
#38061=CARTESIAN_POINT ( 'NONE',  ( 0.6254311100348658448, 46.64066536338342672, -11.78487556908959988 ) ) ;
#38062=ORIENTED_EDGE ( 'NONE', *, *, #11055, .F. ) ;
#38065=CARTESIAN_POINT ( 'NONE',  ( 0.7048096507298579061, -48.10291524268441066, -0.8437160066905596834 ) ) ;
#38068=CARTESIAN_POINT ( 'NONE',  ( -6.016761891674565099, -11.47373234755513671, 14.94721834528410831 ) ) ;
#38071=CARTESIAN_POINT ( 'NONE',  ( 0.1073791018717578927, -30.83464511437158961, 30.14884492832337060 ) ) ;
#38084=FACE_OUTER_BOUND ( 'NONE', #12238, .T. ) ;
#38090=CARTESIAN_POINT ( 'NONE',  ( 0.6031356755773454870, -46.46822857981034360, -12.45109777649093274 ) ) ;
#38096=FACE_OUTER_BOUND ( 'NONE', #29271, .T. ) ;
#38102=EDGE_CURVE ( 'NONE', #10248, #41488, #20375, .T. ) ;
#38113=EDGE_LOOP ( 'NONE', ( #26414, #57798, #19213, #47886 ) ) ;
#38119=CARTESIAN_POINT ( 'NONE',  ( -2.708315649062910779, 14.06540004355476903, 4.041664582652845006 ) ) ;
#38123=CARTESIAN_POINT ( 'NONE',  ( 0.3622758884714600280, 34.70015533914828865, -25.58609868863731407 ) ) ;
#38127=ORIENTED_EDGE ( 'NONE', *, *, #2000, .T. ) ;
#38138=EDGE_CURVE ( 'NONE', #27827, #12730, #48264, .T. ) ;
#38151=B_SPLINE_CURVE_WITH_KNOTS ( 'NONE', 3,
 ( #32867, #51943, #47260, #56948 ),
 .UNSPECIFIED., .F., .F.,
 ( 4, 4 ),
 ( 2.414736334504793503E-17, 0.004564976165746186844 ),
 .UNSPECIFIED. ) ;
#38153=CARTESIAN_POINT ( 'NONE',  ( -6.016489644550736315, -7.215050741357911690, -17.40716454747936481 ) ) ;
#38158=FACE_OUTER_BOUND ( 'NONE', #32798, .T. ) ;
#38161=CARTESIAN_POINT ( 'NONE',  ( 0.1092565886968784455, -5.321013289171980354, 42.79503959566643800 ) ) ;
#38162=ORIENTED_EDGE ( 'NONE', *, *, #2185, .F. ) ;
#38163=ORIENTED_EDGE ( 'NONE', *, *, #28670, .T. ) ;
#38170=ADVANCED_FACE ( 'NONE', ( #36343 ), #28807, .F. ) ;
#38174=CARTESIAN_POINT ( 'NONE',  ( 0.1313383488274136313, -10.54394128763588157, 41.81465294768271690 ) ) ;
#38175=CARTESIAN_POINT ( 'NONE',  ( 4.833616638992205949, 9.466882727842142131, -45.27110352095237999 ) ) ;
#38180=( BOUNDED_SURFACE ( )  B_SPLINE_SURFACE ( 3, 1, ( 
 ( #6476, #35043 ),
 ( #39752, #50048 ),
 ( #25013, #26227 ),
 ( #7102, #44456 ) ),
 .UNSPECIFIED., .F., .F., .F. ) 
 B_SPLINE_SURFACE_WITH_KNOTS ( ( 4, 4 ),
 ( 2, 2 ),
 ( 0.000000000000000000, 1.000000000000000000 ),
 ( 0.000000000000000000, 1.000000000000000000 ),
 .UNSPECIFIED. ) 
 GEOMETRIC_REPRESENTATION_ITEM ( )  RATIONAL_B_SPLINE_SURFACE ( (
 ( 1.000000000000000000, 1.000000000000000000),
 ( 0.7223157951917476005, 0.9931996967497186413),
 ( 0.7223157951917476005, 0.9931996967497186413),
 ( 1.000000000000000000, 1.000000000000000000) ) ) 
 REPRESENTATION_ITEM ( '' )  SURFACE ( )  );
#38183=ORIENTED_EDGE ( 'NONE', *, *, #32189, .F. ) ;
#38184=CARTESIAN_POINT ( 'NONE',  ( 0.8751705887134553219, -13.30665218149330364, -46.21789262997752701 ) ) ;
#38185=CARTESIAN_POINT ( 'NONE',  ( -6.016761891674564211, 7.207804629151548070, -17.41015286184795130 ) ) ;
#38191=B_SPLINE_CURVE_WITH_KNOTS ( 'NONE', 3,
 ( #48799, #38496, #25003, #1470 ),
 .UNSPECIFIED., .F., .F.,
 ( 4, 4 ),
 ( 5.553824967135426632E-18, 0.004566006591234647236 ),
 .UNSPECIFIED. ) ;
#38197=ORIENTED_EDGE ( 'NONE', *, *, #32618, .F. ) ;
#38203=ORIENTED_EDGE ( 'NONE', *, *, #28940, .T. ) ;
#38205=EDGE_CURVE ( 'NONE', #49729, #58534, #2575, .T. ) ;
#38207=CARTESIAN_POINT ( 'NONE',  ( 2.301529144917016101, -37.31001381748753687, 30.25186323939210453 ) ) ;
#38208=ORIENTED_EDGE ( 'NONE', *, *, #52891, .T. ) ;
#38213=DIRECTION ( 'NONE',  ( 0.09835009131224567436, 0.9876177374393975139, -0.1222230102474909375 ) ) ;
#38214=CARTESIAN_POINT ( 'NONE',  ( 0.1100053167205930493, 30.62023953839040047, 30.36644426605150215 ) ) ;
#38221=CARTESIAN_POINT ( 'NONE',  ( 1.827326673878743257, -42.50320212329575043, -6.839036141888421128 ) ) ;
#38227=CARTESIAN_POINT ( 'NONE',  ( 0.6017666602106489515, 0.3491145841132096694, 48.10631669010027878 ) ) ;
#38229=VERTEX_POINT ( 'NONE', #693 ) ;
#38236=DIRECTION ( 'NONE',  ( 0.09835009131224567436, -0.007732607185437541039, 0.9951218349151970122 ) ) ;
#38237=CARTESIAN_POINT ( 'NONE',  ( -2.708315649062910779, -8.698422600177046604, -11.76894112707809015 ) ) ;
#38242=CARTESIAN_POINT ( 'NONE',  ( 0.8751705887134553219, 38.69254731947794568, 28.56654290188667034 ) ) ;
#38244=EDGE_LOOP ( 'NONE', ( #9167, #58264, #49323, #57994 ) ) ;
#38248=VECTOR ( 'NONE', #53217, 1000.000000000000114 ) ;
#38251=ORIENTED_EDGE ( 'NONE', *, *, #35314, .F. ) ;
#38257=B_SPLINE_CURVE_WITH_KNOTS ( 'NONE', 3,
 ( #18003, #27077, #56189, #8896 ),
 .UNSPECIFIED., .F., .F.,
 ( 4, 4 ),
 ( 0.000000000000000000, 0.005014147105413710795 ),
 .UNSPECIFIED. ) ;
#38275=CARTESIAN_POINT ( 'NONE',  ( -6.001507490154110336, 16.31148204059960705, -9.435425682280646598 ) ) ;
#38281=CARTESIAN_POINT ( 'NONE',  ( -6.016489644550736315, 18.20227673842143901, 4.872725758886254255 ) ) ;
#38288=EDGE_CURVE ( 'NONE', #4442, #50113, #42230, .T. ) ;
#38293=CARTESIAN_POINT ( 'NONE',  ( -6.010958268070873523, -17.41463273278783319, 7.197664668556383205 ) ) ;
#38304=CARTESIAN_POINT ( 'NONE',  ( 0.6029303876144825880, 48.10727438003475953, 0.1308990448397389650 ) ) ;
#38305=DIRECTION ( 'NONE',  ( -1.000000000000000000, -0.000000000000000000, -0.000000000000000000 ) ) ;
#38307=CARTESIAN_POINT ( 'NONE',  ( -6.016489644550737204, 14.94663725562916134, 11.47450955518493032 ) ) ;
#38311=CARTESIAN_POINT ( 'NONE',  ( -5.995132425357893702, -18.68182899165013211, 2.468096378288054726 ) ) ;
#38322=CARTESIAN_POINT ( 'NONE',  ( 0.5998501479064708430, -37.84527566984837677, -29.69975237324600315 ) ) ;
#38325=B_SPLINE_CURVE_WITH_KNOTS ( 'NONE', 3,
 ( #11707, #29557, #5721, #40849, #46155, #22952 ),
 .UNSPECIFIED., .F., .F.,
 ( 4, 2, 4 ),
 ( 1.259499515835350888E-16, 0.0002450741128632365705, 0.0004901482257263472652 ),
 .UNSPECIFIED. ) ;
#38329=ORIENTED_EDGE ( 'NONE', *, *, #28293, .T. ) ;
#38330=CARTESIAN_POINT ( 'NONE',  ( 0.1073791018717483448, 16.05399293000815675, -40.02496097243042072 ) ) ;
#38340=CARTESIAN_POINT ( 'NONE',  ( 0.6001305935487315502, -29.70149728382465426, 37.84751346122803994 ) ) ;
#38344=DIRECTION ( 'NONE',  ( 0.09835009131224552170, -0.2500873580884774849, 0.9632152266566380572 ) ) ;
#38348=CARTESIAN_POINT ( 'NONE',  ( 0.6023142530420679819, -12.19802990522833319, 46.53533807097409891 ) ) ;
#38349=CARTESIAN_POINT ( 'NONE',  ( 5.880360259849739535, 3.090325311464862779, -47.87242051977162305 ) ) ;
#38354=ORIENTED_EDGE ( 'NONE', *, *, #34964, .T. ) ;
#38358=CARTESIAN_POINT ( 'NONE',  ( 4.975801465491694664, 45.55012473237754023, -14.85979367497125381 ) ) ;
#38372=DIRECTION ( 'NONE',  ( 1.000000000000000000, 0.000000000000000000, 0.000000000000000000 ) ) ;
#38378=CARTESIAN_POINT ( 'NONE',  ( 0.1098349054025746091, -34.08267426123942556, -26.42143025179976945 ) ) ;
#38379=CARTESIAN_POINT ( 'NONE',  ( 4.833616638992205949, -41.27831852777627120, -20.86133030530276500 ) ) ;
#38382=CARTESIAN_POINT ( 'NONE',  ( 4.975801465491694664, -46.87746200127448049, -9.906103548668065528 ) ) ;
#38383=CARTESIAN_POINT ( 'NONE',  ( 0.8760168074886965917, 44.09317760313724932, 19.22870327415319736 ) ) ;
#38384=CARTESIAN_POINT ( 'NONE',  ( 2.301430502907644282, -22.89309745268860752, -42.22699195640099390 ) ) ;
#38388=CARTESIAN_POINT ( 'NONE',  ( 1.827326673878744145, 27.17438009792331854, -33.38933471001448083 ) ) ;
#38392=B_SPLINE_CURVE_WITH_KNOTS ( 'NONE', 3,
 ( #8370, #9614, #18104, #14340 ),
 .UNSPECIFIED., .F., .F.,
 ( 4, 4 ),
 ( 1.998817200139820460E-17, 0.004444306975806115029 ),
 .UNSPECIFIED. ) ;
#38395=ORIENTED_EDGE ( 'NONE', *, *, #23735, .T. ) ;
#38397=AXIS2_PLACEMENT_3D ( 'NONE', #470, #20527, #23989 ) ;
#38403=CARTESIAN_POINT ( 'NONE',  ( 0.3622758884714600280, 36.91764744403290166, 22.26738722580180507 ) ) ;
#38411=CARTESIAN_POINT ( 'NONE',  ( 0.09136607875274982415, 12.80000000000000071, 3.000000000000000000 ) ) ;
#38413=CARTESIAN_POINT ( 'NONE',  ( 0.3622758884714730732, -41.42293301073634382, 11.95365414648425428 ) ) ;
#38420=CARTESIAN_POINT ( 'NONE',  ( 3.238741278300274029, 35.19027457370178524, -24.69738534405274066 ) ) ;
#38422=CARTESIAN_POINT ( 'NONE',  ( 0.1097557419366048670, -37.45792859959212251, -21.36873056345880784 ) ) ;
#38426=CARTESIAN_POINT ( 'NONE',  ( 4.975801465491694664, 31.15993731089074359, 36.39623109580477234 ) ) ;
#38427=EDGE_CURVE ( 'NONE', #38229, #11266, #48199, .T. ) ;
#38429=CARTESIAN_POINT ( 'NONE',  ( 0.2885700199627505014, -26.88157179738480096, -33.71073713194511612 ) ) ;
#38434=CARTESIAN_POINT ( 'NONE',  ( 4.322998006666165516, -40.45864630878501345, -25.80712523194260655 ) ) ;
#38444=FACE_OUTER_BOUND ( 'NONE', #52331, .T. ) ;
#38445=EDGE_LOOP ( 'NONE', ( #59069, #53226, #33363, #9375 ) ) ;
#38450=CARTESIAN_POINT ( 'NONE',  ( 0.09136607875274982415, 5.281323502666703820E-15, -43.12527911185304674 ) ) ;
#38453=CARTESIAN_POINT ( 'NONE',  ( -6.001507490154111224, 9.408444979392321272, 16.32705935667510744 ) ) ;
#38454=B_SPLINE_CURVE_WITH_KNOTS ( 'NONE', 3,
 ( #26179, #17105, #26799, #45317, #51208, #45937 ),
 .UNSPECIFIED., .F., .F.,
 ( 4, 2, 4 ),
 ( 1.554159946372743606E-17, 0.0002293319059085091138, 0.0004586638118170027235 ),
 .UNSPECIFIED. ) ;
#38455=CARTESIAN_POINT ( 'NONE',  ( 0.7048096507298635682, 44.76417498422291175, 17.62869676200424962 ) ) ;
#38461=VERTEX_POINT ( 'NONE', #29141 ) ;
#38465=CIRCLE ( 'NONE', #19447, 47.91270532121795611 ) ;
#38469=( BOUNDED_SURFACE ( )  B_SPLINE_SURFACE ( 3, 1, ( 
 ( #60414, #55720 ),
 ( #17847, #7173 ),
 ( #12853, #26306 ),
 ( #56035, #3403 ) ),
 .UNSPECIFIED., .F., .F., .F. ) 
 B_SPLINE_SURFACE_WITH_KNOTS ( ( 4, 4 ),
 ( 2, 2 ),
 ( 0.000000000000000000, 1.000000000000000000 ),
 ( 0.000000000000000000, 1.000000000000000000 ),
 .UNSPECIFIED. ) 
 GEOMETRIC_REPRESENTATION_ITEM ( )  RATIONAL_B_SPLINE_SURFACE ( (
 ( 1.000000000000000000, 1.000000000000000000),
 ( 0.9953040768229013402, 0.8617119497784988535),
 ( 0.9953040768229013402, 0.8617119497784988535),
 ( 1.000000000000000000, 1.000000000000000000) ) ) 
 REPRESENTATION_ITEM ( '' )  SURFACE ( )  );
#38470=VERTEX_POINT ( 'NONE', #15984 ) ;
#38484=ORIENTED_EDGE ( 'NONE', *, *, #45361, .T. ) ;
#38496=CARTESIAN_POINT ( 'NONE',  ( 3.238931869106853600, -35.19033040238051768, -24.69728751010273982 ) ) ;
#38503=CARTESIAN_POINT ( 'NONE',  ( 0.6031357023905875581, -34.04794059289672248, 33.98625823839241633 ) ) ;
#38521=VERTEX_POINT ( 'NONE', #29440 ) ;
#38527=CARTESIAN_POINT ( 'NONE',  ( 4.549368137175248350, 0.000000000000000000, 0.000000000000000000 ) ) ;
#38528=CARTESIAN_POINT ( 'NONE',  ( 4.549368137175248350, 0.000000000000000000, 0.000000000000000000 ) ) ;
#38548=ORIENTED_EDGE ( 'NONE', *, *, #29132, .T. ) ;
#38549=EDGE_CURVE ( 'NONE', #12765, #38559, #44781, .T. ) ;
#38554=EDGE_LOOP ( 'NONE', ( #35613, #39875, #12628, #34110 ) ) ;
#38555=CARTESIAN_POINT ( 'NONE',  ( 0.6254311100348686203, -44.70341307176172307, 17.77188277739541888 ) ) ;
#38559=VERTEX_POINT ( 'NONE', #21292 ) ;
#38560=CARTESIAN_POINT ( 'NONE',  ( 0.2224561200757606549, -17.20021002050950898, 39.54039348282952915 ) ) ;
#38572=CARTESIAN_POINT ( 'NONE',  ( 0.6009453534118440743, -38.43042294376934365, 28.93865405070883412 ) ) ;
#38574=ORIENTED_EDGE ( 'NONE', *, *, #44978, .F. ) ;
#38585=ORIENTED_EDGE ( 'NONE', *, *, #51649, .T. ) ;
#38601=ADVANCED_FACE ( 'NONE', ( #35405 ), #3677, .F. ) ;
#38606=DIRECTION ( 'NONE',  ( 0.000000000000000000, 0.000000000000000000, -1.000000000000000000 ) ) ;
#38609=DIRECTION ( 'NONE',  ( 0.09835009131224552170, 0.7847759187265542780, -0.6119264800004700078 ) ) ;
#38614=( BOUNDED_SURFACE ( )  B_SPLINE_SURFACE ( 3, 1, ( 
 ( #42967, #10363 ),
 ( #9416, #10049 ),
 ( #9728, #14450 ),
 ( #24760, #19157 ) ),
 .UNSPECIFIED., .F., .F., .F. ) 
 B_SPLINE_SURFACE_WITH_KNOTS ( ( 4, 4 ),
 ( 2, 2 ),
 ( 0.000000000000000000, 1.000000000000000000 ),
 ( 0.000000000000000000, 1.000000000000000000 ),
 .UNSPECIFIED. ) 
 GEOMETRIC_REPRESENTATION_ITEM ( )  RATIONAL_B_SPLINE_SURFACE ( (
 ( 1.000000000000000000, 1.000000000000000000),
 ( 0.9751682680413298332, 0.9999560080971552356),
 ( 0.9751682680413298332, 0.9999560080971552356),
 ( 1.000000000000000000, 1.000000000000000000) ) ) 
 REPRESENTATION_ITEM ( '' )  SURFACE ( )  );
#38633=VERTEX_POINT ( 'NONE', #2780 ) ;
#38634=ORIENTED_EDGE ( 'NONE', *, *, #19067, .F. ) ;
#38643=CARTESIAN_POINT ( 'NONE',  ( 0.6031356219577718170, -48.10744328000515679, 0.08729769678294060919 ) ) ;
#38646=CARTESIAN_POINT ( 'NONE',  ( -6.016489644550736315, 14.94663725562931766, -11.47450955518472782 ) ) ;
#38649=CARTESIAN_POINT ( 'NONE',  ( 2.643462169533600914, -44.89050350746163787, 17.09809940585581955 ) ) ;
#38652=CARTESIAN_POINT ( 'NONE',  ( 0.1095718737110178698, 5.374020908746366842, 42.78833451865669701 ) ) ;
#38655=DIRECTION ( 'NONE',  ( 0.000000000000000000, 0.000000000000000000, 1.000000000000000000 ) ) ;
#38663=FACE_OUTER_BOUND ( 'NONE', #50382, .T. ) ;
#38669=CARTESIAN_POINT ( 'NONE',  ( -6.016104459813371719, 13.32039631884703113, -13.32794178584983591 ) ) ;
#38673=DIRECTION ( 'NONE',  ( 0.000000000000000000, 0.000000000000000000, -1.000000000000000000 ) ) ;
#38675=LINE ( 'NONE', #58579, #1301 ) ;
#38676=CARTESIAN_POINT ( 'NONE',  ( 0.1073791018717483448, -16.95003405440287381, -39.65380858626208038 ) ) ;
#38679=CARTESIAN_POINT ( 'NONE',  ( 0.5998501479064708430, 18.89267974119668025, -44.24259072156067418 ) ) ;
#38685=B_SPLINE_CURVE_WITH_KNOTS ( 'NONE', 3,
 ( #3564, #3875, #47430, #38061, #18009, #37429 ),
 .UNSPECIFIED., .F., .F.,
 ( 4, 2, 4 ),
 ( 1.266823315017301927E-16, 0.0002450741128632368958, 0.0004901482257263470484 ),
 .UNSPECIFIED. ) ;
#38686=CARTESIAN_POINT ( 'NONE',  ( 0.5980894510889448457, -0.7015180096008225563, 48.10766805928368228 ) ) ;
#38689=CARTESIAN_POINT ( 'NONE',  ( 0.7245667037590746151, 23.33692989609111379, -42.06183421678303347 ) ) ;
#38694=AXIS2_PLACEMENT_3D ( 'NONE', #9832, #58336, #58649 ) ;
#38697=CARTESIAN_POINT ( 'NONE',  ( 0.5998501479064699549, -6.798102206413803472, -47.62484632993685807 ) ) ;
#38698=EDGE_LOOP ( 'NONE', ( #43592, #28413, #51451, #34228 ) ) ;
#38706=CARTESIAN_POINT ( 'NONE',  ( 3.238931869106854489, -3.793313187127262065, 42.82436385108072585 ) ) ;
#38707=DIRECTION ( 'NONE',  ( -1.000000000000000000, -0.000000000000000000, -0.000000000000000000 ) ) ;
#38709=ORIENTED_EDGE ( 'NONE', *, *, #41078, .F. ) ;
#38722=( BOUNDED_SURFACE ( )  B_SPLINE_SURFACE ( 3, 1, ( 
 ( #33680, #43396 ),
 ( #52445, #5737 ),
 ( #48376, #24576 ),
 ( #435, #4511 ) ),
 .UNSPECIFIED., .F., .F., .F. ) 
 B_SPLINE_SURFACE_WITH_KNOTS ( ( 4, 4 ),
 ( 2, 2 ),
 ( 0.000000000000000000, 1.000000000000000000 ),
 ( 0.000000000000000000, 1.000000000000000000 ),
 .UNSPECIFIED. ) 
 GEOMETRIC_REPRESENTATION_ITEM ( )  RATIONAL_B_SPLINE_SURFACE ( (
 ( 1.000000000000000000, 1.000000000000000000),
 ( 0.9751682680413298332, 0.9999560080971552356),
 ( 0.9751682680413298332, 0.9999560080971552356),
 ( 1.000000000000000000, 1.000000000000000000) ) ) 
 REPRESENTATION_ITEM ( '' )  SURFACE ( )  );
#38723=CARTESIAN_POINT ( 'NONE',  ( 0.1073791018717483448, 21.14095454447559419, -37.58707531572184735 ) ) ;
#38724=EDGE_LOOP ( 'NONE', ( #40071, #19216, #56649, #41741 ) ) ;
#38732=CARTESIAN_POINT ( 'NONE',  ( -6.016761891674564211, 9.424569481870250343, 16.31696541414275359 ) ) ;
#38738=CARTESIAN_POINT ( 'NONE',  ( 0.1092565886968784872, -37.50119754628593682, -21.29292791075572921 ) ) ;
#38739=( BOUNDED_SURFACE ( )  B_SPLINE_SURFACE ( 3, 1, ( 
 ( #42291, #4327 ),
 ( #23463, #53196 ),
 ( #49123, #53493 ),
 ( #48815, #44460 ) ),
 .UNSPECIFIED., .F., .F., .F. ) 
 B_SPLINE_SURFACE_WITH_KNOTS ( ( 4, 4 ),
 ( 2, 2 ),
 ( 0.000000000000000000, 1.000000000000000000 ),
 ( 0.000000000000000000, 1.000000000000000000 ),
 .UNSPECIFIED. ) 
 GEOMETRIC_REPRESENTATION_ITEM ( )  RATIONAL_B_SPLINE_SURFACE ( (
 ( 1.000000000000000000, 1.000000000000000000),
 ( 0.9953040768229013402, 0.8617119497784988535),
 ( 0.9953040768229013402, 0.8617119497784988535),
 ( 1.000000000000000000, 1.000000000000000000) ) ) 
 REPRESENTATION_ITEM ( '' )  SURFACE ( )  );
#38743=VERTEX_POINT ( 'NONE', #61941 ) ;
#38744=CARTESIAN_POINT ( 'NONE',  ( -6.001507490154110336, -18.20581304543294365, -4.862106078788116292 ) ) ;
#38746=ORIENTED_EDGE ( 'NONE', *, *, #23573, .T. ) ;
#38749=CARTESIAN_POINT ( 'NONE',  ( 0.6017667736363748743, -47.74032759880258681, 5.933018439714516923 ) ) ;
#38751=CARTESIAN_POINT ( 'NONE',  ( -6.017396004339686577, -7.209881890566677498, 17.40926186480777105 ) ) ;
#38752=CARTESIAN_POINT ( 'NONE',  ( 4.549368137175248350, 0.000000000000000000, 0.000000000000000000 ) ) ;
#38753=CARTESIAN_POINT ( 'NONE',  ( 0.2885697896453113809, 10.38006191081361784, 41.84838128162063953 ) ) ;
#38755=EDGE_CURVE ( 'NONE', #3487, #40811, #33223, .T. ) ;
#38765=CARTESIAN_POINT ( 'NONE',  ( 4.549368137175248350, 0.000000000000000000, 0.000000000000000000 ) ) ;
#38773=CONICAL_SURFACE ( 'NONE', #49880, 42.92674063221959813, 1.485477209440487556 ) ;
#38775=CARTESIAN_POINT ( 'NONE',  ( 4.975801465491695552, -27.09127437476353251, -39.51822597168487050 ) ) ;
#38777=ORIENTED_EDGE ( 'NONE', *, *, #55805, .T. ) ;
#38778=CARTESIAN_POINT ( 'NONE',  ( 4.833616638992205949, -38.20222678111919379, -26.07076047129122287 ) ) ;
#38789=CARTESIAN_POINT ( 'NONE',  ( 0.2885700199627505569, -10.38006184593231573, 41.84838128711406569 ) ) ;
#38790=AXIS2_PLACEMENT_3D ( 'NONE', #40055, #20907, #5850 ) ;
#38791=CARTESIAN_POINT ( 'NONE',  ( 4.691466044806102076, 9.025781474741469523, -43.66525414675633954 ) ) ;
#38793=EDGE_CURVE ( 'NONE', #12765, #35637, #26429, .T. ) ;
#38794=B_SPLINE_CURVE_WITH_KNOTS ( 'NONE', 3,
 ( #7859, #31058, #21349, #46105, #44875, #7533 ),
 .UNSPECIFIED., .F., .F.,
 ( 4, 2, 4 ),
 ( 8.741117365843378158E-19, 0.0002450742804987334172, 0.0004901485609974659671 ),
 .UNSPECIFIED. ) ;
#38802=CARTESIAN_POINT ( 'NONE',  ( 4.549368137175248350, 0.000000000000000000, 0.000000000000000000 ) ) ;
#38803=B_SPLINE_CURVE_WITH_KNOTS ( 'NONE', 3,
 ( #14702, #58496, #54106, #10930 ),
 .UNSPECIFIED., .F., .F.,
 ( 4, 4 ),
 ( 2.120273707634171606E-17, 0.004444306975806115029 ),
 .UNSPECIFIED. ) ;
#38810=VECTOR ( 'NONE', #34650, 1000.000000000000227 ) ;
#38815=ORIENTED_EDGE ( 'NONE', *, *, #17919, .F. ) ;
#38826=B_SPLINE_CURVE_WITH_KNOTS ( 'NONE', 3,
 ( #25545, #6404, #49351, #11459 ),
 .UNSPECIFIED., .F., .F.,
 ( 4, 4 ),
 ( 2.033478910116247305E-17, 0.004444306975806115029 ),
 .UNSPECIFIED. ) ;
#38830=CARTESIAN_POINT ( 'NONE',  ( 4.549368137175248350, 28.14399996863497577, -32.41327393324110773 ) ) ;
#38832=CARTESIAN_POINT ( 'NONE',  ( 0.1064266418746774440, 30.09411284098529649, 30.88821921809858750 ) ) ;
#38843=CARTESIAN_POINT ( 'NONE',  ( 0.6001305935487422083, -41.40054608060309960, 24.50730504006385857 ) ) ;
#38847=CARTESIAN_POINT ( 'NONE',  ( 0.6001305935487315502, -6.798494447612580593, 47.62765676940931314 ) ) ;
#38850=CARTESIAN_POINT ( 'NONE',  ( 2.301430502907646058, 22.89309745268831620, 42.22699195640115022 ) ) ;
#38854=CONICAL_SURFACE ( 'NONE', #49828, 42.92674063221959813, 1.485477209440487556 ) ;
#38857=ORIENTED_EDGE ( 'NONE', *, *, #58031, .F. ) ;
#38864=ORIENTED_EDGE ( 'NONE', *, *, #61164, .F. ) ;
#38871=CARTESIAN_POINT ( 'NONE',  ( 4.549368137175248350, -40.71620287708353914, 13.59764261105679317 ) ) ;
#38873=ORIENTED_EDGE ( 'NONE', *, *, #25322, .T. ) ;
#38885=VERTEX_POINT ( 'NONE', #34400 ) ;
#38896=CARTESIAN_POINT ( 'NONE',  ( 4.549368137175248350, -13.59764261105780214, 40.71620287708320518 ) ) ;
#38900=B_SPLINE_CURVE_WITH_KNOTS ( 'NONE', 3,
 ( #43901, #48870, #25065, #1240, #53855, #49178 ),
 .UNSPECIFIED., .F., .F.,
 ( 4, 2, 4 ),
 ( 8.547914836739547564E-17, 0.0002293366620881469363, 0.0004586733241762083833 ),
 .UNSPECIFIED. ) ;
#38907=CARTESIAN_POINT ( 'NONE',  ( -6.016104459813371719, -4.871830707673185934, 18.20253432612965838 ) ) ;
#38910=CARTESIAN_POINT ( 'NONE',  ( 0.5998501479064699549, -48.10473956285919428, 0.5236536531313263909 ) ) ;
#38911=ORIENTED_EDGE ( 'NONE', *, *, #23837, .T. ) ;
#38914=EDGE_CURVE ( 'NONE', #38229, #53499, #25290, .T. ) ;
#38915=DIRECTION ( 'NONE',  ( 0.09835009131224552170, -0.9632152266566406107, -0.2500873580884673819 ) ) ;
#38923=CARTESIAN_POINT ( 'NONE',  ( 4.549368137175248350, 0.000000000000000000, 0.000000000000000000 ) ) ;
#38932=CARTESIAN_POINT ( 'NONE',  ( 4.322998006666165516, 47.80838462754065432, -4.155494336618213325 ) ) ;
#38937=CARTESIAN_POINT ( 'NONE',  ( 0.7048096507298579061, -24.78213711671627451, 41.23648859290882740 ) ) ;
#38950=CARTESIAN_POINT ( 'NONE',  ( 0.1098349054025746646, 10.95525583467218134, 41.70974743324818235 ) ) ;
#38964=CARTESIAN_POINT ( 'NONE',  ( 0.6001305935487315502, 5.760103278698018414, -47.76436356026962216 ) ) ;
#38968=CARTESIAN_POINT ( 'NONE',  ( 4.322998006666165516, 2.120302895116279451, -47.94177812210862299 ) ) ;
#38970=ORIENTED_EDGE ( 'NONE', *, *, #43146, .T. ) ;
#38980=CARTESIAN_POINT ( 'NONE',  ( 1.827326673878742369, -37.88339879236874452, 20.44853789448387360 ) ) ;
#38981=CARTESIAN_POINT ( 'NONE',  ( -6.016104459813374383, 9.416989654584305924, 16.32137543786086198 ) ) ;
#38999=B_SPLINE_CURVE_WITH_KNOTS ( 'NONE', 3,
 ( #25190, #29579, #39944, #24893 ),
 .UNSPECIFIED., .F., .F.,
 ( 4, 4 ),
 ( 2.343940034265376918E-17, 0.004564976165746186844 ),
 .UNSPECIFIED. ) ;
#39009=CARTESIAN_POINT ( 'NONE',  ( 0.5980894510889448457, -13.12879507229320630, 46.28687279963669710 ) ) ;
#39012=ORIENTED_EDGE ( 'NONE', *, *, #54172, .F. ) ;
#39025=CARTESIAN_POINT ( 'NONE',  ( 0.6025881611877910160, -23.86454577211535977, -41.77096849334441941 ) ) ;
#39026=VECTOR ( 'NONE', #17399, 1000.000000000000000 ) ;
#39028=CARTESIAN_POINT ( 'NONE',  ( -6.010958268070873523, -4.863021950010519845, -18.20513189769813778 ) ) ;
#39037=CARTESIAN_POINT ( 'NONE',  ( 4.691466044806103852, 39.84135254923136671, -20.01963481131618039 ) ) ;
#39040=CARTESIAN_POINT ( 'NONE',  ( -5.995132425357893702, -13.31880955509736530, 13.33084941932902723 ) ) ;
#39051=ORIENTED_EDGE ( 'NONE', *, *, #23844, .F. ) ;
#39055=CARTESIAN_POINT ( 'NONE',  ( 0.8751705887134553219, -5.393078191593054349, 47.79200036674269825 ) ) ;
#39059=B_SPLINE_CURVE_WITH_KNOTS ( 'NONE', 3,
 ( #47218, #4265, #37212, #41918 ),
 .UNSPECIFIED., .F., .F.,
 ( 4, 4 ),
 ( 0.000000000000000000, 0.005014147105413703856 ),
 .UNSPECIFIED. ) ;
#39065=CARTESIAN_POINT ( 'NONE',  ( 0.6025881611877910160, 29.45877655626793512, -38.03302298778312718 ) ) ;
#39066=CARTESIAN_POINT ( 'NONE',  ( 0.8760168074886960365, 7.161346975773699164, -47.56749362999706676 ) ) ;
#39070=DIRECTION ( 'NONE',  ( -1.000000000000000000, -0.000000000000000000, -0.000000000000000000 ) ) ;
#39073=VECTOR ( 'NONE', #27957, 1000.000000000000227 ) ;
#39079=CARTESIAN_POINT ( 'NONE',  ( 0.1073791018717578927, 42.68962945260945929, 6.109314776652849943 ) ) ;
#39080=FACE_OUTER_BOUND ( 'NONE', #24193, .T. ) ;
#39081=CARTESIAN_POINT ( 'NONE',  ( 0.6027935024548037868, 38.27223087442848026, -29.14731236071028775 ) ) ;
#39084=DIRECTION ( 'NONE',  ( 1.000000000000000000, 0.000000000000000000, 0.000000000000000000 ) ) ;
#39090=CARTESIAN_POINT ( 'NONE',  ( 3.238741278300274473, -29.07934833201346336, -31.66556122967947928 ) ) ;
#39105=CIRCLE ( 'NONE', #53062, 42.92674063221959813 ) ;
#39109=CARTESIAN_POINT ( 'NONE',  ( 0.1073791018717578927, -37.10214135362874543, -21.98088480513651888 ) ) ;
#39110=CARTESIAN_POINT ( 'NONE',  ( 0.5998501479064708430, 33.64490850298796687, 34.38546660123309096 ) ) ;
#39117=ORIENTED_EDGE ( 'NONE', *, *, #53974, .T. ) ;
#39121=CARTESIAN_POINT ( 'NONE',  ( 0.2230388203127561253, 20.89822698305265547, -37.71673103297341356 ) ) ;
#39124=ORIENTED_EDGE ( 'NONE', *, *, #15238, .F. ) ;
#39129=CARTESIAN_POINT ( 'NONE',  ( 4.691466044806103852, 29.64918311951081975, 33.30232861642443254 ) ) ;
#39132=VERTEX_POINT ( 'NONE', #5472 ) ;
#39134=ADVANCED_FACE ( 'NONE', ( #24609 ), #33583, .F. ) ;
#39135=B_SPLINE_CURVE_WITH_KNOTS ( 'NONE', 3,
 ( #10945, #20336, #39457, #45089 ),
 .UNSPECIFIED., .F., .F.,
 ( 4, 4 ),
 ( 6.254634441385501517E-18, 0.004566006591234645501 ),
 .UNSPECIFIED. ) ;
#39140=LINE ( 'NONE', #15628, #29965 ) ;
#39144=EDGE_CURVE ( 'NONE', #5090, #39984, #19003, .T. ) ;
#39146=ORIENTED_EDGE ( 'NONE', *, *, #10970, .T. ) ;
#39147=EDGE_CURVE ( 'NONE', #39207, #44040, #48715, .T. ) ;
#39154=VECTOR ( 'NONE', #38609, 1000.000000000000114 ) ;
#39167=CARTESIAN_POINT ( 'NONE',  ( 4.975801465491695552, -2.564218696447830403, 47.84403947906839250 ) ) ;
#39168=B_SPLINE_CURVE_WITH_KNOTS ( 'NONE', 3,
 ( #48148, #5200, #43464, #42235 ),
 .UNSPECIFIED., .F., .F.,
 ( 4, 4 ),
 ( 4.336808689942017736E-19, 0.005014147105413693448 ),
 .UNSPECIFIED. ) ;
#39183=ORIENTED_EDGE ( 'NONE', *, *, #60668, .F. ) ;
#39187=CARTESIAN_POINT ( 'NONE',  ( 0.7246131072078566548, -28.62741613354265624, -38.65593150731038463 ) ) ;
#39195=CARTESIAN_POINT ( 'NONE',  ( 0.6025881611877910160, -38.29866377863859128, 29.11258673756348614 ) ) ;
#39196=EDGE_LOOP ( 'NONE', ( #11860, #47279, #26134, #33574 ) ) ;
#39198=CARTESIAN_POINT ( 'NONE',  ( -4.908599999999999852, 0.000000000000000000, -3.000000000000000000 ) ) ;
#39207=VERTEX_POINT ( 'NONE', #29298 ) ;
#39208=B_SPLINE_CURVE_WITH_KNOTS ( 'NONE', 3,
 ( #37106, #36792, #41491, #26433 ),
 .UNSPECIFIED., .F., .F.,
 ( 4, 4 ),
 ( 2.023134036479838731E-17, 0.004444306975806115896 ),
 .UNSPECIFIED. ) ;
#39212=VERTEX_POINT ( 'NONE', #48110 ) ;
#39214=CARTESIAN_POINT ( 'NONE',  ( 0.7954190325252769034, 37.62416463577109482, -29.96539637359175501 ) ) ;
#39220=EDGE_CURVE ( 'NONE', #39984, #22663, #30147, .T. ) ;
#39230=CARTESIAN_POINT ( 'NONE',  ( -6.016761891674565099, 9.424569481870481269, -16.31696541414262214 ) ) ;
#39233=CARTESIAN_POINT ( 'NONE',  ( 4.833616638992208614, -41.27831852777658384, 20.86133030530218235 ) ) ;
#39242=CARTESIAN_POINT ( 'NONE',  ( 0.6001305935487315502, -24.50730504006486754, 41.40054608060250985 ) ) ;
#39244=DIRECTION ( 'NONE',  ( -0.1024043820194934645, 0.1428674944016148363, -0.9844298967354710994 ) ) ;
#39248=B_SPLINE_CURVE_WITH_KNOTS ( 'NONE', 3,
 ( #8434, #27560, #51972, #23173 ),
 .UNSPECIFIED., .F., .F.,
 ( 4, 4 ),
 ( 6.254634441385501517E-18, 0.004566006591234646368 ),
 .UNSPECIFIED. ) ;
#39256=CARTESIAN_POINT ( 'NONE',  ( 0.6009453534118438522, -29.63106322864213737, 37.89911869481681350 ) ) ;
#39261=CARTESIAN_POINT ( 'NONE',  ( 0.6001305935487315502, -5.760103278698373686, 47.76436356026957952 ) ) ;
#39262=ORIENTED_EDGE ( 'NONE', *, *, #37511, .T. ) ;
#39264=VERTEX_POINT ( 'NONE', #59334 ) ;
#39265=CARTESIAN_POINT ( 'NONE',  ( 0.6023142530420679819, -18.16775455049974042, 44.54505940664454755 ) ) ;
#39267=CARTESIAN_POINT ( 'NONE',  ( 0.1092355843206037486, -30.70542469027345334, 30.28032287551026158 ) ) ;
#39279=DIRECTION ( 'NONE',  ( 0.09835009131224554946, -0.6981896185982771064, 0.7091251765523951534 ) ) ;
#39283=ORIENTED_EDGE ( 'NONE', *, *, #41663, .T. ) ;
#39289=DIRECTION ( 'NONE',  ( 0.000000000000000000, 0.000000000000000000, 1.000000000000000000 ) ) ;
#39290=EDGE_CURVE ( 'NONE', #9871, #19218, #30740, .T. ) ;
#39291=CARTESIAN_POINT ( 'NONE',  ( 0.3622758884714600280, -43.10531414739104861, -0.8252992914326565677 ) ) ;
#39293=CARTESIAN_POINT ( 'NONE',  ( 0.6028618097248862329, -18.57111736963418736, -44.37846879336927941 ) ) ;
#39295=VERTEX_POINT ( 'NONE', #21756 ) ;
#39301=CARTESIAN_POINT ( 'NONE',  ( 0.6030672727741701600, -24.12926094634015328, 41.61859040196942061 ) ) ;
#39315=CARTESIAN_POINT ( 'NONE',  ( 0.1084644655670283231, -10.77688306151832798, 41.75632203164214218 ) ) ;
#39321=CARTESIAN_POINT ( 'NONE',  ( 0.6028618097248863439, -24.20479143424861945, -41.57478760529395601 ) ) ;
#39324=CARTESIAN_POINT ( 'NONE',  ( 0.5988103564986360094, -46.30780741915676657, 13.03604522143276512 ) ) ;
#39330=CIRCLE ( 'NONE', #53290, 47.91270532121795611 ) ;
#39339=VERTEX_POINT ( 'NONE', #46500 ) ;
#39341=CARTESIAN_POINT ( 'NONE',  ( 0.8751705887134553219, 44.76769609654211735, 17.57879340691559378 ) ) ;
#39342=CARTESIAN_POINT ( 'NONE',  ( -6.016104459813371719, 9.426230926598641702, 16.31603998697573132 ) ) ;
#39348=CARTESIAN_POINT ( 'NONE',  ( -2.708315649062916552, 12.80362818457435914, 7.087851317224007630 ) ) ;
#39352=ORIENTED_EDGE ( 'NONE', *, *, #35466, .T. ) ;
#39358=CARTESIAN_POINT ( 'NONE',  ( 0.1064266418746774578, 39.62374465289870074, 17.02047513535245926 ) ) ;
#39359=ADVANCED_FACE ( 'NONE', ( #4166 ), #48026, .F. ) ;
#39364=CARTESIAN_POINT ( 'NONE',  ( 2.643462169533613793, -48.01657676222236404, 1.382267876918295890 ) ) ;
#39377=CARTESIAN_POINT ( 'NONE',  ( -6.001507490154111224, 4.892199142591558747, -18.19774963328903539 ) ) ;
#39383=CARTESIAN_POINT ( 'NONE',  ( 0.6028618097248863439, 38.05975027458337223, -29.42431480658691356 ) ) ;
#39386=EDGE_CURVE ( 'NONE', #16923, #26391, #15198, .T. ) ;
#39391=ORIENTED_EDGE ( 'NONE', *, *, #15553, .F. ) ;
#39402=ORIENTED_EDGE ( 'NONE', *, *, #36796, .F. ) ;
#39422=AXIS2_PLACEMENT_3D ( 'NONE', #54166, #15068, #11602 ) ;
#39423=VERTEX_POINT ( 'NONE', #57396 ) ;
#39427=CARTESIAN_POINT ( 'NONE',  ( 0.3622758884714730732, 20.83792692158972670, -37.74294673546565804 ) ) ;
#39428=EDGE_CURVE ( 'NONE', #55454, #17384, #60766, .T. ) ;
#39436=CARTESIAN_POINT ( 'NONE',  ( 0.6041374136657476912, -18.24862627831563699, 44.51224464244968715 ) ) ;
#39437=CARTESIAN_POINT ( 'NONE',  ( 0.8760168074887090262, -44.77533136581869400, -17.58183840866385594 ) ) ;
#39438=DIRECTION ( 'NONE',  ( 1.000000000000000000, 0.000000000000000000, 0.000000000000000000 ) ) ;
#39439=ORIENTED_EDGE ( 'NONE', *, *, #2245, .F. ) ;
#39444=CARTESIAN_POINT ( 'NONE',  ( 0.8751705887134423323, -42.09020928323391075, 23.27176129838352736 ) ) ;
#39446=FACE_OUTER_BOUND ( 'NONE', #37826, .T. ) ;
#39453=CONICAL_SURFACE ( 'NONE', #9371, 42.92674063221959813, 1.485477209440487556 ) ;
#39457=CARTESIAN_POINT ( 'NONE',  ( 1.827119703190778877, -17.60659059422150463, -39.28489939038881573 ) ) ;
#39464=DIRECTION ( 'NONE',  ( 0.09835009131224549395, -0.7091251765524022588, -0.6981896185982696679 ) ) ;
#39465=CARTESIAN_POINT ( 'NONE',  ( 4.549368137175248350, 0.000000000000000000, 0.000000000000000000 ) ) ;
#39468=CARTESIAN_POINT ( 'NONE',  ( 0.7954196712028480665, 11.60747899261454741, 46.67728755034890042 ) ) ;
#39488=B_SPLINE_CURVE_WITH_KNOTS ( 'NONE', 3,
 ( #5137, #57141, #47467, #47778, #4516, #14274, #28656, #43403, #14580, #3908, #32443, #51521, #9546, #56536, #4825, #23965, #43092, #33380, #8611 ),
 .UNSPECIFIED., .F., .F.,
 ( 4, 3, 3, 3, 3, 3, 4 ),
 ( 1.185767046459373819E-16, 0.0002618519381806248868, 0.0003927759815485986857, 0.0005237000248299433216, 0.0006546240681325007525, 0.0007855481115631354197, 0.0009699050456655109419 ),
 .UNSPECIFIED. ) ;
#39490=CARTESIAN_POINT ( 'NONE',  ( -6.001507490154110336, 4.862106078788180241, -18.20581304543292589 ) ) ;
#39493=ADVANCED_FACE ( 'NONE', ( #41058 ), #42014, .F. ) ;
#39509=CARTESIAN_POINT ( 'NONE',  ( 0.5998501479064708430, 44.24259072156059602, 18.89267974119682947 ) ) ;
#39518=ORIENTED_EDGE ( 'NONE', *, *, #579, .T. ) ;
#39522=CARTESIAN_POINT ( 'NONE',  ( 4.975801465491694664, 3.702618843597456522, -47.76942479135481534 ) ) ;
#39524=CARTESIAN_POINT ( 'NONE',  ( 0.6001305935487422083, 47.62765676940934867, 6.798494447612372760 ) ) ;
#39527=CARTESIAN_POINT ( 'NONE',  ( -2.569797478183790229, -14.62602397812941035, -0.4487456364278306631 ) ) ;
#39533=CARTESIAN_POINT ( 'NONE',  ( 0.3622758884714600280, 6.444611261694588755, -42.62881903538203687 ) ) ;
#39537=CARTESIAN_POINT ( 'NONE',  ( 0.5998501479064699549, 47.62484632993687939, -6.798102206413639159 ) ) ;
#39539=FACE_OUTER_BOUND ( 'NONE', #57092, .T. ) ;
#39546=VECTOR ( 'NONE', #28414, 1000.000000000000114 ) ;
#39553=B_SPLINE_CURVE_WITH_KNOTS ( 'NONE', 3,
 ( #18372, #52474, #19295, #5159 ),
 .UNSPECIFIED., .F., .F.,
 ( 4, 4 ),
 ( 0.000000000000000000, 0.005014147105413702989 ),
 .UNSPECIFIED. ) ;
#39555=ORIENTED_EDGE ( 'NONE', *, *, #22998, .T. ) ;
#39557=EDGE_CURVE ( 'NONE', #40367, #45029, #293, .T. ) ;
#39558=ORIENTED_EDGE ( 'NONE', *, *, #15305, .T. ) ;
#39560=ORIENTED_EDGE ( 'NONE', *, *, #51726, .F. ) ;
#39562=VERTEX_POINT ( 'NONE', #40748 ) ;
#39567=ORIENTED_EDGE ( 'NONE', *, *, #2670, .F. ) ;
#39569=APPLICATION_CONTEXT ( 'automotive_design' ) ;
#39578=CARTESIAN_POINT ( 'NONE',  ( 0.2224561200757617097, 0.7594684977685240979, -43.11279565427788896 ) ) ;
#39579=ADVANCED_FACE ( 'NONE', ( #2483 ), #18394, .F. ) ;
#39580=ORIENTED_EDGE ( 'NONE', *, *, #39290, .F. ) ;
#39582=CARTESIAN_POINT ( 'NONE',  ( 0.1084644655670283508, 41.75632203164217771, 10.77688306151818232 ) ) ;
#39583=FACE_OUTER_BOUND ( 'NONE', #37186, .T. ) ;
#39585=CIRCLE ( 'NONE', #1529, 42.92674063221959813 ) ;
#39588=CARTESIAN_POINT ( 'NONE',  ( 0.2885697896453112699, 42.63514065501006201, 6.424755442172748410 ) ) ;
#39600=CARTESIAN_POINT ( 'NONE',  ( 0.2224561200757614321, -43.11279565427786764, -0.7594684977683735516 ) ) ;
#39604=CARTESIAN_POINT ( 'NONE',  ( 0.6001305935487315502, 37.84751346122855864, -29.70149728382397214 ) ) ;
#39605=CARTESIAN_POINT ( 'NONE',  ( 0.6023142530420679819, -18.65157113320520921, -44.34465601638692789 ) ) ;
#39606=B_SPLINE_CURVE_WITH_KNOTS ( 'NONE', 3,
 ( #24959, #29334, #48442, #53435, #5507, #39081, #58134, #15258, #34363, #10546, #1128, #39383, #58435, #15559, #58743, #15870 ),
 .UNSPECIFIED., .F., .F.,
 ( 4, 3, 3, 3, 3, 4 ),
 ( 1.962735358247464152E-17, 0.0002618515315864419226, 0.0003927756766342003765, 0.0005236998216950570226, 0.0007855159896329932598, 0.001047349442285927870 ),
 .UNSPECIFIED. ) ;
#39610=CARTESIAN_POINT ( 'NONE',  ( 0.8760168074886960365, 37.61398439004493355, 29.98565522133359451 ) ) ;
#39629=( BOUNDED_SURFACE ( )  B_SPLINE_SURFACE ( 3, 1, ( 
 ( #35335, #54394 ),
 ( #15911, #30600 ),
 ( #58174, #49717 ),
 ( #1166, #48796 ) ),
 .UNSPECIFIED., .F., .F., .F. ) 
 B_SPLINE_SURFACE_WITH_KNOTS ( ( 4, 4 ),
 ( 2, 2 ),
 ( 0.000000000000000000, 1.000000000000000000 ),
 ( 0.000000000000000000, 1.000000000000000000 ),
 .UNSPECIFIED. ) 
 GEOMETRIC_REPRESENTATION_ITEM ( )  RATIONAL_B_SPLINE_SURFACE ( (
 ( 1.000000000000000000, 1.000000000000000000),
 ( 0.9751682680413298332, 0.9999560080971552356),
 ( 0.9751682680413298332, 0.9999560080971552356),
 ( 1.000000000000000000, 1.000000000000000000) ) ) 
 REPRESENTATION_ITEM ( '' )  SURFACE ( )  );
#39632=CARTESIAN_POINT ( 'NONE',  ( -6.017396004339687465, -18.20140164570672425, 4.875835690939116063 ) ) ;
#39650=LINE ( 'NONE', #7004, #26554 ) ;
#39651=VERTEX_POINT ( 'NONE', #19088 ) ;
#39652=CARTESIAN_POINT ( 'NONE',  ( -6.015611763856276717, -18.20278301740940208, 4.870987357968111553 ) ) ;
#39655=DIRECTION ( 'NONE',  ( -1.000000000000000000, -0.000000000000000000, -0.000000000000000000 ) ) ;
#39664=CARTESIAN_POINT ( 'NONE',  ( 4.691466044806103852, 44.51344083442435107, 2.583163953528638146 ) ) ;
#39670=CARTESIAN_POINT ( 'NONE',  ( 0.6031356755773454870, -47.69587413076377658, 6.279306815850017820 ) ) ;
#39673=CARTESIAN_POINT ( 'NONE',  ( 0.6001305935487422083, 18.89378601236063560, -44.24520387813809918 ) ) ;
#39690=CARTESIAN_POINT ( 'NONE',  ( 0.3622758884714730732, -39.50828911767010965, 17.25816669464924047 ) ) ;
#39700=CARTESIAN_POINT ( 'NONE',  ( -6.015611763856276717, -7.205255340944737519, 17.41126425312535275 ) ) ;
#39701=ORIENTED_EDGE ( 'NONE', *, *, #18676, .T. ) ;
#39713=EDGE_CURVE ( 'NONE', #16197, #58621, #12211, .T. ) ;
#39718=CARTESIAN_POINT ( 'NONE',  ( 4.975801465491695552, 45.55012473237732706, 14.85979367497190040 ) ) ;
#39724=( BOUNDED_SURFACE ( )  B_SPLINE_SURFACE ( 3, 1, ( 
 ( #17103, #31493 ),
 ( #50288, #12720 ),
 ( #26795, #2979 ),
 ( #36524, #31816 ) ),
 .UNSPECIFIED., .F., .F., .F. ) 
 B_SPLINE_SURFACE_WITH_KNOTS ( ( 4, 4 ),
 ( 2, 2 ),
 ( 0.000000000000000000, 1.000000000000000000 ),
 ( 0.000000000000000000, 1.000000000000000000 ),
 .UNSPECIFIED. ) 
 GEOMETRIC_REPRESENTATION_ITEM ( )  RATIONAL_B_SPLINE_SURFACE ( (
 ( 1.000000000000000000, 1.000000000000000000),
 ( 0.7223157951917476005, 0.9931996967497186413),
 ( 0.7223157951917476005, 0.9931996967497186413),
 ( 1.000000000000000000, 1.000000000000000000) ) ) 
 REPRESENTATION_ITEM ( '' )  SURFACE ( )  );
#39725=B_SPLINE_CURVE_WITH_KNOTS ( 'NONE', 3,
 ( #729, #28321, #48057, #408 ),
 .UNSPECIFIED., .F., .F.,
 ( 4, 4 ),
 ( 0.000000000000000000, 0.004445488388166993383 ),
 .UNSPECIFIED. ) ;
#39726=CARTESIAN_POINT ( 'NONE',  ( 0.2224561200757647350, -36.95704201588776527, -22.21411683958040229 ) ) ;
#39729=ORIENTED_EDGE ( 'NONE', *, *, #25693, .F. ) ;
#39730=CARTESIAN_POINT ( 'NONE',  ( 2.301529144917016101, -25.12312032040481569, -40.93948199333324567 ) ) ;
#39733=CARTESIAN_POINT ( 'NONE',  ( 0.1073791018717578927, 43.12183934961191056, 0.4849339620934667305 ) ) ;
#39751=( BOUNDED_SURFACE ( )  B_SPLINE_SURFACE ( 3, 1, ( 
 ( #43671, #29531 ),
 ( #14231, #712 ),
 ( #58324, #38968 ),
 ( #1021, #38349 ) ),
 .UNSPECIFIED., .F., .F., .F. ) 
 B_SPLINE_SURFACE_WITH_KNOTS ( ( 4, 4 ),
 ( 2, 2 ),
 ( 0.000000000000000000, 1.000000000000000000 ),
 ( 0.000000000000000000, 1.000000000000000000 ),
 .UNSPECIFIED. ) 
 GEOMETRIC_REPRESENTATION_ITEM ( )  RATIONAL_B_SPLINE_SURFACE ( (
 ( 1.000000000000000000, 1.000000000000000000),
 ( 0.7223157951917480446, 0.9931996967497186413),
 ( 0.7223157951917480446, 0.9931996967497186413),
 ( 1.000000000000000000, 1.000000000000000000) ) ) 
 REPRESENTATION_ITEM ( '' )  SURFACE ( )  );
#39752=CARTESIAN_POINT ( 'NONE',  ( -6.001507490154111224, -14.94036486426005261, -11.48377994779716893 ) ) ;
#39753=ORIENTED_EDGE ( 'NONE', *, *, #36764, .T. ) ;
#39755=AXIS2_PLACEMENT_3D ( 'NONE', #4900, #9308, #60997 ) ;
#39756=EDGE_LOOP ( 'NONE', ( #25649, #5839, #21695, #7427 ) ) ;
#39771=CARTESIAN_POINT ( 'NONE',  ( 2.301430502907646947, -19.56449039932759959, 43.86847929982153715 ) ) ;
#39789=CARTESIAN_POINT ( 'NONE',  ( -6.016104459813371719, -18.68131780085933258, 2.464823636987379274 ) ) ;
#39792=EDGE_CURVE ( 'NONE', #56157, #52785, #35465, .T. ) ;
#39796=CARTESIAN_POINT ( 'NONE',  ( 0.1103744047535531458, 43.12441516302519773, 0.03874731383746862767 ) ) ;
#39799=CARTESIAN_POINT ( 'NONE',  ( 0.1073791018717578927, -41.77800844988522755, 10.69234304549982895 ) ) ;
#39803=AXIS2_PLACEMENT_3D ( 'NONE', #53881, #21318, #54812 ) ;
#39806=LINE ( 'NONE', #46259, #17049 ) ;
#39808=EDGE_LOOP ( 'NONE', ( #22801, #34369, #24274, #36733 ) ) ;
#39817=CARTESIAN_POINT ( 'NONE',  ( 0.8751705887134553219, -13.30665218149330364, -46.21789262997752701 ) ) ;
#39821=ORIENTED_EDGE ( 'NONE', *, *, #11710, .F. ) ;
#39822=DIRECTION ( 'NONE',  ( 0.1024043820194936449, 0.9139094329506630698, -0.3927886084231606567 ) ) ;
#39824=VECTOR ( 'NONE', #49514, 1000.000000000000227 ) ;
#39826=CARTESIAN_POINT ( 'NONE',  ( 0.6027935024548037868, 23.90242449907755784, 41.74929432965625864 ) ) ;
#39828=CARTESIAN_POINT ( 'NONE',  ( 0.5980894510889448457, 34.51330645350402904, -33.52121017007792148 ) ) ;
#39838=ORIENTED_EDGE ( 'NONE', *, *, #56209, .T. ) ;
#39845=CARTESIAN_POINT ( 'NONE',  ( 0.3622758884714730732, -22.26738722580142138, -36.91764744403313614 ) ) ;
#39849=EDGE_CURVE ( 'NONE', #5090, #56628, #17480, .T. ) ;
#39850=FILL_AREA_STYLE_COLOUR ( '', #8702 ) ;
#39868=CARTESIAN_POINT ( 'NONE',  ( 4.975801465491695552, -43.22084481528207078, -20.67815041659126862 ) ) ;
#39869=CARTESIAN_POINT ( 'NONE',  ( 0.8760168074886965917, -24.81951362746107392, 41.20610493656867135 ) ) ;
#39875=ORIENTED_EDGE ( 'NONE', *, *, #9451, .F. ) ;
#39880=ORIENTED_EDGE ( 'NONE', *, *, #7037, .T. ) ;
#39884=CARTESIAN_POINT ( 'NONE',  ( 3.680974057930773924, 47.77138393978996334, -4.423547572561821184 ) ) ;
#39887=CARTESIAN_POINT ( 'NONE',  ( 0.1103573494271547495, 0.06145187104178059107, 43.12440049163654976 ) ) ;
#39888=EDGE_CURVE ( 'NONE', #4699, #37185, #59735, .T. ) ;
#39896=CARTESIAN_POINT ( 'NONE',  ( 0.1073791018717578927, 0.4849339620933161288, -43.12183934961191056 ) ) ;
#39911=CARTESIAN_POINT ( 'NONE',  ( 0.1084644655670282815, 34.45367667780531917, 25.93599432281509820 ) ) ;
#39914=CARTESIAN_POINT ( 'NONE',  ( -2.708315649062916552, 3.532515819624345799, -14.20182604343557031 ) ) ;
#39921=FACE_OUTER_BOUND ( 'NONE', #6489, .T. ) ;
#39924=CARTESIAN_POINT ( 'NONE',  ( 0.6031356219577718170, -6.192730535896502353, 47.70727206974374468 ) ) ;
#39926=EDGE_CURVE ( 'NONE', #20551, #9409, #37672, .T. ) ;
#39931=CARTESIAN_POINT ( 'NONE',  ( 0.6009453534118440743, -46.57942464365182644, 12.02914401651092113 ) ) ;
#39936=CARTESIAN_POINT ( 'NONE',  ( 0.1103936448916684188, -0.03072591687012675085, -43.12443171339901227 ) ) ;
#39944=CARTESIAN_POINT ( 'NONE',  ( 3.238741278300274917, -35.19027457370196288, 24.69738534405251329 ) ) ;
#39946=ADVANCED_FACE ( 'NONE', ( #59421 ), #54771, .F. ) ;
#39950=CARTESIAN_POINT ( 'NONE',  ( 0.5998501479064708430, 5.759754759340140140, 47.76154736470759588 ) ) ;
#39958=B_SPLINE_CURVE_WITH_KNOTS ( 'NONE', 3,
 ( #30165, #10775, #19561, #44609 ),
 .UNSPECIFIED., .F., .F.,
 ( 4, 4 ),
 ( 0.000000000000000000, 0.004445488388166993383 ),
 .UNSPECIFIED. ) ;
#39962=DIRECTION ( 'NONE',  ( 0.000000000000000000, 0.000000000000000000, -1.000000000000000000 ) ) ;
#39964=B_SPLINE_CURVE_WITH_KNOTS ( 'NONE', 3,
 ( #7759, #29044, #14342, #9620 ),
 .UNSPECIFIED., .F., .F.,
 ( 4, 4 ),
 ( 6.254634441385501517E-18, 0.004566006591234645501 ),
 .UNSPECIFIED. ) ;
#39982=DIRECTION ( 'NONE',  ( 0.000000000000000000, -1.000000000000000000, -0.000000000000000000 ) ) ;
#39984=VERTEX_POINT ( 'NONE', #45664 ) ;
#39989=DIRECTION ( 'NONE',  ( -0.1024043820194934645, -0.4859385467930338875, -0.8679729669084632615 ) ) ;
#39996=CARTESIAN_POINT ( 'NONE',  ( 0.1097557419366048670, -41.71221507312540666, -10.94578341459255633 ) ) ;
#40003=CARTESIAN_POINT ( 'NONE',  ( 0.7246131072078557667, -0.8205838906006461819, 48.09507913767665599 ) ) ;
#40004=DIRECTION ( 'NONE',  ( -1.000000000000000000, -0.000000000000000000, -0.000000000000000000 ) ) ;
#40014=CARTESIAN_POINT ( 'NONE',  ( 4.833616638992205949, 41.27831852777612198, 20.86133030530305632 ) ) ;
#40015=CARTESIAN_POINT ( 'NONE',  ( 4.322998006666165516, 20.30542865297649158, -43.48102276965681767 ) ) ;
#40020=B_SPLINE_CURVE_WITH_KNOTS ( 'NONE', 3,
 ( #11386, #54263, #2584, #45849, #30469, #40531 ),
 .UNSPECIFIED., .F., .F.,
 ( 4, 2, 4 ),
 ( 8.510565793060200234E-17, 0.0002293366620881441987, 0.0004586733241762032875 ),
 .UNSPECIFIED. ) ;
#40027=CARTESIAN_POINT ( 'NONE',  ( -6.016761891674565099, -14.95139917749712488, 11.46828378093553980 ) ) ;
#40032=CARTESIAN_POINT ( 'NONE',  ( 0.1097557419366048670, -39.92664986079722667, -16.29667732266738867 ) ) ;
#40039=ORIENTED_EDGE ( 'NONE', *, *, #33615, .T. ) ;
#40040=B_SPLINE_CURVE_WITH_KNOTS ( 'NONE', 3,
 ( #14556, #23326, #61510, #24239 ),
 .UNSPECIFIED., .F., .F.,
 ( 4, 4 ),
 ( 2.180944827630287554E-17, 0.004564976165746189446 ),
 .UNSPECIFIED. ) ;
#40043=ORIENTED_EDGE ( 'NONE', *, *, #4718, .T. ) ;
#40052=ADVANCED_FACE ( 'NONE', ( #4250 ), #24790, .F. ) ;
#40055=CARTESIAN_POINT ( 'NONE',  ( 4.975801465491695552, 0.000000000000000000, 0.000000000000000000 ) ) ;
#40058=CARTESIAN_POINT ( 'NONE',  ( 0.1073791018717578927, -30.83464511437158961, 30.14884492832337060 ) ) ;
#40068=CARTESIAN_POINT ( 'NONE',  ( 4.833616638992208614, 30.83411269743515959, 34.47248434257923577 ) ) ;
#40070=DIRECTION ( 'NONE',  ( 0.000000000000000000, 0.000000000000000000, 1.000000000000000000 ) ) ;
#40071=ORIENTED_EDGE ( 'NONE', *, *, #6790, .F. ) ;
#40076=CARTESIAN_POINT ( 'NONE',  ( 0.1103310638050662290, 30.43528225250897989, 30.55179781598007338 ) ) ;
#40082=CARTESIAN_POINT ( 'NONE',  ( 2.301529144917015657, 13.67115311793999943, 46.04684498357985944 ) ) ;
#40084=ADVANCED_FACE ( 'NONE', ( #27158 ), #31186, .F. ) ;
#40085=CARTESIAN_POINT ( 'NONE',  ( 4.975801465491694664, -14.85979367497141546, -45.55012473237748338 ) ) ;
#40092=CARTESIAN_POINT ( 'NONE',  ( 1.827119703190777988, -43.03226500438893964, 1.232688548475876500 ) ) ;
#40096=CARTESIAN_POINT ( 'NONE',  ( 0.8760168074887076939, 46.22580377597785883, -13.30888447662032625 ) ) ;
#40097=CARTESIAN_POINT ( 'NONE',  ( -6.010958268070873523, -14.94067681728557950, 11.48268200989191534 ) ) ;
#40099=B_SPLINE_CURVE_WITH_KNOTS ( 'NONE', 3,
 ( #16568, #50081, #15960, #59784 ),
 .UNSPECIFIED., .F., .F.,
 ( 4, 4 ),
 ( 2.409784148528075715E-17, 0.004564976165746189446 ),
 .UNSPECIFIED. ) ;
#40100=ADVANCED_FACE ( 'NONE', ( #52804 ), #31674, .F. ) ;
#40101=CARTESIAN_POINT ( 'NONE',  ( -6.015611763856276717, -18.68122482568281839, 2.465697960550983225 ) ) ;
#40106=( BOUNDED_SURFACE ( )  B_SPLINE_SURFACE ( 3, 1, ( 
 ( #40027, #59078 ),
 ( #16190, #35303 ),
 ( #30575, #59697 ),
 ( #6744, #25889 ) ),
 .UNSPECIFIED., .F., .F., .F. ) 
 B_SPLINE_SURFACE_WITH_KNOTS ( ( 4, 4 ),
 ( 2, 2 ),
 ( 0.000000000000000000, 1.000000000000000000 ),
 ( 0.000000000000000000, 1.000000000000000000 ),
 .UNSPECIFIED. ) 
 GEOMETRIC_REPRESENTATION_ITEM ( )  RATIONAL_B_SPLINE_SURFACE ( (
 ( 1.000000000000000000, 1.000000000000000000),
 ( 0.9751682680413298332, 0.9999560080971552356),
 ( 0.9751682680413298332, 0.9999560080971552356),
 ( 1.000000000000000000, 1.000000000000000000) ) ) 
 REPRESENTATION_ITEM ( '' )  SURFACE ( )  );
#40109=CARTESIAN_POINT ( 'NONE',  ( 0.8751705887134553219, -47.55935879196475469, 7.160166390003496417 ) ) ;
#40115=CARTESIAN_POINT ( 'NONE',  ( 4.549368137175248350, 38.40568845698277300, -19.17571786012283042 ) ) ;
#40122=ORIENTED_EDGE ( 'NONE', *, *, #4226, .T. ) ;
#40125=DIRECTION ( 'NONE',  ( 1.000000000000000000, 0.000000000000000000, 0.000000000000000000 ) ) ;
#40135=EDGE_CURVE ( 'NONE', #35054, #45423, #25679, .T. ) ;
#40139=EDGE_CURVE ( 'NONE', #44340, #50198, #11489, .T. ) ;
#40156=FACE_OUTER_BOUND ( 'NONE', #51324, .T. ) ;
#40158=ORIENTED_EDGE ( 'NONE', *, *, #6842, .F. ) ;
#40161=CARTESIAN_POINT ( 'NONE',  ( 3.238931869106855377, 31.66562935062897921, 29.07925862215142843 ) ) ;
#40169=CARTESIAN_POINT ( 'NONE',  ( 4.549368137175248350, -38.59302160394766901, 18.79584381673463866 ) ) ;
#40170=EDGE_CURVE ( 'NONE', #56576, #33426, #18144, .T. ) ;
#40179=EDGE_LOOP ( 'NONE', ( #32573, #21372, #39560, #54465 ) ) ;
#40183=CARTESIAN_POINT ( 'NONE',  ( 0.6028618097248863439, -12.61968633793883754, -46.42282207635398805 ) ) ;
#40189=CARTESIAN_POINT ( 'NONE',  ( 0.3622758884714600280, -41.42293301073617329, -11.95365414648482627 ) ) ;
#40197=EDGE_LOOP ( 'NONE', ( #60389, #42415, #37260, #40977 ) ) ;
#40199=CARTESIAN_POINT ( 'NONE',  ( -2.708315649062910779, -13.61924161399637612, 5.356004933109226762 ) ) ;
#40201=CARTESIAN_POINT ( 'NONE',  ( -4.908599999999998964, 0.000000000000000000, 10.00000000000000000 ) ) ;
#40208=CARTESIAN_POINT ( 'NONE',  ( 0.1084644655670281704, -30.21121552071019067, 30.77359411724674132 ) ) ;
#40211=EDGE_CURVE ( 'NONE', #58295, #60046, #32345, .T. ) ;
#40216=ADVANCED_FACE ( 'NONE', ( #2644 ), #24640, .F. ) ;
#40225=CARTESIAN_POINT ( 'NONE',  ( 0.1081432562775997697, 33.95357233988193002, 26.58728936586528491 ) ) ;
#40226=CARTESIAN_POINT ( 'NONE',  ( 0.3622758884714600280, -37.74294673546600620, 20.83792692158906235 ) ) ;
#40228=B_SPLINE_CURVE_WITH_KNOTS ( 'NONE', 3,
 ( #20244, #48424, #49648, #25538, #10842, #39055 ),
 .UNSPECIFIED., .F., .F.,
 ( 4, 2, 4 ),
 ( 1.764953265579307567E-18, 0.0002450742804987335256, 0.0004901485609974652081 ),
 .UNSPECIFIED. ) ;
#40230=CARTESIAN_POINT ( 'NONE',  ( 0.1084644655670282537, 33.96951444491424610, -26.56696682929019815 ) ) ;
#40237=CARTESIAN_POINT ( 'NONE',  ( 0.8751705887134553219, 7.160166390003662507, 47.55935879196473337 ) ) ;
#40239=CARTESIAN_POINT ( 'NONE',  ( -6.016104459813374383, -17.41090761020841171, 7.206059014950020547 ) ) ;
#40243=CARTESIAN_POINT ( 'NONE',  ( 0.6254087463353924514, -19.04342133628015432, -44.17672642933494132 ) ) ;
#40247=CARTESIAN_POINT ( 'NONE',  ( 4.549368137175248350, 24.02461520945271900, -35.57418903283089406 ) ) ;
#40250=ORIENTED_EDGE ( 'NONE', *, *, #47468, .F. ) ;
#40257=FACE_OUTER_BOUND ( 'NONE', #37110, .T. ) ;
#40258=CARTESIAN_POINT ( 'NONE',  ( 0.6029303876144825880, 6.149480157545950121, 47.71279573267361229 ) ) ;
#40262=CARTESIAN_POINT ( 'NONE',  ( 0.8751705887134553219, -38.69254731947813752, -28.56654290188640033 ) ) ;
#40272=CARTESIAN_POINT ( 'NONE',  ( 0.1073791018717483448, 21.98088480513615295, 37.10214135362896570 ) ) ;
#40274=ORIENTED_EDGE ( 'NONE', *, *, #26032, .T. ) ;
#40276=EDGE_CURVE ( 'NONE', #61466, #10506, #42787, .T. ) ;
#40277=CARTESIAN_POINT ( 'NONE',  ( 0.8751705887134423323, 46.21789262997739201, 13.30665218149378504 ) ) ;
#40278=CARTESIAN_POINT ( 'NONE',  ( -5.995132425357893702, 13.31880955509745590, -13.33084941932893486 ) ) ;
#40279=ORIENTED_EDGE ( 'NONE', *, *, #11544, .F. ) ;
#40280=CARTESIAN_POINT ( 'NONE',  ( 3.238931869106854489, -42.82436385108076848, -3.793313187126794883 ) ) ;
#40281=EDGE_CURVE ( 'NONE', #50035, #20684, #55508, .T. ) ;
#40289=DIRECTION ( 'NONE',  ( -0.1024043820194934368, 0.8679729669084648158, -0.4859385467930307234 ) ) ;
#40290=CARTESIAN_POINT ( 'NONE',  ( 0.7245667037590759474, -47.79072416626839725, -5.464144792999212186 ) ) ;
#40300=CARTESIAN_POINT ( 'NONE',  ( 0.09136607875274982415, 0.000000000000000000, 0.000000000000000000 ) ) ;
#40301=DIRECTION ( 'NONE',  ( -1.000000000000000000, -0.000000000000000000, -0.000000000000000000 ) ) ;
#40302=CARTESIAN_POINT ( 'NONE',  ( -6.015611763856276717, 18.19956619163658118, 4.882992715191364574 ) ) ;
#40307=EDGE_LOOP ( 'NONE', ( #53482, #58442, #34534, #53397 ) ) ;
#40309=DIRECTION ( 'NONE',  ( 0.000000000000000000, 0.000000000000000000, -1.000000000000000000 ) ) ;
#40318=CARTESIAN_POINT ( 'NONE',  ( 0.1073791018717578927, 0.4849339620933161288, -43.12183934961191056 ) ) ;
#40322=CARTESIAN_POINT ( 'NONE',  ( 0.1064266418746778603, -34.55203617814607497, 25.80493189480173299 ) ) ;
#40326=CARTESIAN_POINT ( 'NONE',  ( 4.975801465491695552, -40.15204426031515794, -26.14269827151666092 ) ) ;
#40331=CARTESIAN_POINT ( 'NONE',  ( 3.680882792899937250, -47.28852514876961521, 8.091276083384595808 ) ) ;
#40332=CARTESIAN_POINT ( 'NONE',  ( 0.1095718737110178559, -10.91304379105033640, -41.72082389913612843 ) ) ;
#40338=VERTEX_POINT ( 'NONE', #56806 ) ;
#40340=DIRECTION ( 'NONE',  ( 0.000000000000000000, 0.000000000000000000, -1.000000000000000000 ) ) ;
#40342=VERTEX_POINT ( 'NONE', #46210 ) ;
#40343=LINE ( 'NONE', #45346, #35864 ) ;
#40355=ORIENTED_EDGE ( 'NONE', *, *, #47913, .T. ) ;
#40361=CARTESIAN_POINT ( 'NONE',  ( -6.016761891674565099, 7.214149619366596156, -17.40752468084775373 ) ) ;
#40367=VERTEX_POINT ( 'NONE', #55887 ) ;
#40370=ORIENTED_EDGE ( 'NONE', *, *, #39713, .T. ) ;
#40381=CARTESIAN_POINT ( 'NONE',  ( -6.015611763856276717, 11.47596948473810841, 14.94556629257429492 ) ) ;
#40388=( BOUNDED_SURFACE ( )  B_SPLINE_SURFACE ( 3, 1, ( 
 ( #25112, #57989 ),
 ( #5365, #58925 ),
 ( #24809, #24184 ),
 ( #675, #5665 ) ),
 .UNSPECIFIED., .F., .F., .F. ) 
 B_SPLINE_SURFACE_WITH_KNOTS ( ( 4, 4 ),
 ( 2, 2 ),
 ( 0.000000000000000000, 1.000000000000000000 ),
 ( 0.000000000000000000, 1.000000000000000000 ),
 .UNSPECIFIED. ) 
 GEOMETRIC_REPRESENTATION_ITEM ( )  RATIONAL_B_SPLINE_SURFACE ( (
 ( 1.000000000000000000, 1.000000000000000000),
 ( 0.9751682680413298332, 0.9999560080971552356),
 ( 0.9751682680413298332, 0.9999560080971552356),
 ( 1.000000000000000000, 1.000000000000000000) ) ) 
 REPRESENTATION_ITEM ( '' )  SURFACE ( )  );
#40392=CARTESIAN_POINT ( 'NONE',  ( -2.708315649062910779, 11.44805714186559875, 9.116606751444367163 ) ) ;
#40401=CARTESIAN_POINT ( 'NONE',  ( 0.1097557419366048670, 10.94578341459270376, -41.71221507312537824 ) ) ;
#40402=CARTESIAN_POINT ( 'NONE',  ( 0.1103310638050661874, 43.12437788119554227, 0.08238894504410687603 ) ) ;
#40409=AXIS2_PLACEMENT_3D ( 'NONE', #4857, #39655, #48111 ) ;
#40413=ADVANCED_FACE ( 'NONE', ( #47429 ), #30658, .F. ) ;
#40416=CARTESIAN_POINT ( 'NONE',  ( -6.016761891674564211, -13.32657647165345693, -13.32172022638605569 ) ) ;
#40435=CARTESIAN_POINT ( 'NONE',  ( 0.6030672727741701600, 44.41203814406380701, 18.49051564326148878 ) ) ;
#40442=B_SPLINE_CURVE_WITH_KNOTS ( 'NONE', 3,
 ( #33532, #48531, #57914, #44186 ),
 .UNSPECIFIED., .F., .F.,
 ( 4, 4 ),
 ( 2.302551629917872730E-17, 0.004564976165746190313 ),
 .UNSPECIFIED. ) ;
#40444=CARTESIAN_POINT ( 'NONE',  ( 4.975801465491694664, -8.787181743659814970, -47.10002938642139014 ) ) ;
#40447=ORIENTED_EDGE ( 'NONE', *, *, #860, .T. ) ;
#40448=CARTESIAN_POINT ( 'NONE',  ( 0.1092565886968784872, -42.79503959566649485, -5.321013289171513172 ) ) ;
#40450=CARTESIAN_POINT ( 'NONE',  ( 0.6025881611877910160, -29.11258673756386628, -38.29866377863830706 ) ) ;
#40461=CARTESIAN_POINT ( 'NONE',  ( 4.549368137175248350, 40.58005590356690817, -13.99871866169321599 ) ) ;
#40462=CARTESIAN_POINT ( 'NONE',  ( 0.8751705887134423323, 13.30665218149362516, -46.21789262997744885 ) ) ;
#40466=EDGE_CURVE ( 'NONE', #9584, #37089, #718, .T. ) ;
#40467=LINE ( 'NONE', #2199, #53020 ) ;
#40477=DIRECTION ( 'NONE',  ( 0.000000000000000000, 0.000000000000000000, 1.000000000000000000 ) ) ;
#40478=VERTEX_POINT ( 'NONE', #33646 ) ;
#40483=CARTESIAN_POINT ( 'NONE',  ( 4.691466044806102076, 33.30232861642391384, 29.64918311951140595 ) ) ;
#40485=DIRECTION ( 'NONE',  ( 0.1024043820194936311, -0.9844298967354744301, 0.1428674944015907999 ) ) ;
#40489=CARTESIAN_POINT ( 'NONE',  ( 2.643462169533600914, -38.93558293168558748, 28.13401304854654938 ) ) ;
#40497=VECTOR ( 'NONE', #4074, 1000.000000000000114 ) ;
#40500=ADVANCED_FACE ( 'NONE', ( #38663 ), #46394, .F. ) ;
#40501=CARTESIAN_POINT ( 'NONE',  ( 0.5980894510889457338, -5.583794302585608271, 47.78766676462066698 ) ) ;
#40506=CARTESIAN_POINT ( 'NONE',  ( 0.1104177457020373010, -30.49013195371476570, 30.49705356371253018 ) ) ;
#40511=CARTESIAN_POINT ( 'NONE',  ( 0.1102144999581333440, 41.62223437741653953, 11.28312052188161907 ) ) ;
#40513=LINE ( 'NONE', #58326, #20474 ) ;
#40516=ORIENTED_EDGE ( 'NONE', *, *, #44516, .F. ) ;
#40520=FACE_OUTER_BOUND ( 'NONE', #31250, .T. ) ;
#40531=CARTESIAN_POINT ( 'NONE',  ( 0.1073791018717483448, -6.109314776652422729, -42.68962945260951614 ) ) ;
#40532=CARTESIAN_POINT ( 'NONE',  ( 0.5998501479064699549, -5.759754759341138453, 47.76154736470748219 ) ) ;
#40533=CARTESIAN_POINT ( 'NONE',  ( 4.975801465491694664, 8.787181743659507660, 47.10002938642145409 ) ) ;
#40535=EDGE_CURVE ( 'NONE', #41641, #24034, #21692, .T. ) ;
#40537=AXIS2_PLACEMENT_3D ( 'NONE', #45661, #60337, #51557 ) ;
#40539=B_SPLINE_CURVE_WITH_KNOTS ( 'NONE', 3,
 ( #1005, #39884, #5681, #57691 ),
 .UNSPECIFIED., .F., .F.,
 ( 4, 4 ),
 ( 0.000000000000000000, 0.004445488388166993383 ),
 .UNSPECIFIED. ) ;
#40542=CARTESIAN_POINT ( 'NONE',  ( 4.833616638992205949, -35.06988470649588407, 30.15290813935842351 ) ) ;
#40546=CARTESIAN_POINT ( 'NONE',  ( 0.6001305935487422083, -47.76436356026964347, -5.760103278697848772 ) ) ;
#40551=VERTEX_POINT ( 'NONE', #30152 ) ;
#40555=CARTESIAN_POINT ( 'NONE',  ( 0.6001305935487315502, -47.62765676940938420, -6.798494447612060121 ) ) ;
#40556=ORIENTED_EDGE ( 'NONE', *, *, #27151, .F. ) ;
#40559=CARTESIAN_POINT ( 'NONE',  ( 0.1087620492084205442, -37.52665900408533872, 21.24797679669894990 ) ) ;
#40560=( BOUNDED_SURFACE ( )  B_SPLINE_SURFACE ( 3, 1, ( 
 ( #21783, #21465 ),
 ( #44995, #11156 ),
 ( #49655, #20549 ),
 ( #40302, #15545 ) ),
 .UNSPECIFIED., .F., .F., .F. ) 
 B_SPLINE_SURFACE_WITH_KNOTS ( ( 4, 4 ),
 ( 2, 2 ),
 ( 0.000000000000000000, 1.000000000000000000 ),
 ( 0.000000000000000000, 1.000000000000000000 ),
 .UNSPECIFIED. ) 
 GEOMETRIC_REPRESENTATION_ITEM ( )  RATIONAL_B_SPLINE_SURFACE ( (
 ( 1.000000000000000000, 1.000000000000000000),
 ( 0.7223157951917476005, 0.9931996967497186413),
 ( 0.7223157951917476005, 0.9931996967497186413),
 ( 1.000000000000000000, 1.000000000000000000) ) ) 
 REPRESENTATION_ITEM ( '' )  SURFACE ( )  );
#40569=CARTESIAN_POINT ( 'NONE',  ( -6.015611763856276717, -2.453375430804198398, 18.68284711750057525 ) ) ;
#40581=CARTESIAN_POINT ( 'NONE',  ( 0.6031356219577718170, 46.49081620741438314, 12.36679943215677113 ) ) ;
#40583=CONICAL_SURFACE ( 'NONE', #13556, 42.92674063221959813, 1.485477209440487556 ) ;
#40587=CARTESIAN_POINT ( 'NONE',  ( 0.6023143664670691511, 18.16777128831328625, 44.54505257464866474 ) ) ;
#40591=EDGE_LOOP ( 'NONE', ( #61093, #51632, #46748, #37866 ) ) ;
#40595=CARTESIAN_POINT ( 'NONE',  ( 0.8751705887134423323, 7.160166390004303771, -47.55935879196464100 ) ) ;
#40606=CARTESIAN_POINT ( 'NONE',  ( 0.1100247026804066219, -41.61078157869243910, -11.32523219034893636 ) ) ;
#40627=VECTOR ( 'NONE', #50545, 1000.000000000000000 ) ;
#40632=ORIENTED_EDGE ( 'NONE', *, *, #35856, .T. ) ;
#40634=CARTESIAN_POINT ( 'NONE',  ( 0.6254087463353918963, 0.6881259009461112575, 48.10157520235527073 ) ) ;
#40636=ORIENTED_EDGE ( 'NONE', *, *, #57282, .F. ) ;
#40637=VERTEX_POINT ( 'NONE', #12934 ) ;
#40638=CARTESIAN_POINT ( 'NONE',  ( 4.975801465491694664, -47.10002938642148251, 8.787181743659342459 ) ) ;
#40640=CIRCLE ( 'NONE', #21609, 42.92674063221959813 ) ;
#40644=ORIENTED_EDGE ( 'NONE', *, *, #15524, .T. ) ;
#40646=CARTESIAN_POINT ( 'NONE',  ( 0.5998501479064708430, 0.5236536531314925913, -48.10473956285919428 ) ) ;
#40648=B_SPLINE_CURVE_WITH_KNOTS ( 'NONE', 3,
 ( #50256, #40280, #30515, #34946 ),
 .UNSPECIFIED., .F., .F.,
 ( 4, 4 ),
 ( 5.057544569639794935E-18, 0.004566006591234646368 ),
 .UNSPECIFIED. ) ;
#40652=CARTESIAN_POINT ( 'NONE',  ( -6.010958268070873523, 18.68034667844849039, 2.473955915502278113 ) ) ;
#40658=CARTESIAN_POINT ( 'NONE',  ( 0.8760168074887090262, -41.20610493656926820, 24.81951362746006140 ) ) ;
#40660=DIRECTION ( 'NONE',  ( -1.000000000000000000, -0.000000000000000000, -0.000000000000000000 ) ) ;
#40661=CARTESIAN_POINT ( 'NONE',  ( 0.6023142530420679819, 44.34465601638699894, -18.65157113320505644 ) ) ;
#40669=CARTESIAN_POINT ( 'NONE',  ( 0.2224561200757600998, 41.44719785461212780, 11.89200283918804679 ) ) ;
#40672=CARTESIAN_POINT ( 'NONE',  ( 0.1103744047535531458, -26.28322091066901578, 34.18931094754994859 ) ) ;
#40677=CARTESIAN_POINT ( 'NONE',  ( 4.549368137175248350, 0.000000000000000000, 0.000000000000000000 ) ) ;
#40679=ORIENTED_EDGE ( 'NONE', *, *, #34078, .F. ) ;
#40685=CARTESIAN_POINT ( 'NONE',  ( 0.5988103622719991304, -37.79415722405575906, -29.76496569135148107 ) ) ;
#40691=DIRECTION ( 'NONE',  ( 0.000000000000000000, 0.000000000000000000, 1.000000000000000000 ) ) ;
#40704=CARTESIAN_POINT ( 'NONE',  ( -6.015611763856276717, -17.40650793417848519, 7.216738110653220239 ) ) ;
#40710=CARTESIAN_POINT ( 'NONE',  ( 4.549368137175248350, -23.67244292351665536, 35.80950303116058819 ) ) ;
#40711=VERTEX_POINT ( 'NONE', #22941 ) ;
#40712=VECTOR ( 'NONE', #48053, 1000.000000000000114 ) ;
#40720=CARTESIAN_POINT ( 'NONE',  ( 0.1103878639767399139, -41.64243544356636306, 11.20830530106120371 ) ) ;
#40724=CARTESIAN_POINT ( 'NONE',  ( 0.09136607875274982415, 9.539392014169456147, 3.000000000000000000 ) ) ;
#40726=ORIENTED_EDGE ( 'NONE', *, *, #24059, .T. ) ;
#40727=CARTESIAN_POINT ( 'NONE',  ( 0.3622758884714600280, 43.10531414739104150, 0.8252992914329575491 ) ) ;
#40730=DIRECTION ( 'NONE',  ( 0.09835009131224566048, 0.8656670924898616226, -0.4908642831975275067 ) ) ;
#40733=ORIENTED_EDGE ( 'NONE', *, *, #9331, .T. ) ;
#40739=VERTEX_POINT ( 'NONE', #327 ) ;
#40745=EDGE_CURVE ( 'NONE', #58236, #42991, #54603, .T. ) ;
#40748=CARTESIAN_POINT ( 'NONE',  ( 4.549368137175248350, -42.14271863032838894, 8.166781970325002860 ) ) ;
#40751=CARTESIAN_POINT ( 'NONE',  ( 0.1098349054025746785, -16.69989664087480463, 39.75970464594237086 ) ) ;
#40757=ORIENTED_EDGE ( 'NONE', *, *, #18672, .T. ) ;
#40759=CARTESIAN_POINT ( 'NONE',  ( 0.1073791018717578927, -33.91564619577789585, -26.63563652260155123 ) ) ;
#40762=VERTEX_POINT ( 'NONE', #19475 ) ;
#40763=CARTESIAN_POINT ( 'NONE',  ( 0.5988103564986355654, -34.44345003622227352, -33.58571500783047270 ) ) ;
#40767=ORIENTED_EDGE ( 'NONE', *, *, #17206, .F. ) ;
#40768=CARTESIAN_POINT ( 'NONE',  ( 2.643462169533613793, -32.97543604874699241, 34.93025802711668604 ) ) ;
#40771=CARTESIAN_POINT ( 'NONE',  ( 0.3622758884714730732, 31.06363466427686504, 29.89648521331642428 ) ) ;
#40773=B_SPLINE_CURVE_WITH_KNOTS ( 'NONE', 3,
 ( #22627, #52042, #12939, #23860 ),
 .UNSPECIFIED., .F., .F.,
 ( 4, 4 ),
 ( 6.254634441385501517E-18, 0.004566006591234645501 ),
 .UNSPECIFIED. ) ;
#40780=VECTOR ( 'NONE', #599, 1000.000000000000227 ) ;
#40781=CARTESIAN_POINT ( 'NONE',  ( 0.1073791018717483448, -41.77800844988507123, -10.69234304550039383 ) ) ;
#40785=CARTESIAN_POINT ( 'NONE',  ( 0.5998501479064699549, -44.24259072156099393, 18.89267974119588445 ) ) ;
#40792=CARTESIAN_POINT ( 'NONE',  ( 0.8751705887134423323, 33.37254303619506857, 34.63284514348596588 ) ) ;
#40805=VECTOR ( 'NONE', #15219, 1000.000000000000000 ) ;
#40811=VERTEX_POINT ( 'NONE', #37988 ) ;
#40817=FACE_OUTER_BOUND ( 'NONE', #30673, .T. ) ;
#40818=B_SPLINE_CURVE_WITH_KNOTS ( 'NONE', 3,
 ( #18632, #9519, #14250, #13947, #56818, #37760 ),
 .UNSPECIFIED., .F., .F.,
 ( 4, 2, 4 ),
 ( 1.870559545977334001E-17, 0.0002293319059085113364, 0.0004586638118170039704 ),
 .UNSPECIFIED. ) ;
#40825=ORIENTED_EDGE ( 'NONE', *, *, #25592, .F. ) ;
#40833=ORIENTED_EDGE ( 'NONE', *, *, #18596, .F. ) ;
#40836=ADVANCED_FACE ( 'NONE', ( #33577 ), #7567, .F. ) ;
#40839=AXIS2_PLACEMENT_3D ( 'NONE', #32139, #17115, #51217 ) ;
#40843=CARTESIAN_POINT ( 'NONE',  ( 0.1092565886968785011, 34.40108480122215440, 26.00565248013064945 ) ) ;
#40845=CARTESIAN_POINT ( 'NONE',  ( 0.6031356755773454870, 6.279255973231343546, -47.69588082432150600 ) ) ;
#40848=CARTESIAN_POINT ( 'NONE',  ( 0.5998501479064699549, 11.94461217097469685, -46.60114184914306179 ) ) ;
#40849=CARTESIAN_POINT ( 'NONE',  ( 0.6254311100348644015, 38.58047947916330145, -28.73641524052532503 ) ) ;
#40853=FACE_OUTER_BOUND ( 'NONE', #36539, .T. ) ;
#40857=CARTESIAN_POINT ( 'NONE',  ( 0.6027935024548038978, -6.106197519201156609, -47.71838037711331992 ) ) ;
#40861=CARTESIAN_POINT ( 'NONE',  ( 4.549368137175248350, -23.67244292351665536, 35.80950303116058819 ) ) ;
#40873=CARTESIAN_POINT ( 'NONE',  ( 0.1103310638050662013, -37.38800124003726211, 21.49083802119835696 ) ) ;
#40876=ORIENTED_EDGE ( 'NONE', *, *, #21547, .F. ) ;
#40879=CARTESIAN_POINT ( 'NONE',  ( -6.015611763856276717, 13.32857883366851937, -13.31979030221785365 ) ) ;
#40882=CARTESIAN_POINT ( 'NONE',  ( 1.827119703190778432, 40.22835835992442810, 15.32887915442610272 ) ) ;
#40884=FACE_OUTER_BOUND ( 'NONE', #44571, .T. ) ;
#40886=CARTESIAN_POINT ( 'NONE',  ( 0.1102144999581333162, 0.1260305566212060746, -43.12427761225339395 ) ) ;
#40892=ORIENTED_EDGE ( 'NONE', *, *, #3737, .T. ) ;
#40897=EDGE_CURVE ( 'NONE', #29351, #18593, #19589, .T. ) ;
#40900=CARTESIAN_POINT ( 'NONE',  ( 0.5998501479064699549, 18.89267974119604077, 44.24259072156093708 ) ) ;
#40902=CARTESIAN_POINT ( 'NONE',  ( 0.8751705887134423323, 29.98056538504960855, -37.60752970653798855 ) ) ;
#40904=ORIENTED_EDGE ( 'NONE', *, *, #54630, .T. ) ;
#40905=CARTESIAN_POINT ( 'NONE',  ( 0.5998501479064708430, -44.64337787626261189, 17.92509395669028649 ) ) ;
#40908=CARTESIAN_POINT ( 'NONE',  ( 4.833616638992205949, -46.11947910922906146, -3.476827473557714931 ) ) ;
#40914=CARTESIAN_POINT ( 'NONE',  ( 4.549368137175248350, -19.17571786012351254, 38.40568845698243194 ) ) ;
#40921=CARTESIAN_POINT ( 'NONE',  ( 0.1100053167205931048, -41.70112744323661502, -10.98799238780936527 ) ) ;
#40926=CARTESIAN_POINT ( 'NONE',  ( 0.8760168074887090262, 47.80016357497242296, 5.394043284319671727 ) ) ;
#40932=CARTESIAN_POINT ( 'NONE',  ( 0.1073791018717483448, -42.81622261970991161, -5.147744207006710759 ) ) ;
#40937=CARTESIAN_POINT ( 'NONE',  ( 0.6031356755852234075, 0.04363310494615044166, -48.10744332413860747 ) ) ;
#40940=EDGE_LOOP ( 'NONE', ( #50226, #40158, #61424, #43448 ) ) ;
#40954=CARTESIAN_POINT ( 'NONE',  ( -4.908599999999999852, 0.000000000000000000, 0.000000000000000000 ) ) ;
#40956=DIRECTION ( 'NONE',  ( -0.1024043820194934507, -0.8679729669084614851, 0.4859385467930367741 ) ) ;
#40967=CARTESIAN_POINT ( 'NONE',  ( 0.6001305935487315502, 48.10757715638249010, -0.5236757026884391042 ) ) ;
#40972=CARTESIAN_POINT ( 'NONE',  ( 4.322998006666179727, -40.45864630878536161, 25.80712523194204877 ) ) ;
#40977=ORIENTED_EDGE ( 'NONE', *, *, #4413, .F. ) ;
#40983=ORIENTED_EDGE ( 'NONE', *, *, #58570, .T. ) ;
#40987=VECTOR ( 'NONE', #52970, 1000.000000000000227 ) ;
#40990=CARTESIAN_POINT ( 'NONE',  ( -6.016761891674565099, 17.41015286184812894, -7.207804629151121745 ) ) ;
#40999=CARTESIAN_POINT ( 'NONE',  ( 0.1073791018717578927, -16.05399293000789385, -40.02496097243051310 ) ) ;
#41001=CARTESIAN_POINT ( 'NONE',  ( 0.1087620492084206969, 30.23658359364778647, 30.74858804150697011 ) ) ;
#41002=CARTESIAN_POINT ( 'NONE',  ( 0.7954196712028466232, -11.60747899261487071, -46.67728755034880805 ) ) ;
#41004=CARTESIAN_POINT ( 'NONE',  ( 0.3622758884714730732, 11.95365414648439462, 41.42293301073630118 ) ) ;
#41007=ORIENTED_EDGE ( 'NONE', *, *, #59781, .F. ) ;
#41021=CARTESIAN_POINT ( 'NONE',  ( 5.880360259849739535, 45.41096578730646627, -15.46489389606708542 ) ) ;
#41023=CARTESIAN_POINT ( 'NONE',  ( 0.2230388203127610658, 0.7599700551094308310, 43.11276071378622277 ) ) ;
#41026=CARTESIAN_POINT ( 'NONE',  ( 0.5998501479064699549, 11.94461217097469685, -46.60114184914306179 ) ) ;
#41028=EDGE_LOOP ( 'NONE', ( #45866, #12445, #20154, #27389 ) ) ;
#41029=CARTESIAN_POINT ( 'NONE',  ( -5.995132425357893702, -11.46484027925377980, 14.95525565067270968 ) ) ;
#41030=B_SPLINE_CURVE_WITH_KNOTS ( 'NONE', 3,
 ( #55820, #26705, #46763, #45844 ),
 .UNSPECIFIED., .F., .F.,
 ( 4, 4 ),
 ( 6.254634441385501517E-18, 0.004566006591234646368 ),
 .UNSPECIFIED. ) ;
#41045=ORIENTED_EDGE ( 'NONE', *, *, #40276, .T. ) ;
#41050=CARTESIAN_POINT ( 'NONE',  ( 0.6031356755852232965, 5.421189728766411748E-15, -48.10744332413860747 ) ) ;
#41052=ORIENTED_EDGE ( 'NONE', *, *, #21979, .F. ) ;
#41058=FACE_OUTER_BOUND ( 'NONE', #58773, .T. ) ;
#41064=CARTESIAN_POINT ( 'NONE',  ( 0.6023142530420679819, 44.54505940664460439, 18.16775455049960541 ) ) ;
#41068=CARTESIAN_POINT ( 'NONE',  ( 4.975801465491695552, 0.000000000000000000, 0.000000000000000000 ) ) ;
#41072=CARTESIAN_POINT ( 'NONE',  ( 0.1084644655670282676, -21.90577137312966727, -37.14658555883725199 ) ) ;
#41073=CARTESIAN_POINT ( 'NONE',  ( -6.001507490154110336, 2.444174634178409633, -18.68469198366094020 ) ) ;
#41075=ORIENTED_EDGE ( 'NONE', *, *, #36641, .T. ) ;
#41078=EDGE_CURVE ( 'NONE', #51621, #33107, #8349, .T. ) ;
#41081=ORIENTED_EDGE ( 'NONE', *, *, #57480, .T. ) ;
#41082=EDGE_CURVE ( 'NONE', #3613, #11994, #15037, .T. ) ;
#41090=CARTESIAN_POINT ( 'NONE',  ( 0.1313383488274094957, -25.74310646082176035, 34.59671037481825806 ) ) ;
#41107=( BOUNDED_SURFACE ( )  B_SPLINE_SURFACE ( 3, 1, ( 
 ( #31209, #60013 ),
 ( #1755, #16497 ),
 ( #35310, #7375 ),
 ( #59389, #35929 ) ),
 .UNSPECIFIED., .F., .F., .F. ) 
 B_SPLINE_SURFACE_WITH_KNOTS ( ( 4, 4 ),
 ( 2, 2 ),
 ( 0.000000000000000000, 1.000000000000000000 ),
 ( 0.000000000000000000, 1.000000000000000000 ),
 .UNSPECIFIED. ) 
 GEOMETRIC_REPRESENTATION_ITEM ( )  RATIONAL_B_SPLINE_SURFACE ( (
 ( 1.000000000000000000, 1.000000000000000000),
 ( 0.9953040768229013402, 0.8617119497784988535),
 ( 0.9953040768229013402, 0.8617119497784988535),
 ( 1.000000000000000000, 1.000000000000000000) ) ) 
 REPRESENTATION_ITEM ( '' )  SURFACE ( )  );
#41108=DIRECTION ( 'NONE',  ( 0.09835009131224566048, -0.1375559175655364230, 0.9855991218957007582 ) ) ;
#41113=ORIENTED_EDGE ( 'NONE', *, *, #38057, .T. ) ;
#41115=VERTEX_POINT ( 'NONE', #35939 ) ;
#41118=EDGE_LOOP ( 'NONE', ( #32939, #8463, #48014, #32761 ) ) ;
#41121=( BOUNDED_SURFACE ( )  B_SPLINE_SURFACE ( 3, 1, ( 
 ( #27349, #6980 ),
 ( #12656, #7290 ),
 ( #60229, #22344 ),
 ( #2915, #45552 ) ),
 .UNSPECIFIED., .F., .F., .F. ) 
 B_SPLINE_SURFACE_WITH_KNOTS ( ( 4, 4 ),
 ( 2, 2 ),
 ( 0.000000000000000000, 1.000000000000000000 ),
 ( 0.000000000000000000, 1.000000000000000000 ),
 .UNSPECIFIED. ) 
 GEOMETRIC_REPRESENTATION_ITEM ( )  RATIONAL_B_SPLINE_SURFACE ( (
 ( 1.000000000000000000, 1.000000000000000000),
 ( 0.7223157951917476005, 0.9931996967497186413),
 ( 0.7223157951917476005, 0.9931996967497186413),
 ( 1.000000000000000000, 1.000000000000000000) ) ) 
 REPRESENTATION_ITEM ( '' )  SURFACE ( )  );
#41123=CARTESIAN_POINT ( 'NONE',  ( 3.680882792899938138, 16.63701193713989568, -44.99870212802625247 ) ) ;
#41138=CARTESIAN_POINT ( 'NONE',  ( 0.8760168074886965917, 46.68716261866176609, -11.58706983520276879 ) ) ;
#41146=ADVANCED_FACE ( 'NONE', ( #4447 ), #16726, .F. ) ;
#41149=CARTESIAN_POINT ( 'NONE',  ( 0.6031357023905875581, 12.49325238079538103, -46.45693331047446861 ) ) ;
#41152=CARTESIAN_POINT ( 'NONE',  ( 3.238741278300273585, -14.74792908357277099, -40.38334873621877819 ) ) ;
#41155=CARTESIAN_POINT ( 'NONE',  ( 0.5998501479064699549, -34.38546660123274989, -33.64490850298832925 ) ) ;
#41164=CARTESIAN_POINT ( 'NONE',  ( 0.6041374136657476912, 47.67304777898699086, -6.452348380035426878 ) ) ;
#41168=CARTESIAN_POINT ( 'NONE',  ( 0.7245667037590761694, -48.09508190954919371, 0.8205429720402956928 ) ) ;
#41175=VERTEX_POINT ( 'NONE', #50616 ) ;
#41177=CARTESIAN_POINT ( 'NONE',  ( 0.1073791018717578927, 30.83464511437137645, -30.14884492832358731 ) ) ;
#41184=CARTESIAN_POINT ( 'NONE',  ( 0.1098349054025746507, 21.37724154645449914, 37.45309339978490470 ) ) ;
#41187=ORIENTED_EDGE ( 'NONE', *, *, #36217, .T. ) ;
#41192=DIRECTION ( 'NONE',  ( 0.1024043820194936449, -0.9573600124648778964, 0.2701391291102688275 ) ) ;
#41197=ORIENTED_EDGE ( 'NONE', *, *, #34182, .T. ) ;
#41203=ORIENTED_EDGE ( 'NONE', *, *, #60948, .F. ) ;
#41204=CARTESIAN_POINT ( 'NONE',  ( 0.1081432562775998668, 42.80885385101081653, -5.208748643066250850 ) ) ;
#41207=CARTESIAN_POINT ( 'NONE',  ( 0.2230388203127576796, 29.94794547692447395, -31.02270543585797213 ) ) ;
#41213=B_SPLINE_CURVE_WITH_KNOTS ( 'NONE', 3,
 ( #58602, #53296, #48608, #16037, #29501, #15111 ),
 .UNSPECIFIED., .F., .F.,
 ( 4, 2, 4 ),
 ( 1.261467247513764704E-16, 0.0002450741128632345106, 0.0004901482257263428200 ),
 .UNSPECIFIED. ) ;
#41214=CARTESIAN_POINT ( 'NONE',  ( 0.6009452777970412107, -41.44251326863946616, 24.43074291040833756 ) ) ;
#41218=( BOUNDED_SURFACE ( )  B_SPLINE_SURFACE ( 3, 1, ( 
 ( #54840, #45793 ),
 ( #2839, #6584 ),
 ( #25730, #21037 ),
 ( #59857, #21971 ) ),
 .UNSPECIFIED., .F., .F., .F. ) 
 B_SPLINE_SURFACE_WITH_KNOTS ( ( 4, 4 ),
 ( 2, 2 ),
 ( 0.000000000000000000, 1.000000000000000000 ),
 ( 0.000000000000000000, 1.000000000000000000 ),
 .UNSPECIFIED. ) 
 GEOMETRIC_REPRESENTATION_ITEM ( )  RATIONAL_B_SPLINE_SURFACE ( (
 ( 1.000000000000000000, 1.000000000000000000),
 ( 0.9953040768229005630, 0.8617119497784937465),
 ( 0.9953040768229005630, 0.8617119497784937465),
 ( 1.000000000000000000, 1.000000000000000000) ) ) 
 REPRESENTATION_ITEM ( '' )  SURFACE ( )  );
#41222=CARTESIAN_POINT ( 'NONE',  ( 4.833616638992208614, -46.17873762321151787, -2.572717262757827861 ) ) ;
#41233=CARTESIAN_POINT ( 'NONE',  ( -2.569797478183790229, -14.44232325624825108, -2.353985772484699979 ) ) ;
#41236=VERTEX_POINT ( 'NONE', #57081 ) ;
#41239=CARTESIAN_POINT ( 'NONE',  ( -6.001507490154110336, 7.225628667346580158, 17.40350523682697670 ) ) ;
#41245=CARTESIAN_POINT ( 'NONE',  ( 0.1087620492084206830, 41.74735017127130732, -10.81135549499737003 ) ) ;
#41259=CARTESIAN_POINT ( 'NONE',  ( 0.5980894510889457338, 17.76188940524948023, -44.71414919659888199 ) ) ;
#41269=CARTESIAN_POINT ( 'NONE',  ( 5.880360259849752858, -21.17507050419485637, -43.04573319267437626 ) ) ;
#41273=ORIENTED_EDGE ( 'NONE', *, *, #49277, .F. ) ;
#41279=CARTESIAN_POINT ( 'NONE',  ( -2.708315649062910779, 7.087851317223793579, 12.80362818457447638 ) ) ;
#41280=B_SPLINE_CURVE_WITH_KNOTS ( 'NONE', 3,
 ( #58892, #20393, #35432, #39522 ),
 .UNSPECIFIED., .F., .F.,
 ( 4, 4 ),
 ( 2.054184040232706591E-17, 0.004444306975806115896 ),
 .UNSPECIFIED. ) ;
#41281=CARTESIAN_POINT ( 'NONE',  ( 0.1087620492084206414, -26.53886348603028367, 33.99140154262259017 ) ) ;
#41296=CARTESIAN_POINT ( 'NONE',  ( 0.1098349054025746507, 26.42143025179989380, -34.08267426123933319 ) ) ;
#41299=CARTESIAN_POINT ( 'NONE',  ( 0.1100053167205930771, 37.25683392728333132, -21.71746606919068512 ) ) ;
#41311=CARTESIAN_POINT ( 'NONE',  ( -6.017396004339686577, -18.84316306185412415, 0.001173774848916064005 ) ) ;
#41322=B_SPLINE_CURVE_WITH_KNOTS ( 'NONE', 3,
 ( #29901, #53683, #15820, #34935, #1374, #49621 ),
 .UNSPECIFIED., .F., .F.,
 ( 4, 2, 4 ),
 ( 3.496446946337351263E-18, 0.0002450742804987333088, 0.0004901485609974631482 ),
 .UNSPECIFIED. ) ;
#41327=EDGE_CURVE ( 'NONE', #21984, #49864, #18810, .T. ) ;
#41331=EDGE_CURVE ( 'NONE', #42964, #36881, #52395, .T. ) ;
#41339=EDGE_CURVE ( 'NONE', #54484, #17218, #49406, .T. ) ;
#41341=ORIENTED_EDGE ( 'NONE', *, *, #52556, .T. ) ;
#41343=ORIENTED_EDGE ( 'NONE', *, *, #43766, .T. ) ;
#41344=CARTESIAN_POINT ( 'NONE',  ( 0.6041374136657476912, 18.57118264377476535, 44.37863742124674360 ) ) ;
#41348=CARTESIAN_POINT ( 'NONE',  ( 0.1073791018717578927, -25.86618856530687793, -34.50606437925538472 ) ) ;
#41364=ORIENTED_EDGE ( 'NONE', *, *, #37099, .T. ) ;
#41380=VECTOR ( 'NONE', #42232, 1000.000000000000227 ) ;
#41382=PRESENTATION_STYLE_ASSIGNMENT (( #51355 ) ) ;
#41386=CARTESIAN_POINT ( 'NONE',  ( 0.7245667037590750592, 46.24390958543276753, -13.24050682223045783 ) ) ;
#41387=( BOUNDED_SURFACE ( )  B_SPLINE_SURFACE ( 3, 1, ( 
 ( #7023, #17382 ),
 ( #21768, #46211 ),
 ( #31473, #36501 ),
 ( #26154, #2331 ) ),
 .UNSPECIFIED., .F., .F., .F. ) 
 B_SPLINE_SURFACE_WITH_KNOTS ( ( 4, 4 ),
 ( 2, 2 ),
 ( 0.000000000000000000, 1.000000000000000000 ),
 ( 0.000000000000000000, 1.000000000000000000 ),
 .UNSPECIFIED. ) 
 GEOMETRIC_REPRESENTATION_ITEM ( )  RATIONAL_B_SPLINE_SURFACE ( (
 ( 1.000000000000000000, 1.000000000000000000),
 ( 0.9953040768229005630, 0.8617119497784937465),
 ( 0.9953040768229005630, 0.8617119497784937465),
 ( 1.000000000000000000, 1.000000000000000000) ) ) 
 REPRESENTATION_ITEM ( '' )  SURFACE ( )  );
#41388=CARTESIAN_POINT ( 'NONE',  ( 0.3622758884714730732, -0.8252992914325094631, -43.10531414739105571 ) ) ;
#41395=EDGE_CURVE ( 'NONE', #44899, #41864, #49246, .T. ) ;
#41396=EDGE_CURVE ( 'NONE', #29523, #55039, #54539, .T. ) ;
#41405=CARTESIAN_POINT ( 'NONE',  ( 4.975801465491695552, 0.000000000000000000, 0.000000000000000000 ) ) ;
#41423=B_SPLINE_CURVE_WITH_KNOTS ( 'NONE', 3,
 ( #13507, #56697, #51078, #42034, #47632, #41721 ),
 .UNSPECIFIED., .F., .F.,
 ( 4, 2, 4 ),
 ( 7.007167689862070887E-18, 0.0002450742804987350435, 0.0004901485609974631482 ),
 .UNSPECIFIED. ) ;
#41426=CARTESIAN_POINT ( 'NONE',  ( 4.975801465491694664, 27.09127437476381317, -39.51822597168466444 ) ) ;
#41432=CARTESIAN_POINT ( 'NONE',  ( 0.7246131072078531021, -41.24126838495085678, -24.75818606403435851 ) ) ;
#41445=CARTESIAN_POINT ( 'NONE',  ( 0.5980894510889448457, 11.77356634613253306, 46.65000524237092350 ) ) ;
#41450=DIRECTION ( 'NONE',  ( -0.1024043820194934368, 0.7811075516170080668, 0.6159418278945573144 ) ) ;
#41453=CARTESIAN_POINT ( 'NONE',  ( 0.6023143664670691511, 6.538774821499189649, -47.66103278671584320 ) ) ;
#41460=CARTESIAN_POINT ( 'NONE',  ( 0.1084644655670284064, -21.21700107124074819, 37.54424727804264705 ) ) ;
#41462=CARTESIAN_POINT ( 'NONE',  ( 0.6017666602106489515, -34.26316403931537025, -33.76944145963963706 ) ) ;
#41463=CARTESIAN_POINT ( 'NONE',  ( 0.7245667037590773907, -19.16327388244031837, -44.12005358974296598 ) ) ;
#41470=CARTESIAN_POINT ( 'NONE',  ( 4.691466044806104740, -24.49380602310839805, 37.25818859570263442 ) ) ;
#41473=ORIENTED_EDGE ( 'NONE', *, *, #19728, .F. ) ;
#41478=ORIENTED_EDGE ( 'NONE', *, *, #44797, .F. ) ;
#41486=LINE ( 'NONE', #49938, #21969 ) ;
#41488=VERTEX_POINT ( 'NONE', #30132 ) ;
#41490=FACE_OUTER_BOUND ( 'NONE', #42332, .T. ) ;
#41491=CARTESIAN_POINT ( 'NONE',  ( 3.680882792899937250, -47.77138407787919760, -4.423598386734230559 ) ) ;
#41492=CARTESIAN_POINT ( 'NONE',  ( 0.1098349054025746091, 0.2133124578264728455, -43.12395110775227636 ) ) ;
#41493=ORIENTED_EDGE ( 'NONE', *, *, #50546, .F. ) ;
#41510=CARTESIAN_POINT ( 'NONE',  ( 0.1092355843206037486, 42.79374386763046090, -5.330717085612877604 ) ) ;
#41513=CARTESIAN_POINT ( 'NONE',  ( 0.1064266379913940547, 30.09411261783690605, -30.88821943652580515 ) ) ;
#41519=CARTESIAN_POINT ( 'NONE',  ( 0.8760168074887076939, -0.8912768426702952773, -48.09529047980637273 ) ) ;
#41521=CARTESIAN_POINT ( 'NONE',  ( 0.6028618097248862329, -41.57478760529421180, 24.20479143424818247 ) ) ;
#41522=CARTESIAN_POINT ( 'NONE',  ( 0.8760168074886960365, 41.20610493656875661, 24.81951362746092116 ) ) ;
#41524=DIRECTION ( 'NONE',  ( -1.000000000000000000, -0.000000000000000000, -0.000000000000000000 ) ) ;
#41530=CARTESIAN_POINT ( 'NONE',  ( 4.975801465491695552, 0.000000000000000000, 0.000000000000000000 ) ) ;
#41536=CARTESIAN_POINT ( 'NONE',  ( 0.6017667736363750963, -44.57803721604164338, 18.08696174077311625 ) ) ;
#41537=B_SPLINE_CURVE_WITH_KNOTS ( 'NONE', 3,
 ( #16505, #58461, #25280, #15587, #44426, #1452 ),
 .UNSPECIFIED., .F., .F.,
 ( 4, 2, 4 ),
 ( 8.833954287279779637E-17, 0.0002293366620881460689, 0.0004586733241762038296 ),
 .UNSPECIFIED. ) ;
#41539=CARTESIAN_POINT ( 'NONE',  ( 0.5998501479064708430, 41.92175333043619645, -23.59887241503310307 ) ) ;
#41540=EDGE_CURVE ( 'NONE', #20535, #49864, #36108, .T. ) ;
#41541=DIRECTION ( 'NONE',  ( -0.1024043820194934645, 0.9844298967354725427, 0.1428674944016040949 ) ) ;
#41547=LINE ( 'NONE', #45948, #42793 ) ;
#41552=CARTESIAN_POINT ( 'NONE',  ( 0.1097557419366048670, 5.407604117549707823, -42.78407272074152701 ) ) ;
#41554=ORIENTED_EDGE ( 'NONE', *, *, #60765, .F. ) ;
#41560=ADVANCED_FACE ( 'NONE', ( #40817 ), #60809, .F. ) ;
#41569=CARTESIAN_POINT ( 'NONE',  ( 0.6030672727741701600, -47.68443224372866496, -6.365785297724608327 ) ) ;
#41573=ORIENTED_EDGE ( 'NONE', *, *, #48810, .F. ) ;
#41576=CARTESIAN_POINT ( 'NONE',  ( 2.301430502907644726, -38.87758534782525999, 28.20897229937338224 ) ) ;
#41580=ORIENTED_EDGE ( 'NONE', *, *, #33779, .T. ) ;
#41581=CARTESIAN_POINT ( 'NONE',  ( 0.6001305935487422083, -18.89378601236034427, -44.24520387813821287 ) ) ;
#41591=EDGE_CURVE ( 'NONE', #20061, #19329, #16457, .T. ) ;
#41595=CARTESIAN_POINT ( 'NONE',  ( 3.680882792899939471, 42.44216617524785562, 22.36818923730784903 ) ) ;
#41598=EDGE_CURVE ( 'NONE', #45197, #23651, #8479, .T. ) ;
#41599=CARTESIAN_POINT ( 'NONE',  ( 0.1098349054025746507, 37.45309339978484076, -21.37724154645462704 ) ) ;
#41600=CARTESIAN_POINT ( 'NONE',  ( -6.015611763856276717, 18.68284711750061788, -2.453375430803879986 ) ) ;
#41608=CARTESIAN_POINT ( 'NONE',  ( -6.016104459813371719, 18.68131780085935034, -2.464823636987256261 ) ) ;
#41612=CARTESIAN_POINT ( 'NONE',  ( -6.016761891674565099, -18.84319130225482297, -0.003433883959981760738 ) ) ;
#41616=CARTESIAN_POINT ( 'NONE',  ( -5.995132425357893702, -17.40647075750121431, 7.219211173946431082 ) ) ;
#41640=CARTESIAN_POINT ( 'NONE',  ( -6.016104459813374383, 18.19977249352310267, 4.882138007282813774 ) ) ;
#41641=VERTEX_POINT ( 'NONE', #52632 ) ;
#41643=CARTESIAN_POINT ( 'NONE',  ( 0.1092565886968783900, 26.49813811968539312, 34.02318727879972471 ) ) ;
#41646=CARTESIAN_POINT ( 'NONE',  ( 0.1087620492084205720, -25.96440931622107229, -34.43219573047424120 ) ) ;
#41647=B_SPLINE_CURVE_WITH_KNOTS ( 'NONE', 3,
 ( #14935, #5486, #24625, #808 ),
 .UNSPECIFIED., .F., .F.,
 ( 4, 4 ),
 ( 5.553824967135426632E-18, 0.004566006591234645501 ),
 .UNSPECIFIED. ) ;
#41651=CARTESIAN_POINT ( 'NONE',  ( -5.995132425357893702, -0.008513469642939168122, 18.84415457712583475 ) ) ;
#41656=CARTESIAN_POINT ( 'NONE',  ( 0.5998501479064699549, -11.94461217097501837, 46.60114184914296942 ) ) ;
#41659=CARTESIAN_POINT ( 'NONE',  ( 0.1084644655670282676, -16.13497904887329426, 39.99242539812087216 ) ) ;
#41660=FACE_OUTER_BOUND ( 'NONE', #26807, .T. ) ;
#41663=EDGE_CURVE ( 'NONE', #27614, #16034, #48263, .T. ) ;
#41672=CARTESIAN_POINT ( 'NONE',  ( 0.1064266379913943877, -42.67882137217595329, 6.185137063632299537 ) ) ;
#41679=ORIENTED_EDGE ( 'NONE', *, *, #43275, .T. ) ;
#41707=ORIENTED_EDGE ( 'NONE', *, *, #40170, .T. ) ;
#41710=CARTESIAN_POINT ( 'NONE',  ( 2.301529144917016989, 38.87759814529778879, 28.20894756932154834 ) ) ;
#41713=CARTESIAN_POINT ( 'NONE',  ( 4.975801465491695552, 47.10002938642130488, 8.787181743660319455 ) ) ;
#41721=CARTESIAN_POINT ( 'NONE',  ( 0.8751705887134553219, 24.81530984069150136, 41.19904111682516401 ) ) ;
#41722=ORIENTED_EDGE ( 'NONE', *, *, #46027, .F. ) ;
#41723=CARTESIAN_POINT ( 'NONE',  ( 0.3622758884714730732, 39.50828911766998175, -17.25816669464953534 ) ) ;
#41726=CARTESIAN_POINT ( 'NONE',  ( 0.3622758884714730732, -42.84426538328728640, -4.808133778521729518 ) ) ;
#41728=CARTESIAN_POINT ( 'NONE',  ( 0.7048096507298635682, -13.26491767067483707, -46.24547838151364942 ) ) ;
#41732=AXIS2_PLACEMENT_3D ( 'NONE', #57191, #33433, #23401 ) ;
#41740=CARTESIAN_POINT ( 'NONE',  ( -2.708315649062916552, 13.61924161399626421, 5.356004933109508315 ) ) ;
#41741=ORIENTED_EDGE ( 'NONE', *, *, #26409, .F. ) ;
#41748=CARTESIAN_POINT ( 'NONE',  ( 0.3622758884714600280, -41.42293301073617329, -11.95365414648482627 ) ) ;
#41759=EDGE_CURVE ( 'NONE', #19838, #10899, #32741, .T. ) ;
#41762=FACE_OUTER_BOUND ( 'NONE', #3283, .T. ) ;
#41771=CARTESIAN_POINT ( 'NONE',  ( 0.1313383488274104394, -15.91164383651771885, 40.08066228784235108 ) ) ;
#41779=LINE ( 'NONE', #60842, #13491 ) ;
#41780=CIRCLE ( 'NONE', #29719, 10.00000000000000000 ) ;
#41784=VERTEX_POINT ( 'NONE', #39817 ) ;
#41792=CARTESIAN_POINT ( 'NONE',  ( 0.6009452777970415438, 6.711700115492909013, 47.63713033690756049 ) ) ;
#41794=UNCERTAINTY_MEASURE_WITH_UNIT (LENGTH_MEASURE( 1.000000000000000082E-05 ), #42001, 'distance_accuracy_value', 'NONE');
#41796=ORIENTED_EDGE ( 'NONE', *, *, #18549, .T. ) ;
#41803=B_SPLINE_CURVE_WITH_KNOTS ( 'NONE', 3,
 ( #9352, #32878, #27847, #37270, #51952, #24076, #57248, #9044, #38503, #46980, #37900, #4015, #28150, #57555, #14692, #4318 ),
 .UNSPECIFIED., .F., .F.,
 ( 4, 3, 3, 3, 3, 4 ),
 ( 1.962735358247464152E-17, 0.0002618515315864422478, 0.0003927756766341962565, 0.0005236998216950601668, 0.0007855159896329981387, 0.001047349442285927870 ),
 .UNSPECIFIED. ) ;
#41806=DIRECTION ( 'NONE',  ( -1.000000000000000000, -0.000000000000000000, -0.000000000000000000 ) ) ;
#41807=CARTESIAN_POINT ( 'NONE',  ( 0.5998501479064708430, -48.10473956285919428, -0.5236536531313246146 ) ) ;
#41812=CARTESIAN_POINT ( 'NONE',  ( -6.016761891674565099, 4.880293656735219088, -18.20023637398594119 ) ) ;
#41815=CARTESIAN_POINT ( 'NONE',  ( -6.016761891674565099, 11.46828378093559131, 14.95139917749708758 ) ) ;
#41816=CARTESIAN_POINT ( 'NONE',  ( 2.643462169533613793, -7.637863311827277180, -47.42536612906426541 ) ) ;
#41818=CARTESIAN_POINT ( 'NONE',  ( 0.6041374136657476912, -23.90252055111350415, 41.74951251761532234 ) ) ;
#41828=VECTOR ( 'NONE', #38213, 1000.000000000000114 ) ;
#41830=CARTESIAN_POINT ( 'NONE',  ( 0.1073791018717483448, 39.65380858626214433, -16.95003405440273525 ) ) ;
#41832=FACE_OUTER_BOUND ( 'NONE', #12210, .T. ) ;
#41850=LINE ( 'NONE', #22718, #60129 ) ;
#41858=CARTESIAN_POINT ( 'NONE',  ( 0.6031356219577717059, -46.49081620741446841, -12.36679943215644961 ) ) ;
#41862=LINE ( 'NONE', #26494, #1497 ) ;
#41864=VERTEX_POINT ( 'NONE', #29756 ) ;
#41867=CARTESIAN_POINT ( 'NONE',  ( 0.1095718737110177449, 5.883530294870134902, -42.72125633542928824 ) ) ;
#41870=EDGE_CURVE ( 'NONE', #54056, #2081, #38900, .T. ) ;
#41872=VECTOR ( 'NONE', #859, 1000.000000000000114 ) ;
#41874=CARTESIAN_POINT ( 'NONE',  ( 0.7048096507298579061, 46.24547838151348600, 13.26491767067531136 ) ) ;
#41890=ORIENTED_EDGE ( 'NONE', *, *, #7431, .T. ) ;
#41895=CARTESIAN_POINT ( 'NONE',  ( 0.1310142868023716212, 25.74368468368890106, 34.59629828998422596 ) ) ;
#41896=ORIENTED_EDGE ( 'NONE', *, *, #9148, .T. ) ;
#41902=CARTESIAN_POINT ( 'NONE',  ( 4.975801465491694664, 32.01766832630313075, -35.64402118370923489 ) ) ;
#41903=ORIENTED_EDGE ( 'NONE', *, *, #51493, .F. ) ;
#41909=VERTEX_POINT ( 'NONE', #41050 ) ;
#41913=CARTESIAN_POINT ( 'NONE',  ( 4.975801465491694664, 42.71626295676232843, 21.70134120755216145 ) ) ;
#41916=CARTESIAN_POINT ( 'NONE',  ( -5.995132425357893702, -9.429450169547841654, -16.31525984181043043 ) ) ;
#41918=CARTESIAN_POINT ( 'NONE',  ( 4.975801465491695552, 40.15204426031497320, 26.14269827151694514 ) ) ;
#41925=CARTESIAN_POINT ( 'NONE',  ( 0.8760168074886960365, 48.09529047980636562, 0.8912768426707899927 ) ) ;
#41926=CARTESIAN_POINT ( 'NONE',  ( 0.6001305935487315502, -11.94532529598410875, 46.60388846085702141 ) ) ;
#41928=CARTESIAN_POINT ( 'NONE',  ( 0.6029303876144825880, 38.08638053211497976, 29.38970229176916860 ) ) ;
#41930=CARTESIAN_POINT ( 'NONE',  ( 4.833616638992208614, -45.27110352095254342, 9.466882727841344547 ) ) ;
#41931=CARTESIAN_POINT ( 'NONE',  ( -6.015611763856276717, -9.427003116184289766, 16.31561949997072958 ) ) ;
#41938=CARTESIAN_POINT ( 'NONE',  ( 0.1310142868023661811, 26.75450212504321001, -33.82067078731319043 ) ) ;
#41939=CARTESIAN_POINT ( 'NONE',  ( 0.6023142530420679819, -38.00626667377541423, 29.49327578399123695 ) ) ;
#41944=B_SPLINE_CURVE_WITH_KNOTS ( 'NONE', 3,
 ( #43218, #47284, #56970, #33196, #28468, #4635 ),
 .UNSPECIFIED., .F., .F.,
 ( 4, 2, 4 ),
 ( 1.823789517034659149E-17, 0.0002293319059085100083, 0.0004586638118170017478 ),
 .UNSPECIFIED. ) ;
#41945=CARTESIAN_POINT ( 'NONE',  ( -6.015611763856276717, -18.68284711750056815, -2.453375430804263235 ) ) ;
#41948=ORIENTED_EDGE ( 'NONE', *, *, #46090, .F. ) ;
#41952=CARTESIAN_POINT ( 'NONE',  ( 0.6025881611877910160, 24.24244696985808289, -41.55278713510058708 ) ) ;
#41958=CARTESIAN_POINT ( 'NONE',  ( 5.880360259849752858, 47.87242051977165858, -3.090325311464368507 ) ) ;
#41962=CARTESIAN_POINT ( 'NONE',  ( -6.016761891674565099, -7.207804629151182141, -17.41015286184810407 ) ) ;
#41964=ORIENTED_EDGE ( 'NONE', *, *, #33677, .F. ) ;
#41969=ORIENTED_EDGE ( 'NONE', *, *, #30518, .F. ) ;
#41972=EDGE_CURVE ( 'NONE', #17539, #19838, #4437, .T. ) ;
#41982=ADVANCED_FACE ( 'NONE', ( #21915 ), #27167, .F. ) ;
#41987=VERTEX_POINT ( 'NONE', #12841 ) ;
#41991=CARTESIAN_POINT ( 'NONE',  ( -6.017396004339687465, -16.31924478664281963, 9.420565012089369361 ) ) ;
#42001=( LENGTH_UNIT ( ) NAMED_UNIT ( * ) SI_UNIT ( .MILLI., .METRE. ) );
#42005=CARTESIAN_POINT ( 'NONE',  ( 0.1064266379913939298, 5.071708164747061431, -42.82540706760017457 ) ) ;
#42007=CARTESIAN_POINT ( 'NONE',  ( 4.691466044806102076, -20.01963481131688027, 39.84135254923101144 ) ) ;
#42014=( BOUNDED_SURFACE ( )  B_SPLINE_SURFACE ( 3, 1, ( 
 ( #26000, #7802 ),
 ( #3100, #26929 ),
 ( #59813, #45740 ),
 ( #7481, #49801 ) ),
 .UNSPECIFIED., .F., .F., .F. ) 
 B_SPLINE_SURFACE_WITH_KNOTS ( ( 4, 4 ),
 ( 2, 2 ),
 ( 0.000000000000000000, 1.000000000000000000 ),
 ( 0.000000000000000000, 1.000000000000000000 ),
 .UNSPECIFIED. ) 
 GEOMETRIC_REPRESENTATION_ITEM ( )  RATIONAL_B_SPLINE_SURFACE ( (
 ( 1.000000000000000000, 1.000000000000000000),
 ( 0.9751682680413298332, 0.9999560080971552356),
 ( 0.9751682680413298332, 0.9999560080971552356),
 ( 1.000000000000000000, 1.000000000000000000) ) ) 
 REPRESENTATION_ITEM ( '' )  SURFACE ( )  );
#42016=CARTESIAN_POINT ( 'NONE',  ( -2.569797478183790229, 13.68441171582016125, -5.182550149005160200 ) ) ;
#42019=AXIS2_PLACEMENT_3D ( 'NONE', #15557, #34063, #43463 ) ;
#42025=EDGE_CURVE ( 'NONE', #49335, #39339, #23233, .T. ) ;
#42029=( BOUNDED_SURFACE ( )  B_SPLINE_SURFACE ( 3, 1, ( 
 ( #45896, #27690 ),
 ( #46821, #61185 ),
 ( #51791, #22683 ),
 ( #27998, #47120 ) ),
 .UNSPECIFIED., .F., .F., .F. ) 
 B_SPLINE_SURFACE_WITH_KNOTS ( ( 4, 4 ),
 ( 2, 2 ),
 ( 0.000000000000000000, 1.000000000000000000 ),
 ( 0.000000000000000000, 1.000000000000000000 ),
 .UNSPECIFIED. ) 
 GEOMETRIC_REPRESENTATION_ITEM ( )  RATIONAL_B_SPLINE_SURFACE ( (
 ( 1.000000000000000000, 1.000000000000000000),
 ( 0.9751682680413298332, 0.9999560080971552356),
 ( 0.9751682680413298332, 0.9999560080971552356),
 ( 1.000000000000000000, 1.000000000000000000) ) ) 
 REPRESENTATION_ITEM ( '' )  SURFACE ( )  );
#42034=CARTESIAN_POINT ( 'NONE',  ( 0.7245667037590770576, 24.75815201345788807, 41.24129124474305286 ) ) ;
#42035=EDGE_LOOP ( 'NONE', ( #6982, #61348, #18930, #34018 ) ) ;
#42036=CARTESIAN_POINT ( 'NONE',  ( 5.880360259849739535, -39.86101557989688615, 26.69116321728503394 ) ) ;
#42037=B_SPLINE_CURVE_WITH_KNOTS ( 'NONE', 3,
 ( #18613, #13005, #12691, #37743, #51478, #46506 ),
 .UNSPECIFIED., .F., .F.,
 ( 4, 2, 4 ),
 ( 1.275615807185303638E-16, 0.0002450741128632364621, 0.0004901482257263454221 ),
 .UNSPECIFIED. ) ;
#42038=ORIENTED_EDGE ( 'NONE', *, *, #60436, .T. ) ;
#42044=VERTEX_POINT ( 'NONE', #47884 ) ;
#42045=CARTESIAN_POINT ( 'NONE',  ( -2.569797478183783568, -13.68441171582012750, -5.182550149005254347 ) ) ;
#42047=CARTESIAN_POINT ( 'NONE',  ( 4.975801465491694664, 47.84403947906843513, -2.564218696446985302 ) ) ;
#42049=ORIENTED_EDGE ( 'NONE', *, *, #3098, .F. ) ;
#42065=VERTEX_POINT ( 'NONE', #23757 ) ;
#42070=B_SPLINE_CURVE_WITH_KNOTS ( 'NONE', 3,
 ( #7644, #3561, #54951, #51484, #36193, #8575, #3871, #50879, #59970, #26772, #55258, #31158, #45906, #50266, #27702, #41510, #2952, #41204, #37125 ),
 .UNSPECIFIED., .F., .F.,
 ( 4, 3, 3, 3, 3, 3, 4 ),
 ( 1.161956753697875813E-16, 0.0002618519381806248868, 0.0003927759815485977100, 0.0005237000248299422374, 0.0006546240681324978251, 0.0007855481115631330344, 0.0009699050456655102914 ),
 .UNSPECIFIED. ) ;
#42082=CARTESIAN_POINT ( 'NONE',  ( 0.8751705887134423323, 44.08562551107055327, 19.22545746485676688 ) ) ;
#42090=CARTESIAN_POINT ( 'NONE',  ( 0.5980894510889448457, -41.31170365136871681, -24.66136644716806359 ) ) ;
#42092=CARTESIAN_POINT ( 'NONE',  ( 0.6025881611877910160, 46.52425620537270134, -12.24025891548874512 ) ) ;
#42099=ORIENTED_EDGE ( 'NONE', *, *, #26726, .F. ) ;
#42102=DIRECTION ( 'NONE',  ( 0.09835009131224566048, -0.9876177374393984021, 0.1222230102474844704 ) ) ;
#42104=EDGE_CURVE ( 'NONE', #34503, #61620, #17915, .T. ) ;
#42107=ORIENTED_EDGE ( 'NONE', *, *, #10409, .T. ) ;
#42111=EDGE_CURVE ( 'NONE', #31002, #22293, #47759, .T. ) ;
#42114=B_SPLINE_CURVE_WITH_KNOTS ( 'NONE', 3,
 ( #21639, #59845, #35760, #7205 ),
 .UNSPECIFIED., .F., .F.,
 ( 4, 4 ),
 ( 0.000000000000000000, 0.005014147105413702989 ),
 .UNSPECIFIED. ) ;
#42115=EDGE_CURVE ( 'NONE', #3613, #30211, #49106, .T. ) ;
#42122=CARTESIAN_POINT ( 'NONE',  ( 0.8751705887134423323, -46.21789262997747727, -13.30665218149346529 ) ) ;
#42126=ORIENTED_EDGE ( 'NONE', *, *, #35502, .F. ) ;
#42129=EDGE_LOOP ( 'NONE', ( #44952, #55109, #46891, #31537 ) ) ;
#42140=CARTESIAN_POINT ( 'NONE',  ( 0.1100053167205930216, 39.77279469894213548, -16.66867746965606045 ) ) ;
#42141=B_SPLINE_CURVE_WITH_KNOTS ( 'NONE', 3,
 ( #33590, #52980, #5354, #41, #4117, #61436 ),
 .UNSPECIFIED., .F., .F.,
 ( 4, 2, 4 ),
 ( 8.541065402288461036E-17, 0.0002293366620881447679, 0.0004586733241762041549 ),
 .UNSPECIFIED. ) ;
#42144=CARTESIAN_POINT ( 'NONE',  ( -5.995132425357893702, 13.31880955509727293, 13.33084941932912137 ) ) ;
#42155=EDGE_CURVE ( 'NONE', #42953, #6465, #45765, .T. ) ;
#42157=CARTESIAN_POINT ( 'NONE',  ( 0.5998501479064708430, -46.33007877220729398, -12.95623334615486222 ) ) ;
#42159=CARTESIAN_POINT ( 'NONE',  ( 4.975801465491695552, -47.84403947906842092, -2.564218696447329027 ) ) ;
#42160=ORIENTED_EDGE ( 'NONE', *, *, #35886, .T. ) ;
#42163=CARTESIAN_POINT ( 'NONE',  ( 0.8751705887134553219, -11.58504748649232496, 46.67919521768867241 ) ) ;
#42165=CARTESIAN_POINT ( 'NONE',  ( -6.016761891674564211, 14.95139917749704495, 11.46828378093564460 ) ) ;
#42167=CARTESIAN_POINT ( 'NONE',  ( 0.1087620492084205859, 42.70684898916388761, 5.987629195157958328 ) ) ;
#42169=CARTESIAN_POINT ( 'NONE',  ( 0.8751705887134423323, -34.63284514348608667, 33.37254303619495488 ) ) ;
#42173=ORIENTED_EDGE ( 'NONE', *, *, #52815, .F. ) ;
#42180=CARTESIAN_POINT ( 'NONE',  ( 0.6029303876144825880, -44.39523326884624765, -18.53079182983329432 ) ) ;
#42184=ADVANCED_FACE ( 'NONE', ( #34104 ), #39629, .F. ) ;
#42190=CARTESIAN_POINT ( 'NONE',  ( -6.015611763856276717, 13.31979030221799398, 13.32857883366838081 ) ) ;
#42191=CARTESIAN_POINT ( 'NONE',  ( 0.8751705887134423323, -23.27176129838396790, -42.09020928323367627 ) ) ;
#42209=( BOUNDED_SURFACE ( )  B_SPLINE_SURFACE ( 3, 1, ( 
 ( #26710, #51123 ),
 ( #8516, #12640 ),
 ( #50820, #13248 ),
 ( #32352, #31417 ) ),
 .UNSPECIFIED., .F., .F., .F. ) 
 B_SPLINE_SURFACE_WITH_KNOTS ( ( 4, 4 ),
 ( 2, 2 ),
 ( 0.000000000000000000, 1.000000000000000000 ),
 ( 0.000000000000000000, 1.000000000000000000 ),
 .UNSPECIFIED. ) 
 GEOMETRIC_REPRESENTATION_ITEM ( )  RATIONAL_B_SPLINE_SURFACE ( (
 ( 1.000000000000000000, 1.000000000000000000),
 ( 0.7223157951917480446, 0.9931996967497186413),
 ( 0.7223157951917480446, 0.9931996967497186413),
 ( 1.000000000000000000, 1.000000000000000000) ) ) 
 REPRESENTATION_ITEM ( '' )  SURFACE ( )  );
#42216=VERTEX_POINT ( 'NONE', #21837 ) ;
#42223=CARTESIAN_POINT ( 'NONE',  ( 0.6023143664670691511, 47.72938193173972365, -6.019611522082831456 ) ) ;
#42230=B_SPLINE_CURVE_WITH_KNOTS ( 'NONE', 3,
 ( #3164, #22292, #11991, #11661 ),
 .UNSPECIFIED., .F., .F.,
 ( 4, 4 ),
 ( 0.000000000000000000, 0.004445488388166994251 ),
 .UNSPECIFIED. ) ;
#42232=DIRECTION ( 'NONE',  ( 0.1024043820194936449, 0.7811075516170125077, -0.6159418278945518743 ) ) ;
#42235=CARTESIAN_POINT ( 'NONE',  ( 4.549368137175248350, 3.018832571116558672, -42.82045902618769873 ) ) ;
#42236=CARTESIAN_POINT ( 'NONE',  ( 0.5998501479064708430, -11.94461217097437000, -46.60114184914313995 ) ) ;
#42243=CARTESIAN_POINT ( 'NONE',  ( 0.8760168074887076939, 23.27577685234598093, -42.09738177923931346 ) ) ;
#42247=B_SPLINE_CURVE_WITH_KNOTS ( 'NONE', 3,
 ( #27622, #37984, #52342, #32025, #9432, #41748 ),
 .UNSPECIFIED., .F., .F.,
 ( 4, 2, 4 ),
 ( 1.710438460654249876E-17, 0.0002293319059085089241, 0.0004586638118170007720 ),
 .UNSPECIFIED. ) ;
#42251=B_SPLINE_CURVE_WITH_KNOTS ( 'NONE', 3,
 ( #25079, #10376, #44225, #40444 ),
 .UNSPECIFIED., .F., .F.,
 ( 4, 4 ),
 ( 2.043828937333572736E-17, 0.004444306975806115029 ),
 .UNSPECIFIED. ) ;
#42254=EDGE_CURVE ( 'NONE', #50038, #30020, #5675, .T. ) ;
#42256=CARTESIAN_POINT ( 'NONE',  ( 2.643462169533600914, 30.32726672320799821, -37.25264019563384466 ) ) ;
#42266=CARTESIAN_POINT ( 'NONE',  ( -6.016761891674565099, -11.46828378093549361, -14.95139917749716041 ) ) ;
#42270=CARTESIAN_POINT ( 'NONE',  ( 0.1100247026804066219, 26.11768802553199365, 34.31594964380191470 ) ) ;
#42276=VERTEX_POINT ( 'NONE', #26528 ) ;
#42279=ORIENTED_EDGE ( 'NONE', *, *, #46624, .T. ) ;
#42291=CARTESIAN_POINT ( 'NONE',  ( -6.016761891674564211, -2.462934516563682230, -18.68153697670644320 ) ) ;
#42294=EDGE_CURVE ( 'NONE', #44566, #51524, #18743, .T. ) ;
#42295=CARTESIAN_POINT ( 'NONE',  ( 0.1081432562775999084, -34.46918062033768138, 25.91533557232832408 ) ) ;
#42300=FACE_OUTER_BOUND ( 'NONE', #59881, .T. ) ;
#42314=CARTESIAN_POINT ( 'NONE',  ( 2.301529144917014769, -43.86846428170474610, 19.56451384728966403 ) ) ;
#42325=CARTESIAN_POINT ( 'NONE',  ( 0.8751705887134553219, 5.393078191592700854, -47.79200036674274088 ) ) ;
#42329=CARTESIAN_POINT ( 'NONE',  ( 0.8760168074886960365, -11.58706983520293754, -46.68716261866172346 ) ) ;
#42331=EDGE_CURVE ( 'NONE', #9726, #20133, #17749, .T. ) ;
#42332=EDGE_LOOP ( 'NONE', ( #23608, #49252, #33770, #30363 ) ) ;
#42333=DIRECTION ( 'NONE',  ( -1.000000000000000000, -0.000000000000000000, -0.000000000000000000 ) ) ;
#42345=EDGE_CURVE ( 'NONE', #36881, #46133, #19352, .T. ) ;
#42349=CARTESIAN_POINT ( 'NONE',  ( 0.6031356755852232965, -8.546889681428286551E-06, -48.10744332413860747 ) ) ;
#42356=LINE ( 'NONE', #4700, #53755 ) ;
#42357=B_SPLINE_CURVE_WITH_KNOTS ( 'NONE', 3,
 ( #29797, #1276, #35763, #40169 ),
 .UNSPECIFIED., .F., .F.,
 ( 4, 4 ),
 ( 0.000000000000000000, 0.005014147105413700387 ),
 .UNSPECIFIED. ) ;
#42361=ORIENTED_EDGE ( 'NONE', *, *, #39888, .F. ) ;
#42386=CARTESIAN_POINT ( 'NONE',  ( 4.975801465491694664, 9.906103548668228953, -46.87746200127445206 ) ) ;
#42388=DIRECTION ( 'NONE',  ( 1.000000000000000000, 0.000000000000000000, 0.000000000000000000 ) ) ;
#42390=ADVANCED_FACE ( 'NONE', ( #60960 ), #46502, .F. ) ;
#42394=ORIENTED_EDGE ( 'NONE', *, *, #49623, .T. ) ;
#42395=CARTESIAN_POINT ( 'NONE',  ( 4.549368137175248350, -40.58005590356700765, 13.99871866169291579 ) ) ;
#42396=CARTESIAN_POINT ( 'NONE',  ( -5.995132425357893702, 18.20425902871274459, -4.869002713216382006 ) ) ;
#42397=CARTESIAN_POINT ( 'NONE',  ( 3.680974057930774812, -32.59081219554006736, -35.20670187740648061 ) ) ;
#42407=ORIENTED_EDGE ( 'NONE', *, *, #32998, .F. ) ;
#42408=CARTESIAN_POINT ( 'NONE',  ( 0.5998501479064699549, -38.48283596222010061, -28.86886762351111457 ) ) ;
#42415=ORIENTED_EDGE ( 'NONE', *, *, #48091, .F. ) ;
#42419=CARTESIAN_POINT ( 'NONE',  ( -2.569797478183790229, -3.352038560005818457, -14.24379821351256226 ) ) ;
#42433=B_SPLINE_CURVE_WITH_KNOTS ( 'NONE', 3,
 ( #14349, #27501, #47240, #3366, #13119, #60690 ),
 .UNSPECIFIED., .F., .F.,
 ( 4, 2, 4 ),
 ( 0.000000000000000000, 0.0002450742804987322246, 0.0004901485609974644492 ),
 .UNSPECIFIED. ) ;
#42447=CARTESIAN_POINT ( 'NONE',  ( -2.708315649062916552, -11.76894112707806883, -8.698422600177076802 ) ) ;
#42449=DIRECTION ( 'NONE',  ( 0.1024043820194936172, 0.3684880688409203353, -0.9239750460186112457 ) ) ;
#42455=EDGE_CURVE ( 'NONE', #17384, #41864, #8127, .T. ) ;
#42456=CARTESIAN_POINT ( 'NONE',  ( -6.016489644550736315, 17.41053539857199439, 7.206912786933354020 ) ) ;
#42457=ORIENTED_EDGE ( 'NONE', *, *, #14332, .F. ) ;
#42459=CARTESIAN_POINT ( 'NONE',  ( -6.016104459813371719, -9.426230926598529791, -16.31603998697579527 ) ) ;
#42460=CARTESIAN_POINT ( 'NONE',  ( 0.1103744047535531458, -34.18931094755022571, -26.28322091066863564 ) ) ;
#42462=CARTESIAN_POINT ( 'NONE',  ( 0.5998501479064699549, -24.50586714782575726, -41.39809967730479201 ) ) ;
#42472=CARTESIAN_POINT ( 'NONE',  ( 0.6017666602106488405, -46.55749120190036905, -12.11361215600163632 ) ) ;
#42474=ORIENTED_EDGE ( 'NONE', *, *, #47624, .T. ) ;
#42477=DIRECTION ( 'NONE',  ( 0.000000000000000000, 0.000000000000000000, -1.000000000000000000 ) ) ;
#42480=CARTESIAN_POINT ( 'NONE',  ( 0.1310142868023675966, -30.03916697317195883, -30.94009702668463646 ) ) ;
#42481=CARTESIAN_POINT ( 'NONE',  ( -6.015611763856276717, -13.32857883366824048, -13.31979030221813254 ) ) ;
#42485=CARTESIAN_POINT ( 'NONE',  ( -2.569797478183783568, 4.218948559326054948, 14.01151037928424437 ) ) ;
#42488=CARTESIAN_POINT ( 'NONE',  ( 0.7048096507298635682, -34.61049487267037250, -33.41730025321742659 ) ) ;
#42495=CARTESIAN_POINT ( 'NONE',  ( 4.322998006666179727, 22.13465289016626514, -42.57894920390106108 ) ) ;
#42508=CARTESIAN_POINT ( 'NONE',  ( 0.6001305935487422083, 6.798494447611586722, 47.62765676940946236 ) ) ;
#42523=CARTESIAN_POINT ( 'NONE',  ( 0.5998501479064699549, 47.62484632993687939, -6.798102206413639159 ) ) ;
#42524=CARTESIAN_POINT ( 'NONE',  ( 5.880360259849752858, 9.312491912827496776, 47.05949693022710534 ) ) ;
#42525=VERTEX_POINT ( 'NONE', #16760 ) ;
#42536=CARTESIAN_POINT ( 'NONE',  ( -5.995132425357893702, -18.84415457712583475, 0.008513469642740825044 ) ) ;
#42539=CARTESIAN_POINT ( 'NONE',  ( 0.6027935024548038978, 47.67281620606623704, 6.452291758824889811 ) ) ;
#42543=CARTESIAN_POINT ( 'NONE',  ( 0.1092355843206037486, -5.926758618548289448, 42.71527351115368987 ) ) ;
#42549=CARTESIAN_POINT ( 'NONE',  ( 0.1073791018717483448, 37.58707531572176919, 21.14095454447572564 ) ) ;
#42561=ORIENTED_EDGE ( 'NONE', *, *, #14683, .T. ) ;
#42564=ORIENTED_EDGE ( 'NONE', *, *, #4560, .F. ) ;
#42565=FACE_OUTER_BOUND ( 'NONE', #43432, .T. ) ;
#42569=DIRECTION ( 'NONE',  ( 1.000000000000000000, 0.000000000000000000, 0.000000000000000000 ) ) ;
#42579=VERTEX_POINT ( 'NONE', #35259 ) ;
#42586=CARTESIAN_POINT ( 'NONE',  ( -6.015611763856276717, -7.205255340944484388, -17.41126425312545223 ) ) ;
#42589=VECTOR ( 'NONE', #9214, 1000.000000000000114 ) ;
#42590=ORIENTED_EDGE ( 'NONE', *, *, #51619, .T. ) ;
#42594=CARTESIAN_POINT ( 'NONE',  ( 0.1103878639767399694, -21.60424693647530958, -37.32258098927759704 ) ) ;
#42608=CARTESIAN_POINT ( 'NONE',  ( 0.6031356755773454870, 2.564066871919272342E-05, 48.10744332413212021 ) ) ;
#42612=CARTESIAN_POINT ( 'NONE',  ( -6.015611763856276717, -9.416239407363420355, 16.32183393015593609 ) ) ;
#42620=VERTEX_POINT ( 'NONE', #8260 ) ;
#42624=CARTESIAN_POINT ( 'NONE',  ( -6.016761891674565099, -4.873659902332239113, -18.20201388312100477 ) ) ;
#42626=ORIENTED_EDGE ( 'NONE', *, *, #30106, .F. ) ;
#42632=ADVANCED_FACE ( 'NONE', ( #61192 ), #50508, .F. ) ;
#42642=ORIENTED_EDGE ( 'NONE', *, *, #38205, .F. ) ;
#42643=B_SPLINE_CURVE_WITH_KNOTS ( 'NONE', 3,
 ( #20659, #2456, #35081, #49463, #59156, #54139, #16265, #40720, #30657, #6513, #35389, #54448, #11575, #6834, #49774, #50091, #59466, #25975, #39799 ),
 .UNSPECIFIED., .F., .F.,
 ( 4, 3, 3, 3, 3, 3, 4 ),
 ( 1.144439277862597989E-16, 0.0002618519381806271636, 0.0003927759815485981436, 0.0005237000248299445142, 0.0006546240681324981504, 0.0007855481115631322755, 0.0009699050456655115924 ),
 .UNSPECIFIED. ) ;
#42644=ORIENTED_EDGE ( 'NONE', *, *, #51969, .T. ) ;
#42660=CARTESIAN_POINT ( 'NONE',  ( -6.016104459813371719, 18.20253432612966904, 4.871830707673121097 ) ) ;
#42661=CARTESIAN_POINT ( 'NONE',  ( 0.6041374136657475802, -29.42442150067225981, 38.05989626241380819 ) ) ;
#42674=EDGE_CURVE ( 'NONE', #30112, #21310, #56899, .T. ) ;
#42677=ADVANCED_FACE ( 'NONE', ( #4469 ), #52512, .F. ) ;
#42683=B_SPLINE_CURVE_WITH_KNOTS ( 'NONE', 3,
 ( #37343, #59891, #27932, #60493 ),
 .UNSPECIFIED., .F., .F.,
 ( 4, 4 ),
 ( 0.000000000000000000, 0.004445488388166994251 ),
 .UNSPECIFIED. ) ;
#42686=FACE_OUTER_BOUND ( 'NONE', #22565, .T. ) ;
#42688=CARTESIAN_POINT ( 'NONE',  ( -6.010958268070873523, -7.224487401384422469, 17.40352239307055271 ) ) ;
#42707=CARTESIAN_POINT ( 'NONE',  ( 4.975801465491695552, 43.22084481528192157, 20.67815041659156705 ) ) ;
#42711=ORIENTED_EDGE ( 'NONE', *, *, #18837, .F. ) ;
#42715=ORIENTED_EDGE ( 'NONE', *, *, #27977, .T. ) ;
#42717=CARTESIAN_POINT ( 'NONE',  ( 4.549368137175248350, 0.000000000000000000, 0.000000000000000000 ) ) ;
#42719=CARTESIAN_POINT ( 'NONE',  ( 0.1081432562775999084, -30.19275717928102409, -30.79166192943834801 ) ) ;
#42724=EDGE_CURVE ( 'NONE', #43333, #51621, #2900, .T. ) ;
#42729=CARTESIAN_POINT ( 'NONE',  ( -6.016489644550737204, -2.463898142942892555, 18.68142234211823549 ) ) ;
#42732=CARTESIAN_POINT ( 'NONE',  ( -5.995132425357893702, 2.451215106828342982, 18.68405145320025085 ) ) ;
#42733=VERTEX_POINT ( 'NONE', #19851 ) ;
#42737=( BOUNDED_SURFACE ( )  B_SPLINE_SURFACE ( 3, 1, ( 
 ( #4792, #53636 ),
 ( #10769, #53954 ),
 ( #38669, #29238 ),
 ( #23934, #48971 ) ),
 .UNSPECIFIED., .F., .F., .F. ) 
 B_SPLINE_SURFACE_WITH_KNOTS ( ( 4, 4 ),
 ( 2, 2 ),
 ( 0.000000000000000000, 1.000000000000000000 ),
 ( 0.000000000000000000, 1.000000000000000000 ),
 .UNSPECIFIED. ) 
 GEOMETRIC_REPRESENTATION_ITEM ( )  RATIONAL_B_SPLINE_SURFACE ( (
 ( 1.000000000000000000, 1.000000000000000000),
 ( 0.9953040768229013402, 0.8617119497784988535),
 ( 0.9953040768229013402, 0.8617119497784988535),
 ( 1.000000000000000000, 1.000000000000000000) ) ) 
 REPRESENTATION_ITEM ( '' )  SURFACE ( )  );
#42739=VERTEX_POINT ( 'NONE', #29530 ) ;
#42741=CARTESIAN_POINT ( 'NONE',  ( -6.015611763856276717, 18.19956619163665223, -4.882992715191109667 ) ) ;
#42743=EDGE_CURVE ( 'NONE', #60753, #46133, #36913, .T. ) ;
#42756=DIRECTION ( 'NONE',  ( 0.000000000000000000, 0.000000000000000000, 1.000000000000000000 ) ) ;
#42757=CARTESIAN_POINT ( 'NONE',  ( 0.2885697896453111033, 42.84523253470161563, -4.828949182955488695 ) ) ;
#42758=CARTESIAN_POINT ( 'NONE',  ( 0.6254087463353913412, 29.82831063981281972, 37.74264085326067431 ) ) ;
#42768=EDGE_CURVE ( 'NONE', #49434, #47393, #6534, .T. ) ;
#42777=CARTESIAN_POINT ( 'NONE',  ( 0.6009453534118439633, -46.35353704332102609, -12.87216801774528996 ) ) ;
#42779=ORIENTED_EDGE ( 'NONE', *, *, #29655, .T. ) ;
#42782=CARTESIAN_POINT ( 'NONE',  ( 2.643462169533613793, 37.25264019563415729, -30.32726672320761097 ) ) ;
#42783=ORIENTED_EDGE ( 'NONE', *, *, #24738, .T. ) ;
#42784=CARTESIAN_POINT ( 'NONE',  ( -4.908599999999999852, 12.80000000000000071, 0.000000000000000000 ) ) ;
#42787=B_SPLINE_CURVE_WITH_KNOTS ( 'NONE', 3,
 ( #11766, #40908, #16152, #54022 ),
 .UNSPECIFIED., .F., .F.,
 ( 4, 4 ),
 ( 4.336808689942017736E-19, 0.005014147105413698652 ),
 .UNSPECIFIED. ) ;
#42792=CARTESIAN_POINT ( 'NONE',  ( 0.8760168074886960365, -29.98565522133374373, 37.61398439004481986 ) ) ;
#42793=VECTOR ( 'NONE', #31195, 1000.000000000000114 ) ;
#42802=ADVANCED_FACE ( 'NONE', ( #19235 ), #34884, .F. ) ;
#42808=CARTESIAN_POINT ( 'NONE',  ( 0.8751705887134423323, 17.57879340691479797, 44.76769609654243709 ) ) ;
#42817=CARTESIAN_POINT ( 'NONE',  ( 0.3622758884714600280, 25.58609868863721459, 34.70015533914837391 ) ) ;
#42819=ORIENTED_EDGE ( 'NONE', *, *, #41339, .T. ) ;
#42822=CARTESIAN_POINT ( 'NONE',  ( -6.017396004339686577, 0.001173774848981854477, 18.84316306185412415 ) ) ;
#42826=ORIENTED_EDGE ( 'NONE', *, *, #36168, .T. ) ;
#42829=CARTESIAN_POINT ( 'NONE',  ( 0.1073791018717578927, 34.50606437925546999, -25.86618856530675714 ) ) ;
#42831=VERTEX_POINT ( 'NONE', #50718 ) ;
#42837=ORIENTED_EDGE ( 'NONE', *, *, #51165, .T. ) ;
#42838=CARTESIAN_POINT ( 'NONE',  ( -2.569797478183783568, -7.701637110048594970, -12.44213550320650619 ) ) ;
#42841=ORIENTED_EDGE ( 'NONE', *, *, #39557, .F. ) ;
#42851=CARTESIAN_POINT ( 'NONE',  ( 0.6009453534118438522, 47.63713118507418187, 6.711694149738390180 ) ) ;
#42858=VECTOR ( 'NONE', #39464, 1000.000000000000114 ) ;
#42861=CARTESIAN_POINT ( 'NONE',  ( 0.6254311100348668440, -48.10157347124187766, -0.6881768005100848962 ) ) ;
#42862=LINE ( 'NONE', #24973, #50168 ) ;
#42872=FACE_OUTER_BOUND ( 'NONE', #23980, .T. ) ;
#42876=ORIENTED_EDGE ( 'NONE', *, *, #14097, .F. ) ;
#42882=ADVANCED_FACE ( 'NONE', ( #27853 ), #11740, .F. ) ;
#42883=CARTESIAN_POINT ( 'NONE',  ( 0.8760168074886965917, 33.37827814204077015, 34.63873394077499768 ) ) ;
#42884=CARTESIAN_POINT ( 'NONE',  ( 0.8760168074886965917, -19.22870327415332881, 44.09317760313719248 ) ) ;
#42902=CARTESIAN_POINT ( 'NONE',  ( 0.1310142868023677076, 21.00772081177026607, 37.66054729763597919 ) ) ;
#42906=FACE_OUTER_BOUND ( 'NONE', #34415, .T. ) ;
#42911=CARTESIAN_POINT ( 'NONE',  ( 3.680882792899937694, -47.94008871805917948, 1.849662971458055472 ) ) ;
#42913=CARTESIAN_POINT ( 'NONE',  ( 0.1092565886968785149, 30.71235995742698677, 30.27341312544124818 ) ) ;
#42915=CARTESIAN_POINT ( 'NONE',  ( 0.6001305935487315502, 41.92422178329137239, 23.60027211631843969 ) ) ;
#42922=CARTESIAN_POINT ( 'NONE',  ( 0.6028618097248863439, 0.1745704727159134717, 48.10721794025128162 ) ) ;
#42924=ADVANCED_FACE ( 'NONE', ( #560 ), #48496, .F. ) ;
#42930=B_SPLINE_CURVE_WITH_KNOTS ( 'NONE', 3,
 ( #36329, #36024, #55393, #55089 ),
 .UNSPECIFIED., .F., .F.,
 ( 4, 4 ),
 ( 6.254634441385501517E-18, 0.004566006591234646368 ),
 .UNSPECIFIED. ) ;
#42938=VECTOR ( 'NONE', #1031, 1000.000000000000114 ) ;
#42939=CARTESIAN_POINT ( 'NONE',  ( 0.1100247026804066219, 37.26174279786183519, 21.70899701554537131 ) ) ;
#42941=CARTESIAN_POINT ( 'NONE',  ( -6.015611763856276717, -4.870987357968047604, -18.20278301740941629 ) ) ;
#42953=VERTEX_POINT ( 'NONE', #10603 ) ;
#42955=CARTESIAN_POINT ( 'NONE',  ( -6.016761891674565099, 14.94721834528414917, 11.47373234755508342 ) ) ;
#42959=EDGE_CURVE ( 'NONE', #38559, #49335, #28197, .T. ) ;
#42963=CARTESIAN_POINT ( 'NONE',  ( -6.016104459813374383, 4.871830707673057148, 18.20253432612968680 ) ) ;
#42964=VERTEX_POINT ( 'NONE', #20616 ) ;
#42967=CARTESIAN_POINT ( 'NONE',  ( -6.016761891674565099, -18.20023637398595540, -4.880293656735155139 ) ) ;
#42975=ADVANCED_FACE ( 'NONE', ( #15314 ), #35349, .F. ) ;
#42976=CARTESIAN_POINT ( 'NONE',  ( 0.7246131072078558777, -13.24054562911158150, 46.24389631750663199 ) ) ;
#42981=B_SPLINE_CURVE_WITH_KNOTS ( 'NONE', 3,
 ( #45202, #22525, #22219, #14067 ),
 .UNSPECIFIED., .F., .F.,
 ( 4, 4 ),
 ( 0.000000000000000000, 0.004445488388166995118 ),
 .UNSPECIFIED. ) ;
#42985=ORIENTED_EDGE ( 'NONE', *, *, #30418, .F. ) ;
#42989=CARTESIAN_POINT ( 'NONE',  ( 0.8751705887134423323, 13.30665218149362516, -46.21789262997744885 ) ) ;
#42991=VERTEX_POINT ( 'NONE', #30613 ) ;
#42999=CARTESIAN_POINT ( 'NONE',  ( -6.016761891674565099, -2.456125503350587991, -18.68243340030205246 ) ) ;
#43011=( BOUNDED_SURFACE ( )  B_SPLINE_SURFACE ( 3, 1, ( 
 ( #4302, #56633 ),
 ( #37884, #32861 ),
 ( #51936, #23439 ),
 ( #61624, #19366 ) ),
 .UNSPECIFIED., .F., .F., .F. ) 
 B_SPLINE_SURFACE_WITH_KNOTS ( ( 4, 4 ),
 ( 2, 2 ),
 ( 0.000000000000000000, 1.000000000000000000 ),
 ( 0.000000000000000000, 1.000000000000000000 ),
 .UNSPECIFIED. ) 
 GEOMETRIC_REPRESENTATION_ITEM ( )  RATIONAL_B_SPLINE_SURFACE ( (
 ( 1.000000000000000000, 1.000000000000000000),
 ( 0.9751682680413298332, 0.9999560080971552356),
 ( 0.9751682680413298332, 0.9999560080971552356),
 ( 1.000000000000000000, 1.000000000000000000) ) ) 
 REPRESENTATION_ITEM ( '' )  SURFACE ( )  );
#43013=ORIENTED_EDGE ( 'NONE', *, *, #51184, .T. ) ;
#43033=ORIENTED_EDGE ( 'NONE', *, *, #3878, .F. ) ;
#43035=CARTESIAN_POINT ( 'NONE',  ( 4.549368137175248350, -18.79584381673505789, -38.59302160394747006 ) ) ;
#43037=ORIENTED_EDGE ( 'NONE', *, *, #56679, .F. ) ;
#43042=DIRECTION ( 'NONE',  ( 0.09835009131224552170, -0.3736726418952377449, 0.9223318362920724933 ) ) ;
#43045=FACE_OUTER_BOUND ( 'NONE', #27891, .T. ) ;
#43060=CARTESIAN_POINT ( 'NONE',  ( 0.1064266418746774301, 37.62465821955101575, -21.07422140941967825 ) ) ;
#43062=CARTESIAN_POINT ( 'NONE',  ( -6.016761891674564211, -11.46828378093569789, 14.95139917749700587 ) ) ;
#43066=CARTESIAN_POINT ( 'NONE',  ( 4.549368137175248350, -13.59764261105721950, -40.71620287708339703 ) ) ;
#43073=CARTESIAN_POINT ( 'NONE',  ( 0.5980894510889448457, 23.44630161211528119, 42.01322166096928612 ) ) ;
#43074=CARTESIAN_POINT ( 'NONE',  ( 0.1087620492084206275, -33.99140154262286728, -26.53886348602990353 ) ) ;
#43076=CARTESIAN_POINT ( 'NONE',  ( -6.015611763856276717, -14.94556629257433578, 11.47596948473805689 ) ) ;
#43081=FACE_OUTER_BOUND ( 'NONE', #6703, .T. ) ;
#43083=CARTESIAN_POINT ( 'NONE',  ( -2.569797478183783568, -9.259773107242986967, -11.33042594333545061 ) ) ;
#43089=VERTEX_POINT ( 'NONE', #26541 ) ;
#43091=CARTESIAN_POINT ( 'NONE',  ( 0.1097557419366048670, -43.12388302211984126, 0.2231007852158213567 ) ) ;
#43092=CARTESIAN_POINT ( 'NONE',  ( 0.1087620492084206969, 39.70193592734180754, 16.83695155255847453 ) ) ;
#43096=CARTESIAN_POINT ( 'NONE',  ( 4.975801465491695552, 47.76942479135485797, -3.702618843596948039 ) ) ;
#43098=ORIENTED_EDGE ( 'NONE', *, *, #27026, .F. ) ;
#43100=FACE_OUTER_BOUND ( 'NONE', #14089, .T. ) ;
#43101=ADVANCED_FACE ( 'NONE', ( #60973 ), #18141, .F. ) ;
#43102=CARTESIAN_POINT ( 'NONE',  ( 4.975801465491694664, -27.09127437476410805, 39.51822597168447260 ) ) ;
#43105=CARTESIAN_POINT ( 'NONE',  ( -6.016761891674565099, 13.32172022638591713, 13.32657647165359904 ) ) ;
#43106=B_SPLINE_CURVE_WITH_KNOTS ( 'NONE', 3,
 ( #16530, #35967, #35656, #19548 ),
 .UNSPECIFIED., .F., .F.,
 ( 4, 4 ),
 ( 0.000000000000000000, 0.005014147105413706458 ),
 .UNSPECIFIED. ) ;
#43116=DIRECTION ( 'NONE',  ( 0.09835009131224549395, 0.4908642831975363330, -0.8656670924898565156 ) ) ;
#43121=ORIENTED_EDGE ( 'NONE', *, *, #55068, .F. ) ;
#43122=CARTESIAN_POINT ( 'NONE',  ( -6.016761891674565099, -11.47373234755513671, 14.94721834528410831 ) ) ;
#43124=CARTESIAN_POINT ( 'NONE',  ( 0.1095718737110177726, -37.21776476380641441, -21.78439022773142852 ) ) ;
#43131=CARTESIAN_POINT ( 'NONE',  ( 0.1064266379913941518, -26.69589650908261547, -33.86837498006617153 ) ) ;
#43134=CARTESIAN_POINT ( 'NONE',  ( 0.7245667037590747261, -33.42814706018044291, 34.58857005974894605 ) ) ;
#43137=B_SPLINE_CURVE_WITH_KNOTS ( 'NONE', 3,
 ( #59293, #30474, #2590, #16395, #20793, #30790 ),
 .UNSPECIFIED., .F., .F.,
 ( 4, 2, 4 ),
 ( 8.741117365843378158E-19, 0.0002450742804987339051, 0.0004901485609974669429 ),
 .UNSPECIFIED. ) ;
#43140=CARTESIAN_POINT ( 'NONE',  ( 4.975801465491694664, 21.70134120755201224, -42.71626295676241369 ) ) ;
#43142=CARTESIAN_POINT ( 'NONE',  ( 0.5998501479064708430, 29.69975237324613460, -37.84527566984826308 ) ) ;
#43143=CARTESIAN_POINT ( 'NONE',  ( -6.015611763856276717, -2.453375430803944823, -18.68284711750060723 ) ) ;
#43144=ORIENTED_EDGE ( 'NONE', *, *, #29760, .F. ) ;
#43146=EDGE_CURVE ( 'NONE', #37089, #22212, #3553, .T. ) ;
#43163=CARTESIAN_POINT ( 'NONE',  ( 0.1095718737110177865, -5.883530294870451094, 42.72125633542923140 ) ) ;
#43169=CARTESIAN_POINT ( 'NONE',  ( 0.5988103622719989083, -48.10388392585942796, -0.6065097949911955055 ) ) ;
#43183=ORIENTED_EDGE ( 'NONE', *, *, #53168, .F. ) ;
#43187=CARTESIAN_POINT ( 'NONE',  ( 0.7245667037590785009, -13.24050682223062125, -46.24390958543271068 ) ) ;
#43188=CARTESIAN_POINT ( 'NONE',  ( 0.6009453534118438522, 33.70725662590610483, 34.32439302680979409 ) ) ;
#43189=ORIENTED_EDGE ( 'NONE', *, *, #13128, .T. ) ;
#43198=B_SPLINE_CURVE_WITH_KNOTS ( 'NONE', 3,
 ( #6051, #52764, #44626, #48082, #48381, #57757 ),
 .UNSPECIFIED., .F., .F.,
 ( 4, 2, 4 ),
 ( 1.870625823323990238E-17, 0.0002293319059085113093, 0.0004586638118170039162 ),
 .UNSPECIFIED. ) ;
#43201=ORIENTED_EDGE ( 'NONE', *, *, #10675, .T. ) ;
#43202=ORIENTED_EDGE ( 'NONE', *, *, #25666, .F. ) ;
#43208=CARTESIAN_POINT ( 'NONE',  ( 0.8760168074887090262, 19.22870327415240155, 44.09317760313759749 ) ) ;
#43212=VECTOR ( 'NONE', #11026, 1000.000000000000114 ) ;
#43213=EDGE_LOOP ( 'NONE', ( #60481, #53980, #13593, #34917 ) ) ;
#43218=CARTESIAN_POINT ( 'NONE',  ( 0.1073791018717578927, -42.68962945260949482, -6.109314776652552403 ) ) ;
#43222=ADVANCED_FACE ( 'NONE', ( #15849 ), #48144, .F. ) ;
#43225=CARTESIAN_POINT ( 'NONE',  ( -2.708315649062916552, 4.041664582652610527, 14.06540004355483831 ) ) ;
#43228=EDGE_CURVE ( 'NONE', #59719, #23902, #40228, .T. ) ;
#43229=LINE ( 'NONE', #4968, #23857 ) ;
#43234=EDGE_CURVE ( 'NONE', #16525, #12730, #11809, .T. ) ;
#43255=VECTOR ( 'NONE', #32215, 1000.000000000000114 ) ;
#43256=CARTESIAN_POINT ( 'NONE',  ( 3.680882792899938138, 32.59085259319688532, -35.20667105325183144 ) ) ;
#43260=B_SPLINE_CURVE_WITH_KNOTS ( 'NONE', 3,
 ( #22965, #23565, #38012, #33297 ),
 .UNSPECIFIED., .F., .F.,
 ( 4, 4 ),
 ( 0.000000000000000000, 0.004445488388166995118 ),
 .UNSPECIFIED. ) ;
#43265=ORIENTED_EDGE ( 'NONE', *, *, #28155, .F. ) ;
#43275=EDGE_CURVE ( 'NONE', #45586, #199, #41647, .T. ) ;
#43277=ORIENTED_EDGE ( 'NONE', *, *, #25902, .F. ) ;
#43279=CARTESIAN_POINT ( 'NONE',  ( 0.6254311100348666219, 5.596225872411388913, 47.77988293940236275 ) ) ;
#43282=DIRECTION ( 'NONE',  ( 0.000000000000000000, 0.000000000000000000, 1.000000000000000000 ) ) ;
#43290=CARTESIAN_POINT ( 'NONE',  ( 4.549368137175248350, 0.000000000000000000, 0.000000000000000000 ) ) ;
#43295=CARTESIAN_POINT ( 'NONE',  ( 0.6028618097248863439, 18.24855319618746563, -44.51207924874658772 ) ) ;
#43302=( BOUNDED_SURFACE ( )  B_SPLINE_SURFACE ( 3, 1, ( 
 ( #31265, #50364 ),
 ( #7432, #26563 ),
 ( #46305, #4578 ),
 ( #18717, #52205 ) ),
 .UNSPECIFIED., .F., .F., .F. ) 
 B_SPLINE_SURFACE_WITH_KNOTS ( ( 4, 4 ),
 ( 2, 2 ),
 ( 0.000000000000000000, 1.000000000000000000 ),
 ( 0.000000000000000000, 1.000000000000000000 ),
 .UNSPECIFIED. ) 
 GEOMETRIC_REPRESENTATION_ITEM ( )  RATIONAL_B_SPLINE_SURFACE ( (
 ( 1.000000000000000000, 1.000000000000000000),
 ( 0.9751682680413298332, 0.9999560080971552356),
 ( 0.9751682680413298332, 0.9999560080971552356),
 ( 1.000000000000000000, 1.000000000000000000) ) ) 
 REPRESENTATION_ITEM ( '' )  SURFACE ( )  );
#43304=CARTESIAN_POINT ( 'NONE',  ( -5.995132425357893702, 14.94489030678151487, 11.47834865841101148 ) ) ;
#43306=FACE_OUTER_BOUND ( 'NONE', #46736, .T. ) ;
#43307=EDGE_CURVE ( 'NONE', #51963, #37474, #45592, .T. ) ;
#43310=CARTESIAN_POINT ( 'NONE',  ( 0.2885697896453101041, -22.25146201964169990, 36.93108635218660396 ) ) ;
#43311=CARTESIAN_POINT ( 'NONE',  ( 0.6009452777970413218, 48.10564074251961841, -0.4363873594207403617 ) ) ;
#43317=VECTOR ( 'NONE', #19431, 1000.000000000000114 ) ;
#43333=VERTEX_POINT ( 'NONE', #60579 ) ;
#43339=CARTESIAN_POINT ( 'NONE',  ( -6.016761891674565099, -13.32172022638582121, -13.32657647165369141 ) ) ;
#43340=CARTESIAN_POINT ( 'NONE',  ( 3.238931869106854045, -32.96367555688129869, 27.59912060131716416 ) ) ;
#43355=ORIENTED_EDGE ( 'NONE', *, *, #7617, .T. ) ;
#43356=CARTESIAN_POINT ( 'NONE',  ( 0.6030672727741701600, -12.53539249098747099, 46.44558360016990406 ) ) ;
#43359=CARTESIAN_POINT ( 'NONE',  ( 0.6001305935487422083, 6.798494447612207559, -47.62765676940936999 ) ) ;
#43360=VERTEX_POINT ( 'NONE', #60270 ) ;
#43371=DIRECTION ( 'NONE',  ( 1.000000000000000000, 0.000000000000000000, 0.000000000000000000 ) ) ;
#43372=FACE_OUTER_BOUND ( 'NONE', #37836, .T. ) ;
#43379=CARTESIAN_POINT ( 'NONE',  ( 0.6017667736363750963, -18.08696174077359586, -44.57803721604144442 ) ) ;
#43380=( BOUNDED_SURFACE ( )  B_SPLINE_SURFACE ( 3, 1, ( 
 ( #1383, #16433 ),
 ( #2314, #49023 ),
 ( #35561, #58702 ),
 ( #15827, #21441 ) ),
 .UNSPECIFIED., .F., .F., .F. ) 
 B_SPLINE_SURFACE_WITH_KNOTS ( ( 4, 4 ),
 ( 2, 2 ),
 ( 0.000000000000000000, 1.000000000000000000 ),
 ( 0.000000000000000000, 1.000000000000000000 ),
 .UNSPECIFIED. ) 
 GEOMETRIC_REPRESENTATION_ITEM ( )  RATIONAL_B_SPLINE_SURFACE ( (
 ( 1.000000000000000000, 1.000000000000000000),
 ( 0.7223157951917476005, 0.9931996967497186413),
 ( 0.7223157951917476005, 0.9931996967497186413),
 ( 1.000000000000000000, 1.000000000000000000) ) ) 
 REPRESENTATION_ITEM ( '' )  SURFACE ( )  );
#43382=EDGE_LOOP ( 'NONE', ( #53697, #10033, #1307, #7292 ) ) ;
#43385=CARTESIAN_POINT ( 'NONE',  ( 0.1095718737110178143, -34.05592812063363795, -26.45591486700744355 ) ) ;
#43387=CARTESIAN_POINT ( 'NONE',  ( -6.016761891674564211, -0.003433883959652091721, -18.84319130225482297 ) ) ;
#43388=CARTESIAN_POINT ( 'NONE',  ( 3.680882792899937694, -46.78529781139681631, -10.62117075007632039 ) ) ;
#43390=CARTESIAN_POINT ( 'NONE',  ( 0.6029303876144825880, -46.50193792184033015, 12.32464004947798664 ) ) ;
#43391=CARTESIAN_POINT ( 'NONE',  ( 0.5998501479064699549, 23.59887241503354716, -41.92175333043595487 ) ) ;
#43396=CARTESIAN_POINT ( 'NONE',  ( 0.6001305935487422083, -12.95698906763778879, -46.33281397023058901 ) ) ;
#43398=DIRECTION ( 'NONE',  ( 0.000000000000000000, 1.000000000000000000, 0.000000000000000000 ) ) ;
#43403=CARTESIAN_POINT ( 'NONE',  ( 0.1103878639767399000, 39.86034920885563082, 16.45816205842777791 ) ) ;
#43408=CARTESIAN_POINT ( 'NONE',  ( 0.2224561200757608492, -29.94832483818017366, -31.02237548791941890 ) ) ;
#43413=CARTESIAN_POINT ( 'NONE',  ( 0.3622758884714600280, 17.25816669464994746, -39.50828911766980411 ) ) ;
#43428=CARTESIAN_POINT ( 'NONE',  ( 0.2885700199627500018, 37.73587457854637250, 20.85752789928075046 ) ) ;
#43429=CARTESIAN_POINT ( 'NONE',  ( 0.6029303876144825880, 46.43417959025973829, 12.57751758557285982 ) ) ;
#43431=VECTOR ( 'NONE', #1123, 1000.000000000000000 ) ;
#43432=EDGE_LOOP ( 'NONE', ( #21750, #20906, #2916, #60691 ) ) ;
#43442=CARTESIAN_POINT ( 'NONE',  ( 0.6001305935487315502, -41.92422178329153581, -23.60027211631814481 ) ) ;
#43448=ORIENTED_EDGE ( 'NONE', *, *, #50949, .F. ) ;
#43452=DIRECTION ( 'NONE',  ( 0.000000000000000000, 0.000000000000000000, 1.000000000000000000 ) ) ;
#43462=DIRECTION ( 'NONE',  ( 0.000000000000000000, 0.000000000000000000, -1.000000000000000000 ) ) ;
#43463=DIRECTION ( 'NONE',  ( 0.000000000000000000, 0.000000000000000000, -1.000000000000000000 ) ) ;
#43464=CARTESIAN_POINT ( 'NONE',  ( 4.691466044806102076, 3.249105306918426805, -44.46979273209132089 ) ) ;
#43469=CARTESIAN_POINT ( 'NONE',  ( 0.1064266379913942212, -41.79703901861809356, -10.61815631313347552 ) ) ;
#43474=VERTEX_POINT ( 'NONE', #41830 ) ;
#43480=CARTESIAN_POINT ( 'NONE',  ( 4.549368137175248350, 24.02461520945271900, -35.57418903283089406 ) ) ;
#43482=( BOUNDED_SURFACE ( )  B_SPLINE_SURFACE ( 3, 1, ( 
 ( #24642, #28403 ),
 ( #4576, #10234 ),
 ( #10541, #29636 ),
 ( #61896, #23716 ) ),
 .UNSPECIFIED., .F., .F., .F. ) 
 B_SPLINE_SURFACE_WITH_KNOTS ( ( 4, 4 ),
 ( 2, 2 ),
 ( 0.000000000000000000, 1.000000000000000000 ),
 ( 0.000000000000000000, 1.000000000000000000 ),
 .UNSPECIFIED. ) 
 GEOMETRIC_REPRESENTATION_ITEM ( )  RATIONAL_B_SPLINE_SURFACE ( (
 ( 1.000000000000000000, 1.000000000000000000),
 ( 0.7223157951917476005, 0.9931996967497186413),
 ( 0.7223157951917476005, 0.9931996967497186413),
 ( 1.000000000000000000, 1.000000000000000000) ) ) 
 REPRESENTATION_ITEM ( '' )  SURFACE ( )  );
#43488=ORIENTED_EDGE ( 'NONE', *, *, #49263, .F. ) ;
#43492=ORIENTED_EDGE ( 'NONE', *, *, #9034, .F. ) ;
#43495=VERTEX_POINT ( 'NONE', #47433 ) ;
#43497=CARTESIAN_POINT ( 'NONE',  ( 0.6254087463353930065, -13.11428234126331205, -46.28445368454747211 ) ) ;
#43505=ORIENTED_EDGE ( 'NONE', *, *, #25097, .T. ) ;
#43510=VECTOR ( 'NONE', #58839, 1000.000000000000000 ) ;
#43511=ORIENTED_EDGE ( 'NONE', *, *, #15022, .T. ) ;
#43517=ORIENTED_EDGE ( 'NONE', *, *, #28670, .F. ) ;
#43530=ORIENTED_EDGE ( 'NONE', *, *, #25506, .F. ) ;
#43540=ORIENTED_EDGE ( 'NONE', *, *, #8152, .F. ) ;
#43541=FACE_OUTER_BOUND ( 'NONE', #7112, .T. ) ;
#43549=B_SPLINE_CURVE_WITH_KNOTS ( 'NONE', 3,
 ( #48306, #5663, #4737, #34839 ),
 .UNSPECIFIED., .F., .F.,
 ( 4, 4 ),
 ( 2.294131830766625192E-17, 0.004564976165746188579 ),
 .UNSPECIFIED. ) ;
#43554=CARTESIAN_POINT ( 'NONE',  ( -6.016761891674564211, -4.880293656734836283, -18.20023637398604066 ) ) ;
#43556=LINE ( 'NONE', #10961, #40780 ) ;
#43561=B_SPLINE_CURVE_WITH_KNOTS ( 'NONE', 3,
 ( #3664, #36298, #2745, #21877, #46620, #7124, #41928, #55364, #55058, #2436, #50369, #32205, #60678, #12185, #36922, #55671 ),
 .UNSPECIFIED., .F., .F.,
 ( 4, 3, 3, 3, 3, 4 ),
 ( 2.221635811791082109E-17, 0.0002618515315864433320, 0.0003927756766342010270, 0.0005236998216950543121, 0.0007855159896329938019, 0.001047349442285927870 ),
 .UNSPECIFIED. ) ;
#43564=CARTESIAN_POINT ( 'NONE',  ( 0.1073791018717483448, -16.95003405440287381, -39.65380858626208038 ) ) ;
#43572=ORIENTED_EDGE ( 'NONE', *, *, #59624, .F. ) ;
#43575=EDGE_CURVE ( 'NONE', #58937, #13269, #43936, .T. ) ;
#43583=CARTESIAN_POINT ( 'NONE',  ( 0.6027935024548037868, -38.27223087442867211, 29.14731236071003906 ) ) ;
#43585=VERTEX_POINT ( 'NONE', #29544 ) ;
#43590=DIRECTION ( 'NONE',  ( 0.1024043820194936449, 0.7971196296869256237, 0.5950744814819269868 ) ) ;
#43592=ORIENTED_EDGE ( 'NONE', *, *, #19048, .F. ) ;
#43595=VERTEX_POINT ( 'NONE', #24859 ) ;
#43606=CARTESIAN_POINT ( 'NONE',  ( 0.5988103622719985752, 13.03604477829290786, -46.30780754281420286 ) ) ;
#43608=ORIENTED_EDGE ( 'NONE', *, *, #34774, .F. ) ;
#43609=CARTESIAN_POINT ( 'NONE',  ( 0.6031356219577718170, 18.32926896140831019, -44.47888959008680132 ) ) ;
#43610=CARTESIAN_POINT ( 'NONE',  ( 2.301430502907645614, -46.71331171933241677, 11.18388433759636413 ) ) ;
#43622=EDGE_CURVE ( 'NONE', #35346, #4544, #48654, .T. ) ;
#43625=CARTESIAN_POINT ( 'NONE',  ( 0.7048096507298579061, -11.63498350884304244, -46.68221792389235958 ) ) ;
#43637=B_SPLINE_CURVE_WITH_KNOTS ( 'NONE', 3,
 ( #26825, #46882, #3608, #8019 ),
 .UNSPECIFIED., .F., .F.,
 ( 4, 4 ),
 ( 0.000000000000000000, 0.005014147105413705591 ),
 .UNSPECIFIED. ) ;
#43651=CARTESIAN_POINT ( 'NONE',  ( 0.6001305935487422083, -41.92422178329154292, -23.60027211631814126 ) ) ;
#43653=ADVANCED_FACE ( 'NONE', ( #1639 ), #2927, .F. ) ;
#43656=CARTESIAN_POINT ( 'NONE',  ( 0.6009452777970412107, -48.10564074251961131, 0.4363873594210762041 ) ) ;
#43660=CARTESIAN_POINT ( 'NONE',  ( 0.8760168074886965917, -29.98565522133375083, 37.61398439004481986 ) ) ;
#43661=VECTOR ( 'NONE', #28996, 1000.000000000000000 ) ;
#43671=CARTESIAN_POINT ( 'NONE',  ( -6.015611763856276717, 0.006214430185141332774, 18.84324252354755203 ) ) ;
#43672=( BOUNDED_SURFACE ( )  B_SPLINE_SURFACE ( 3, 1, ( 
 ( #15630, #6799 ),
 ( #6181, #1492 ),
 ( #48820, #48505 ),
 ( #1804, #35362 ) ),
 .UNSPECIFIED., .F., .F., .F. ) 
 B_SPLINE_SURFACE_WITH_KNOTS ( ( 4, 4 ),
 ( 2, 2 ),
 ( 0.000000000000000000, 1.000000000000000000 ),
 ( 0.000000000000000000, 1.000000000000000000 ),
 .UNSPECIFIED. ) 
 GEOMETRIC_REPRESENTATION_ITEM ( )  RATIONAL_B_SPLINE_SURFACE ( (
 ( 1.000000000000000000, 1.000000000000000000),
 ( 0.7223157951917480446, 0.9931996967497186413),
 ( 0.7223157951917480446, 0.9931996967497186413),
 ( 1.000000000000000000, 1.000000000000000000) ) ) 
 REPRESENTATION_ITEM ( '' )  SURFACE ( )  );
#43678=CARTESIAN_POINT ( 'NONE',  ( -6.016104459813371719, 18.19977249352317372, -4.882138007282559755 ) ) ;
#43685=CARTESIAN_POINT ( 'NONE',  ( 0.5980894510889457338, -19.05812566676475583, -44.17723055703945079 ) ) ;
#43690=B_SPLINE_CURVE_WITH_KNOTS ( 'NONE', 3,
 ( #28721, #53127, #47843, #24329 ),
 .UNSPECIFIED., .F., .F.,
 ( 4, 4 ),
 ( 2.410497451455474575E-17, 0.004564976165746185977 ),
 .UNSPECIFIED. ) ;
#43691=CARTESIAN_POINT ( 'NONE',  ( 1.827326673878742147, 31.30008222956382724, -29.55671596281176505 ) ) ;
#43692=CARTESIAN_POINT ( 'NONE',  ( 4.691466044806103852, -42.32811009116544909, -14.01607102724528353 ) ) ;
#43693=CARTESIAN_POINT ( 'NONE',  ( 0.6031356219577718170, -18.49057407199426706, -44.41207482560199793 ) ) ;
#43699=CARTESIAN_POINT ( 'NONE',  ( 0.7048096507298579061, 38.67623024744047910, -28.61383451045657722 ) ) ;
#43700=CARTESIAN_POINT ( 'NONE',  ( 0.8760168074887090262, -17.58183840866430003, 44.77533136581851636 ) ) ;
#43701=CARTESIAN_POINT ( 'NONE',  ( 0.6017666602106488405, -46.37677619531720552, 12.78804974226019553 ) ) ;
#43704=CARTESIAN_POINT ( 'NONE',  ( 4.549368137175248350, 0.000000000000000000, 0.000000000000000000 ) ) ;
#43709=CARTESIAN_POINT ( 'NONE',  ( 2.301430502907646058, 46.04685681264146524, 13.67112791032058361 ) ) ;
#43714=VECTOR ( 'NONE', #41108, 999.9999999999998863 ) ;
#43720=CARTESIAN_POINT ( 'NONE',  ( 2.301529144917013436, -33.04216096093427524, 34.86298839095273649 ) ) ;
#43724=ORIENTED_EDGE ( 'NONE', *, *, #27825, .F. ) ;
#43734=EDGE_CURVE ( 'NONE', #34317, #23714, #26648, .T. ) ;
#43740=CARTESIAN_POINT ( 'NONE',  ( -2.708315649062910779, -3.532515819624256537, -14.20182604343558985 ) ) ;
#43743=CARTESIAN_POINT ( 'NONE',  ( 4.975801465491695552, 21.70134120755140827, 42.71626295676271212 ) ) ;
#43746=CARTESIAN_POINT ( 'NONE',  ( 0.5980894510889448457, -23.44630161211557606, -42.01322166096910848 ) ) ;
#43750=CARTESIAN_POINT ( 'NONE',  ( 0.6041374136657475802, -44.37863742124655175, -18.57118264377523076 ) ) ;
#43753=ORIENTED_EDGE ( 'NONE', *, *, #41759, .T. ) ;
#43756=VERTEX_POINT ( 'NONE', #6954 ) ;
#43763=CARTESIAN_POINT ( 'NONE',  ( -6.017396004339686577, -4.875835690939308797, 18.20140164570667807 ) ) ;
#43765=CARTESIAN_POINT ( 'NONE',  ( 0.6017666602106490625, -47.64919188470832978, 6.625262199740270752 ) ) ;
#43766=EDGE_CURVE ( 'NONE', #61780, #33708, #31409, .T. ) ;
#43784=B_SPLINE_CURVE_WITH_KNOTS ( 'NONE', 3,
 ( #30086, #6558, #25083, #11004 ),
 .UNSPECIFIED., .F., .F.,
 ( 4, 4 ),
 ( 0.000000000000000000, 0.004445488388166991649 ),
 .UNSPECIFIED. ) ;
#43785=CARTESIAN_POINT ( 'NONE',  ( -6.016489644550737204, -17.40716454747924047, -7.215050741358225217 ) ) ;
#43788=CARTESIAN_POINT ( 'NONE',  ( 0.8751705887134423323, 17.57879340691479797, 44.76769609654243709 ) ) ;
#43792=CARTESIAN_POINT ( 'NONE',  ( 0.2885697896453109368, -25.60460893337453214, -34.69058521462526556 ) ) ;
#43794=VERTEX_POINT ( 'NONE', #25778 ) ;
#43797=CARTESIAN_POINT ( 'NONE',  ( 0.7048096507298635682, 0.8437160066900629696, 48.10291524268443197 ) ) ;
#43798=CARTESIAN_POINT ( 'NONE',  ( 0.1101816497532063233, 16.62841624476621050, 39.78963561881071342 ) ) ;
#43801=CARTESIAN_POINT ( 'NONE',  ( 0.7245667037590752813, 11.65533952568352483, -46.66865388241075152 ) ) ;
#43803=AXIS2_PLACEMENT_3D ( 'NONE', #54011, #21445, #11134 ) ;
#43818=FACE_OUTER_BOUND ( 'NONE', #8593, .T. ) ;
#43820=FACE_OUTER_BOUND ( 'NONE', #23371, .T. ) ;
#43827=CARTESIAN_POINT ( 'NONE',  ( 0.6017666602106490625, -0.3491145841135456229, -48.10631669010027878 ) ) ;
#43837=ORIENTED_EDGE ( 'NONE', *, *, #30725, .F. ) ;
#43838=CARTESIAN_POINT ( 'NONE',  ( 4.549368137175248350, 28.46244473166628097, 32.13400537129935230 ) ) ;
#43844=CARTESIAN_POINT ( 'NONE',  ( 4.691466044806102076, 43.79545162262309077, -8.371234562541387092 ) ) ;
#43851=ORIENTED_EDGE ( 'NONE', *, *, #33615, .F. ) ;
#43853=CARTESIAN_POINT ( 'NONE',  ( 0.6029303876144825880, 12.32464004947814651, 46.50193792184029462 ) ) ;
#43861=CARTESIAN_POINT ( 'NONE',  ( 4.549368137175248350, 23.67244292351589507, 35.80950303116109268 ) ) ;
#43863=( BOUNDED_SURFACE ( )  B_SPLINE_SURFACE ( 3, 1, ( 
 ( #23999, #163 ),
 ( #9580, #47819 ),
 ( #48121, #4867 ),
 ( #53411, #4248 ) ),
 .UNSPECIFIED., .F., .F., .F. ) 
 B_SPLINE_SURFACE_WITH_KNOTS ( ( 4, 4 ),
 ( 2, 2 ),
 ( 0.000000000000000000, 1.000000000000000000 ),
 ( 0.000000000000000000, 1.000000000000000000 ),
 .UNSPECIFIED. ) 
 GEOMETRIC_REPRESENTATION_ITEM ( )  RATIONAL_B_SPLINE_SURFACE ( (
 ( 1.000000000000000000, 1.000000000000000000),
 ( 0.9751682680413298332, 0.9999560080971552356),
 ( 0.9751682680413298332, 0.9999560080971552356),
 ( 1.000000000000000000, 1.000000000000000000) ) ) 
 REPRESENTATION_ITEM ( '' )  SURFACE ( )  );
#43871=VERTEX_POINT ( 'NONE', #18543 ) ;
#43879=DIRECTION ( 'NONE',  ( 0.000000000000000000, 0.000000000000000000, 1.000000000000000000 ) ) ;
#43880=LINE ( 'NONE', #34768, #5892 ) ;
#43892=VERTEX_POINT ( 'NONE', #3494 ) ;
#43897=CARTESIAN_POINT ( 'NONE',  ( 0.8751705887134423323, -28.56654290188627243, -38.69254731947824411 ) ) ;
#43901=CARTESIAN_POINT ( 'NONE',  ( 0.3622758884714730732, -41.42293301073634382, 11.95365414648425428 ) ) ;
#43908=B_SPLINE_CURVE_WITH_KNOTS ( 'NONE', 3,
 ( #11166, #57502, #14641, #9934 ),
 .UNSPECIFIED., .F., .F.,
 ( 4, 4 ),
 ( 0.000000000000000000, 0.004445488388166994251 ),
 .UNSPECIFIED. ) ;
#43911=CARTESIAN_POINT ( 'NONE',  ( 4.833616638992205949, 38.20222678111901615, 26.07076047129148932 ) ) ;
#43915=CARTESIAN_POINT ( 'NONE',  ( 0.5988103622719992414, -13.03604477829323116, 46.30780754281411049 ) ) ;
#43916=ORIENTED_EDGE ( 'NONE', *, *, #61302, .F. ) ;
#43936=CIRCLE ( 'NONE', #12889, 42.92674063221959813 ) ;
#43939=EDGE_CURVE ( 'NONE', #4, #3487, #23527, .T. ) ;
#43940=CARTESIAN_POINT ( 'NONE',  ( -6.015611763856276717, -16.31561949997082905, 9.427003116184113907 ) ) ;
#43941=LINE ( 'NONE', #52670, #39154 ) ;
#43944=EDGE_CURVE ( 'NONE', #31565, #44340, #40773, .T. ) ;
#43950=CIRCLE ( 'NONE', #50245, 42.92674063221959813 ) ;
#43954=ORIENTED_EDGE ( 'NONE', *, *, #60314, .F. ) ;
#43958=ORIENTED_EDGE ( 'NONE', *, *, #50062, .F. ) ;
#43962=CARTESIAN_POINT ( 'NONE',  ( 0.8751705887134553219, -17.57879340691572878, 44.76769609654206050 ) ) ;
#43963=EDGE_CURVE ( 'NONE', #49963, #11438, #52655, .T. ) ;
#43969=CARTESIAN_POINT ( 'NONE',  ( 4.549368137175248350, 0.000000000000000000, 0.000000000000000000 ) ) ;
#43973=EDGE_CURVE ( 'NONE', #28832, #14276, #10957, .T. ) ;
#43974=( BOUNDED_SURFACE ( )  B_SPLINE_SURFACE ( 3, 1, ( 
 ( #42396, #14196 ),
 ( #13265, #18573 ),
 ( #32995, #32677 ),
 ( #51759, #9161 ) ),
 .UNSPECIFIED., .F., .F., .F. ) 
 B_SPLINE_SURFACE_WITH_KNOTS ( ( 4, 4 ),
 ( 2, 2 ),
 ( 0.000000000000000000, 1.000000000000000000 ),
 ( 0.000000000000000000, 1.000000000000000000 ),
 .UNSPECIFIED. ) 
 GEOMETRIC_REPRESENTATION_ITEM ( )  RATIONAL_B_SPLINE_SURFACE ( (
 ( 1.000000000000000000, 1.000000000000000000),
 ( 0.7223157951917476005, 0.9931996967497186413),
 ( 0.7223157951917476005, 0.9931996967497186413),
 ( 1.000000000000000000, 1.000000000000000000) ) ) 
 REPRESENTATION_ITEM ( '' )  SURFACE ( )  );
#43975=FACE_OUTER_BOUND ( 'NONE', #2375, .T. ) ;
#43977=ORIENTED_EDGE ( 'NONE', *, *, #43234, .T. ) ;
#43996=AXIS2_PLACEMENT_3D ( 'NONE', #57810, #52819, #57187 ) ;
#43999=DIRECTION ( 'NONE',  ( -1.000000000000000000, -0.000000000000000000, -0.000000000000000000 ) ) ;
#44002=LINE ( 'NONE', #39914, #36818 ) ;
#44009=CARTESIAN_POINT ( 'NONE',  ( 0.1081432562775997280, 30.79166192943845104, -30.19275717928091396 ) ) ;
#44014=EDGE_CURVE ( 'NONE', #16034, #37474, #12351, .T. ) ;
#44016=CARTESIAN_POINT ( 'NONE',  ( -6.016489644550736315, -14.94663725562923773, 11.47450955518482374 ) ) ;
#44020=FACE_OUTER_BOUND ( 'NONE', #37192, .T. ) ;
#44024=ADVANCED_FACE ( 'NONE', ( #57341 ), #44153, .F. ) ;
#44033=ADVANCED_FACE ( 'NONE', ( #45158 ), #9706, .F. ) ;
#44040=VERTEX_POINT ( 'NONE', #30393 ) ;
#44041=ORIENTED_EDGE ( 'NONE', *, *, #12060, .F. ) ;
#44043=CARTESIAN_POINT ( 'NONE',  ( 0.6031356755773454870, -24.05374386753687688, -41.66225520948395911 ) ) ;
#44047=DIRECTION ( 'NONE',  ( -1.000000000000000000, -0.000000000000000000, -0.000000000000000000 ) ) ;
#44049=CARTESIAN_POINT ( 'NONE',  ( 0.8751705887134423323, -41.19904111682490822, -24.81530984069193480 ) ) ;
#44054=EDGE_LOOP ( 'NONE', ( #19092, #21697, #59420, #56261 ) ) ;
#44060=CARTESIAN_POINT ( 'NONE',  ( -6.001507490154110336, -13.31361390284169133, 13.33564355450103633 ) ) ;
#44070=ORIENTED_EDGE ( 'NONE', *, *, #37941, .F. ) ;
#44073=CARTESIAN_POINT ( 'NONE',  ( 4.691466044806102076, -37.25818859570323838, 24.49380602310747790 ) ) ;
#44083=CARTESIAN_POINT ( 'NONE',  ( 0.1313383488274169619, -21.00709374781567362, 37.66088038379808722 ) ) ;
#44084=CARTESIAN_POINT ( 'NONE',  ( 4.833616638992208614, 20.04871863793809439, -41.67905425467686342 ) ) ;
#44085=ORIENTED_EDGE ( 'NONE', *, *, #52302, .T. ) ;
#44089=AXIS2_PLACEMENT_3D ( 'NONE', #978, #25405, #34515 ) ;
#44092=CARTESIAN_POINT ( 'NONE',  ( -2.708315649062910779, -13.41752550814506861, -5.842990691604553533 ) ) ;
#44095=CARTESIAN_POINT ( 'NONE',  ( 0.6001305935487315502, 44.64600790884030346, 17.92615948558555772 ) ) ;
#44100=CARTESIAN_POINT ( 'NONE',  ( 0.7245667037590769466, 46.66865388241069468, 11.65533952568368647 ) ) ;
#44113=CARTESIAN_POINT ( 'NONE',  ( 0.6254087463353920073, 11.78492518233810493, -46.64065386173403738 ) ) ;
#44114=VERTEX_POINT ( 'NONE', #26022 ) ;
#44120=ORIENTED_EDGE ( 'NONE', *, *, #30259, .F. ) ;
#44121=ADVANCED_FACE ( 'NONE', ( #59206 ), #37358, .F. ) ;
#44123=CARTESIAN_POINT ( 'NONE',  ( 0.1103872315293168843, -0.02583155086994256763, 43.12442619660166088 ) ) ;
#44125=ORIENTED_EDGE ( 'NONE', *, *, #53041, .T. ) ;
#44131=CARTESIAN_POINT ( 'NONE',  ( 0.6025881611877910160, 33.86250327239848446, 34.17105830828427315 ) ) ;
#44145=VERTEX_POINT ( 'NONE', #39845 ) ;
#44153=( BOUNDED_SURFACE ( )  B_SPLINE_SURFACE ( 3, 1, ( 
 ( #14473, #5034 ),
 ( #24159, #332 ),
 ( #55431, #7825 ),
 ( #30709, #59515 ) ),
 .UNSPECIFIED., .F., .F., .F. ) 
 B_SPLINE_SURFACE_WITH_KNOTS ( ( 4, 4 ),
 ( 2, 2 ),
 ( 0.000000000000000000, 1.000000000000000000 ),
 ( 0.000000000000000000, 1.000000000000000000 ),
 .UNSPECIFIED. ) 
 GEOMETRIC_REPRESENTATION_ITEM ( )  RATIONAL_B_SPLINE_SURFACE ( (
 ( 1.000000000000000000, 1.000000000000000000),
 ( 0.9953040768229013402, 0.8617119497784988535),
 ( 0.9953040768229013402, 0.8617119497784988535),
 ( 1.000000000000000000, 1.000000000000000000) ) ) 
 REPRESENTATION_ITEM ( '' )  SURFACE ( )  );
#44154=B_SPLINE_CURVE_WITH_KNOTS ( 'NONE', 3,
 ( #13367, #60957, #4543, #37817, #23679, #14299 ),
 .UNSPECIFIED., .F., .F.,
 ( 4, 2, 4 ),
 ( 1.274743298368305687E-16, 0.0002450741128632359200, 0.0004901482257263444463 ),
 .UNSPECIFIED. ) ;
#44164=ORIENTED_EDGE ( 'NONE', *, *, #21708, .F. ) ;
#44166=ORIENTED_EDGE ( 'NONE', *, *, #43939, .F. ) ;
#44167=CARTESIAN_POINT ( 'NONE',  ( 0.6027935024548037868, 12.28245664247781477, 46.51312430684509991 ) ) ;
#44170=CARTESIAN_POINT ( 'NONE',  ( 4.691466044806103852, -20.01963481131631539, -39.84135254923129565 ) ) ;
#44171=CARTESIAN_POINT ( 'NONE',  ( 0.8751705887134553219, 44.08562551107081617, -19.22545746485614870 ) ) ;
#44182=CARTESIAN_POINT ( 'NONE',  ( 0.6001305935487315502, 47.76436356026967900, -5.760103278697520146 ) ) ;
#44186=CARTESIAN_POINT ( 'NONE',  ( 4.549368137175248350, 3.018832571115968033, 42.82045902618773425 ) ) ;
#44204=CARTESIAN_POINT ( 'NONE',  ( 4.833616638992205949, 30.15290813935854430, 35.06988470649578460 ) ) ;
#44215=CARTESIAN_POINT ( 'NONE',  ( 0.6025881611877910160, 23.86454577211506844, 41.77096849334458284 ) ) ;
#44218=CARTESIAN_POINT ( 'NONE',  ( 0.6041374136657476912, -46.51335992032610278, -12.28249295042029132 ) ) ;
#44220=ORIENTED_EDGE ( 'NONE', *, *, #21576, .F. ) ;
#44223=B_SPLINE_CURVE_WITH_KNOTS ( 'NONE', 3,
 ( #17119, #2995, #6433, #45331, #35926, #16814, #54366, #55300, #2059, #35003, #12123, #31201, #49688, #50605, #30889, #21190, #41245, #11488, #12421 ),
 .UNSPECIFIED., .F., .F.,
 ( 4, 3, 3, 3, 3, 3, 4 ),
 ( 1.161276725443423652E-16, 0.0002618519381806254831, 0.0003927759815485982521, 0.0005237000248299445142, 0.0006546240681324981504, 0.0007855481115631305408, 0.0009699050456655098577 ),
 .UNSPECIFIED. ) ;
#44225=CARTESIAN_POINT ( 'NONE',  ( 3.680882792899937250, -8.091276083385070095, -47.28852514876952995 ) ) ;
#44233=CARTESIAN_POINT ( 'NONE',  ( 0.6030672727741701600, 18.49051564326133601, -44.41203814406388517 ) ) ;
#44243=CARTESIAN_POINT ( 'NONE',  ( 3.680974057930772592, -16.63696281867829185, -44.99871514631785629 ) ) ;
#44261=ORIENTED_EDGE ( 'NONE', *, *, #34378, .F. ) ;
#44263=FACE_OUTER_BOUND ( 'NONE', #60889, .T. ) ;
#44267=ORIENTED_EDGE ( 'NONE', *, *, #49804, .F. ) ;
#44270=DIRECTION ( 'NONE',  ( 0.000000000000000000, 0.000000000000000000, 1.000000000000000000 ) ) ;
#44280=CARTESIAN_POINT ( 'NONE',  ( 0.1092565886968784594, -30.27341312544135477, 30.71235995742688374 ) ) ;
#44283=VERTEX_POINT ( 'NONE', #54692 ) ;
#44284=CARTESIAN_POINT ( 'NONE',  ( 0.6009453534118439633, -12.87216801774577668, 46.35353704332089819 ) ) ;
#44286=CARTESIAN_POINT ( 'NONE',  ( 4.833616638992205949, -3.476827473558217640, 46.11947910922901883 ) ) ;
#44290=CARTESIAN_POINT ( 'NONE',  ( 3.680882792899939027, 30.65151321162949571, 36.90742604464134757 ) ) ;
#44304=CARTESIAN_POINT ( 'NONE',  ( 0.1098349054025746369, 34.34238705454303897, -26.08296594991503881 ) ) ;
#44311=CARTESIAN_POINT ( 'NONE',  ( 0.6009453534118440743, -18.00606795643245306, -44.61081284455525520 ) ) ;
#44318=CARTESIAN_POINT ( 'NONE',  ( 0.5988103622719992414, -44.21009254328991744, -18.96890139669977771 ) ) ;
#44323=CARTESIAN_POINT ( 'NONE',  ( 0.7246131072078555446, -47.57651137777910577, -7.091231226024629741 ) ) ;
#44336=CARTESIAN_POINT ( 'NONE',  ( 0.1095718737110178698, -37.47471772507234533, 21.33933464366355537 ) ) ;
#44337=VECTOR ( 'NONE', #13983, 1000.000000000000114 ) ;
#44340=VERTEX_POINT ( 'NONE', #60318 ) ;
#44342=CARTESIAN_POINT ( 'NONE',  ( 0.6001305935487422083, 46.60388846085722037, -11.94532529598331649 ) ) ;
#44348=B_SPLINE_CURVE_WITH_KNOTS ( 'NONE', 3,
 ( #58586, #44243, #6263, #977 ),
 .UNSPECIFIED., .F., .F.,
 ( 4, 4 ),
 ( 0.000000000000000000, 0.004445488388166994251 ),
 .UNSPECIFIED. ) ;
#44355=ORIENTED_EDGE ( 'NONE', *, *, #8804, .T. ) ;
#44357=CARTESIAN_POINT ( 'NONE',  ( 0.1064266379913942628, 37.62465837278045200, 21.07422113734176961 ) ) ;
#44370=EDGE_CURVE ( 'NONE', #26859, #9792, #36323, .T. ) ;
#44372=CARTESIAN_POINT ( 'NONE',  ( 0.5988103564986355654, 48.10388392110854738, -0.6065102550368329792 ) ) ;
#44373=CARTESIAN_POINT ( 'NONE',  ( 0.8760168074887076939, -42.09738177923939162, -23.27577685234582816 ) ) ;
#44374=EDGE_CURVE ( 'NONE', #52485, #9403, #47512, .T. ) ;
#44379=CARTESIAN_POINT ( 'NONE',  ( 0.6023143664670691511, -47.72938193173976629, 6.019611522082517041 ) ) ;
#44380=CARTESIAN_POINT ( 'NONE',  ( 4.549368137175248350, 2.596185425821331272, 42.84816078363931524 ) ) ;
#44387=CARTESIAN_POINT ( 'NONE',  ( 1.827326673878744145, -9.946825761454215709, -41.88502433275000669 ) ) ;
#44388=ORIENTED_EDGE ( 'NONE', *, *, #26726, .T. ) ;
#44394=CARTESIAN_POINT ( 'NONE',  ( 0.5988103622719990193, -0.6065097949916992137, 48.10388392585941375 ) ) ;
#44395=DIRECTION ( 'NONE',  ( 1.000000000000000000, 0.000000000000000000, 0.000000000000000000 ) ) ;
#44406=ORIENTED_EDGE ( 'NONE', *, *, #28719, .T. ) ;
#44410=CARTESIAN_POINT ( 'NONE',  ( 0.1104177457020373149, 16.50753524010242401, 39.83992599038892024 ) ) ;
#44419=ORIENTED_EDGE ( 'NONE', *, *, #60668, .T. ) ;
#44421=CARTESIAN_POINT ( 'NONE',  ( 0.1092565886968784733, -39.95965440403635682, -16.21587544131310210 ) ) ;
#44423=VERTEX_POINT ( 'NONE', #20586 ) ;
#44426=CARTESIAN_POINT ( 'NONE',  ( 0.1064266379913939020, 37.06314005629914021, -22.04679939086795670 ) ) ;
#44438=B_SPLINE_CURVE_WITH_KNOTS ( 'NONE', 3,
 ( #50057, #27476, #55659, #32187 ),
 .UNSPECIFIED., .F., .F.,
 ( 4, 4 ),
 ( 0.000000000000000000, 0.005014147105413710795 ),
 .UNSPECIFIED. ) ;
#44439=VECTOR ( 'NONE', #3707, 1000.000000000000114 ) ;
#44440=ORIENTED_EDGE ( 'NONE', *, *, #700, .T. ) ;
#44447=ORIENTED_EDGE ( 'NONE', *, *, #23142, .F. ) ;
#44452=ORIENTED_EDGE ( 'NONE', *, *, #59609, .T. ) ;
#44456=CARTESIAN_POINT ( 'NONE',  ( 0.8760168074887090262, 38.69913431881784049, 28.57146030081993970 ) ) ;
#44460=CARTESIAN_POINT ( 'NONE',  ( 0.8760168074886965917, 5.394043284318857268, 47.80016357497251533 ) ) ;
#44463=CARTESIAN_POINT ( 'NONE',  ( 0.1102144999581332885, 30.40435207217186075, 30.58258619461932071 ) ) ;
#44468=VERTEX_POINT ( 'NONE', #20891 ) ;
#44471=CARTESIAN_POINT ( 'NONE',  ( 4.549368137175248350, 0.000000000000000000, 0.000000000000000000 ) ) ;
#44472=CIRCLE ( 'NONE', #11437, 47.91270532121795611 ) ;
#44474=CARTESIAN_POINT ( 'NONE',  ( 3.680974057930775700, -20.05478739720764025, 43.58300585207889100 ) ) ;
#44485=EDGE_CURVE ( 'NONE', #4004, #5670, #7900, .T. ) ;
#44489=CARTESIAN_POINT ( 'NONE',  ( 0.6001305935487422083, 11.94532529598315129, 46.60388846085726300 ) ) ;
#44495=DIRECTION ( 'NONE',  ( -0.1024043820194934368, 0.9878630899050878655, -0.1167898032637170735 ) ) ;
#44500=ORIENTED_EDGE ( 'NONE', *, *, #20106, .F. ) ;
#44504=CARTESIAN_POINT ( 'NONE',  ( 0.8751705887134423323, -46.67919521768896374, 11.58504748649118810 ) ) ;
#44507=CARTESIAN_POINT ( 'NONE',  ( 0.5998501479064708430, -28.86886762351098312, -38.48283596222019298 ) ) ;
#44509=ORIENTED_EDGE ( 'NONE', *, *, #29289, .T. ) ;
#44510=VERTEX_POINT ( 'NONE', #46256 ) ;
#44512=EDGE_CURVE ( 'NONE', #46085, #26923, #43637, .T. ) ;
#44516=EDGE_CURVE ( 'NONE', #58767, #50035, #25751, .T. ) ;
#44520=B_SPLINE_CURVE_WITH_KNOTS ( 'NONE', 3,
 ( #10200, #34022, #13994, #28070 ),
 .UNSPECIFIED., .F., .F.,
 ( 4, 4 ),
 ( 0.000000000000000000, 0.004445488388166992516 ),
 .UNSPECIFIED. ) ;
#44522=CARTESIAN_POINT ( 'NONE',  ( 0.6029303876144825880, 23.94027529185494885, 41.72757124235830162 ) ) ;
#44524=ORIENTED_EDGE ( 'NONE', *, *, #11230, .T. ) ;
#44531=ORIENTED_EDGE ( 'NONE', *, *, #23837, .F. ) ;
#44532=CARTESIAN_POINT ( 'NONE',  ( -6.015611763856276717, 13.32857883366833462, 13.31979030221804017 ) ) ;
#44535=CARTESIAN_POINT ( 'NONE',  ( 0.7048096507298579061, 13.26491767067515504, -46.24547838151354995 ) ) ;
#44542=EDGE_CURVE ( 'NONE', #50113, #31710, #13055, .T. ) ;
#44543=FACE_OUTER_BOUND ( 'NONE', #2641, .T. ) ;
#44549=CARTESIAN_POINT ( 'NONE',  ( 0.1313383488274121325, 6.260443365526796811, 42.66669366003524999 ) ) ;
#44552=CARTESIAN_POINT ( 'NONE',  ( 0.7954190325252782356, 47.56618055754175600, -7.138712176114947461 ) ) ;
#44554=FACE_OUTER_BOUND ( 'NONE', #21413, .T. ) ;
#44559=CARTESIAN_POINT ( 'NONE',  ( 0.3622758884714600280, -41.42293301073617329, -11.95365414648482627 ) ) ;
#44563=CARTESIAN_POINT ( 'NONE',  ( 3.238741278300274029, 38.98370040185400143, 18.12697907494908378 ) ) ;
#44566=VERTEX_POINT ( 'NONE', #56240 ) ;
#44571=EDGE_LOOP ( 'NONE', ( #2612, #36967, #27469, #54785 ) ) ;
#44572=ORIENTED_EDGE ( 'NONE', *, *, #34255, .T. ) ;
#44580=CARTESIAN_POINT ( 'NONE',  ( 0.7048096507298635682, -5.442192462019818322, 47.80151517212777890 ) ) ;
#44583=CARTESIAN_POINT ( 'NONE',  ( 0.6029303876144825880, -18.53079182983373130, 44.39523326884606291 ) ) ;
#44584=CARTESIAN_POINT ( 'NONE',  ( -6.015611763856276717, -17.40650793417838571, -7.216738110653465377 ) ) ;
#44592=CARTESIAN_POINT ( 'NONE',  ( 0.8760168074887090262, 42.09738177923922819, 23.27577685234613014 ) ) ;
#44604=CARTESIAN_POINT ( 'NONE',  ( 0.1103310638050661735, -39.87325896099753919, 16.42686748615336256 ) ) ;
#44609=CARTESIAN_POINT ( 'NONE',  ( 0.8751705887134423323, 28.56654290188602019, 38.69254731947842885 ) ) ;
#44611=DIRECTION ( 'NONE',  ( 1.000000000000000000, 0.000000000000000000, 0.000000000000000000 ) ) ;
#44612=CARTESIAN_POINT ( 'NONE',  ( 0.6027935024548037868, -6.452291758825078105, 47.67281620606621573 ) ) ;
#44613=CARTESIAN_POINT ( 'NONE',  ( 3.680882792899938138, 36.90742604464125520, -30.65151321162960940 ) ) ;
#44619=CARTESIAN_POINT ( 'NONE',  ( 0.3622758884714600280, -43.10531414739104861, -0.8252992914326565677 ) ) ;
#44620=CARTESIAN_POINT ( 'NONE',  ( 0.1100053167205930632, -0.1794603581041471496, -43.12409768020066281 ) ) ;
#44626=CARTESIAN_POINT ( 'NONE',  ( 0.1310142868023714269, -37.66054729763607867, 21.00772081177013462 ) ) ;
#44632=CARTESIAN_POINT ( 'NONE',  ( 0.1103744047535531458, -11.19884698423395797, 41.64495780681018999 ) ) ;
#44634=CARTESIAN_POINT ( 'NONE',  ( 0.1092565886968784872, -37.19081526480840694, 21.83052579204398214 ) ) ;
#44641=CARTESIAN_POINT ( 'NONE',  ( 0.6001305935487315502, -6.798494447611894920, -47.62765676940940551 ) ) ;
#44643=VERTEX_POINT ( 'NONE', #9249 ) ;
#44645=CARTESIAN_POINT ( 'NONE',  ( 1.827119703190778877, -41.24693285842936774, 12.32825544177764954 ) ) ;
#44648=ORIENTED_EDGE ( 'NONE', *, *, #47368, .T. ) ;
#44666=EDGE_LOOP ( 'NONE', ( #41081, #60011, #56574, #58314 ) ) ;
#44670=CARTESIAN_POINT ( 'NONE',  ( 3.238741278300276694, 24.69738534405263763, 35.19027457370187051 ) ) ;
#44676=B_SPLINE_CURVE_WITH_KNOTS ( 'NONE', 3,
 ( #2719, #50339, #36574, #7408, #60649, #8046 ),
 .UNSPECIFIED., .F., .F.,
 ( 4, 2, 4 ),
 ( 0.000000000000000000, 0.0002450742804987306525, 0.0004901485609974613050 ),
 .UNSPECIFIED. ) ;
#44679=CARTESIAN_POINT ( 'NONE',  ( 0.6009453534118439633, -41.87889766923471768, 23.67490308139332456 ) ) ;
#44682=CARTESIAN_POINT ( 'NONE',  ( 0.1103878639767399555, -41.66755962011272629, -11.11454059769185854 ) ) ;
#44687=ORIENTED_EDGE ( 'NONE', *, *, #39147, .F. ) ;
#44690=CARTESIAN_POINT ( 'NONE',  ( 0.7954196712028469562, -0.8690072546828989664, 48.09103417491924404 ) ) ;
#44691=CARTESIAN_POINT ( 'NONE',  ( 0.8760168074887090262, -11.58706983520358769, 46.68716261866156003 ) ) ;
#44693=CARTESIAN_POINT ( 'NONE',  ( 3.238931869106853600, -38.98364358950757946, 18.12707634097755260 ) ) ;
#44700=VECTOR ( 'NONE', #24252, 1000.000000000000000 ) ;
#44701=CARTESIAN_POINT ( 'NONE',  ( 4.975801465491695552, -31.15993731089151808, 36.39623109580413285 ) ) ;
#44706=CARTESIAN_POINT ( 'NONE',  ( 0.8751705887134423323, 0.8911681664088411114, -48.08707113907595243 ) ) ;
#44711=CARTESIAN_POINT ( 'NONE',  ( -6.016104459813371719, -16.31603998697576685, 9.426230926598584858 ) ) ;
#44719=CARTESIAN_POINT ( 'NONE',  ( 0.1100053167205930216, -11.33468317718527096, -41.60823192620004107 ) ) ;
#44721=ORIENTED_EDGE ( 'NONE', *, *, #55849, .T. ) ;
#44723=CARTESIAN_POINT ( 'NONE',  ( 0.5988103564986356764, -11.86435738293476128, 46.62176022926367835 ) ) ;
#44732=ORIENTED_EDGE ( 'NONE', *, *, #45503, .T. ) ;
#44740=CARTESIAN_POINT ( 'NONE',  ( 4.833616638992208614, 8.578242093415751057, -45.44786513329589894 ) ) ;
#44742=ORIENTED_EDGE ( 'NONE', *, *, #24738, .F. ) ;
#44743=EDGE_CURVE ( 'NONE', #43892, #5799, #30173, .T. ) ;
#44744=ORIENTED_EDGE ( 'NONE', *, *, #27977, .F. ) ;
#44763=CARTESIAN_POINT ( 'NONE',  ( 0.1102847568649952675, -5.720244683738307856, -42.74337176234127611 ) ) ;
#44768=CARTESIAN_POINT ( 'NONE',  ( 0.8751705887134423323, -46.67919521768896374, 11.58504748649118810 ) ) ;
#44769=ORIENTED_EDGE ( 'NONE', *, *, #33550, .F. ) ;
#44770=CARTESIAN_POINT ( 'NONE',  ( 0.6001305935487315502, -28.87057754790910735, -38.48510059944037920 ) ) ;
#44780=CARTESIAN_POINT ( 'NONE',  ( 0.5980894510889457338, -46.28687279963700973, 13.12879507229208009 ) ) ;
#44781=CIRCLE ( 'NONE', #58716, 42.92674063221959813 ) ;
#44797=EDGE_CURVE ( 'NONE', #41488, #35221, #41423, .T. ) ;
#44798=CARTESIAN_POINT ( 'NONE',  ( 0.1103878639767399555, 43.12442673975421314, -0.04853618198075116547 ) ) ;
#44802=ADVANCED_FACE ( 'NONE', ( #4367 ), #59276, .F. ) ;
#44803=ORIENTED_EDGE ( 'NONE', *, *, #14169, .T. ) ;
#44804=B_SPLINE_CURVE_WITH_KNOTS ( 'NONE', 3,
 ( #3101, #16926, #3400, #22539 ),
 .UNSPECIFIED., .F., .F.,
 ( 4, 4 ),
 ( 0.000000000000000000, 0.005014147105413706458 ),
 .UNSPECIFIED. ) ;
#44811=CARTESIAN_POINT ( 'NONE',  ( 0.3622758884714600280, 41.42293301073608802, 11.95365414648511582 ) ) ;
#44824=ORIENTED_EDGE ( 'NONE', *, *, #4918, .T. ) ;
#44832=ORIENTED_EDGE ( 'NONE', *, *, #59974, .T. ) ;
#44835=ORIENTED_EDGE ( 'NONE', *, *, #17678, .T. ) ;
#44838=LINE ( 'NONE', #21313, #1493 ) ;
#44842=CARTESIAN_POINT ( 'NONE',  ( -6.015611763856276717, -4.870987357968304288, 18.20278301740935234 ) ) ;
#44843=FACE_OUTER_BOUND ( 'NONE', #26907, .T. ) ;
#44845=CARTESIAN_POINT ( 'NONE',  ( 4.975801465491694664, -15.94009207553080643, 45.18341283946430309 ) ) ;
#44847=EDGE_LOOP ( 'NONE', ( #33923, #43517, #9071, #2085 ) ) ;
#44855=AXIS2_PLACEMENT_3D ( 'NONE', #265, #59923, #52592 ) ;
#44867=ORIENTED_EDGE ( 'NONE', *, *, #13395, .F. ) ;
#44869=AXIS2_PLACEMENT_3D ( 'NONE', #16562, #12191, #35690 ) ;
#44875=CARTESIAN_POINT ( 'NONE',  ( 0.7954190325252783467, 47.79303692714234586, 5.415566973723409561 ) ) ;
#44899=VERTEX_POINT ( 'NONE', #5599 ) ;
#44901=CARTESIAN_POINT ( 'NONE',  ( -6.001507490154111224, -17.40350523682689854, -7.225628667346763123 ) ) ;
#44903=VECTOR ( 'NONE', #21798, 1000.000000000000000 ) ;
#44907=CARTESIAN_POINT ( 'NONE',  ( 0.1103878639767399278, 41.66755962011264103, 11.11454059769214808 ) ) ;
#44914=CARTESIAN_POINT ( 'NONE',  ( 0.6029303876144825880, -41.59667219751865730, -24.16699908817946962 ) ) ;
#44917=VERTEX_POINT ( 'NONE', #9716 ) ;
#44921=CARTESIAN_POINT ( 'NONE',  ( 0.2230388203127610103, -43.11276071378622277, 0.7599700551098830248 ) ) ;
#44927=CONICAL_SURFACE ( 'NONE', #50922, 42.92674063221959813, 1.485477209440487556 ) ;
#44930=CARTESIAN_POINT ( 'NONE',  ( 0.7048096507298635682, 44.11842270945974320, -19.18768066167077180 ) ) ;
#44932=CARTESIAN_POINT ( 'NONE',  ( 0.6031356219577718170, -34.07882816221597722, -33.95537057546173543 ) ) ;
#44938=CARTESIAN_POINT ( 'NONE',  ( 3.680974057930773924, 45.82782223000855026, 14.19449211152953438 ) ) ;
#44950=CARTESIAN_POINT ( 'NONE',  ( 0.1081432562775997974, -37.55692207416040418, 21.19449538864492766 ) ) ;
#44951=( BOUNDED_SURFACE ( )  B_SPLINE_SURFACE ( 3, 1, ( 
 ( #53030, #11066 ),
 ( #30148, #24224 ),
 ( #53945, #1023 ),
 ( #29229, #43359 ) ),
 .UNSPECIFIED., .F., .F., .F. ) 
 B_SPLINE_SURFACE_WITH_KNOTS ( ( 4, 4 ),
 ( 2, 2 ),
 ( 0.000000000000000000, 1.000000000000000000 ),
 ( 0.000000000000000000, 1.000000000000000000 ),
 .UNSPECIFIED. ) 
 GEOMETRIC_REPRESENTATION_ITEM ( )  RATIONAL_B_SPLINE_SURFACE ( (
 ( 1.000000000000000000, 1.000000000000000000),
 ( 0.9751682680413298332, 0.9999560080971552356),
 ( 0.9751682680413298332, 0.9999560080971552356),
 ( 1.000000000000000000, 1.000000000000000000) ) ) 
 REPRESENTATION_ITEM ( '' )  SURFACE ( )  );
#44952=ORIENTED_EDGE ( 'NONE', *, *, #15553, .T. ) ;
#44955=AXIS2_PLACEMENT_3D ( 'NONE', #6205, #35700, #49771 ) ;
#44970=CARTESIAN_POINT ( 'NONE',  ( 5.880360259849752858, 45.44137230084881907, -15.37531919565188865 ) ) ;
#44978=EDGE_CURVE ( 'NONE', #19158, #5605, #21976, .T. ) ;
#44983=CARTESIAN_POINT ( 'NONE',  ( 4.833616638992208614, 46.17873762321149655, 2.572717262758150270 ) ) ;
#44987=B_SPLINE_CURVE_WITH_KNOTS ( 'NONE', 3,
 ( #13222, #47345, #12080, #37658 ),
 .UNSPECIFIED., .F., .F.,
 ( 4, 4 ),
 ( 0.000000000000000000, 0.005014147105413702989 ),
 .UNSPECIFIED. ) ;
#44990=CARTESIAN_POINT ( 'NONE',  ( 0.5998501479064708430, 37.84527566984816360, 29.69975237324626605 ) ) ;
#44991=CARTESIAN_POINT ( 'NONE',  ( 0.2885700199627511675, 25.60460887553377773, -34.69058524452987768 ) ) ;
#44995=CARTESIAN_POINT ( 'NONE',  ( -6.001507490154111224, 18.19774963328908157, 4.892199142591368677 ) ) ;
#44997=CARTESIAN_POINT ( 'NONE',  ( 0.1102847568649952675, -41.67876919128915603, -11.07236323260738686 ) ) ;
#45000=CARTESIAN_POINT ( 'NONE',  ( -6.016761891674564211, 2.462934516563804355, 18.68153697670642543 ) ) ;
#45003=AXIS2_PLACEMENT_3D ( 'NONE', #27062, #7628, #51783 ) ;
#45011=LINE ( 'NONE', #50292, #44903 ) ;
#45014=EDGE_CURVE ( 'NONE', #20551, #25364, #30245, .T. ) ;
#45021=CARTESIAN_POINT ( 'NONE',  ( 0.5980894510889457338, 0.7015180095998205800, 48.10766805928369649 ) ) ;
#45023=EDGE_CURVE ( 'NONE', #7371, #21985, #25710, .T. ) ;
#45024=ORIENTED_EDGE ( 'NONE', *, *, #43307, .F. ) ;
#45029=VERTEX_POINT ( 'NONE', #17207 ) ;
#45031=FACE_BOUND ( 'NONE', #8035, .T. ) ;
#45032=( BOUNDED_SURFACE ( )  B_SPLINE_SURFACE ( 3, 1, ( 
 ( #14971, #6133 ),
 ( #5825, #34683 ),
 ( #10256, #19353 ),
 ( #5525, #20578 ) ),
 .UNSPECIFIED., .F., .F., .F. ) 
 B_SPLINE_SURFACE_WITH_KNOTS ( ( 4, 4 ),
 ( 2, 2 ),
 ( 0.000000000000000000, 1.000000000000000000 ),
 ( 0.000000000000000000, 1.000000000000000000 ),
 .UNSPECIFIED. ) 
 GEOMETRIC_REPRESENTATION_ITEM ( )  RATIONAL_B_SPLINE_SURFACE ( (
 ( 1.000000000000000000, 1.000000000000000000),
 ( 0.7223157951917480446, 0.9931996967497186413),
 ( 0.7223157951917480446, 0.9931996967497186413),
 ( 1.000000000000000000, 1.000000000000000000) ) ) 
 REPRESENTATION_ITEM ( '' )  SURFACE ( )  );
#45037=ORIENTED_EDGE ( 'NONE', *, *, #49220, .T. ) ;
#45048=CARTESIAN_POINT ( 'NONE',  ( 0.6254311100348632912, 23.45480814408369952, 42.00127298835432299 ) ) ;
#45054=CARTESIAN_POINT ( 'NONE',  ( 0.6027935024548037868, 44.51201578381226653, -18.24855952726183617 ) ) ;
#45060=VERTEX_POINT ( 'NONE', #35091 ) ;
#45061=CARTESIAN_POINT ( 'NONE',  ( 0.6001305935487422083, -0.5236757026892572275, 48.10757715638247589 ) ) ;
#45068=EDGE_CURVE ( 'NONE', #56628, #3699, #4824, .T. ) ;
#45071=ORIENTED_EDGE ( 'NONE', *, *, #18696, .T. ) ;
#45076=CARTESIAN_POINT ( 'NONE',  ( 4.549368137175248350, 23.67244292351589507, 35.80950303116109268 ) ) ;
#45088=DIRECTION ( 'NONE',  ( -0.1024043820194934507, 0.9641676559171120653, -0.2447326578667160801 ) ) ;
#45089=CARTESIAN_POINT ( 'NONE',  ( 0.3622758884714730732, -17.25816669464967035, -39.50828911766992491 ) ) ;
#45090=B_SPLINE_CURVE_WITH_KNOTS ( 'NONE', 3,
 ( #1313, #16679, #59573, #1624, #35489, #6615 ),
 .UNSPECIFIED., .F., .F.,
 ( 4, 2, 4 ),
 ( 1.764953265579307567E-18, 0.0002450742804987342304, 0.0004901485609974666176 ),
 .UNSPECIFIED. ) ;
#45095=CARTESIAN_POINT ( 'NONE',  ( 0.6001305935487315502, 46.33281397023063874, -12.95698906763762359 ) ) ;
#45096=EDGE_CURVE ( 'NONE', #58621, #35726, #42930, .T. ) ;
#45100=EDGE_CURVE ( 'NONE', #26391, #52654, #32486, .T. ) ;
#45102=ORIENTED_EDGE ( 'NONE', *, *, #966, .T. ) ;
#45104=CARTESIAN_POINT ( 'NONE',  ( 0.1087620492084205304, 37.16461718700635686, 21.87505161834429757 ) ) ;
#45110=CARTESIAN_POINT ( 'NONE',  ( 3.680974057930773924, 30.65154904503179267, -36.90739001595142099 ) ) ;
#45113=B_SPLINE_CURVE_WITH_KNOTS ( 'NONE', 3,
 ( #54362, #58144, #49685, #29967, #15269, #43798, #5822, #24657, #44410, #6130, #16186, #54060, #29654, #10252, #11484, #49076, #6739, #25572, #1748 ),
 .UNSPECIFIED., .F., .F.,
 ( 4, 3, 3, 3, 3, 3, 4 ),
 ( 1.153344816771540786E-16, 0.0002618519381806258626, 0.0003927759815485975473, 0.0005237000248299470079, 0.0006546240681324973915, 0.0007855481115631335765, 0.0009699050456655115924 ),
 .UNSPECIFIED. ) ;
#45115=VERTEX_POINT ( 'NONE', #32858 ) ;
#45120=CARTESIAN_POINT ( 'NONE',  ( 0.6025881611877910160, -29.45877655626822289, 38.03302298778292112 ) ) ;
#45125=CARTESIAN_POINT ( 'NONE',  ( 0.1100053167205930493, -26.39466280306244883, -34.10339839758277236 ) ) ;
#45154=CARTESIAN_POINT ( 'NONE',  ( 2.301529144917014325, -17.18548816179652405, 44.85388898586996476 ) ) ;
#45158=FACE_OUTER_BOUND ( 'NONE', #20603, .T. ) ;
#45166=ORIENTED_EDGE ( 'NONE', *, *, #34050, .F. ) ;
#45167=CARTESIAN_POINT ( 'NONE',  ( 0.1064266379913938743, -25.80493164505229586, 34.55203636557764924 ) ) ;
#45177=DIRECTION ( 'NONE',  ( 0.000000000000000000, 0.000000000000000000, 1.000000000000000000 ) ) ;
#45191=VERTEX_POINT ( 'NONE', #538 ) ;
#45193=EDGE_CURVE ( 'NONE', #39295, #52389, #28699, .T. ) ;
#45194=CARTESIAN_POINT ( 'NONE',  ( 0.6001305935487315502, -33.64689939321917933, -34.38748867424702382 ) ) ;
#45197=VERTEX_POINT ( 'NONE', #48469 ) ;
#45200=ORIENTED_EDGE ( 'NONE', *, *, #400, .T. ) ;
#45202=CARTESIAN_POINT ( 'NONE',  ( 4.975801465491695552, 35.64402118370958306, -32.01766832630274706 ) ) ;
#45204=CARTESIAN_POINT ( 'NONE',  ( 0.1102847568649952675, 0.09217763870840627038, 43.12433804869904463 ) ) ;
#45211=ORIENTED_EDGE ( 'NONE', *, *, #57680, .T. ) ;
#45212=B_SPLINE_CURVE_WITH_KNOTS ( 'NONE', 3,
 ( #11158, #58732, #44084, #59049 ),
 .UNSPECIFIED., .F., .F.,
 ( 4, 4 ),
 ( 0.000000000000000000, 0.005014147105413707325 ),
 .UNSPECIFIED. ) ;
#45213=ORIENTED_EDGE ( 'NONE', *, *, #22659, .F. ) ;
#45227=ORIENTED_EDGE ( 'NONE', *, *, #60378, .F. ) ;
#45236=CARTESIAN_POINT ( 'NONE',  ( -6.015611763856276717, -18.19956619163654565, -4.882992715191491584 ) ) ;
#45239=DIRECTION ( 'NONE',  ( -1.000000000000000000, -0.000000000000000000, -0.000000000000000000 ) ) ;
#45241=DIRECTION ( 'NONE',  ( -0.1024043820194934645, 0.1167898032637269823, 0.9878630899050867553 ) ) ;
#45243=CARTESIAN_POINT ( 'NONE',  ( 0.6027935024548037868, -33.89348162668954245, -34.14031893787213079 ) ) ;
#45244=CARTESIAN_POINT ( 'NONE',  ( 0.5998501479064699549, -18.89267974119636406, -44.24259072156078787 ) ) ;
#45246=( BOUNDED_SURFACE ( )  B_SPLINE_SURFACE ( 3, 1, ( 
 ( #12363, #53011 ),
 ( #27988, #8878 ),
 ( #38040, #57382 ),
 ( #10113, #61779 ) ),
 .UNSPECIFIED., .F., .F., .F. ) 
 B_SPLINE_SURFACE_WITH_KNOTS ( ( 4, 4 ),
 ( 2, 2 ),
 ( 0.000000000000000000, 1.000000000000000000 ),
 ( 0.000000000000000000, 1.000000000000000000 ),
 .UNSPECIFIED. ) 
 GEOMETRIC_REPRESENTATION_ITEM ( )  RATIONAL_B_SPLINE_SURFACE ( (
 ( 1.000000000000000000, 1.000000000000000000),
 ( 0.7223157951917480446, 0.9931996967497186413),
 ( 0.7223157951917480446, 0.9931996967497186413),
 ( 1.000000000000000000, 1.000000000000000000) ) ) 
 REPRESENTATION_ITEM ( '' )  SURFACE ( )  );
#45248=DIRECTION ( 'NONE',  ( 0.000000000000000000, 0.000000000000000000, 1.000000000000000000 ) ) ;
#45255=CARTESIAN_POINT ( 'NONE',  ( 0.8760168074886965917, -47.56749362999708808, -7.161346975773540180 ) ) ;
#45259=CARTESIAN_POINT ( 'NONE',  ( 0.1092355843206037486, -37.49628696754474078, 21.30139719602306059 ) ) ;
#45264=DIRECTION ( 'NONE',  ( -0.1024043820194934368, -0.9641676559171102889, 0.2447326578667227415 ) ) ;
#45265=FACE_OUTER_BOUND ( 'NONE', #16722, .T. ) ;
#45269=CIRCLE ( 'NONE', #18252, 47.91270532121795611 ) ;
#45270=FACE_OUTER_BOUND ( 'NONE', #22909, .T. ) ;
#45278=CARTESIAN_POINT ( 'NONE',  ( 0.5998501479064699549, 46.60114184914301205, 11.94461217097485672 ) ) ;
#45282=CARTESIAN_POINT ( 'NONE',  ( 4.549368137175248350, 35.57418903283081590, 24.02461520945284690 ) ) ;
#45287=DIRECTION ( 'NONE',  ( 0.000000000000000000, 0.000000000000000000, -1.000000000000000000 ) ) ;
#45289=CARTESIAN_POINT ( 'NONE',  ( 0.1064266379913939575, -5.071708164747380287, 42.82540706760014615 ) ) ;
#45290=CARTESIAN_POINT ( 'NONE',  ( 0.8751705887134553219, 48.08707113907595243, -0.8911681664083408450 ) ) ;
#45291=CARTESIAN_POINT ( 'NONE',  ( 0.1073791018717483448, 41.52698815987167791, -11.62916352156108779 ) ) ;
#45306=VERTEX_POINT ( 'NONE', #1156 ) ;
#45314=CARTESIAN_POINT ( 'NONE',  ( 0.5988103564986356764, 17.84821699813482709, -44.67429521517314583 ) ) ;
#45317=CARTESIAN_POINT ( 'NONE',  ( 0.2224561200757630419, 36.95704201588763027, 22.21411683958066163 ) ) ;
#45318=( BOUNDED_SURFACE ( )  B_SPLINE_SURFACE ( 3, 1, ( 
 ( #43387, #19569 ),
 ( #53056, #38686 ),
 ( #48673, #5728 ),
 ( #23640, #48069 ) ),
 .UNSPECIFIED., .F., .F., .F. ) 
 B_SPLINE_SURFACE_WITH_KNOTS ( ( 4, 4 ),
 ( 2, 2 ),
 ( 0.000000000000000000, 1.000000000000000000 ),
 ( 0.000000000000000000, 1.000000000000000000 ),
 .UNSPECIFIED. ) 
 GEOMETRIC_REPRESENTATION_ITEM ( )  RATIONAL_B_SPLINE_SURFACE ( (
 ( 1.000000000000000000, 1.000000000000000000),
 ( 0.9953040768229013402, 0.8617119497784988535),
 ( 0.9953040768229013402, 0.8617119497784988535),
 ( 1.000000000000000000, 1.000000000000000000) ) ) 
 REPRESENTATION_ITEM ( '' )  SURFACE ( )  );
#45320=CARTESIAN_POINT ( 'NONE',  ( 0.5998501479064699549, 41.39809967730487017, -24.50586714782561160 ) ) ;
#45321=CARTESIAN_POINT ( 'NONE',  ( 4.691466044806102076, 39.84135254923108249, 20.01963481131674172 ) ) ;
#45325=CARTESIAN_POINT ( 'NONE',  ( 0.3622758884714600280, -34.70015533914845918, 25.58609868863709380 ) ) ;
#45331=CARTESIAN_POINT ( 'NONE',  ( 0.1097557419366048670, 41.59672960874312508, -11.37678103520293149 ) ) ;
#45333=ORIENTED_EDGE ( 'NONE', *, *, #60812, .T. ) ;
#45336=CARTESIAN_POINT ( 'NONE',  ( 0.1087620492084205442, -10.81135549499751747, -41.74735017127127179 ) ) ;
#45341=CARTESIAN_POINT ( 'NONE',  ( 0.7954196712028467342, 0.8690072546825631239, -48.09103417491925825 ) ) ;
#45346=CARTESIAN_POINT ( 'NONE',  ( -2.569797478183790229, -14.01151037928420173, -4.218948559326200609 ) ) ;
#45348=ORIENTED_EDGE ( 'NONE', *, *, #57907, .F. ) ;
#45352=CARTESIAN_POINT ( 'NONE',  ( 5.880360259849752858, -39.91356965504166254, 26.61251048557179644 ) ) ;
#45354=DIRECTION ( 'NONE',  ( -1.000000000000000000, -0.000000000000000000, -0.000000000000000000 ) ) ;
#45361=EDGE_CURVE ( 'NONE', #56157, #41236, #11007, .T. ) ;
#45363=CARTESIAN_POINT ( 'NONE',  ( -6.017396004339686577, -0.001173774848850273316, -18.84316306185412415 ) ) ;
#45379=CARTESIAN_POINT ( 'NONE',  ( 0.2885700199627521112, 41.84838128711407990, 10.38006184593217185 ) ) ;
#45384=FACE_OUTER_BOUND ( 'NONE', #12629, .T. ) ;
#45403=CARTESIAN_POINT ( 'NONE',  ( 0.1100247026804066219, 11.32523219034908202, -41.61078157869240357 ) ) ;
#45410=CARTESIAN_POINT ( 'NONE',  ( 0.8751705887134423323, 29.98056538504960855, -37.60752970653798855 ) ) ;
#45415=ORIENTED_EDGE ( 'NONE', *, *, #49081, .T. ) ;
#45417=CARTESIAN_POINT ( 'NONE',  ( 3.238741278300274029, 42.95313747363661605, 1.828728677531976210 ) ) ;
#45418=ORIENTED_EDGE ( 'NONE', *, *, #51184, .F. ) ;
#45419=DIRECTION ( 'NONE',  ( -1.000000000000000000, -0.000000000000000000, -0.000000000000000000 ) ) ;
#45422=CARTESIAN_POINT ( 'NONE',  ( 5.880360259849739535, -43.04573319267431231, -21.17507050419500558 ) ) ;
#45423=VERTEX_POINT ( 'NONE', #6762 ) ;
#45433=ADVANCED_FACE ( 'NONE', ( #35636 ), #25971, .F. ) ;
#45437=CARTESIAN_POINT ( 'NONE',  ( 4.975801465491694664, -3.702618843597810905, 47.76942479135478692 ) ) ;
#45439=CARTESIAN_POINT ( 'NONE',  ( 0.6029303876144825880, 44.39523326884611265, 18.53079182983359985 ) ) ;
#45444=B_SPLINE_CURVE_WITH_KNOTS ( 'NONE', 3,
 ( #13292, #32400, #51471, #8565 ),
 .UNSPECIFIED., .F., .F.,
 ( 4, 4 ),
 ( 0.000000000000000000, 0.005014147105413701254 ),
 .UNSPECIFIED. ) ;
#45447=ORIENTED_EDGE ( 'NONE', *, *, #43734, .T. ) ;
#45449=CARTESIAN_POINT ( 'NONE',  ( 4.322998006666165516, -8.359821156456828106, 47.25487450103521070 ) ) ;
#45452=CARTESIAN_POINT ( 'NONE',  ( 1.827119703190778432, -29.55676396270206041, 31.30004882613791750 ) ) ;
#45454=CARTESIAN_POINT ( 'NONE',  ( 0.6030672727741701600, -29.21669544497223470, -38.21927534816974514 ) ) ;
#45457=CARTESIAN_POINT ( 'NONE',  ( 0.8760168074887076939, 38.69913431881784049, 28.57146030081993615 ) ) ;
#45458=ORIENTED_EDGE ( 'NONE', *, *, #21042, .T. ) ;
#45475=DIRECTION ( 'NONE',  ( 0.000000000000000000, 0.000000000000000000, 1.000000000000000000 ) ) ;
#45476=ORIENTED_EDGE ( 'NONE', *, *, #33498, .T. ) ;
#45481=EDGE_CURVE ( 'NONE', #52654, #16193, #22131, .T. ) ;
#45484=ADVANCED_FACE ( 'NONE', ( #60626 ), #28920, .F. ) ;
#45488=CARTESIAN_POINT ( 'NONE',  ( -6.016489644550737204, -13.32104266208090060, -13.32727118274452138 ) ) ;
#45495=ORIENTED_EDGE ( 'NONE', *, *, #17089, .T. ) ;
#45498=CARTESIAN_POINT ( 'NONE',  ( 0.6254311100348659558, 42.00127298835423773, -23.45480814408383807 ) ) ;
#45503=EDGE_CURVE ( 'NONE', #35346, #57844, #11508, .T. ) ;
#45513=CARTESIAN_POINT ( 'NONE',  ( 0.1098349054025745952, 41.59932877996182299, 11.36734385884019360 ) ) ;
#45515=CONICAL_SURFACE ( 'NONE', #9446, 42.92674063221959813, 1.485477209440487556 ) ;
#45520=CARTESIAN_POINT ( 'NONE',  ( 2.643462169533600914, 28.13401304854668084, 38.93558293168548090 ) ) ;
#45526=CARTESIAN_POINT ( 'NONE',  ( 0.6009453534118438522, 6.711694149738223203, -47.63713118507420319 ) ) ;
#45529=FACE_OUTER_BOUND ( 'NONE', #1362, .T. ) ;
#45532=CARTESIAN_POINT ( 'NONE',  ( 0.6023142530420679819, 12.19802990522800812, -46.53533807097419128 ) ) ;
#45537=CARTESIAN_POINT ( 'NONE',  ( 5.880360259849739535, 36.09847387447815947, 31.59460303415995241 ) ) ;
#45549=ORIENTED_EDGE ( 'NONE', *, *, #7696, .T. ) ;
#45552=CARTESIAN_POINT ( 'NONE',  ( 0.8760168074887090262, 34.63873394077441503, 33.37827814204137411 ) ) ;
#45553=VERTEX_POINT ( 'NONE', #38723 ) ;
#45555=CARTESIAN_POINT ( 'NONE',  ( 3.238931869106854489, 42.34694073502591039, -7.419701784410695389 ) ) ;
#45556=CARTESIAN_POINT ( 'NONE',  ( 0.1097557419366048670, -37.23482781437660805, 21.75515245866060354 ) ) ;
#45558=ORIENTED_EDGE ( 'NONE', *, *, #11551, .F. ) ;
#45567=CARTESIAN_POINT ( 'NONE',  ( -6.016489644550736315, -2.455165042129866748, 18.68257207665195452 ) ) ;
#45569=VECTOR ( 'NONE', #17513, 1000.000000000000114 ) ;
#45571=VERTEX_POINT ( 'NONE', #9256 ) ;
#45586=VERTEX_POINT ( 'NONE', #24917 ) ;
#45589=CARTESIAN_POINT ( 'NONE',  ( 0.3622758884714600280, 25.58609868863721459, 34.70015533914837391 ) ) ;
#45592=LINE ( 'NONE', #54641, #25883 ) ;
#45599=( BOUNDED_SURFACE ( )  B_SPLINE_SURFACE ( 3, 1, ( 
 ( #51379, #8465 ),
 ( #37318, #61390 ),
 ( #13505, #27594 ),
 ( #46720, #3763 ) ),
 .UNSPECIFIED., .F., .F., .F. ) 
 B_SPLINE_SURFACE_WITH_KNOTS ( ( 4, 4 ),
 ( 2, 2 ),
 ( 0.000000000000000000, 1.000000000000000000 ),
 ( 0.000000000000000000, 1.000000000000000000 ),
 .UNSPECIFIED. ) 
 GEOMETRIC_REPRESENTATION_ITEM ( )  RATIONAL_B_SPLINE_SURFACE ( (
 ( 1.000000000000000000, 1.000000000000000000),
 ( 0.9953040768229005630, 0.8617119497784937465),
 ( 0.9953040768229005630, 0.8617119497784937465),
 ( 1.000000000000000000, 1.000000000000000000) ) ) 
 REPRESENTATION_ITEM ( '' )  SURFACE ( )  );
#45607=CARTESIAN_POINT ( 'NONE',  ( 4.322998006666179727, 47.80838462754059748, 4.155494336618874129 ) ) ;
#45615=CARTESIAN_POINT ( 'NONE',  ( 0.6017667736363749853, 0.3491025323180517170, -48.10631678344241635 ) ) ;
#45617=ORIENTED_EDGE ( 'NONE', *, *, #41395, .F. ) ;
#45632=EDGE_CURVE ( 'NONE', #49021, #60939, #57078, .T. ) ;
#45636=CARTESIAN_POINT ( 'NONE',  ( 0.5998501479064699549, 41.92175333043586960, 23.59887241503369282 ) ) ;
#45638=ADVANCED_FACE ( 'NONE', ( #45270 ), #20513, .F. ) ;
#45641=CARTESIAN_POINT ( 'NONE',  ( 0.5988103622719989083, 0.6065097949913632602, -48.10388392585942796 ) ) ;
#45654=ORIENTED_EDGE ( 'NONE', *, *, #28104, .T. ) ;
#45656=LINE ( 'NONE', #11516, #16015 ) ;
#45661=CARTESIAN_POINT ( 'NONE',  ( -4.908599999999998964, 0.000000000000000000, 0.000000000000000000 ) ) ;
#45664=CARTESIAN_POINT ( 'NONE',  ( 0.5998501479064708430, 46.33007877220720871, 12.95623334615518374 ) ) ;
#45669=CARTESIAN_POINT ( 'NONE',  ( 0.8760168074887076939, -44.09317760313766144, 19.22870327415225589 ) ) ;
#45672=ORIENTED_EDGE ( 'NONE', *, *, #22149, .F. ) ;
#45673=VERTEX_POINT ( 'NONE', #49318 ) ;
#45675=CARTESIAN_POINT ( 'NONE',  ( 4.975801465491694664, 35.64402118370912120, 32.01766832630325155 ) ) ;
#45678=CARTESIAN_POINT ( 'NONE',  ( 3.238741278300274473, -36.28414388564879545, -23.06029422818990682 ) ) ;
#45679=EDGE_CURVE ( 'NONE', #59715, #19827, #2001, .T. ) ;
#45682=ORIENTED_EDGE ( 'NONE', *, *, #59158, .F. ) ;
#45684=CARTESIAN_POINT ( 'NONE',  ( 4.975801465491695552, 46.87746200127456575, -9.906103548667728020 ) ) ;
#45686=ORIENTED_EDGE ( 'NONE', *, *, #5865, .T. ) ;
#45692=CARTESIAN_POINT ( 'NONE',  ( 0.8751705887134423323, -47.55935879196466232, -7.160166390004136794 ) ) ;
#45701=B_SPLINE_CURVE_WITH_KNOTS ( 'NONE', 3,
 ( #22499, #60688, #51294, #45704 ),
 .UNSPECIFIED., .F., .F.,
 ( 4, 4 ),
 ( 1.939025188362721105E-17, 0.004444306975806117631 ),
 .UNSPECIFIED. ) ;
#45704=CARTESIAN_POINT ( 'NONE',  ( 4.975801465491694664, -45.18341283946446651, -15.94009207553035523 ) ) ;
#45710=CARTESIAN_POINT ( 'NONE',  ( 0.1081432562775997835, 11.56998286599535852, -41.54352569227150838 ) ) ;
#45711=B_SPLINE_CURVE_WITH_KNOTS ( 'NONE', 3,
 ( #26317, #2181, #45452, #2501 ),
 .UNSPECIFIED., .F., .F.,
 ( 4, 4 ),
 ( 6.254634441385501517E-18, 0.004566006591234647236 ),
 .UNSPECIFIED. ) ;
#45718=EDGE_CURVE ( 'NONE', #10248, #4699, #18957, .T. ) ;
#45726=CARTESIAN_POINT ( 'NONE',  ( -6.017396004339687465, -13.32329839588545717, -13.32495836419638557 ) ) ;
#45729=ORIENTED_EDGE ( 'NONE', *, *, #55858, .T. ) ;
#45731=CARTESIAN_POINT ( 'NONE',  ( 0.1092565886968785149, -26.49813811968561694, -34.02318727879954707 ) ) ;
#45732=ADVANCED_FACE ( 'NONE', ( #13595 ), #32703, .F. ) ;
#45735=CARTESIAN_POINT ( 'NONE',  ( -6.015611763856276717, 9.416239407363534042, -16.32183393015586503 ) ) ;
#45740=CARTESIAN_POINT ( 'NONE',  ( 0.6041374136657475802, 23.90252055111265150, 41.74951251761581972 ) ) ;
#45750=ORIENTED_EDGE ( 'NONE', *, *, #16762, .F. ) ;
#45754=ORIENTED_EDGE ( 'NONE', *, *, #34749, .T. ) ;
#45755=CARTESIAN_POINT ( 'NONE',  ( 0.1097557419366048670, -42.78407272074154832, -5.407604117549557721 ) ) ;
#45758=( BOUNDED_SURFACE ( )  B_SPLINE_SURFACE ( 3, 1, ( 
 ( #41945, #17502 ),
 ( #17811, #32223 ),
 ( #32530, #23126 ),
 ( #36939, #8384 ) ),
 .UNSPECIFIED., .F., .F., .F. ) 
 B_SPLINE_SURFACE_WITH_KNOTS ( ( 4, 4 ),
 ( 2, 2 ),
 ( 0.000000000000000000, 1.000000000000000000 ),
 ( 0.000000000000000000, 1.000000000000000000 ),
 .UNSPECIFIED. ) 
 GEOMETRIC_REPRESENTATION_ITEM ( )  RATIONAL_B_SPLINE_SURFACE ( (
 ( 1.000000000000000000, 1.000000000000000000),
 ( 0.7223157951917480446, 0.9931996967497186413),
 ( 0.7223157951917480446, 0.9931996967497186413),
 ( 1.000000000000000000, 1.000000000000000000) ) ) 
 REPRESENTATION_ITEM ( '' )  SURFACE ( )  );
#45765=CIRCLE ( 'NONE', #4697, 42.92674063221959813 ) ;
#45772=ORIENTED_EDGE ( 'NONE', *, *, #42111, .F. ) ;
#45774=CARTESIAN_POINT ( 'NONE',  ( 0.2885700199627493356, -25.60460887553402998, 34.69058524452970715 ) ) ;
#45779=CARTESIAN_POINT ( 'NONE',  ( 0.1084644655670282121, 21.21700107124048529, -37.54424727804280337 ) ) ;
#45781=CARTESIAN_POINT ( 'NONE',  ( 0.6254087463353934506, -44.17672642933517579, 19.04342133627966405 ) ) ;
#45793=CARTESIAN_POINT ( 'NONE',  ( 0.8760168074887076939, -47.56749362999718045, 7.161346975772899803 ) ) ;
#45796=EDGE_CURVE ( 'NONE', #60819, #34095, #24140, .T. ) ;
#45797=CARTESIAN_POINT ( 'NONE',  ( 2.301430502907646058, 7.543848632415214084, -47.43735983879645346 ) ) ;
#45806=CARTESIAN_POINT ( 'NONE',  ( -5.995132425357893702, 14.94489030678166941, -11.47834865841080720 ) ) ;
#45813=EDGE_CURVE ( 'NONE', #49511, #52728, #60744, .T. ) ;
#45820=B_SPLINE_CURVE_WITH_KNOTS ( 'NONE', 3,
 ( #51050, #61366, #28178, #24407, #14411, #51668 ),
 .UNSPECIFIED., .F., .F.,
 ( 4, 2, 4 ),
 ( 1.964907063297894324E-17, 0.0002293319059085095475, 0.0004586638118169994167 ),
 .UNSPECIFIED. ) ;
#45822=FACE_OUTER_BOUND ( 'NONE', #8862, .T. ) ;
#45826=VERTEX_POINT ( 'NONE', #24208 ) ;
#45828=DIRECTION ( 'NONE',  ( -1.000000000000000000, -0.000000000000000000, -0.000000000000000000 ) ) ;
#45833=CARTESIAN_POINT ( 'NONE',  ( 0.8760168074886965917, 11.58706983520260536, 46.68716261866180872 ) ) ;
#45843=CARTESIAN_POINT ( 'NONE',  ( 0.6041374136657476912, 41.74951251761541471, 23.90252055111336205 ) ) ;
#45844=CARTESIAN_POINT ( 'NONE',  ( 0.3622758884714730732, 39.50828911766998175, -17.25816669464953534 ) ) ;
#45849=CARTESIAN_POINT ( 'NONE',  ( 0.1313383488274127153, -6.260443365527081028, -42.66669366003520025 ) ) ;
#45856=CARTESIAN_POINT ( 'NONE',  ( 0.5998501479064699549, 37.84527566984857572, -29.69975237324574024 ) ) ;
#45862=CARTESIAN_POINT ( 'NONE',  ( 5.880360259849739535, 9.405269135694590332, 47.04104239318770198 ) ) ;
#45864=FACE_OUTER_BOUND ( 'NONE', #46546, .T. ) ;
#45866=ORIENTED_EDGE ( 'NONE', *, *, #28567, .T. ) ;
#45877=EDGE_LOOP ( 'NONE', ( #32784, #17614, #10275, #29512 ) ) ;
#45884=EDGE_CURVE ( 'NONE', #37253, #2911, #4695, .T. ) ;
#45885=B_SPLINE_CURVE_WITH_KNOTS ( 'NONE', 3,
 ( #59685, #36219, #41536, #7673, #17718, #35606, #2981, #7358, #55284, #26484, #2046, #25873, #21177, #55593, #2667, #12723 ),
 .UNSPECIFIED., .F., .F.,
 ( 4, 3, 3, 3, 3, 4 ),
 ( 2.194378057379452319E-17, 0.0002618515315864398084, 0.0003927756766341980454, 0.0005236998216950549626, 0.0007855159896329879472, 0.001047349442285926569 ),
 .UNSPECIFIED. ) ;
#45888=CARTESIAN_POINT ( 'NONE',  ( 0.6031357023905875581, -48.10744334619843698, -0.04361601114896231091 ) ) ;
#45890=VECTOR ( 'NONE', #40730, 999.9999999999998863 ) ;
#45895=CARTESIAN_POINT ( 'NONE',  ( -6.017396004339687465, 4.878103249821321263, -18.20079405513545012 ) ) ;
#45896=CARTESIAN_POINT ( 'NONE',  ( -6.016761891674565099, -13.32657647165364700, 13.32172022638586917 ) ) ;
#45904=CARTESIAN_POINT ( 'NONE',  ( 0.1102144999581333024, 39.88986724628635017, -16.38650952318868903 ) ) ;
#45906=CARTESIAN_POINT ( 'NONE',  ( 0.1100247026804066219, 42.77732815928600019, -5.460606496326462000 ) ) ;
#45916=ADVANCED_FACE ( 'NONE', ( #43975 ), #26920, .F. ) ;
#45917=DIRECTION ( 'NONE',  ( 0.000000000000000000, 0.000000000000000000, 1.000000000000000000 ) ) ;
#45922=CARTESIAN_POINT ( 'NONE',  ( 0.1087620492084205859, -41.55994353650434192, -11.51076657762320643 ) ) ;
#45930=DIRECTION ( 'NONE',  ( 0.000000000000000000, 0.000000000000000000, 1.000000000000000000 ) ) ;
#45937=CARTESIAN_POINT ( 'NONE',  ( 0.3622758884714600280, 36.91764744403290166, 22.26738722580180507 ) ) ;
#45943=ORIENTED_EDGE ( 'NONE', *, *, #1898, .F. ) ;
#45946=CARTESIAN_POINT ( 'NONE',  ( -6.015611763856276717, -18.19956619163661671, 4.882992715191235789 ) ) ;
#45947=CARTESIAN_POINT ( 'NONE',  ( 5.880360259849739535, -15.46489389606724707, -45.41096578730640942 ) ) ;
#45948=CARTESIAN_POINT ( 'NONE',  ( -2.569797478183790229, 14.01151037928417153, 4.218948559326298309 ) ) ;
#45955=B_SPLINE_CURVE_WITH_KNOTS ( 'NONE', 3,
 ( #467, #56865, #4854, #42808 ),
 .UNSPECIFIED., .F., .F.,
 ( 4, 4 ),
 ( 0.000000000000000000, 0.004445488388166993383 ),
 .UNSPECIFIED. ) ;
#45957=FACE_OUTER_BOUND ( 'NONE', #47743, .T. ) ;
#45962=EDGE_CURVE ( 'NONE', #49832, #20913, #34861, .T. ) ;
#45964=CARTESIAN_POINT ( 'NONE',  ( 0.8760168074887076939, 17.58183840866400516, -44.77533136581864426 ) ) ;
#45965=ORIENTED_EDGE ( 'NONE', *, *, #18672, .F. ) ;
#45967=CARTESIAN_POINT ( 'NONE',  ( 0.8760168074887076939, 48.09529047980637984, -0.8912768426701273006 ) ) ;
#45968=ORIENTED_EDGE ( 'NONE', *, *, #6790, .T. ) ;
#45972=CARTESIAN_POINT ( 'NONE',  ( 0.8760168074887090262, -19.22870327415273195, -44.09317760313745538 ) ) ;
#45977=CARTESIAN_POINT ( 'NONE',  ( 0.5998501479064699549, 44.24259072156085182, -18.89267974119621485 ) ) ;
#45978=VERTEX_POINT ( 'NONE', #40201 ) ;
#45982=( BOUNDED_SURFACE ( )  B_SPLINE_SURFACE ( 3, 1, ( 
 ( #26054, #45194 ),
 ( #54849, #11983 ),
 ( #31064, #22594 ),
 ( #27907, #52004 ) ),
 .UNSPECIFIED., .F., .F., .F. ) 
 B_SPLINE_SURFACE_WITH_KNOTS ( ( 4, 4 ),
 ( 2, 2 ),
 ( 0.000000000000000000, 1.000000000000000000 ),
 ( 0.000000000000000000, 1.000000000000000000 ),
 .UNSPECIFIED. ) 
 GEOMETRIC_REPRESENTATION_ITEM ( )  RATIONAL_B_SPLINE_SURFACE ( (
 ( 1.000000000000000000, 1.000000000000000000),
 ( 0.9953040768229013402, 0.8617119497784988535),
 ( 0.9953040768229013402, 0.8617119497784988535),
 ( 1.000000000000000000, 1.000000000000000000) ) ) 
 REPRESENTATION_ITEM ( '' )  SURFACE ( )  );
#45989=CARTESIAN_POINT ( 'NONE',  ( 0.2885697896453112699, -20.85752796052987179, -37.73587455644740629 ) ) ;
#45993=CARTESIAN_POINT ( 'NONE',  ( 0.8751705887134553219, 47.55935879196470495, -7.160166390003808168 ) ) ;
#45998=FACE_OUTER_BOUND ( 'NONE', #50686, .T. ) ;
#46002=CARTESIAN_POINT ( 'NONE',  ( 1.827119703190780653, 36.65069040194709515, -22.58367210012853121 ) ) ;
#46004=EDGE_CURVE ( 'NONE', #46173, #15890, #31585, .T. ) ;
#46008=CIRCLE ( 'NONE', #53951, 42.92674063221959813 ) ;
#46016=DIRECTION ( 'NONE',  ( 0.000000000000000000, 0.000000000000000000, 1.000000000000000000 ) ) ;
#46018=CARTESIAN_POINT ( 'NONE',  ( 4.975801465491695552, -43.22084481528207078, -20.67815041659126862 ) ) ;
#46024=CARTESIAN_POINT ( 'NONE',  ( 0.1064266379913941657, 30.88821943652570212, 30.09411261783700908 ) ) ;
#46027=EDGE_CURVE ( 'NONE', #11351, #29999, #6922, .T. ) ;
#46031=CARTESIAN_POINT ( 'NONE',  ( 0.1102144999581333440, 11.28312052188147518, -41.62223437741658216 ) ) ;
#46034=CARTESIAN_POINT ( 'NONE',  ( 50.00005079999999680, 1.224646799147353256E-15, -10.00000000000000000 ) ) ;
#46044=CARTESIAN_POINT ( 'NONE',  ( -6.015611763856276717, -18.84324252354755203, -0.006214430185339674118 ) ) ;
#46047=ORIENTED_EDGE ( 'NONE', *, *, #40281, .T. ) ;
#46057=VERTEX_POINT ( 'NONE', #7556 ) ;
#46059=CARTESIAN_POINT ( 'NONE',  ( 0.5998501479064699549, 34.38546660123250120, 33.64490850298857083 ) ) ;
#46060=CARTESIAN_POINT ( 'NONE',  ( -2.708315649062910779, -14.63219292706382824, -0.2635547933243013730 ) ) ;
#46062=CARTESIAN_POINT ( 'NONE',  ( 0.5998501479064708430, 11.94461217097404493, 46.60114184914321811 ) ) ;
#46063=CARTESIAN_POINT ( 'NONE',  ( 4.975801465491695552, 8.787181743660156030, -47.10002938642133330 ) ) ;
#46064=ORIENTED_EDGE ( 'NONE', *, *, #7037, .F. ) ;
#46066=CARTESIAN_POINT ( 'NONE',  ( 0.7954190325252782356, 7.138712176114802688, 47.56618055754177021 ) ) ;
#46080=EDGE_LOOP ( 'NONE', ( #4133, #9905, #44687, #4091 ) ) ;
#46085=VERTEX_POINT ( 'NONE', #52015 ) ;
#46088=CARTESIAN_POINT ( 'NONE',  ( 0.1064266418746777770, -39.62374465289885705, -17.02047513535218926 ) ) ;
#46089=CARTESIAN_POINT ( 'NONE',  ( 0.1097557419366048670, -16.70891382096342781, -39.75589591229780950 ) ) ;
#46090=EDGE_CURVE ( 'NONE', #41909, #29351, #54752, .T. ) ;
#46096=CARTESIAN_POINT ( 'NONE',  ( -6.016761891674564211, -11.47373234755493243, -14.94721834528426463 ) ) ;
#46098=CARTESIAN_POINT ( 'NONE',  ( 0.6254311100348675101, 33.52633430496182854, 34.49956326955429375 ) ) ;
#46100=CARTESIAN_POINT ( 'NONE',  ( 0.1073791018717578927, 6.109314776652701617, -42.68962945260948061 ) ) ;
#46102=CARTESIAN_POINT ( 'NONE',  ( -6.016761891674565099, 11.47373234755524862, -14.94721834528402660 ) ) ;
#46105=CARTESIAN_POINT ( 'NONE',  ( 0.7245667037590768356, 47.79072416626837594, 5.464144792999545253 ) ) ;
#46119=FACE_OUTER_BOUND ( 'NONE', #29295, .T. ) ;
#46121=CARTESIAN_POINT ( 'NONE',  ( 4.322998006666179727, -42.57894920390112503, -22.13465289016611948 ) ) ;
#46124=( BOUNDED_SURFACE ( )  B_SPLINE_SURFACE ( 3, 1, ( 
 ( #45946, #17412 ),
 ( #17113, #22110 ),
 ( #1512, #3285 ),
 ( #58838, #60606 ) ),
 .UNSPECIFIED., .F., .F., .F. ) 
 B_SPLINE_SURFACE_WITH_KNOTS ( ( 4, 4 ),
 ( 2, 2 ),
 ( 0.000000000000000000, 1.000000000000000000 ),
 ( 0.000000000000000000, 1.000000000000000000 ),
 .UNSPECIFIED. ) 
 GEOMETRIC_REPRESENTATION_ITEM ( )  RATIONAL_B_SPLINE_SURFACE ( (
 ( 1.000000000000000000, 1.000000000000000000),
 ( 0.7223157951917480446, 0.9931996967497186413),
 ( 0.7223157951917480446, 0.9931996967497186413),
 ( 1.000000000000000000, 1.000000000000000000) ) ) 
 REPRESENTATION_ITEM ( '' )  SURFACE ( )  );
#46133=VERTEX_POINT ( 'NONE', #18523 ) ;
#46134=DIRECTION ( 'NONE',  ( 0.000000000000000000, 0.000000000000000000, 1.000000000000000000 ) ) ;
#46140=FACE_OUTER_BOUND ( 'NONE', #10616, .T. ) ;
#46144=( BOUNDED_SURFACE ( )  B_SPLINE_SURFACE ( 3, 1, ( 
 ( #8531, #27654 ),
 ( #46786, #61149 ),
 ( #18268, #13566 ),
 ( #5920, #34475 ) ),
 .UNSPECIFIED., .F., .F., .F. ) 
 B_SPLINE_SURFACE_WITH_KNOTS ( ( 4, 4 ),
 ( 2, 2 ),
 ( 0.000000000000000000, 1.000000000000000000 ),
 ( 0.000000000000000000, 1.000000000000000000 ),
 .UNSPECIFIED. ) 
 GEOMETRIC_REPRESENTATION_ITEM ( )  RATIONAL_B_SPLINE_SURFACE ( (
 ( 1.000000000000000000, 1.000000000000000000),
 ( 0.9953040768229005630, 0.8617119497784937465),
 ( 0.9953040768229005630, 0.8617119497784937465),
 ( 1.000000000000000000, 1.000000000000000000) ) ) 
 REPRESENTATION_ITEM ( '' )  SURFACE ( )  );
#46146=VERTEX_POINT ( 'NONE', #13521 ) ;
#46155=CARTESIAN_POINT ( 'NONE',  ( 0.5988103622719990193, 38.53259676306921477, -28.80261254779997770 ) ) ;
#46160=CARTESIAN_POINT ( 'NONE',  ( 0.6031357023905875581, -33.98625823839277160, -34.04794059289636721 ) ) ;
#46161=FACE_OUTER_BOUND ( 'NONE', #56326, .T. ) ;
#46162=CARTESIAN_POINT ( 'NONE',  ( 0.6017667736363752073, -5.933018439714995651, -47.74032759880252996 ) ) ;
#46167=CARTESIAN_POINT ( 'NONE',  ( 1.827119703190779765, 43.03226500438895386, -1.232688548475576074 ) ) ;
#46168=EDGE_LOOP ( 'NONE', ( #7796, #611, #27619, #61040 ) ) ;
#46173=VERTEX_POINT ( 'NONE', #51711 ) ;
#46177=B_SPLINE_CURVE_WITH_KNOTS ( 'NONE', 3,
 ( #13987, #32775, #456, #9562, #19600, #51853 ),
 .UNSPECIFIED., .F., .F.,
 ( 4, 2, 4 ),
 ( 0.000000000000000000, 0.0002450742804987337425, 0.0004901485609974674850 ),
 .UNSPECIFIED. ) ;
#46185=CARTESIAN_POINT ( 'NONE',  ( 4.549368137175248350, 40.58005590356670211, 13.99871866169379508 ) ) ;
#46189=CARTESIAN_POINT ( 'NONE',  ( 0.1103936448916665869, 5.228610780659758526E-15, -43.12443171339897674 ) ) ;
#46196=CARTESIAN_POINT ( 'NONE',  ( -5.995132425357893702, -0.008513469642675032187, -18.84415457712583475 ) ) ;
#46199=CARTESIAN_POINT ( 'NONE',  ( -6.010958268070873523, 2.445171577615762537, 18.68413620842265033 ) ) ;
#46206=CARTESIAN_POINT ( 'NONE',  ( 2.301430502907643838, 37.31003439265366239, 30.25184447737447613 ) ) ;
#46210=CARTESIAN_POINT ( 'NONE',  ( 0.8751705887134553219, -48.08707113907594533, 0.8911681664086766874 ) ) ;
#46211=CARTESIAN_POINT ( 'NONE',  ( 0.7048096507298635682, 11.63498350884336574, -46.68221792389230984 ) ) ;
#46213=ORIENTED_EDGE ( 'NONE', *, *, #50062, .T. ) ;
#46217=CARTESIAN_POINT ( 'NONE',  ( 0.7048096507298635682, -0.8437160066903991451, -48.10291524268441776 ) ) ;
#46218=EDGE_CURVE ( 'NONE', #48340, #60124, #45656, .T. ) ;
#46231=CARTESIAN_POINT ( 'NONE',  ( -6.015611763856276717, 14.95313250337430055, 11.46610900684727952 ) ) ;
#46238=CARTESIAN_POINT ( 'NONE',  ( 3.238741278300274029, 32.96375560769460122, 27.59904135366547351 ) ) ;
#46248=CARTESIAN_POINT ( 'NONE',  ( -6.010958268070873523, -13.33459572764748202, -13.31406649671976794 ) ) ;
#46251=ORIENTED_EDGE ( 'NONE', *, *, #48779, .T. ) ;
#46256=CARTESIAN_POINT ( 'NONE',  ( 0.3622758884714600280, -42.62881903538205108, -6.444611261694439541 ) ) ;
#46258=EDGE_CURVE ( 'NONE', #33003, #43585, #21944, .T. ) ;
#46259=CARTESIAN_POINT ( 'NONE',  ( -4.908599999999999852, 0.000000000000000000, 3.000000000000000000 ) ) ;
#46265=EDGE_CURVE ( 'NONE', #51250, #50661, #57612, .T. ) ;
#46271=EDGE_CURVE ( 'NONE', #19605, #19530, #10621, .T. ) ;
#46274=ORIENTED_EDGE ( 'NONE', *, *, #32549, .T. ) ;
#46276=CARTESIAN_POINT ( 'NONE',  ( 4.549368137175248350, 0.000000000000000000, 0.000000000000000000 ) ) ;
#46287=CARTESIAN_POINT ( 'NONE',  ( 0.1073791018717578927, -26.63563652260192427, 33.91564619577761874 ) ) ;
#46295=CARTESIAN_POINT ( 'NONE',  ( 0.5980894510889448457, -44.71414919659918752, 17.76188940524868443 ) ) ;
#46296=CARTESIAN_POINT ( 'NONE',  ( 0.6023142530420679819, 47.66103033449098803, -6.538792732869364244 ) ) ;
#46300=CARTESIAN_POINT ( 'NONE',  ( 2.643462169533613793, -47.42536612906434357, 7.637863311826802892 ) ) ;
#46301=ORIENTED_EDGE ( 'NONE', *, *, #23189, .T. ) ;
#46305=CARTESIAN_POINT ( 'NONE',  ( -6.017396004339686577, -14.95000090562873396, -11.47005965438154362 ) ) ;
#46308=CARTESIAN_POINT ( 'NONE',  ( 0.3622758884714730732, -17.25816669464967035, -39.50828911766992491 ) ) ;
#46317=CARTESIAN_POINT ( 'NONE',  ( 0.3622758884714730732, 31.06363466427686504, 29.89648521331642428 ) ) ;
#46324=CARTESIAN_POINT ( 'NONE',  ( 0.6009452777970413218, -37.89911497740590818, 29.63106797105349699 ) ) ;
#46329=CARTESIAN_POINT ( 'NONE',  ( 0.09136607875274982415, 0.000000000000000000, 0.000000000000000000 ) ) ;
#46335=CARTESIAN_POINT ( 'NONE',  ( 0.6031356755773454870, 24.05369945659533926, -41.66228085015301730 ) ) ;
#46339=ORIENTED_EDGE ( 'NONE', *, *, #23361, .F. ) ;
#46371=CARTESIAN_POINT ( 'NONE',  ( 0.1102144999581332607, -42.73889315046716320, -5.753800096705892209 ) ) ;
#46379=VECTOR ( 'NONE', #58739, 999.9999999999998863 ) ;
#46386=CARTESIAN_POINT ( 'NONE',  ( 0.8751705887134553219, 46.21789262997757675, -13.30665218149314200 ) ) ;
#46392=B_SPLINE_CURVE_WITH_KNOTS ( 'NONE', 3,
 ( #177, #47212, #19950, #29021, #4259, #52194 ),
 .UNSPECIFIED., .F., .F.,
 ( 4, 2, 4 ),
 ( 8.551243849294126806E-17, 0.0002293366620881463671, 0.0004586733241762071906 ),
 .UNSPECIFIED. ) ;
#46394=( BOUNDED_SURFACE ( )  B_SPLINE_SURFACE ( 3, 1, ( 
 ( #29850, #14847 ),
 ( #52724, #4475 ),
 ( #43678, #9825 ),
 ( #42741, #5408 ) ),
 .UNSPECIFIED., .F., .F., .F. ) 
 B_SPLINE_SURFACE_WITH_KNOTS ( ( 4, 4 ),
 ( 2, 2 ),
 ( 0.000000000000000000, 1.000000000000000000 ),
 ( 0.000000000000000000, 1.000000000000000000 ),
 .UNSPECIFIED. ) 
 GEOMETRIC_REPRESENTATION_ITEM ( )  RATIONAL_B_SPLINE_SURFACE ( (
 ( 1.000000000000000000, 1.000000000000000000),
 ( 0.9953040768229013402, 0.8617119497784988535),
 ( 0.9953040768229013402, 0.8617119497784988535),
 ( 1.000000000000000000, 1.000000000000000000) ) ) 
 REPRESENTATION_ITEM ( '' )  SURFACE ( )  );
#46395=CARTESIAN_POINT ( 'NONE',  ( 0.3622758884714600280, 33.69533458712307095, 26.89560658783397074 ) ) ;
#46396=CARTESIAN_POINT ( 'NONE',  ( 4.549368137175248350, -2.596185425821630588, -42.84816078363929392 ) ) ;
#46400=CARTESIAN_POINT ( 'NONE',  ( 0.7246131072078559887, -38.65593150731067595, 28.62741613354226544 ) ) ;
#46404=CARTESIAN_POINT ( 'NONE',  ( -6.001507490154110336, 4.892199142591303840, 18.19774963328910289 ) ) ;
#46413=CARTESIAN_POINT ( 'NONE',  ( 0.6017666602106489515, 29.56224131406219158, 37.95277954208646065 ) ) ;
#46416=ADVANCED_FACE ( 'NONE', ( #1094 ), #52888, .F. ) ;
#46417=ORIENTED_EDGE ( 'NONE', *, *, #10726, .F. ) ;
#46418=CARTESIAN_POINT ( 'NONE',  ( 0.1313383488274124378, -42.83318330237621296, -4.995828979989310525 ) ) ;
#46421=B_SPLINE_CURVE_WITH_KNOTS ( 'NONE', 3,
 ( #27046, #12971, #55222, #12346, #50533, #26735 ),
 .UNSPECIFIED., .F., .F.,
 ( 4, 2, 4 ),
 ( 1.268664800107929448E-16, 0.0002450741128632364079, 0.0004901482257263459642 ),
 .UNSPECIFIED. ) ;
#46430=CARTESIAN_POINT ( 'NONE',  ( 4.691466044806103852, -29.14742760351135331, 33.74235639413277710 ) ) ;
#46440=B_SPLINE_CURVE_WITH_KNOTS ( 'NONE', 3,
 ( #34289, #9233, #53367, #47461 ),
 .UNSPECIFIED., .F., .F.,
 ( 4, 4 ),
 ( 0.000000000000000000, 0.004445488388166992516 ),
 .UNSPECIFIED. ) ;
#46443=CARTESIAN_POINT ( 'NONE',  ( -2.708315649062916552, 14.06540004355482587, -4.041664582652659377 ) ) ;
#46455=EDGE_CURVE ( 'NONE', #17061, #58789, #24035, .T. ) ;
#46460=CARTESIAN_POINT ( 'NONE',  ( 0.8751705887134553219, 48.08707113907595243, -0.8911681664083408450 ) ) ;
#46462=CARTESIAN_POINT ( 'NONE',  ( -6.015611763856276717, -7.216738110653404981, 17.40650793417841413 ) ) ;
#46483=EDGE_CURVE ( 'NONE', #12277, #24298, #16145, .T. ) ;
#46484=( BOUNDED_SURFACE ( )  B_SPLINE_SURFACE ( 3, 1, ( 
 ( #9552, #4830 ),
 ( #53379, #33694 ),
 ( #15195, #29274 ),
 ( #28662, #57146 ) ),
 .UNSPECIFIED., .F., .F., .F. ) 
 B_SPLINE_SURFACE_WITH_KNOTS ( ( 4, 4 ),
 ( 2, 2 ),
 ( 0.000000000000000000, 1.000000000000000000 ),
 ( 0.000000000000000000, 1.000000000000000000 ),
 .UNSPECIFIED. ) 
 GEOMETRIC_REPRESENTATION_ITEM ( )  RATIONAL_B_SPLINE_SURFACE ( (
 ( 1.000000000000000000, 1.000000000000000000),
 ( 0.9953040768229005630, 0.8617119497784937465),
 ( 0.9953040768229005630, 0.8617119497784937465),
 ( 1.000000000000000000, 1.000000000000000000) ) ) 
 REPRESENTATION_ITEM ( '' )  SURFACE ( )  );
#46490=CARTESIAN_POINT ( 'NONE',  ( 2.301529144917016101, 25.12312032040453147, 40.93948199333342330 ) ) ;
#46497=VERTEX_POINT ( 'NONE', #45282 ) ;
#46500=CARTESIAN_POINT ( 'NONE',  ( 0.8751705887134423323, 33.37254303619506857, 34.63284514348596588 ) ) ;
#46501=CARTESIAN_POINT ( 'NONE',  ( -2.708315649062910779, -10.16016146078282034, -10.53288422393052315 ) ) ;
#46502=( BOUNDED_SURFACE ( )  B_SPLINE_SURFACE ( 3, 1, ( 
 ( #56257, #4860 ),
 ( #23992, #47499 ),
 ( #33409, #27453 ),
 ( #43122, #158 ) ),
 .UNSPECIFIED., .F., .F., .F. ) 
 B_SPLINE_SURFACE_WITH_KNOTS ( ( 4, 4 ),
 ( 2, 2 ),
 ( 0.000000000000000000, 1.000000000000000000 ),
 ( 0.000000000000000000, 1.000000000000000000 ),
 .UNSPECIFIED. ) 
 GEOMETRIC_REPRESENTATION_ITEM ( )  RATIONAL_B_SPLINE_SURFACE ( (
 ( 1.000000000000000000, 1.000000000000000000),
 ( 0.9953040768229005630, 0.8617119497784937465),
 ( 0.9953040768229005630, 0.8617119497784937465),
 ( 1.000000000000000000, 1.000000000000000000) ) ) 
 REPRESENTATION_ITEM ( '' )  SURFACE ( )  );
#46506=CARTESIAN_POINT ( 'NONE',  ( 0.5998501479064708430, 24.50586714782604858, -41.39809967730462859 ) ) ;
#46507=B_SPLINE_CURVE_WITH_KNOTS ( 'NONE', 3,
 ( #57947, #43911, #15072, #25690 ),
 .UNSPECIFIED., .F., .F.,
 ( 4, 4 ),
 ( 0.000000000000000000, 0.005014147105413702989 ),
 .UNSPECIFIED. ) ;
#46508=CARTESIAN_POINT ( 'NONE',  ( 0.1103744047535531458, 39.85659247569260089, -16.46720136312940852 ) ) ;
#46510=CARTESIAN_POINT ( 'NONE',  ( 0.3622758884714730732, 42.84426538328725798, 4.808133778522027058 ) ) ;
#46517=CARTESIAN_POINT ( 'NONE',  ( 4.549368137175248350, -28.46244473166650479, -32.13400537129916046 ) ) ;
#46520=B_SPLINE_CURVE_WITH_KNOTS ( 'NONE', 3,
 ( #33623, #43340, #8554, #5988 ),
 .UNSPECIFIED., .F., .F.,
 ( 4, 4 ),
 ( 4.336808689942017736E-18, 0.004566006591234645501 ),
 .UNSPECIFIED. ) ;
#46531=CARTESIAN_POINT ( 'NONE',  ( -5.995132425357893702, -18.68182899165009658, -2.468096378288315851 ) ) ;
#46532=CARTESIAN_POINT ( 'NONE',  ( 0.5998501479064708430, -33.64490850298820845, -34.38546660123286358 ) ) ;
#46539=CARTESIAN_POINT ( 'NONE',  ( 4.549368137175248350, 0.000000000000000000, 0.000000000000000000 ) ) ;
#46545=CARTESIAN_POINT ( 'NONE',  ( 0.3622758884714730732, -6.444611261694294768, -42.62881903538208661 ) ) ;
#46546=EDGE_LOOP ( 'NONE', ( #18571, #16665, #11769, #49629 ) ) ;
#46547=ORIENTED_EDGE ( 'NONE', *, *, #54153, .F. ) ;
#46550=CARTESIAN_POINT ( 'NONE',  ( 0.5998501479064699549, 47.62484632993687939, -6.798102206413639159 ) ) ;
#46561=CARTESIAN_POINT ( 'NONE',  ( 0.5980894510889448457, 46.28687279963673973, 13.12879507229304288 ) ) ;
#46568=CARTESIAN_POINT ( 'NONE',  ( 0.3622758884714600280, 11.95365414648497193, -41.42293301073613776 ) ) ;
#46569=ORIENTED_EDGE ( 'NONE', *, *, #52231, .F. ) ;
#46574=CARTESIAN_POINT ( 'NONE',  ( 0.6009453534118438522, -47.63713118507423161, -6.711694149738057114 ) ) ;
#46578=EDGE_CURVE ( 'NONE', #48340, #19272, #42037, .T. ) ;
#46584=CARTESIAN_POINT ( 'NONE',  ( 0.6041374136657476912, 6.452348380035281217, 47.67304777898701218 ) ) ;
#46585=( BOUNDED_SURFACE ( )  B_SPLINE_SURFACE ( 3, 1, ( 
 ( #32653, #56432 ),
 ( #52045, #13546 ),
 ( #38293, #23246 ),
 ( #28243, #334 ) ),
 .UNSPECIFIED., .F., .F., .F. ) 
 B_SPLINE_SURFACE_WITH_KNOTS ( ( 4, 4 ),
 ( 2, 2 ),
 ( 0.000000000000000000, 1.000000000000000000 ),
 ( 0.000000000000000000, 1.000000000000000000 ),
 .UNSPECIFIED. ) 
 GEOMETRIC_REPRESENTATION_ITEM ( )  RATIONAL_B_SPLINE_SURFACE ( (
 ( 1.000000000000000000, 1.000000000000000000),
 ( 0.7223157951917476005, 0.9931996967497186413),
 ( 0.7223157951917476005, 0.9931996967497186413),
 ( 1.000000000000000000, 1.000000000000000000) ) ) 
 REPRESENTATION_ITEM ( '' )  SURFACE ( )  );
#46587=CARTESIAN_POINT ( 'NONE',  ( -6.016761891674565099, 13.32657647165373760, -13.32172022638577680 ) ) ;
#46589=CARTESIAN_POINT ( 'NONE',  ( 0.6041374136657476912, -0.1745662470641466957, -48.10739871142803992 ) ) ;
#46600=CARTESIAN_POINT ( 'NONE',  ( 0.6030672727741701600, 47.70721108823349255, -6.192762795893955285 ) ) ;
#46614=CIRCLE ( 'NONE', #55558, 42.92674063221959813 ) ;
#46615=CARTESIAN_POINT ( 'NONE',  ( 0.2885697896453121025, -11.93479333319053559, 41.43179225254745290 ) ) ;
#46620=CARTESIAN_POINT ( 'NONE',  ( 0.6025881611877910160, 38.03302298778302770, 29.45877655626806657 ) ) ;
#46624=EDGE_CURVE ( 'NONE', #60046, #32260, #38257, .T. ) ;
#46634=EDGE_CURVE ( 'NONE', #4388, #5237, #16609, .T. ) ;
#46639=CARTESIAN_POINT ( 'NONE',  ( 0.6023143664670691511, 24.28012784216878117, -41.53077189784239209 ) ) ;
#46640=EDGE_CURVE ( 'NONE', #47578, #9208, #47127, .T. ) ;
#46644=VERTEX_POINT ( 'NONE', #3867 ) ;
#46645=CARTESIAN_POINT ( 'NONE',  ( 0.8760168074887076939, 29.98565522133296213, 37.61398439004543803 ) ) ;
#46646=CARTESIAN_POINT ( 'NONE',  ( 0.1313383488274112720, 22.11173226734840469, 37.02311703718862645 ) ) ;
#46659=EDGE_CURVE ( 'NONE', #51385, #59613, #3727, .T. ) ;
#46660=ORIENTED_EDGE ( 'NONE', *, *, #55667, .F. ) ;
#46665=DIRECTION ( 'NONE',  ( 0.09835009131224552170, 0.8656670924898548503, 0.4908642831975393306 ) ) ;
#46666=CARTESIAN_POINT ( 'NONE',  ( 0.1100053167205930771, -16.33707796615732377, 39.91014771056750021 ) ) ;
#46691=CARTESIAN_POINT ( 'NONE',  ( 0.1073791018717483448, 5.147744207006859973, -42.81622261970989030 ) ) ;
#46694=CARTESIAN_POINT ( 'NONE',  ( -2.708315649062916552, -14.06540004355485252, 4.041664582652561677 ) ) ;
#46696=CARTESIAN_POINT ( 'NONE',  ( 0.1087620492084205442, 21.87505161834417322, -37.16461718700644923 ) ) ;
#46702=CARTESIAN_POINT ( 'NONE',  ( 2.643462169533600914, 17.09809940585597232, 44.89050350746158102 ) ) ;
#46705=( BOUNDED_SURFACE ( )  B_SPLINE_SURFACE ( 3, 1, ( 
 ( #82, #19534 ),
 ( #51790, #38649 ),
 ( #57703, #14834 ),
 ( #33943, #61483 ) ),
 .UNSPECIFIED., .F., .F., .F. ) 
 B_SPLINE_SURFACE_WITH_KNOTS ( ( 4, 4 ),
 ( 2, 2 ),
 ( 0.000000000000000000, 1.000000000000000000 ),
 ( 0.000000000000000000, 1.000000000000000000 ),
 .UNSPECIFIED. ) 
 GEOMETRIC_REPRESENTATION_ITEM ( )  RATIONAL_B_SPLINE_SURFACE ( (
 ( 1.000000000000000000, 1.000000000000000000),
 ( 0.7223157951917480446, 0.9931996967497186413),
 ( 0.7223157951917480446, 0.9931996967497186413),
 ( 1.000000000000000000, 1.000000000000000000) ) ) 
 REPRESENTATION_ITEM ( '' )  SURFACE ( )  );
#46709=ORIENTED_EDGE ( 'NONE', *, *, #25322, .F. ) ;
#46711=CARTESIAN_POINT ( 'NONE',  ( 0.3622758884714600280, 25.58609868863721459, 34.70015533914837391 ) ) ;
#46720=CARTESIAN_POINT ( 'NONE',  ( -6.016761891674565099, 18.68153697670641833, 2.462934516563870080 ) ) ;
#46721=CARTESIAN_POINT ( 'NONE',  ( 0.8760168074886965917, -5.394043284319169018, -47.80016357497247981 ) ) ;
#46724=CARTESIAN_POINT ( 'NONE',  ( 0.6023142530420679819, 29.49327578399137195, 38.00626667377531476 ) ) ;
#46726=ORIENTED_EDGE ( 'NONE', *, *, #4112, .F. ) ;
#46728=ORIENTED_EDGE ( 'NONE', *, *, #41598, .T. ) ;
#46729=CARTESIAN_POINT ( 'NONE',  ( -6.016761891674565099, 4.873659902332367011, 18.20201388312097279 ) ) ;
#46730=ORIENTED_EDGE ( 'NONE', *, *, #37947, .T. ) ;
#46731=CARTESIAN_POINT ( 'NONE',  ( 5.880360259849752858, -43.00389496650600307, -21.25991003419937542 ) ) ;
#46736=EDGE_LOOP ( 'NONE', ( #41364, #61607, #28746, #1683 ) ) ;
#46738=( GEOMETRIC_REPRESENTATION_CONTEXT ( 3 ) GLOBAL_UNCERTAINTY_ASSIGNED_CONTEXT ( ( #46799 ) ) GLOBAL_UNIT_ASSIGNED_CONTEXT ( ( #50445, #58904, #49829 ) ) REPRESENTATION_CONTEXT ( 'NONE', 'WORKASPACE' ) );
#46748=ORIENTED_EDGE ( 'NONE', *, *, #55638, .T. ) ;
#46763=CARTESIAN_POINT ( 'NONE',  ( 1.827119703190777988, 39.28489939038887258, -17.60659059422136608 ) ) ;
#46770=ADVANCED_FACE ( 'NONE', ( #5402 ), #2701, .F. ) ;
#46773=ADVANCED_FACE ( 'NONE', ( #9503 ), #39751, .F. ) ;
#46776=CARTESIAN_POINT ( 'NONE',  ( 0.3622758884714730732, -15.73321244754880688, 40.13994584881756111 ) ) ;
#46782=( BOUNDED_SURFACE ( )  B_SPLINE_SURFACE ( 3, 1, ( 
 ( #6499, #30333 ),
 ( #6192, #12188 ),
 ( #59770, #44780 ),
 ( #35375, #54431 ) ),
 .UNSPECIFIED., .F., .F., .F. ) 
 B_SPLINE_SURFACE_WITH_KNOTS ( ( 4, 4 ),
 ( 2, 2 ),
 ( 0.000000000000000000, 1.000000000000000000 ),
 ( 0.000000000000000000, 1.000000000000000000 ),
 .UNSPECIFIED. ) 
 GEOMETRIC_REPRESENTATION_ITEM ( )  RATIONAL_B_SPLINE_SURFACE ( (
 ( 1.000000000000000000, 1.000000000000000000),
 ( 0.9953040768229005630, 0.8617119497784937465),
 ( 0.9953040768229005630, 0.8617119497784937465),
 ( 1.000000000000000000, 1.000000000000000000) ) ) 
 REPRESENTATION_ITEM ( '' )  SURFACE ( )  );
#46784=LINE ( 'NONE', #9461, #34302 ) ;
#46786=CARTESIAN_POINT ( 'NONE',  ( -6.016104459813374383, -9.416989654584190461, -16.32137543786092237 ) ) ;
#46799=UNCERTAINTY_MEASURE_WITH_UNIT (LENGTH_MEASURE( 1.000000000000000082E-05 ), #50445, 'distance_accuracy_value', 'NONE');
#46805=ORIENTED_EDGE ( 'NONE', *, *, #60703, .T. ) ;
#46821=CARTESIAN_POINT ( 'NONE',  ( -6.017396004339687465, -13.32495836419633761, 13.32329839588550335 ) ) ;
#46827=DIRECTION ( 'NONE',  ( 0.1024043820194936449, 0.9844298967354735419, -0.1428674944015972947 ) ) ;
#46828=CARTESIAN_POINT ( 'NONE',  ( 0.1092565886968785704, 39.72209809039397754, -16.78938711553589158 ) ) ;
#46834=CIRCLE ( 'NONE', #54797, 47.91270532121795611 ) ;
#46846=EDGE_CURVE ( 'NONE', #42831, #28832, #50211, .T. ) ;
#46857=CARTESIAN_POINT ( 'NONE',  ( 0.1073791018717483448, 42.81622261970987608, 5.147744207007008299 ) ) ;
#46864=CARTESIAN_POINT ( 'NONE',  ( 0.6030672727741701600, -46.44558360017003906, -12.53539249098698427 ) ) ;
#46870=EDGE_CURVE ( 'NONE', #7624, #5090, #6806, .T. ) ;
#46875=CARTESIAN_POINT ( 'NONE',  ( 0.1081432562775997419, 6.048481838666034172, -42.69830087850306199 ) ) ;
#46882=CARTESIAN_POINT ( 'NONE',  ( 4.691466044806103852, 3.249105306917819735, 44.46979273209136352 ) ) ;
#46887=CARTESIAN_POINT ( 'NONE',  ( 0.1073791018717578927, 11.62916352156150346, -41.52698815987157133 ) ) ;
#46890=CONICAL_SURFACE ( 'NONE', #15892, 42.92674063221959813, 1.485477209440487556 ) ;
#46891=ORIENTED_EDGE ( 'NONE', *, *, #6820, .F. ) ;
#46892=CARTESIAN_POINT ( 'NONE',  ( 0.6031356755773454870, -47.69588082432152021, -6.279255973231177457 ) ) ;
#46896=B_SPLINE_CURVE_WITH_KNOTS ( 'NONE', 3,
 ( #26537, #13078, #50639, #31238, #26851, #12157 ),
 .UNSPECIFIED., .F., .F.,
 ( 4, 2, 4 ),
 ( 1.265278335494562270E-16, 0.0002450741128632358658, 0.0004901482257263452052 ),
 .UNSPECIFIED. ) ;
#46916=ORIENTED_EDGE ( 'NONE', *, *, #134, .F. ) ;
#46919=CARTESIAN_POINT ( 'NONE',  ( -6.016761891674564211, 17.40752468084793136, -7.214149619366169830 ) ) ;
#46920=LINE ( 'NONE', #51894, #25766 ) ;
#46922=EDGE_CURVE ( 'NONE', #13823, #46085, #55737, .T. ) ;
#46923=CARTESIAN_POINT ( 'NONE',  ( 5.880360259849739535, 21.25991003419893488, 43.00389496650622334 ) ) ;
#46926=VERTEX_POINT ( 'NONE', #32639 ) ;
#46936=CARTESIAN_POINT ( 'NONE',  ( 0.5998501479064708430, 47.62484632993678701, 6.798102206414301740 ) ) ;
#46948=CARTESIAN_POINT ( 'NONE',  ( 0.5998501479064699549, -37.84527566984877467, 29.69975237324549155 ) ) ;
#46954=ORIENTED_EDGE ( 'NONE', *, *, #60895, .F. ) ;
#46956=CARTESIAN_POINT ( 'NONE',  ( 4.549368137175248350, 0.000000000000000000, 0.000000000000000000 ) ) ;
#46961=EDGE_LOOP ( 'NONE', ( #18196, #61845, #42626, #8934 ) ) ;
#46972=EDGE_CURVE ( 'NONE', #58372, #5948, #42683, .T. ) ;
#46974=EDGE_LOOP ( 'NONE', ( #10004, #12347, #60769, #22598 ) ) ;
#46978=VERTEX_POINT ( 'NONE', #17609 ) ;
#46980=CARTESIAN_POINT ( 'NONE',  ( 0.6031356755773454870, -34.01708126935065479, 34.01711753073199418 ) ) ;
#46988=ORIENTED_EDGE ( 'NONE', *, *, #56222, .T. ) ;
#46989=B_SPLINE_CURVE_WITH_KNOTS ( 'NONE', 3,
 ( #9028, #51623, #61325, #22825 ),
 .UNSPECIFIED., .F., .F.,
 ( 4, 4 ),
 ( 2.294131830766625192E-17, 0.004564976165746188579 ),
 .UNSPECIFIED. ) ;
#46995=FACE_OUTER_BOUND ( 'NONE', #25380, .T. ) ;
#47010=CARTESIAN_POINT ( 'NONE',  ( 0.1073791018717578927, -16.05399293000789385, -40.02496097243051310 ) ) ;
#47011=AXIS2_PLACEMENT_3D ( 'NONE', #6146, #25908, #40340 ) ;
#47018=ORIENTED_EDGE ( 'NONE', *, *, #34041, .T. ) ;
#47030=( BOUNDED_SURFACE ( )  B_SPLINE_SURFACE ( 3, 1, ( 
 ( #37982, #52646 ),
 ( #38281, #33267 ),
 ( #42660, #27935 ),
 ( #57956, #14465 ) ),
 .UNSPECIFIED., .F., .F., .F. ) 
 B_SPLINE_SURFACE_WITH_KNOTS ( ( 4, 4 ),
 ( 2, 2 ),
 ( 0.000000000000000000, 1.000000000000000000 ),
 ( 0.000000000000000000, 1.000000000000000000 ),
 .UNSPECIFIED. ) 
 GEOMETRIC_REPRESENTATION_ITEM ( )  RATIONAL_B_SPLINE_SURFACE ( (
 ( 1.000000000000000000, 1.000000000000000000),
 ( 0.9953040768229013402, 0.8617119497784988535),
 ( 0.9953040768229013402, 0.8617119497784988535),
 ( 1.000000000000000000, 1.000000000000000000) ) ) 
 REPRESENTATION_ITEM ( '' )  SURFACE ( )  );
#47032=CARTESIAN_POINT ( 'NONE',  ( 0.7954196712028465122, 46.22745629466055561, 13.28627209367592954 ) ) ;
#47041=EDGE_CURVE ( 'NONE', #61654, #42964, #58277, .T. ) ;
#47053=EDGE_CURVE ( 'NONE', #11266, #56932, #10374, .T. ) ;
#47054=CARTESIAN_POINT ( 'NONE',  ( -6.017396004339687465, 9.420565012089426205, 16.31924478664278766 ) ) ;
#47064=CARTESIAN_POINT ( 'NONE',  ( 0.2885700199627532769, -37.73587457854652882, -20.85752789928049111 ) ) ;
#47065=CARTESIAN_POINT ( 'NONE',  ( 0.8751705887134553219, 48.08707113907595243, -0.8911681664083408450 ) ) ;
#47073=FACE_OUTER_BOUND ( 'NONE', #40940, .T. ) ;
#47081=CARTESIAN_POINT ( 'NONE',  ( 0.1103878639767399417, -21.52017980327924462, 37.37111717125835497 ) ) ;
#47082=CARTESIAN_POINT ( 'NONE',  ( -6.017396004339687465, -11.47005965438128783, -14.95000090562892936 ) ) ;
#47084=ADVANCED_FACE ( 'NONE', ( #11293 ), #60742, .T. ) ;
#47085=CARTESIAN_POINT ( 'NONE',  ( 4.975801465491694664, 46.87746200127440943, 9.906103548668390602 ) ) ;
#47099=ORIENTED_EDGE ( 'NONE', *, *, #8249, .T. ) ;
#47100=CARTESIAN_POINT ( 'NONE',  ( 0.6028618097248863439, -38.27229381545031828, -29.14732267129559773 ) ) ;
#47111=CARTESIAN_POINT ( 'NONE',  ( 0.1103310638050661735, 0.08238894504395631591, -43.12437788119554227 ) ) ;
#47116=CARTESIAN_POINT ( 'NONE',  ( 0.5980894510889448457, -38.59343625445466586, 28.72954109785538890 ) ) ;
#47118=ORIENTED_EDGE ( 'NONE', *, *, #36588, .F. ) ;
#47120=CARTESIAN_POINT ( 'NONE',  ( 0.6001305935487422083, 34.38748867424712330, -33.64689939321907275 ) ) ;
#47123=CARTESIAN_POINT ( 'NONE',  ( -6.016104459813374383, 11.46679299034580168, 14.95258000663136499 ) ) ;
#47127=LINE ( 'NONE', #37421, #8751 ) ;
#47129=CARTESIAN_POINT ( 'NONE',  ( 0.1087620492084205581, 39.97903073778065419, -16.16798550313382066 ) ) ;
#47134=EDGE_LOOP ( 'NONE', ( #60180, #20590, #22379, #14673 ) ) ;
#47137=CARTESIAN_POINT ( 'NONE',  ( 0.1103310638050662013, -42.76619676553140437, 5.547176740492814950 ) ) ;
#47147=B_SPLINE_CURVE_WITH_KNOTS ( 'NONE', 3,
 ( #33836, #52599, #10320, #1210 ),
 .UNSPECIFIED., .F., .F.,
 ( 4, 4 ),
 ( 6.254634441385501517E-18, 0.004566006591234643766 ),
 .UNSPECIFIED. ) ;
#47148=CARTESIAN_POINT ( 'NONE',  ( -6.001507490154111224, 2.475062734132707387, -18.68062548815622748 ) ) ;
#47157=CARTESIAN_POINT ( 'NONE',  ( 0.1103878639767399278, 42.76182653383950338, 5.580746265797182026 ) ) ;
#47159=CARTESIAN_POINT ( 'NONE',  ( 4.975801465491695552, -21.70134120755170315, -42.71626295676257001 ) ) ;
#47162=CARTESIAN_POINT ( 'NONE',  ( 4.975801465491695552, 0.000000000000000000, 0.000000000000000000 ) ) ;
#47172=CARTESIAN_POINT ( 'NONE',  ( 0.5998501479064699549, -44.64337787626236320, -17.92509395669093308 ) ) ;
#47177=CARTESIAN_POINT ( 'NONE',  ( -6.016104459813371719, -18.20253432612963351, -4.871830707673248995 ) ) ;
#47197=CARTESIAN_POINT ( 'NONE',  ( 0.8751705887134423323, -38.69254731947852832, 28.56654290188588163 ) ) ;
#47198=B_SPLINE_CURVE_WITH_KNOTS ( 'NONE', 3,
 ( #19426, #53526, #4662, #33845, #9389, #10641, #52921, #28491, #24113, #29118, #23811, #5897, #42939, #26939, #2764, #30044, #45104, #7140, #30347 ),
 .UNSPECIFIED., .F., .F.,
 ( 4, 3, 3, 3, 3, 3, 4 ),
 ( 1.149162571898268292E-16, 0.0002618519381806242905, 0.0003927759815485966258, 0.0005237000248299457069, 0.0006546240681324996683, 0.0007855481115631327092, 0.0009699050456655109419 ),
 .UNSPECIFIED. ) ;
#47212=CARTESIAN_POINT ( 'NONE',  ( 0.2885700199627515561, 26.88157179738457714, 33.71073713194529375 ) ) ;
#47213=CARTESIAN_POINT ( 'NONE',  ( 0.6028618097248864549, 47.67286800277443604, -6.452328974163124009 ) ) ;
#47217=( BOUNDED_SURFACE ( )  B_SPLINE_SURFACE ( 3, 1, ( 
 ( #21742, #35858 ),
 ( #45567, #50857 ),
 ( #50544, #27060 ),
 ( #40569, #2620 ) ),
 .UNSPECIFIED., .F., .F., .F. ) 
 B_SPLINE_SURFACE_WITH_KNOTS ( ( 4, 4 ),
 ( 2, 2 ),
 ( 0.000000000000000000, 1.000000000000000000 ),
 ( 0.000000000000000000, 1.000000000000000000 ),
 .UNSPECIFIED. ) 
 GEOMETRIC_REPRESENTATION_ITEM ( )  RATIONAL_B_SPLINE_SURFACE ( (
 ( 1.000000000000000000, 1.000000000000000000),
 ( 0.9953040768229013402, 0.8617119497784988535),
 ( 0.9953040768229013402, 0.8617119497784988535),
 ( 1.000000000000000000, 1.000000000000000000) ) ) 
 REPRESENTATION_ITEM ( '' )  SURFACE ( )  );
#47218=CARTESIAN_POINT ( 'NONE',  ( 4.549368137175248350, 35.80950303116068056, 23.67244292351653101 ) ) ;
#47220=DIRECTION ( 'NONE',  ( 0.09835009131224567436, -0.7847759187265501701, -0.6119264800004754479 ) ) ;
#47229=CARTESIAN_POINT ( 'NONE',  ( 0.6017667736363750963, 47.64919355032679249, 6.625250263233795067 ) ) ;
#47236=CARTESIAN_POINT ( 'NONE',  ( 0.8751705887134423323, 28.56654290188602019, 38.69254731947842885 ) ) ;
#47240=CARTESIAN_POINT ( 'NONE',  ( 0.6254087463353918963, -42.00124903776053031, -23.45485308995585072 ) ) ;
#47247=DIRECTION ( 'NONE',  ( -1.000000000000000000, -0.000000000000000000, -0.000000000000000000 ) ) ;
#47251=VERTEX_POINT ( 'NONE', #23742 ) ;
#47252=B_SPLINE_CURVE_WITH_KNOTS ( 'NONE', 3,
 ( #29231, #18616, #13613, #52107 ),
 .UNSPECIFIED., .F., .F.,
 ( 4, 4 ),
 ( 0.000000000000000000, 0.004445488388166994251 ),
 .UNSPECIFIED. ) ;
#47255=ORIENTED_EDGE ( 'NONE', *, *, #8687, .F. ) ;
#47257=CARTESIAN_POINT ( 'NONE',  ( 0.1103878639767399278, 26.29099398937401588, 34.18336104662747488 ) ) ;
#47258=EDGE_CURVE ( 'NONE', #39651, #22299, #10265, .T. ) ;
#47260=CARTESIAN_POINT ( 'NONE',  ( 3.238741278300274917, 23.06029422819004182, -36.28414388564873150 ) ) ;
#47273=CARTESIAN_POINT ( 'NONE',  ( 0.1073791018717578927, 5.147744207006301309, 42.81622261970996135 ) ) ;
#47276=CARTESIAN_POINT ( 'NONE',  ( -5.995132425357893702, -7.203480333238950095, -17.41298668506978231 ) ) ;
#47279=ORIENTED_EDGE ( 'NONE', *, *, #57680, .F. ) ;
#47284=CARTESIAN_POINT ( 'NONE',  ( 0.1064266418746775827, -42.67882141624140502, -6.185136754498182121 ) ) ;
#47287=CARTESIAN_POINT ( 'NONE',  ( 4.975801465491695552, -14.85979367497206205, 45.55012473237727733 ) ) ;
#47299=EDGE_CURVE ( 'NONE', #57072, #44468, #52294, .T. ) ;
#47300=CARTESIAN_POINT ( 'NONE',  ( 4.975801465491694664, -39.51822597168476392, -27.09127437476367106 ) ) ;
#47312=CARTESIAN_POINT ( 'NONE',  ( 0.7048096507298635682, 13.26491767067451200, 46.24547838151373469 ) ) ;
#47314=ORIENTED_EDGE ( 'NONE', *, *, #23346, .F. ) ;
#47318=ORIENTED_EDGE ( 'NONE', *, *, #3639, .T. ) ;
#47327=ORIENTED_EDGE ( 'NONE', *, *, #47624, .F. ) ;
#47330=ORIENTED_EDGE ( 'NONE', *, *, #45962, .T. ) ;
#47335=CARTESIAN_POINT ( 'NONE',  ( 3.238741278300274917, 42.82436441900173207, -3.793425828152205970 ) ) ;
#47337=ORIENTED_EDGE ( 'NONE', *, *, #5891, .F. ) ;
#47345=CARTESIAN_POINT ( 'NONE',  ( 4.691466044806103852, -33.30232861642453202, 29.64918311951070606 ) ) ;
#47349=ORIENTED_EDGE ( 'NONE', *, *, #39792, .T. ) ;
#47350=LINE ( 'NONE', #10064, #53498 ) ;
#47360=CARTESIAN_POINT ( 'NONE',  ( 4.975801465491694664, -20.67815041659109809, -43.22084481528213473 ) ) ;
#47368=EDGE_CURVE ( 'NONE', #3337, #32695, #46834, .T. ) ;
#47369=CARTESIAN_POINT ( 'NONE',  ( 0.3622758884714600280, -29.89648521331609743, -31.06363466427717412 ) ) ;
#47375=CARTESIAN_POINT ( 'NONE',  ( 0.6001305935487315502, -41.40054608060276564, -24.50730504006443411 ) ) ;
#47393=VERTEX_POINT ( 'NONE', #36661 ) ;
#47397=ORIENTED_EDGE ( 'NONE', *, *, #13547, .T. ) ;
#47401=ORIENTED_EDGE ( 'NONE', *, *, #24867, .F. ) ;
#47408=CARTESIAN_POINT ( 'NONE',  ( 0.1095718737110178698, -30.31138510522973561, -30.67477146794362497 ) ) ;
#47409=ORIENTED_EDGE ( 'NONE', *, *, #36380, .T. ) ;
#47414=FACE_OUTER_BOUND ( 'NONE', #1418, .T. ) ;
#47419=CARTESIAN_POINT ( 'NONE',  ( 0.1098349054025746646, 5.417317591399238630, 42.78286259078964804 ) ) ;
#47420=CARTESIAN_POINT ( 'NONE',  ( 0.3622758884714730732, 29.89648521331631414, -31.06363466427696807 ) ) ;
#47421=EDGE_CURVE ( 'NONE', #43089, #15076, #13496, .T. ) ;
#47422=EDGE_LOOP ( 'NONE', ( #30084, #43958, #22278, #51713 ) ) ;
#47429=FACE_OUTER_BOUND ( 'NONE', #26987, .T. ) ;
#47430=CARTESIAN_POINT ( 'NONE',  ( 0.7246131072078572100, 46.66866179549018057, -11.65529928397590531 ) ) ;
#47433=CARTESIAN_POINT ( 'NONE',  ( 0.1073791018717578927, -39.65380858626204486, -16.95003405440299460 ) ) ;
#47450=ADVANCED_FACE ( 'NONE', ( #7182 ), #9342, .F. ) ;
#47452=CARTESIAN_POINT ( 'NONE',  ( 0.8760168074886965917, 38.69913431881823129, -28.57146030081939259 ) ) ;
#47459=CARTESIAN_POINT ( 'NONE',  ( 2.301430502907645170, -34.86297247504497676, 33.04218380901160401 ) ) ;
#47461=CARTESIAN_POINT ( 'NONE',  ( 0.8751705887134423323, -44.08562551107069538, -19.22545746485646490 ) ) ;
#47462=EDGE_CURVE ( 'NONE', #32330, #40711, #56349, .T. ) ;
#47463=CARTESIAN_POINT ( 'NONE',  ( 0.6027935024548038978, -46.42277558035033991, -12.61964268015540647 ) ) ;
#47464=VERTEX_POINT ( 'NONE', #32891 ) ;
#47467=CARTESIAN_POINT ( 'NONE',  ( 0.1092565886968784733, 39.95965440403623603, 16.21587544131337921 ) ) ;
#47468=EDGE_CURVE ( 'NONE', #15890, #16986, #33820, .T. ) ;
#47470=EDGE_LOOP ( 'NONE', ( #54921, #45682, #32293, #58441 ) ) ;
#47473=CARTESIAN_POINT ( 'NONE',  ( 0.1104177457020372871, 5.624018123398638380, -42.75615561261995623 ) ) ;
#47476=ORIENTED_EDGE ( 'NONE', *, *, #45796, .T. ) ;
#47496=AXIS2_PLACEMENT_3D ( 'NONE', #40300, #26160, #45917 ) ;
#47499=CARTESIAN_POINT ( 'NONE',  ( 0.7048096507298635682, 28.61383451045698223, -38.67623024744019489 ) ) ;
#47500=CARTESIAN_POINT ( 'NONE',  ( 0.2885697896453113254, -42.84523253470164406, 4.828949182955208919 ) ) ;
#47501=CARTESIAN_POINT ( 'NONE',  ( 0.2885697896453122135, 25.60460893337430477, 34.69058521462543609 ) ) ;
#47512=B_SPLINE_CURVE_WITH_KNOTS ( 'NONE', 3,
 ( #55000, #7378, #50013, #30278 ),
 .UNSPECIFIED., .F., .F.,
 ( 4, 4 ),
 ( 2.302551629917872730E-17, 0.004564976165746187711 ),
 .UNSPECIFIED. ) ;
#47519=CARTESIAN_POINT ( 'NONE',  ( 0.1103310638050662429, 16.57910240621641762, -39.81020119244065114 ) ) ;
#47524=CARTESIAN_POINT ( 'NONE',  ( 4.975801465491695552, 0.000000000000000000, 0.000000000000000000 ) ) ;
#47527=CARTESIAN_POINT ( 'NONE',  ( 0.1310142868023694562, -11.77532653407867436, 41.48473022063161153 ) ) ;
#47529=CARTESIAN_POINT ( 'NONE',  ( -6.010958268070873523, 9.409153349053585913, 16.32616437357115657 ) ) ;
#47530=CARTESIAN_POINT ( 'NONE',  ( 4.549368137175248350, -23.67244292351614376, -35.80950303116092925 ) ) ;
#47539=CARTESIAN_POINT ( 'NONE',  ( 0.2885697896453107703, 22.25146201964144765, -36.93108635218676028 ) ) ;
#47541=CIRCLE ( 'NONE', #59496, 10.00000000000000000 ) ;
#47543=FACE_OUTER_BOUND ( 'NONE', #47650, .T. ) ;
#47556=EDGE_CURVE ( 'NONE', #57516, #46146, #34356, .T. ) ;
#47572=EDGE_LOOP ( 'NONE', ( #21823, #51867, #45102, #29308 ) ) ;
#47574=EDGE_LOOP ( 'NONE', ( #17245, #33548, #59732, #27075 ) ) ;
#47578=VERTEX_POINT ( 'NONE', #47592 ) ;
#47586=CARTESIAN_POINT ( 'NONE',  ( 4.322998006666179727, -30.86725474310334150, -36.74401119231399093 ) ) ;
#47589=ORIENTED_EDGE ( 'NONE', *, *, #1987, .T. ) ;
#47591=CARTESIAN_POINT ( 'NONE',  ( 0.1087620492084205720, -21.24797679669934070, -37.52665900408511135 ) ) ;
#47592=CARTESIAN_POINT ( 'NONE',  ( 0.3622758884714730732, 42.62881903538210793, -6.444611261694146442 ) ) ;
#47594=CARTESIAN_POINT ( 'NONE',  ( 0.1101816497532063094, -34.13008584880309826, 26.36013219694213916 ) ) ;
#47598=FACE_OUTER_BOUND ( 'NONE', #50760, .T. ) ;
#47603=( BOUNDED_SURFACE ( )  B_SPLINE_SURFACE ( 3, 1, ( 
 ( #52999, #10103 ),
 ( #57997, #53302 ),
 ( #15119, #34230 ),
 ( #29816, #25121 ) ),
 .UNSPECIFIED., .F., .F., .F. ) 
 B_SPLINE_SURFACE_WITH_KNOTS ( ( 4, 4 ),
 ( 2, 2 ),
 ( 0.000000000000000000, 1.000000000000000000 ),
 ( 0.000000000000000000, 1.000000000000000000 ),
 .UNSPECIFIED. ) 
 GEOMETRIC_REPRESENTATION_ITEM ( )  RATIONAL_B_SPLINE_SURFACE ( (
 ( 1.000000000000000000, 1.000000000000000000),
 ( 0.7223157951917476005, 0.9931996967497186413),
 ( 0.7223157951917476005, 0.9931996967497186413),
 ( 1.000000000000000000, 1.000000000000000000) ) ) 
 REPRESENTATION_ITEM ( '' )  SURFACE ( )  );
#47613=B_SPLINE_CURVE_WITH_KNOTS ( 'NONE', 3,
 ( #31907, #22808, #41938, #60376, #23121, #56305 ),
 .UNSPECIFIED., .F., .F.,
 ( 4, 2, 4 ),
 ( 1.964907063297894324E-17, 0.0002293319059085081922, 0.0004586638118169967062 ),
 .UNSPECIFIED. ) ;
#47617=ORIENTED_EDGE ( 'NONE', *, *, #4992, .F. ) ;
#47624=EDGE_CURVE ( 'NONE', #30492, #6976, #3691, .T. ) ;
#47632=CARTESIAN_POINT ( 'NONE',  ( 0.7954190325252789018, 24.79809930825928532, 41.21355377862707314 ) ) ;
#47637=CARTESIAN_POINT ( 'NONE',  ( 5.880360259849752858, -43.04573319267461073, 21.17507050419438741 ) ) ;
#47640=CARTESIAN_POINT ( 'NONE',  ( -5.995132425357893702, 17.41298668506970770, 7.203480333239141942 ) ) ;
#47643=B_SPLINE_CURVE_WITH_KNOTS ( 'NONE', 3,
 ( #8486, #46430, #22611, #51716 ),
 .UNSPECIFIED., .F., .F.,
 ( 4, 4 ),
 ( 0.000000000000000000, 0.005014147105413703856 ),
 .UNSPECIFIED. ) ;
#47646=CARTESIAN_POINT ( 'NONE',  ( 0.6030672727741701600, -38.21927534817003647, 29.21669544497185100 ) ) ;
#47647=EDGE_CURVE ( 'NONE', #44468, #23596, #27570, .T. ) ;
#47650=EDGE_LOOP ( 'NONE', ( #33002, #24448, #56810, #26954 ) ) ;
#47655=EDGE_CURVE ( 'NONE', #14894, #12273, #38803, .T. ) ;
#47659=VERTEX_POINT ( 'NONE', #57568 ) ;
#47660=CARTESIAN_POINT ( 'NONE',  ( 0.8751705887134423323, 13.30665218149362516, -46.21789262997744885 ) ) ;
#47674=B_SPLINE_CURVE_WITH_KNOTS ( 'NONE', 3,
 ( #2207, #2833, #16329, #55144, #8157, #46395 ),
 .UNSPECIFIED., .F., .F.,
 ( 4, 2, 4 ),
 ( 1.964907063297894324E-17, 0.0002293319059085101709, 0.0004586638118170006636 ),
 .UNSPECIFIED. ) ;
#47683=CARTESIAN_POINT ( 'NONE',  ( 0.6009453534118438522, 48.10564080474284054, 0.4363813339959712878 ) ) ;
#47685=CARTESIAN_POINT ( 'NONE',  ( -6.017396004339686577, -11.47192209077577196, -14.94857180792004669 ) ) ;
#47687=DIRECTION ( 'NONE',  ( 0.09835009131224552170, -0.5042575517176627331, -0.8579344853044326147 ) ) ;
#47707=CARTESIAN_POINT ( 'NONE',  ( 0.3622758884714600280, -6.444611261694905835, 42.62881903538198713 ) ) ;
#47709=ORIENTED_EDGE ( 'NONE', *, *, #54677, .F. ) ;
#47730=B_SPLINE_CURVE_WITH_KNOTS ( 'NONE', 3,
 ( #49833, #45774, #21024, #41090, #45167, #26030 ),
 .UNSPECIFIED., .F., .F.,
 ( 4, 2, 4 ),
 ( 8.440430351524944310E-17, 0.0002293366620881473158, 0.0004586733241762102264 ),
 .UNSPECIFIED. ) ;
#47733=CONICAL_SURFACE ( 'NONE', #55708, 42.92674063221959813, 1.485477209440487556 ) ;
#47737=VERTEX_POINT ( 'NONE', #36280 ) ;
#47743=EDGE_LOOP ( 'NONE', ( #47854, #47337, #24634, #34541 ) ) ;
#47745=FACE_OUTER_BOUND ( 'NONE', #24043, .T. ) ;
#47749=CARTESIAN_POINT ( 'NONE',  ( -6.017396004339687465, -11.47192209077597447, 14.94857180791989215 ) ) ;
#47751=CARTESIAN_POINT ( 'NONE',  ( 4.549368137175248350, 0.000000000000000000, 0.000000000000000000 ) ) ;
#47755=( BOUNDED_SURFACE ( )  B_SPLINE_SURFACE ( 3, 1, ( 
 ( #43339, #15127 ),
 ( #45726, #12215 ),
 ( #31299, #7154 ),
 ( #40416, #30993 ) ),
 .UNSPECIFIED., .F., .F., .F. ) 
 B_SPLINE_SURFACE_WITH_KNOTS ( ( 4, 4 ),
 ( 2, 2 ),
 ( 0.000000000000000000, 1.000000000000000000 ),
 ( 0.000000000000000000, 1.000000000000000000 ),
 .UNSPECIFIED. ) 
 GEOMETRIC_REPRESENTATION_ITEM ( )  RATIONAL_B_SPLINE_SURFACE ( (
 ( 1.000000000000000000, 1.000000000000000000),
 ( 0.9751682680413298332, 0.9999560080971552356),
 ( 0.9751682680413298332, 0.9999560080971552356),
 ( 1.000000000000000000, 1.000000000000000000) ) ) 
 REPRESENTATION_ITEM ( '' )  SURFACE ( )  );
#47759=CIRCLE ( 'NONE', #38790, 47.91270532121795611 ) ;
#47760=EDGE_CURVE ( 'NONE', #43756, #53679, #30552, .T. ) ;
#47767=CARTESIAN_POINT ( 'NONE',  ( 0.1097557419366048670, 42.78407272074150569, 5.407604117549856149 ) ) ;
#47772=CARTESIAN_POINT ( 'NONE',  ( 0.3622758884714600280, 26.89560658783384994, -33.69533458712316332 ) ) ;
#47773=( BOUNDED_SURFACE ( )  B_SPLINE_SURFACE ( 3, 1, ( 
 ( #37060, #56125 ),
 ( #13239, #59907 ),
 ( #32343, #17019 ),
 ( #61128, #22948 ) ),
 .UNSPECIFIED., .F., .F., .F. ) 
 B_SPLINE_SURFACE_WITH_KNOTS ( ( 4, 4 ),
 ( 2, 2 ),
 ( 0.000000000000000000, 1.000000000000000000 ),
 ( 0.000000000000000000, 1.000000000000000000 ),
 .UNSPECIFIED. ) 
 GEOMETRIC_REPRESENTATION_ITEM ( )  RATIONAL_B_SPLINE_SURFACE ( (
 ( 1.000000000000000000, 1.000000000000000000),
 ( 0.9751682680413298332, 0.9999560080971552356),
 ( 0.9751682680413298332, 0.9999560080971552356),
 ( 1.000000000000000000, 1.000000000000000000) ) ) 
 REPRESENTATION_ITEM ( '' )  SURFACE ( )  );
#47776=EDGE_LOOP ( 'NONE', ( #24737, #53038, #7942, #25374 ) ) ;
#47777=CARTESIAN_POINT ( 'NONE',  ( 0.8751705887134553219, 46.67919521768871505, 11.58504748649215976 ) ) ;
#47778=CARTESIAN_POINT ( 'NONE',  ( 0.1097557419366048670, 39.92664986079710587, 16.29667732266766222 ) ) ;
#47783=VERTEX_POINT ( 'NONE', #25938 ) ;
#47790=CARTESIAN_POINT ( 'NONE',  ( 1.827326673878742591, 36.65065268305627910, 22.58371678864595111 ) ) ;
#47791=CIRCLE ( 'NONE', #40839, 42.92674063221959813 ) ;
#47795=B_SPLINE_CURVE_WITH_KNOTS ( 'NONE', 3,
 ( #57118, #33659, #57729, #33972 ),
 .UNSPECIFIED., .F., .F.,
 ( 4, 4 ),
 ( 1.969819611697804288E-17, 0.004444306975806115896 ),
 .UNSPECIFIED. ) ;
#47797=B_SPLINE_CURVE_WITH_KNOTS ( 'NONE', 3,
 ( #35529, #44938, #43709, #29571 ),
 .UNSPECIFIED., .F., .F.,
 ( 4, 4 ),
 ( 0.000000000000000000, 0.004445488388166993383 ),
 .UNSPECIFIED. ) ;
#47799=VERTEX_POINT ( 'NONE', #40999 ) ;
#47800=B_SPLINE_CURVE_WITH_KNOTS ( 'NONE', 3,
 ( #46857, #28339, #51206, #47767, #32435, #4814, #116, #47157, #37148, #3898, #51510, #57431, #23038, #8290, #9531, #37775, #42167, #61221, #33369 ),
 .UNSPECIFIED., .F., .F.,
 ( 4, 3, 3, 3, 3, 3, 4 ),
 ( 1.161956753697875813E-16, 0.0002618519381806256457, 0.0003927759815485963547, 0.0005237000248299426711, 0.0006546240681324986925, 0.0007855481115631319502, 0.0009699050456655111587 ),
 .UNSPECIFIED. ) ;
#47804=ORIENTED_EDGE ( 'NONE', *, *, #3295, .T. ) ;
#47808=CARTESIAN_POINT ( 'NONE',  ( 0.6017667736363748743, 46.37677940471279925, 12.78803812527904249 ) ) ;
#47811=ORIENTED_EDGE ( 'NONE', *, *, #32269, .F. ) ;
#47814=CARTESIAN_POINT ( 'NONE',  ( 0.6041374136657476912, -44.51224464244987900, -18.24862627831519646 ) ) ;
#47816=CARTESIAN_POINT ( 'NONE',  ( 0.1103310638050662290, -37.30561229499315345, -21.63353985999675189 ) ) ;
#47819=CARTESIAN_POINT ( 'NONE',  ( 0.6041374136657476912, -46.42299778158164258, 12.61972904329520340 ) ) ;
#47820=ADVANCED_FACE ( 'NONE', ( #18946 ), #54141, .F. ) ;
#47825=ORIENTED_EDGE ( 'NONE', *, *, #46634, .T. ) ;
#47828=LINE ( 'NONE', #61880, #5724 ) ;
#47831=ORIENTED_EDGE ( 'NONE', *, *, #39386, .F. ) ;
#47832=CARTESIAN_POINT ( 'NONE',  ( 0.7954196712028469562, 47.79303691884131666, -5.415566793624839725 ) ) ;
#47834=CARTESIAN_POINT ( 'NONE',  ( 4.975801465491694664, 47.76942479135480824, 3.702618843597622167 ) ) ;
#47836=CARTESIAN_POINT ( 'NONE',  ( 0.6017667736363750963, 29.56223180955331387, -37.95278695280779857 ) ) ;
#47837=CARTESIAN_POINT ( 'NONE',  ( 4.975801465491695552, 0.000000000000000000, 0.000000000000000000 ) ) ;
#47839=CARTESIAN_POINT ( 'NONE',  ( 4.322998006666165516, -36.74401119231389146, -30.86725474310346584 ) ) ;
#47843=CARTESIAN_POINT ( 'NONE',  ( 3.238741278300275805, 29.07934833201323599, 31.66556122967967823 ) ) ;
#47847=CARTESIAN_POINT ( 'NONE',  ( 0.5998501479064699549, -41.39809967730504781, 24.50586714782532027 ) ) ;
#47848=LINE ( 'NONE', #8366, #20091 ) ;
#47851=CARTESIAN_POINT ( 'NONE',  ( 5.880360259849739535, -47.04104239318773040, 9.405269135694428684 ) ) ;
#47852=CARTESIAN_POINT ( 'NONE',  ( 0.1073791018717578927, -25.86618856530687793, -34.50606437925538472 ) ) ;
#47853=CARTESIAN_POINT ( 'NONE',  ( 0.1103878639767399139, -5.580746265797351668, 42.76182653383947496 ) ) ;
#47854=ORIENTED_EDGE ( 'NONE', *, *, #39144, .T. ) ;
#47861=CARTESIAN_POINT ( 'NONE',  ( 0.3622758884714730732, 17.25816669464937902, 39.50828911767005280 ) ) ;
#47866=CARTESIAN_POINT ( 'NONE',  ( 0.2885697896453110478, -4.828949182955637909, -42.84523253470159432 ) ) ;
#47870=ORIENTED_EDGE ( 'NONE', *, *, #52891, .F. ) ;
#47878=ORIENTED_EDGE ( 'NONE', *, *, #12552, .F. ) ;
#47879=CARTESIAN_POINT ( 'NONE',  ( 4.549368137175248350, 23.67244292351589507, 35.80950303116109268 ) ) ;
#47881=CARTESIAN_POINT ( 'NONE',  ( 3.238931869106855377, 27.59912060131728140, 32.96367555688120632 ) ) ;
#47884=CARTESIAN_POINT ( 'NONE',  ( 4.975801465491695552, -20.67815041659169495, 43.22084481528186473 ) ) ;
#47886=ORIENTED_EDGE ( 'NONE', *, *, #13814, .F. ) ;
#47889=EDGE_CURVE ( 'NONE', #16525, #4313, #33654, .T. ) ;
#47904=CARTESIAN_POINT ( 'NONE',  ( 2.301529144917015213, -48.01619158420457723, 1.287519423137106100 ) ) ;
#47907=CARTESIAN_POINT ( 'NONE',  ( 0.1103744047535531458, -34.23648668783411608, 26.22174028894811926 ) ) ;
#47912=ORIENTED_EDGE ( 'NONE', *, *, #15780, .F. ) ;
#47913=EDGE_CURVE ( 'NONE', #7184, #34476, #28788, .T. ) ;
#47921=ORIENTED_EDGE ( 'NONE', *, *, #4560, .T. ) ;
#47926=CARTESIAN_POINT ( 'NONE',  ( 0.1087620492084206414, -16.16798550313395921, -39.97903073778059024 ) ) ;
#47942=CARTESIAN_POINT ( 'NONE',  ( -6.016104459813374383, -18.68131780085930060, -2.464823636987640398 ) ) ;
#47946=FACE_OUTER_BOUND ( 'NONE', #20090, .T. ) ;
#47949=CARTESIAN_POINT ( 'NONE',  ( 0.1073791018717578927, -11.62916352156179123, 41.52698815987148606 ) ) ;
#47954=CARTESIAN_POINT ( 'NONE',  ( 3.680882792899938138, -45.82784180332847512, 14.19444521819950822 ) ) ;
#47969=EDGE_LOOP ( 'NONE', ( #7410, #41052, #39124, #27295 ) ) ;
#47970=CARTESIAN_POINT ( 'NONE',  ( -2.708315649062916552, -14.54141329178161257, -1.648584381066990678 ) ) ;
#47972=AXIS2_PLACEMENT_3D ( 'NONE', #53995, #50242, #2301 ) ;
#47977=CARTESIAN_POINT ( 'NONE',  ( 0.1073791018717483448, -37.58707531572191840, -21.14095454447545919 ) ) ;
#47987=CARTESIAN_POINT ( 'NONE',  ( 0.8760168074886965917, 48.09529047980636562, 0.8912768426707960989 ) ) ;
#47996=CARTESIAN_POINT ( 'NONE',  ( -2.569797478183790229, 12.44213550320642625, 7.701637110048724644 ) ) ;
#47997=CARTESIAN_POINT ( 'NONE',  ( 0.6023142530420679819, 48.10676733004997629, -0.2618396477462503480 ) ) ;
#48001=CARTESIAN_POINT ( 'NONE',  ( 4.549368137175248350, 40.58005590356670211, 13.99871866169379508 ) ) ;
#48007=CARTESIAN_POINT ( 'NONE',  ( 4.549368137175248350, -38.59302160394740611, -18.79584381673521065 ) ) ;
#48008=CARTESIAN_POINT ( 'NONE',  ( 0.5980894510889448457, -24.66136644716850057, 41.31170365136845390 ) ) ;
#48014=ORIENTED_EDGE ( 'NONE', *, *, #3639, .F. ) ;
#48022=FACE_OUTER_BOUND ( 'NONE', #39756, .T. ) ;
#48026=( BOUNDED_SURFACE ( )  B_SPLINE_SURFACE ( 3, 1, ( 
 ( #12687, #26761 ),
 ( #47123, #56489 ),
 ( #23303, #31460 ),
 ( #41815, #60881 ) ),
 .UNSPECIFIED., .F., .F., .F. ) 
 B_SPLINE_SURFACE_WITH_KNOTS ( ( 4, 4 ),
 ( 2, 2 ),
 ( 0.000000000000000000, 1.000000000000000000 ),
 ( 0.000000000000000000, 1.000000000000000000 ),
 .UNSPECIFIED. ) 
 GEOMETRIC_REPRESENTATION_ITEM ( )  RATIONAL_B_SPLINE_SURFACE ( (
 ( 1.000000000000000000, 1.000000000000000000),
 ( 0.9953040768229005630, 0.8617119497784937465),
 ( 0.9953040768229005630, 0.8617119497784937465),
 ( 1.000000000000000000, 1.000000000000000000) ) ) 
 REPRESENTATION_ITEM ( '' )  SURFACE ( )  );
#48031=ORIENTED_EDGE ( 'NONE', *, *, #90, .T. ) ;
#48041=CARTESIAN_POINT ( 'NONE',  ( 0.6031356755773454870, -12.45109777649142124, 46.46822857981022281 ) ) ;
#48050=ORIENTED_EDGE ( 'NONE', *, *, #11187, .T. ) ;
#48053=DIRECTION ( 'NONE',  ( 0.09835009131224552170, 0.7941905447268735596, 0.5996571005210433736 ) ) ;
#48055=EDGE_CURVE ( 'NONE', #25998, #15054, #44002, .T. ) ;
#48057=CARTESIAN_POINT ( 'NONE',  ( 2.301430502907646058, -13.67112791032074703, 46.04685681264140840 ) ) ;
#48063=CARTESIAN_POINT ( 'NONE',  ( 5.880360259849752858, 31.66572319753561970, -36.03610316515350576 ) ) ;
#48067=CARTESIAN_POINT ( 'NONE',  ( 0.1092565886968784455, -34.40108480122233914, -26.00565248013041142 ) ) ;
#48069=CARTESIAN_POINT ( 'NONE',  ( 0.8760168074886965917, -0.8912768426709639646, 48.09529047980636562 ) ) ;
#48082=CARTESIAN_POINT ( 'NONE',  ( 0.2224561200757635415, -37.71651051365644491, 20.89867881469703548 ) ) ;
#48084=CARTESIAN_POINT ( 'NONE',  ( 4.322998006666179727, 36.74401119231410462, -30.86725474310321360 ) ) ;
#48091=EDGE_CURVE ( 'NONE', #27049, #25537, #17040, .T. ) ;
#48094=CARTESIAN_POINT ( 'NONE',  ( 0.2224561200757595725, 17.20021002050924963, -39.54039348282962152 ) ) ;
#48103=ADVANCED_FACE ( 'NONE', ( #36437 ), #47773, .F. ) ;
#48104=ORIENTED_EDGE ( 'NONE', *, *, #37151, .F. ) ;
#48105=CARTESIAN_POINT ( 'NONE',  ( 4.975801465491694664, 21.70134120755201224, -42.71626295676241369 ) ) ;
#48107=ORIENTED_EDGE ( 'NONE', *, *, #41870, .T. ) ;
#48108=DIRECTION ( 'NONE',  ( -1.000000000000000000, -0.000000000000000000, -0.000000000000000000 ) ) ;
#48110=CARTESIAN_POINT ( 'NONE',  ( 4.549368137175248350, -40.71620287708353914, 13.59764261105679317 ) ) ;
#48111=DIRECTION ( 'NONE',  ( 0.000000000000000000, 0.000000000000000000, 1.000000000000000000 ) ) ;
#48118=CIRCLE ( 'NONE', #51135, 42.92674063221959813 ) ;
#48121=CARTESIAN_POINT ( 'NONE',  ( -6.017396004339686577, 18.20079405513556736, -4.878103249820876286 ) ) ;
#48122=ORIENTED_EDGE ( 'NONE', *, *, #9277, .T. ) ;
#48126=ORIENTED_EDGE ( 'NONE', *, *, #48055, .F. ) ;
#48130=EDGE_CURVE ( 'NONE', #45673, #5852, #41030, .T. ) ;
#48132=CARTESIAN_POINT ( 'NONE',  ( 0.6254311100348639574, 47.77988293940229170, -5.596225872411531910 ) ) ;
#48133=FACE_OUTER_BOUND ( 'NONE', #14811, .T. ) ;
#48135=CARTESIAN_POINT ( 'NONE',  ( 0.6009453534118438522, 29.63106322864184605, -37.89911869481701956 ) ) ;
#48137=ORIENTED_EDGE ( 'NONE', *, *, #11415, .F. ) ;
#48140=( BOUNDED_SURFACE ( )  B_SPLINE_SURFACE ( 3, 1, ( 
 ( #40704, #31584 ),
 ( #31275, #59774 ),
 ( #2751, #21883 ),
 ( #41616, #41021 ) ),
 .UNSPECIFIED., .F., .F., .F. ) 
 B_SPLINE_SURFACE_WITH_KNOTS ( ( 4, 4 ),
 ( 2, 2 ),
 ( 0.000000000000000000, 1.000000000000000000 ),
 ( 0.000000000000000000, 1.000000000000000000 ),
 .UNSPECIFIED. ) 
 GEOMETRIC_REPRESENTATION_ITEM ( )  RATIONAL_B_SPLINE_SURFACE ( (
 ( 1.000000000000000000, 1.000000000000000000),
 ( 0.7223157951917480446, 0.9931996967497186413),
 ( 0.7223157951917480446, 0.9931996967497186413),
 ( 1.000000000000000000, 1.000000000000000000) ) ) 
 REPRESENTATION_ITEM ( '' )  SURFACE ( )  );
#48142=ORIENTED_EDGE ( 'NONE', *, *, #53926, .T. ) ;
#48144=( BOUNDED_SURFACE ( )  B_SPLINE_SURFACE ( 3, 1, ( 
 ( #1712, #1104 ),
 ( #485, #57803 ),
 ( #43763, #20850 ),
 ( #24939, #29618 ) ),
 .UNSPECIFIED., .F., .F., .F. ) 
 B_SPLINE_SURFACE_WITH_KNOTS ( ( 4, 4 ),
 ( 2, 2 ),
 ( 0.000000000000000000, 1.000000000000000000 ),
 ( 0.000000000000000000, 1.000000000000000000 ),
 .UNSPECIFIED. ) 
 GEOMETRIC_REPRESENTATION_ITEM ( )  RATIONAL_B_SPLINE_SURFACE ( (
 ( 1.000000000000000000, 1.000000000000000000),
 ( 0.9751682680413298332, 0.9999560080971552356),
 ( 0.9751682680413298332, 0.9999560080971552356),
 ( 1.000000000000000000, 1.000000000000000000) ) ) 
 REPRESENTATION_ITEM ( '' )  SURFACE ( )  );
#48145=DIRECTION ( 'NONE',  ( -1.000000000000000000, -0.000000000000000000, -0.000000000000000000 ) ) ;
#48148=CARTESIAN_POINT ( 'NONE',  ( 4.975801465491694664, 3.702618843597456522, -47.76942479135481534 ) ) ;
#48150=CARTESIAN_POINT ( 'NONE',  ( 0.5980894510889457338, -11.77356634613350295, 46.65000524237065349 ) ) ;
#48153=CARTESIAN_POINT ( 'NONE',  ( 4.549368137175248350, 0.000000000000000000, 0.000000000000000000 ) ) ;
#48155=B_SPLINE_CURVE_WITH_KNOTS ( 'NONE', 3,
 ( #37733, #33026, #61788, #53322, #10747, #49556 ),
 .UNSPECIFIED., .F., .F.,
 ( 4, 2, 4 ),
 ( 8.547914836739548796E-17, 0.0002293366620881453642, 0.0004586733241762052391 ),
 .UNSPECIFIED. ) ;
#48158=ORIENTED_EDGE ( 'NONE', *, *, #2245, .T. ) ;
#48162=CARTESIAN_POINT ( 'NONE',  ( 0.5998501479064708430, -48.10473956285919428, -0.5236536531313246146 ) ) ;
#48171=ADVANCED_FACE ( 'NONE', ( #47073 ), #22157, .F. ) ;
#48174=CARTESIAN_POINT ( 'NONE',  ( 4.549368137175248350, 8.582197505784431968, -42.06008734272388239 ) ) ;
#48175=ORIENTED_EDGE ( 'NONE', *, *, #1824, .T. ) ;
#48182=EDGE_CURVE ( 'NONE', #50188, #7184, #3578, .T. ) ;
#48183=CARTESIAN_POINT ( 'NONE',  ( 0.7954190325252786797, -13.28627193046336963, -46.22745637125036211 ) ) ;
#48184=CARTESIAN_POINT ( 'NONE',  ( 0.6029303876144825880, 33.92442033626736020, 34.10953954078152606 ) ) ;
#48190=B_SPLINE_CURVE_WITH_KNOTS ( 'NONE', 3,
 ( #31563, #17468, #60661, #27173, #40685, #60063 ),
 .UNSPECIFIED., .F., .F.,
 ( 4, 2, 4 ),
 ( 1.267602517345562747E-16, 0.0002450741128632333721, 0.0004901482257263400011 ),
 .UNSPECIFIED. ) ;
#48194=CARTESIAN_POINT ( 'NONE',  ( 4.975801465491694664, -43.22084481528235500, 20.67815041659062913 ) ) ;
#48199=B_SPLINE_CURVE_WITH_KNOTS ( 'NONE', 3,
 ( #41726, #37962, #33552, #46418, #60787, #3464 ),
 .UNSPECIFIED., .F., .F.,
 ( 4, 2, 4 ),
 ( 8.554130121340520410E-17, 0.0002293366620881455268, 0.0004586733241762055101 ),
 .UNSPECIFIED. ) ;
#48200=CARTESIAN_POINT ( 'NONE',  ( 0.3622758884714600280, 20.83792692158919735, 37.74294673546592804 ) ) ;
#48201=ORIENTED_EDGE ( 'NONE', *, *, #50700, .T. ) ;
#48202=CARTESIAN_POINT ( 'NONE',  ( 2.643462169533613793, -30.32726672320774242, -37.25264019563404361 ) ) ;
#48203=CARTESIAN_POINT ( 'NONE',  ( -6.001507490154111224, 17.40350523682695183, 7.225628667346644107 ) ) ;
#48206=EDGE_LOOP ( 'NONE', ( #7680, #8134, #36882, #42826 ) ) ;
#48216=CARTESIAN_POINT ( 'NONE',  ( 0.6009453534118438522, 12.02914401651108101, 46.57942464365178381 ) ) ;
#48219=CARTESIAN_POINT ( 'NONE',  ( -5.995132425357893702, -17.41298668506965441, -7.203480333239262734 ) ) ;
#48221=CARTESIAN_POINT ( 'NONE',  ( -6.017396004339687465, 16.31924478664288358, -9.420565012089255674 ) ) ;
#48229=( BOUNDED_SURFACE ( )  B_SPLINE_SURFACE ( 3, 1, ( 
 ( #10435, #5396 ),
 ( #44901, #15139 ),
 ( #48954, #29525 ),
 ( #44584, #30442 ) ),
 .UNSPECIFIED., .F., .F., .F. ) 
 B_SPLINE_SURFACE_WITH_KNOTS ( ( 4, 4 ),
 ( 2, 2 ),
 ( 0.000000000000000000, 1.000000000000000000 ),
 ( 0.000000000000000000, 1.000000000000000000 ),
 .UNSPECIFIED. ) 
 GEOMETRIC_REPRESENTATION_ITEM ( )  RATIONAL_B_SPLINE_SURFACE ( (
 ( 1.000000000000000000, 1.000000000000000000),
 ( 0.7223157951917476005, 0.9931996967497186413),
 ( 0.7223157951917476005, 0.9931996967497186413),
 ( 1.000000000000000000, 1.000000000000000000) ) ) 
 REPRESENTATION_ITEM ( '' )  SURFACE ( )  );
#48230=CARTESIAN_POINT ( 'NONE',  ( 4.975801465491695552, 32.01766832630263337, 35.64402118370968964 ) ) ;
#48254=CARTESIAN_POINT ( 'NONE',  ( 0.2885697896453109368, -17.24062360132741389, 39.51953439758081288 ) ) ;
#48257=ORIENTED_EDGE ( 'NONE', *, *, #1457, .F. ) ;
#48263=LINE ( 'NONE', #52944, #54753 ) ;
#48264=LINE ( 'NONE', #5317, #18738 ) ;
#48265=CARTESIAN_POINT ( 'NONE',  ( 0.3622758884714730732, 25.58609868863768355, -34.70015533914803285 ) ) ;
#48295=CARTESIAN_POINT ( 'NONE',  ( 0.6031356755773454870, 48.10744332413212021, -2.564066888715896384E-05 ) ) ;
#48296=B_SPLINE_CURVE_WITH_KNOTS ( 'NONE', 3,
 ( #27850, #51954, #42902, #14383, #9989, #48200 ),
 .UNSPECIFIED., .F., .F.,
 ( 4, 2, 4 ),
 ( 1.870559545977334001E-17, 0.0002293319059085083820, 0.0004586638118169980615 ),
 .UNSPECIFIED. ) ;
#48297=CARTESIAN_POINT ( 'NONE',  ( 0.1073791018717578927, -21.98088480513690968, 37.10214135362851096 ) ) ;
#48301=VECTOR ( 'NONE', #42102, 999.9999999999998863 ) ;
#48302=EDGE_CURVE ( 'NONE', #18536, #58789, #34505, .T. ) ;
#48306=CARTESIAN_POINT ( 'NONE',  ( 0.3622758884714600280, -0.8252992914331080954, 43.10531414739104150 ) ) ;
#48320=CARTESIAN_POINT ( 'NONE',  ( 0.1102847568649952675, 11.25043675627740569, 41.63105453442841508 ) ) ;
#48324=B_SPLINE_CURVE_WITH_KNOTS ( 'NONE', 3,
 ( #39537, #21029, #15724, #49214, #44552, #1582 ),
 .UNSPECIFIED., .F., .F.,
 ( 4, 2, 4 ),
 ( 8.741117365843378158E-19, 0.0002450742804987333088, 0.0004901485609974657503 ),
 .UNSPECIFIED. ) ;
#48327=ORIENTED_EDGE ( 'NONE', *, *, #21019, .F. ) ;
#48329=( BOUNDED_SURFACE ( )  B_SPLINE_SURFACE ( 3, 1, ( 
 ( #18840, #37963 ),
 ( #57017, #33244 ),
 ( #28212, #4374 ),
 ( #47640, #45422 ) ),
 .UNSPECIFIED., .F., .F., .F. ) 
 B_SPLINE_SURFACE_WITH_KNOTS ( ( 4, 4 ),
 ( 2, 2 ),
 ( 0.000000000000000000, 1.000000000000000000 ),
 ( 0.000000000000000000, 1.000000000000000000 ),
 .UNSPECIFIED. ) 
 GEOMETRIC_REPRESENTATION_ITEM ( )  RATIONAL_B_SPLINE_SURFACE ( (
 ( 1.000000000000000000, 1.000000000000000000),
 ( 0.7223157951917480446, 0.9931996967497186413),
 ( 0.7223157951917480446, 0.9931996967497186413),
 ( 1.000000000000000000, 1.000000000000000000) ) ) 
 REPRESENTATION_ITEM ( '' )  SURFACE ( )  );
#48333=CARTESIAN_POINT ( 'NONE',  ( 0.6001305935487315502, -38.48510059944067763, 28.87057754790872721 ) ) ;
#48338=CARTESIAN_POINT ( 'NONE',  ( 4.549368137175248350, 18.79584381673477012, 38.59302160394760506 ) ) ;
#48340=VERTEX_POINT ( 'NONE', #34822 ) ;
#48341=CARTESIAN_POINT ( 'NONE',  ( 0.3622758884714600280, 20.83792692158919735, 37.74294673546592804 ) ) ;
#48342=DIRECTION ( 'NONE',  ( -1.000000000000000000, -0.000000000000000000, -0.000000000000000000 ) ) ;
#48351=ORIENTED_EDGE ( 'NONE', *, *, #15565, .T. ) ;
#48354=CARTESIAN_POINT ( 'NONE',  ( 0.5998501479064699549, -33.64490850298868452, 34.38546660123239462 ) ) ;
#48361=CARTESIAN_POINT ( 'NONE',  ( 0.5988103622719987973, 18.96890139669993047, -44.21009254328985350 ) ) ;
#48369=CARTESIAN_POINT ( 'NONE',  ( 0.7954196712028480665, -34.61997730204605261, 33.39101545667277549 ) ) ;
#48370=CARTESIAN_POINT ( 'NONE',  ( 0.6028618097248864549, -46.42282207635412306, 12.61968633793835082 ) ) ;
#48376=CARTESIAN_POINT ( 'NONE',  ( -6.017396004339686577, 4.878103249821066356, 18.20079405513551407 ) ) ;
#48379=B_SPLINE_CURVE_WITH_KNOTS ( 'NONE', 3,
 ( #42989, #10688, #5031, #58267, #43606, #24156 ),
 .UNSPECIFIED., .F., .F.,
 ( 4, 2, 4 ),
 ( 1.266794085606387986E-16, 0.0002450741128632352695, 0.0004901482257263437958 ),
 .UNSPECIFIED. ) ;
#48381=CARTESIAN_POINT ( 'NONE',  ( 0.2885697896453110478, -37.73587455644762656, 20.85752796052947389 ) ) ;
#48387=CARTESIAN_POINT ( 'NONE',  ( 0.1073791018717483448, -10.69234304550083081, 41.77800844988496465 ) ) ;
#48393=CARTESIAN_POINT ( 'NONE',  ( 0.5998501479064708430, -23.59887241503325228, -41.92175333043611829 ) ) ;
#48398=CARTESIAN_POINT ( 'NONE',  ( 3.238931869106854933, -41.01619136531535759, 12.88361013339092409 ) ) ;
#48407=CARTESIAN_POINT ( 'NONE',  ( 4.549368137175248350, 0.000000000000000000, 0.000000000000000000 ) ) ;
#48413=CARTESIAN_POINT ( 'NONE',  ( 0.2885697896453107147, 4.828949182955358133, 42.84523253470162985 ) ) ;
#48420=CARTESIAN_POINT ( 'NONE',  ( 0.3622758884714730732, -26.89560658783362612, -33.69533458712334806 ) ) ;
#48424=CARTESIAN_POINT ( 'NONE',  ( 0.5988103564986354543, -5.677495323491076107, 47.77151399983768698 ) ) ;
#48432=CARTESIAN_POINT ( 'NONE',  ( -2.708315649062916552, -5.842990691604515341, -13.41752550814508105 ) ) ;
#48439=CARTESIAN_POINT ( 'NONE',  ( 0.6254311100348657337, -0.6881768005105882713, 48.10157347124184923 ) ) ;
#48442=CARTESIAN_POINT ( 'NONE',  ( 0.6017667736363749853, 38.37782726569690794, -29.00830848931586914 ) ) ;
#48445=CARTESIAN_POINT ( 'NONE',  ( 0.5988103564986354543, 46.62176022926370678, 11.86435738293459430 ) ) ;
#48447=CARTESIAN_POINT ( 'NONE',  ( 4.549368137175248350, -35.57418903283131328, 24.02461520945210793 ) ) ;
#48452=CARTESIAN_POINT ( 'NONE',  ( 1.827326673878743479, -29.55671596281188229, -31.30008222956372066 ) ) ;
#48469=CARTESIAN_POINT ( 'NONE',  ( 0.3622758884714730732, 40.13994584881760375, 15.73321244754868964 ) ) ;
#48473=CARTESIAN_POINT ( 'NONE',  ( -6.016761891674565099, 18.20023637398599092, 4.880293656735028129 ) ) ;
#48475=CARTESIAN_POINT ( 'NONE',  ( 5.880360259849752858, 39.91356965504147780, -26.61251048557207355 ) ) ;
#48477=CARTESIAN_POINT ( 'NONE',  ( 0.3622758884714730732, 26.89560658783340585, 33.69533458712353280 ) ) ;
#48483=CARTESIAN_POINT ( 'NONE',  ( 0.1073791018717578927, 11.62916352156150346, -41.52698815987157133 ) ) ;
#48485=EDGE_LOOP ( 'NONE', ( #54699, #15824, #19719, #53334 ) ) ;
#48490=ADVANCED_FACE ( 'NONE', ( #31963 ), #49770, .F. ) ;
#48496=( BOUNDED_SURFACE ( )  B_SPLINE_SURFACE ( 3, 1, ( 
 ( #47276, #24080 ),
 ( #52886, #34116 ),
 ( #4322, #23458 ),
 ( #42586, #43208 ) ),
 .UNSPECIFIED., .F., .F., .F. ) 
 B_SPLINE_SURFACE_WITH_KNOTS ( ( 4, 4 ),
 ( 2, 2 ),
 ( 0.000000000000000000, 1.000000000000000000 ),
 ( 0.000000000000000000, 1.000000000000000000 ),
 .UNSPECIFIED. ) 
 GEOMETRIC_REPRESENTATION_ITEM ( )  RATIONAL_B_SPLINE_SURFACE ( (
 ( 1.000000000000000000, 1.000000000000000000),
 ( 0.7223157951917476005, 0.9931996967497186413),
 ( 0.7223157951917476005, 0.9931996967497186413),
 ( 1.000000000000000000, 1.000000000000000000) ) ) 
 REPRESENTATION_ITEM ( '' )  SURFACE ( )  );
#48497=CARTESIAN_POINT ( 'NONE',  ( 0.8751705887134553219, -37.60752970653848593, 29.98056538504896906 ) ) ;
#48498=EDGE_LOOP ( 'NONE', ( #34017, #33707, #3536, #37199 ) ) ;
#48505=CARTESIAN_POINT ( 'NONE',  ( 4.322998006666165516, 4.155494336618067663, 47.80838462754066143 ) ) ;
#48511=ORIENTED_EDGE ( 'NONE', *, *, #7416, .T. ) ;
#48519=CARTESIAN_POINT ( 'NONE',  ( 0.8760168074886965917, -7.161346975774058876, 47.56749362999700992 ) ) ;
#48522=CARTESIAN_POINT ( 'NONE',  ( 3.680882792899936362, 20.05474345988747231, 43.58303137875414279 ) ) ;
#48524=CARTESIAN_POINT ( 'NONE',  ( 0.8751705887134423323, 19.22545746485661766, -44.08562551107063143 ) ) ;
#48531=CARTESIAN_POINT ( 'NONE',  ( 1.827326673878744145, 4.394636550976061429, 42.82501343454097054 ) ) ;
#48541=CARTESIAN_POINT ( 'NONE',  ( 0.1064266379913940963, -30.88821943652591173, -30.09411261783680303 ) ) ;
#48552=DIRECTION ( 'NONE',  ( 0.1024043820194936449, -0.6940285268068357993, 0.7126273545981369750 ) ) ;
#48559=CARTESIAN_POINT ( 'NONE',  ( 0.1073791018717483448, 30.14884492832389284, -30.83464511437107447 ) ) ;
#48563=B_SPLINE_CURVE_WITH_KNOTS ( 'NONE', 3,
 ( #51586, #20869, #6418, #25559, #53731, #828 ),
 .UNSPECIFIED., .F., .F.,
 ( 4, 2, 4 ),
 ( 8.560751122900633232E-17, 0.0002293366620881450661, 0.0004586733241762045343 ),
 .UNSPECIFIED. ) ;
#48566=CARTESIAN_POINT ( 'NONE',  ( 0.6009453534118439633, 23.67490308139347022, 41.87889766923463242 ) ) ;
#48572=CARTESIAN_POINT ( 'NONE',  ( 0.8751705887134423323, 38.69254731947834358, -28.56654290188613032 ) ) ;
#48582=CARTESIAN_POINT ( 'NONE',  ( 0.3622758884714600280, -40.13994584881793770, 15.73321244754782811 ) ) ;
#48583=EDGE_CURVE ( 'NONE', #46644, #30061, #11834, .T. ) ;
#48594=CONICAL_SURFACE ( 'NONE', #13600, 42.92674063221959813, 1.485477209440487556 ) ;
#48600=CARTESIAN_POINT ( 'NONE',  ( -6.017396004339687465, -17.40836349643162251, -7.212050743684361720 ) ) ;
#48606=CARTESIAN_POINT ( 'NONE',  ( 0.8751705887134423323, 0.8911681664088411114, -48.08707113907595243 ) ) ;
#48608=CARTESIAN_POINT ( 'NONE',  ( 0.7246131072078584312, 28.62741613354240755, 38.65593150731059069 ) ) ;
#48613=ORIENTED_EDGE ( 'NONE', *, *, #61732, .F. ) ;
#48614=ORIENTED_EDGE ( 'NONE', *, *, #43307, .T. ) ;
#48617=ORIENTED_EDGE ( 'NONE', *, *, #26365, .T. ) ;
#48618=CARTESIAN_POINT ( 'NONE',  ( -6.016761891674564211, -9.418621820384613486, 16.32039929810254009 ) ) ;
#48623=CARTESIAN_POINT ( 'NONE',  ( 0.6017667736363750963, -29.56223180955360164, 37.95278695280759251 ) ) ;
#48638=CARTESIAN_POINT ( 'NONE',  ( 0.1073791018717483448, 6.109314776652144729, 42.68962945260955877 ) ) ;
#48639=EDGE_LOOP ( 'NONE', ( #13339, #36801, #29267, #61733 ) ) ;
#48650=VECTOR ( 'NONE', #58522, 999.9999999999998863 ) ;
#48652=ORIENTED_EDGE ( 'NONE', *, *, #51532, .T. ) ;
#48654=LINE ( 'NONE', #33965, #42938 ) ;
#48657=CARTESIAN_POINT ( 'NONE',  ( 0.1104177457020373287, -39.83992599038897708, 16.50753524010228546 ) ) ;
#48658=B_SPLINE_CURVE_WITH_KNOTS ( 'NONE', 3,
 ( #43897, #20071, #39187, #15370, #20983, #44507 ),
 .UNSPECIFIED., .F., .F.,
 ( 4, 2, 4 ),
 ( 1.261467247513764704E-16, 0.0002450741128632373837, 0.0004901482257263485662 ),
 .UNSPECIFIED. ) ;
#48665=CARTESIAN_POINT ( 'NONE',  ( 0.1092355843206037486, 30.70542469027324728, -30.28032287551047119 ) ) ;
#48673=CARTESIAN_POINT ( 'NONE',  ( -6.016104459813371719, -0.005335450884934395989, -18.84322058118302579 ) ) ;
#48674=CARTESIAN_POINT ( 'NONE',  ( 0.1073791018717578927, -37.10214135362874543, -21.98088480513651888 ) ) ;
#48675=CARTESIAN_POINT ( 'NONE',  ( 0.6009452777970412107, -46.35353542372332925, 12.87217382175413327 ) ) ;
#48679=B_SPLINE_CURVE_WITH_KNOTS ( 'NONE', 3,
 ( #1049, #16094, #742, #25471 ),
 .UNSPECIFIED., .F., .F.,
 ( 4, 4 ),
 ( 2.250920953359534068E-17, 0.004564976165746187711 ),
 .UNSPECIFIED. ) ;
#48680=VECTOR ( 'NONE', #26780, 1000.000000000000114 ) ;
#48682=B_SPLINE_CURVE_WITH_KNOTS ( 'NONE', 3,
 ( #12550, #36364, #40448, #45755, #50433, #16621, #7499, #2806, #6878, #36057, #31329, #46371, #31642, #21938, #3119, #17860, #3417, #7185, #36985 ),
 .UNSPECIFIED., .F., .F.,
 ( 4, 3, 3, 3, 3, 3, 4 ),
 ( 1.153344816771540786E-16, 0.0002618519381806247784, 0.0003927759815485972763, 0.0005237000248299418037, 0.0006546240681324968494, 0.0007855481115631319502, 0.0009699050456655100745 ),
 .UNSPECIFIED. ) ;
#48685=ORIENTED_EDGE ( 'NONE', *, *, #23735, .F. ) ;
#48686=AXIS2_PLACEMENT_3D ( 'NONE', #61108, #31083, #60489 ) ;
#48687=CARTESIAN_POINT ( 'NONE',  ( 0.1098349054025746230, -43.12395110775227636, -0.2133124578263222715 ) ) ;
#48691=ORIENTED_EDGE ( 'NONE', *, *, #27414, .T. ) ;
#48692=CARTESIAN_POINT ( 'NONE',  ( 0.1087620492084205442, -11.51076657762363986, 41.55994353650422113 ) ) ;
#48693=CARTESIAN_POINT ( 'NONE',  ( 0.1064266418746777354, -30.09411284098551320, -30.88821921809838145 ) ) ;
#48699=CARTESIAN_POINT ( 'NONE',  ( 0.6031356219577718170, -24.12932366310838006, -41.61861914321203670 ) ) ;
#48715=LINE ( 'NONE', #15522, #40805 ) ;
#48729=AXIS2_PLACEMENT_3D ( 'NONE', #19852, #23922, #9201 ) ;
#48735=CARTESIAN_POINT ( 'NONE',  ( 4.549368137175248350, 18.79584381673477012, 38.59302160394760506 ) ) ;
#48736=CARTESIAN_POINT ( 'NONE',  ( -2.708315649062916552, 2.171184472130498477, 14.47261168455370317 ) ) ;
#48741=ORIENTED_EDGE ( 'NONE', *, *, #25902, .T. ) ;
#48749=EDGE_CURVE ( 'NONE', #3699, #59613, #52854, .T. ) ;
#48750=FACE_OUTER_BOUND ( 'NONE', #12549, .T. ) ;
#48754=CARTESIAN_POINT ( 'NONE',  ( 0.2885700199627516116, -41.84838128711415806, -10.38006184593188053 ) ) ;
#48756=CARTESIAN_POINT ( 'NONE',  ( 0.6030672459662954621, -0.08726629989097470230, 48.10738700891300823 ) ) ;
#48758=CARTESIAN_POINT ( 'NONE',  ( 0.8751705887134553219, -44.76769609654225235, -17.57879340691528469 ) ) ;
#48765=CARTESIAN_POINT ( 'NONE',  ( 4.975801465491694664, 27.09127437476381317, -39.51822597168466444 ) ) ;
#48767=( BOUNDED_SURFACE ( )  B_SPLINE_SURFACE ( 3, 1, ( 
 ( #3207, #36762 ),
 ( #55520, #9152 ),
 ( #38307, #32054 ),
 ( #32669, #3823 ) ),
 .UNSPECIFIED., .F., .F., .F. ) 
 B_SPLINE_SURFACE_WITH_KNOTS ( ( 4, 4 ),
 ( 2, 2 ),
 ( 0.000000000000000000, 1.000000000000000000 ),
 ( 0.000000000000000000, 1.000000000000000000 ),
 .UNSPECIFIED. ) 
 GEOMETRIC_REPRESENTATION_ITEM ( )  RATIONAL_B_SPLINE_SURFACE ( (
 ( 1.000000000000000000, 1.000000000000000000),
 ( 0.9953040768229005630, 0.8617119497784937465),
 ( 0.9953040768229005630, 0.8617119497784937465),
 ( 1.000000000000000000, 1.000000000000000000) ) ) 
 REPRESENTATION_ITEM ( '' )  SURFACE ( )  );
#48769=ORIENTED_EDGE ( 'NONE', *, *, #44374, .F. ) ;
#48778=ORIENTED_EDGE ( 'NONE', *, *, #33498, .F. ) ;
#48779=EDGE_CURVE ( 'NONE', #14372, #44114, #58049, .T. ) ;
#48790=CARTESIAN_POINT ( 'NONE',  ( 2.301529144917014325, -28.20894756932170466, 38.87759814529768931 ) ) ;
#48795=B_SPLINE_CURVE_WITH_KNOTS ( 'NONE', 3,
 ( #17394, #27720, #36516, #3889 ),
 .UNSPECIFIED., .F., .F.,
 ( 4, 4 ),
 ( 0.000000000000000000, 0.005014147105413707325 ),
 .UNSPECIFIED. ) ;
#48796=CARTESIAN_POINT ( 'NONE',  ( 0.6001305935487422083, 44.64600790884054504, -17.92615948558495376 ) ) ;
#48799=CARTESIAN_POINT ( 'NONE',  ( 4.549368137175248350, -35.57418903283098643, -24.02461520945259466 ) ) ;
#48803=VECTOR ( 'NONE', #36777, 1000.000000000000114 ) ;
#48810=EDGE_CURVE ( 'NONE', #6553, #55243, #6113, .T. ) ;
#48815=CARTESIAN_POINT ( 'NONE',  ( -6.015611763856276717, -2.465697960550925938, -18.68122482568282550 ) ) ;
#48818=CARTESIAN_POINT ( 'NONE',  ( 2.301430502907643838, -42.22699195640122838, 22.89309745268816343 ) ) ;
#48819=CARTESIAN_POINT ( 'NONE',  ( 3.238741278300274029, -27.59904135366560496, 32.96375560769450175 ) ) ;
#48820=CARTESIAN_POINT ( 'NONE',  ( -6.001507490154110336, -2.475062734132314812, -18.68062548815628432 ) ) ;
#48827=ADVANCED_FACE ( 'NONE', ( #58740 ), #26823, .F. ) ;
#48830=CARTESIAN_POINT ( 'NONE',  ( 0.5988103564986360094, -47.61318305157298880, 6.880138274944153309 ) ) ;
#48839=LINE ( 'NONE', #38237, #24694 ) ;
#48854=EDGE_LOOP ( 'NONE', ( #30215, #60561, #8409, #9006 ) ) ;
#48855=CARTESIAN_POINT ( 'NONE',  ( -6.016761891674565099, -18.68153697670640057, -2.462934516564000198 ) ) ;
#48869=VERTEX_POINT ( 'NONE', #49060 ) ;
#48870=CARTESIAN_POINT ( 'NONE',  ( 0.2885700199627501683, -41.43179222486428159, 11.93479339212595391 ) ) ;
#48886=EDGE_CURVE ( 'NONE', #49767, #18458, #43908, .T. ) ;
#48896=VERTEX_POINT ( 'NONE', #10542 ) ;
#48897=CARTESIAN_POINT ( 'NONE',  ( 0.6009453534118439633, 18.81239552212984734, -44.27682103112812229 ) ) ;
#48906=CARTESIAN_POINT ( 'NONE',  ( 0.1073791018717483448, 6.109314776652144729, 42.68962945260955877 ) ) ;
#48909=CARTESIAN_POINT ( 'NONE',  ( 4.975801465491695552, -36.39623109580445259, -31.15993731089111662 ) ) ;
#48911=CARTESIAN_POINT ( 'NONE',  ( 4.975801465491695552, 0.000000000000000000, 0.000000000000000000 ) ) ;
#48913=CARTESIAN_POINT ( 'NONE',  ( -6.016104459813371719, 4.882138007282748937, 18.19977249352312398 ) ) ;
#48914=B_SPLINE_CURVE_WITH_KNOTS ( 'NONE', 3,
 ( #59591, #60507, #2579, #50201 ),
 .UNSPECIFIED., .F., .F.,
 ( 4, 4 ),
 ( 2.338762560254090381E-17, 0.004564976165746187711 ),
 .UNSPECIFIED. ) ;
#48925=CARTESIAN_POINT ( 'NONE',  ( 0.1313383488274120214, -39.59253935480808906, 17.09007684155433537 ) ) ;
#48938=CARTESIAN_POINT ( 'NONE',  ( 0.1092355843206037486, 10.87081649985031362, 41.73183925352184787 ) ) ;
#48943=ORIENTED_EDGE ( 'NONE', *, *, #23632, .F. ) ;
#48950=EDGE_CURVE ( 'NONE', #45191, #3699, #32880, .T. ) ;
#48954=CARTESIAN_POINT ( 'NONE',  ( -6.010958268070873523, -17.40352239307052784, -7.224487401384482865 ) ) ;
#48958=CARTESIAN_POINT ( 'NONE',  ( 0.6031357023905875581, -12.49325238079570610, 46.45693331047437624 ) ) ;
#48971=CARTESIAN_POINT ( 'NONE',  ( 0.8760168074886965917, -34.63873394077511136, 33.37827814204064936 ) ) ;
#48972=CARTESIAN_POINT ( 'NONE',  ( 0.1103878639767399417, -39.82320122342716928, 16.54784522866399499 ) ) ;
#48974=EDGE_CURVE ( 'NONE', #5781, #25122, #20640, .T. ) ;
#48975=CARTESIAN_POINT ( 'NONE',  ( 0.1102847568649952675, 34.15672344772088564, -26.32556309315081222 ) ) ;
#48981=CARTESIAN_POINT ( 'NONE',  ( 0.1100053167205930493, 30.36644426605139913, -30.62023953839050705 ) ) ;
#48982=CARTESIAN_POINT ( 'NONE',  ( 0.6009453534118439633, -6.711694149738577586, 47.63713118507416056 ) ) ;
#48987=CARTESIAN_POINT ( 'NONE',  ( 0.6009453534118440743, -24.43073772334946980, 41.44251633523849421 ) ) ;
#48992=CARTESIAN_POINT ( 'NONE',  ( 0.7954196712028467342, -47.56618050291069721, -7.138712347928016122 ) ) ;
#48998=CARTESIAN_POINT ( 'NONE',  ( 0.1103310638050661874, -43.12437788119554227, -0.08238894504380574191 ) ) ;
#49006=EDGE_CURVE ( 'NONE', #25607, #11251, #57217, .T. ) ;
#49012=CONICAL_SURFACE ( 'NONE', #42019, 42.92674063221959813, 1.485477209440487556 ) ;
#49021=VERTEX_POINT ( 'NONE', #42462 ) ;
#49023=CARTESIAN_POINT ( 'NONE',  ( 4.322998006666179727, 25.80712523194219088, 40.45864630878526924 ) ) ;
#49025=CARTESIAN_POINT ( 'NONE',  ( 5.880360259849739535, 36.03610316515383261, -31.66572319753524312 ) ) ;
#49039=CARTESIAN_POINT ( 'NONE',  ( 4.833616638992208614, 15.29495699393663344, 43.64812679991126743 ) ) ;
#49042=CARTESIAN_POINT ( 'NONE',  ( -6.001507490154110336, 16.32705935667506836, 9.408444979392378116 ) ) ;
#49054=CARTESIAN_POINT ( 'NONE',  ( 4.549368137175248350, 0.000000000000000000, 0.000000000000000000 ) ) ;
#49056=VECTOR ( 'NONE', #16096, 999.9999999999998863 ) ;
#49060=CARTESIAN_POINT ( 'NONE',  ( 0.5998501479064699549, -44.24259072156099393, 18.89267974119588445 ) ) ;
#49061=CARTESIAN_POINT ( 'NONE',  ( 0.6001305935487315502, 17.92615948558476546, 44.64600790884062320 ) ) ;
#49064=CARTESIAN_POINT ( 'NONE',  ( 0.5998501479064699549, 48.10473956285920138, -0.5236536531309904374 ) ) ;
#49069=CARTESIAN_POINT ( 'NONE',  ( 0.8751705887134553219, 46.67919521768871505, 11.58504748649215976 ) ) ;
#49076=CARTESIAN_POINT ( 'NONE',  ( 0.1092355843206037486, 16.22491322981570860, 39.95589129953373941 ) ) ;
#49081=EDGE_CURVE ( 'NONE', #45060, #42739, #54217, .T. ) ;
#49083=ORIENTED_EDGE ( 'NONE', *, *, #58755, .T. ) ;
#49084=ADVANCED_FACE ( 'NONE', ( #56828 ), #26911, .F. ) ;
#49088=VERTEX_POINT ( 'NONE', #18027 ) ;
#49090=CARTESIAN_POINT ( 'NONE',  ( 0.1092355843206037486, -0.3005923759136885365, 43.12343565949664992 ) ) ;
#49092=ORIENTED_EDGE ( 'NONE', *, *, #55367, .F. ) ;
#49097=EDGE_CURVE ( 'NONE', #61466, #35404, #15828, .T. ) ;
#49106=LINE ( 'NONE', #53476, #10732 ) ;
#49118=CARTESIAN_POINT ( 'NONE',  ( 4.691466044806103852, -14.64802401911199503, -42.11359095667484098 ) ) ;
#49123=CARTESIAN_POINT ( 'NONE',  ( -6.016104459813371719, -2.464823636987321986, -18.68131780085934324 ) ) ;
#49125=CARTESIAN_POINT ( 'NONE',  ( 1.827119703190778877, 25.21842556008185099, -34.89020442382232545 ) ) ;
#49126=CARTESIAN_POINT ( 'NONE',  ( 0.1073791018717483448, 30.83464511437097499, 30.14884492832400298 ) ) ;
#49128=CARTESIAN_POINT ( 'NONE',  ( 0.2224561200757582402, 29.94832483817993918, 31.02237548791962496 ) ) ;
#49138=( BOUNDED_SURFACE ( )  B_SPLINE_SURFACE ( 3, 1, ( 
 ( #16090, #11384 ),
 ( #49583, #4113 ),
 ( #4412, #56438 ),
 ( #13246, #18876 ) ),
 .UNSPECIFIED., .F., .F., .F. ) 
 B_SPLINE_SURFACE_WITH_KNOTS ( ( 4, 4 ),
 ( 2, 2 ),
 ( 0.000000000000000000, 1.000000000000000000 ),
 ( 0.000000000000000000, 1.000000000000000000 ),
 .UNSPECIFIED. ) 
 GEOMETRIC_REPRESENTATION_ITEM ( )  RATIONAL_B_SPLINE_SURFACE ( (
 ( 1.000000000000000000, 1.000000000000000000),
 ( 0.9751682680413298332, 0.9999560080971552356),
 ( 0.9751682680413298332, 0.9999560080971552356),
 ( 1.000000000000000000, 1.000000000000000000) ) ) 
 REPRESENTATION_ITEM ( '' )  SURFACE ( )  );
#49153=CARTESIAN_POINT ( 'NONE',  ( -6.016761891674565099, -4.873659902332239113, -18.20201388312100477 ) ) ;
#49157=EDGE_CURVE ( 'NONE', #19838, #38743, #31063, .T. ) ;
#49158=CARTESIAN_POINT ( 'NONE',  ( 4.691466044806103852, 14.01607102724543097, -42.32811009116542067 ) ) ;
#49163=ORIENTED_EDGE ( 'NONE', *, *, #41082, .F. ) ;
#49164=CARTESIAN_POINT ( 'NONE',  ( 0.8751705887134423323, -44.76769609654249393, 17.57879340691464165 ) ) ;
#49168=ORIENTED_EDGE ( 'NONE', *, *, #28361, .T. ) ;
#49172=CARTESIAN_POINT ( 'NONE',  ( 4.691466044806102964, 29.14742760351063566, 33.74235639413337395 ) ) ;
#49174=CARTESIAN_POINT ( 'NONE',  ( 0.8751705887134553219, -46.21789262997766201, 13.30665218149281870 ) ) ;
#49177=ORIENTED_EDGE ( 'NONE', *, *, #56174, .T. ) ;
#49178=CARTESIAN_POINT ( 'NONE',  ( 0.1073791018717483448, -41.52698815987176317, 11.62916352156079824 ) ) ;
#49179=CARTESIAN_POINT ( 'NONE',  ( 0.1064266379913938604, 33.86837498006626390, -26.69589650908249467 ) ) ;
#49188=FACE_OUTER_BOUND ( 'NONE', #47422, .T. ) ;
#49194=CARTESIAN_POINT ( 'NONE',  ( 5.880360259849739535, -31.66572319753537101, -36.03610316515372602 ) ) ;
#49210=EDGE_CURVE ( 'NONE', #45553, #11417, #52016, .T. ) ;
#49214=CARTESIAN_POINT ( 'NONE',  ( 0.7245667037590765025, 47.57651946688177702, -7.091191019330373102 ) ) ;
#49220=EDGE_CURVE ( 'NONE', #28915, #42953, #51234, .T. ) ;
#49227=EDGE_CURVE ( 'NONE', #34790, #24212, #55006, .T. ) ;
#49245=ORIENTED_EDGE ( 'NONE', *, *, #37883, .T. ) ;
#49246=LINE ( 'NONE', #49871, #50685 ) ;
#49247=DIRECTION ( 'NONE',  ( 0.1024043820194936449, -0.7811075516170163935, 0.6159418278945469893 ) ) ;
#49252=ORIENTED_EDGE ( 'NONE', *, *, #52265, .F. ) ;
#49256=CARTESIAN_POINT ( 'NONE',  ( 2.643462169533613793, 42.27470921730908771, 22.81120928486510024 ) ) ;
#49257=FACE_OUTER_BOUND ( 'NONE', #40197, .T. ) ;
#49263=EDGE_CURVE ( 'NONE', #351, #47799, #22857, .T. ) ;
#49264=ORIENTED_EDGE ( 'NONE', *, *, #33245, .F. ) ;
#49266=CARTESIAN_POINT ( 'NONE',  ( 4.549368137175248350, 0.000000000000000000, 0.000000000000000000 ) ) ;
#49269=CARTESIAN_POINT ( 'NONE',  ( 0.1087620492084205859, -39.97903073778078209, 16.16798550313352578 ) ) ;
#49272=DIRECTION ( 'NONE',  ( -1.000000000000000000, -0.000000000000000000, -0.000000000000000000 ) ) ;
#49277=EDGE_CURVE ( 'NONE', #47251, #9480, #29611, .T. ) ;
#49282=CARTESIAN_POINT ( 'NONE',  ( 4.322998006666165516, 36.74401119231367119, 30.86725474310372519 ) ) ;
#49285=CARTESIAN_POINT ( 'NONE',  ( 0.6254311100348644015, -44.17670535157497369, -19.04346769887678192 ) ) ;
#49287=B_SPLINE_CURVE_WITH_KNOTS ( 'NONE', 3,
 ( #25514, #58393, #1691, #25213 ),
 .UNSPECIFIED., .F., .F.,
 ( 4, 4 ),
 ( 0.000000000000000000, 0.005014147105413699519 ),
 .UNSPECIFIED. ) ;
#49296=CARTESIAN_POINT ( 'NONE',  ( 0.1073791018717483448, -33.91564619577824402, 26.63563652260111070 ) ) ;
#49300=ORIENTED_EDGE ( 'NONE', *, *, #23690, .T. ) ;
#49303=CARTESIAN_POINT ( 'NONE',  ( 0.1084644655670281704, -37.14658555883747937, 21.90577137312928002 ) ) ;
#49307=ORIENTED_EDGE ( 'NONE', *, *, #29289, .F. ) ;
#49308=ORIENTED_EDGE ( 'NONE', *, *, #2451, .F. ) ;
#49318=CARTESIAN_POINT ( 'NONE',  ( 4.549368137175248350, 38.59302160394752690, -18.79584381673492288 ) ) ;
#49320=ORIENTED_EDGE ( 'NONE', *, *, #19699, .F. ) ;
#49321=CARTESIAN_POINT ( 'NONE',  ( 4.975801465491695552, 42.71626295676264817, -21.70134120755155394 ) ) ;
#49323=ORIENTED_EDGE ( 'NONE', *, *, #41395, .T. ) ;
#49324=CARTESIAN_POINT ( 'NONE',  ( -2.708315649062916552, -8.698422600177206476, 11.76894112707797646 ) ) ;
#49326=CARTESIAN_POINT ( 'NONE',  ( 0.6023142530420679819, 46.53533807097414154, 12.19802990522816977 ) ) ;
#49330=CARTESIAN_POINT ( 'NONE',  ( 0.1064266418746776799, 5.071708474752668394, 42.82540703015434502 ) ) ;
#49335=VERTEX_POINT ( 'NONE', #48230 ) ;
#49337=CARTESIAN_POINT ( 'NONE',  ( 0.5988103564986355654, -47.77151399983773672, -5.677495323490556522 ) ) ;
#49338=ORIENTED_EDGE ( 'NONE', *, *, #19005, .T. ) ;
#49342=ORIENTED_EDGE ( 'NONE', *, *, #2670, .T. ) ;
#49344=CARTESIAN_POINT ( 'NONE',  ( 0.6023142530420679819, -47.66103033449103066, 6.538792732869052493 ) ) ;
#49351=CARTESIAN_POINT ( 'NONE',  ( 3.680882792899937694, -1.849662971457888272, -47.94008871805917948 ) ) ;
#49352=CARTESIAN_POINT ( 'NONE',  ( -6.001507490154110336, -2.444174634178271521, 18.68469198366096151 ) ) ;
#49356=CARTESIAN_POINT ( 'NONE',  ( 0.5998501479064708430, -17.92509395669076966, -44.64337787626241294 ) ) ;
#49357=EDGE_CURVE ( 'NONE', #20018, #49695, #25960, .T. ) ;
#49359=VERTEX_POINT ( 'NONE', #20340 ) ;
#49372=CARTESIAN_POINT ( 'NONE',  ( 0.6030672459662951290, 0.08726629989075269933, -48.10738700891300823 ) ) ;
#49373=CARTESIAN_POINT ( 'NONE',  ( 0.3622758884714730732, -37.74294673546571488, -20.83792692158958815 ) ) ;
#49375=ORIENTED_EDGE ( 'NONE', *, *, #35528, .F. ) ;
#49386=CARTESIAN_POINT ( 'NONE',  ( 0.1103744047535531458, -11.12399292196407963, -41.66501489234560296 ) ) ;
#49393=EDGE_LOOP ( 'NONE', ( #32559, #8854, #5338, #29997 ) ) ;
#49394=EDGE_CURVE ( 'NONE', #38461, #14894, #16252, .T. ) ;
#49405=ORIENTED_EDGE ( 'NONE', *, *, #1401, .T. ) ;
#49406=B_SPLINE_CURVE_WITH_KNOTS ( 'NONE', 3,
 ( #4764, #52706, #5992, #16357, #6931, #35483, #45204, #39887, #15439, #25754 ),
 .UNSPECIFIED., .F., .F.,
 ( 4, 3, 3, 4 ),
 ( 1.157434093048479169E-16, 0.0002618519381806256457, 0.0003927759815485974389, 0.0004849530346204834448 ),
 .UNSPECIFIED. ) ;
#49410=CARTESIAN_POINT ( 'NONE',  ( 4.975801465491694664, 47.76942479135480824, 3.702618843597622167 ) ) ;
#49411=ORIENTED_EDGE ( 'NONE', *, *, #48182, .F. ) ;
#49416=ORIENTED_EDGE ( 'NONE', *, *, #42294, .T. ) ;
#49418=CARTESIAN_POINT ( 'NONE',  ( -6.010958268070873523, 17.40352239307057403, 7.224487401384361185 ) ) ;
#49422=ORIENTED_EDGE ( 'NONE', *, *, #12674, .T. ) ;
#49427=CARTESIAN_POINT ( 'NONE',  ( 4.975801465491694664, -14.85979367497141546, -45.55012473237748338 ) ) ;
#49434=VERTEX_POINT ( 'NONE', #10632 ) ;
#49435=ADVANCED_FACE ( 'NONE', ( #29721 ), #28912, .F. ) ;
#49436=CARTESIAN_POINT ( 'NONE',  ( -6.016489644550736315, 11.47450955518487525, 14.94663725562919865 ) ) ;
#49450=CARTESIAN_POINT ( 'NONE',  ( 2.643462169533600914, 38.93558293168539564, -28.13401304854679807 ) ) ;
#49458=CARTESIAN_POINT ( 'NONE',  ( 0.1073791018717578927, -33.91564619577789585, -26.63563652260155123 ) ) ;
#49459=B_SPLINE_CURVE_WITH_KNOTS ( 'NONE', 3,
 ( #53639, #40230, #11701, #30162, #15465, #6024, #48975, #49900, #25158, #24864, #59280, #1644, #10772, #44304, #1959, #25463, #58977, #1333, #5714 ),
 .UNSPECIFIED., .F., .F.,
 ( 4, 3, 3, 3, 3, 3, 4 ),
 ( 1.165802754517233128E-16, 0.0002618519381806232063, 0.0003927759815485978184, 0.0005237000248299410448, 0.0006546240681324946810, 0.0007855481115631255534, 0.0009699050456655074724 ),
 .UNSPECIFIED. ) ;
#49460=CARTESIAN_POINT ( 'NONE',  ( 0.1100247026804066219, 43.12411436000287779, 0.1696715072118848977 ) ) ;
#49463=CARTESIAN_POINT ( 'NONE',  ( 0.1097557419366048670, -41.59672960874321035, 11.37678103520264195 ) ) ;
#49486=ORIENTED_EDGE ( 'NONE', *, *, #7018, .F. ) ;
#49490=CARTESIAN_POINT ( 'NONE',  ( 0.6031356755773454870, 24.05374386753658555, 41.66225520948412253 ) ) ;
#49496=ORIENTED_EDGE ( 'NONE', *, *, #21868, .F. ) ;
#49501=LINE ( 'NONE', #16302, #55511 ) ;
#49504=DIRECTION ( 'NONE',  ( 0.000000000000000000, 0.000000000000000000, 1.000000000000000000 ) ) ;
#49511=VERTEX_POINT ( 'NONE', #34141 ) ;
#49514=DIRECTION ( 'NONE',  ( 0.09835009131224552170, 0.3879606369183508097, 0.9164135549743797071 ) ) ;
#49517=DIRECTION ( 'NONE',  ( 0.000000000000000000, 0.000000000000000000, 1.000000000000000000 ) ) ;
#49518=FACE_OUTER_BOUND ( 'NONE', #14748, .T. ) ;
#49524=CARTESIAN_POINT ( 'NONE',  ( 0.8760168074886965917, 28.57146030081927890, 38.69913431881832366 ) ) ;
#49532=CARTESIAN_POINT ( 'NONE',  ( 0.8751705887134553219, -23.27176129838455054, 42.09020928323333521 ) ) ;
#49533=CARTESIAN_POINT ( 'NONE',  ( 4.549368137175248350, 13.59764261105693350, 40.71620287708348940 ) ) ;
#49534=CARTESIAN_POINT ( 'NONE',  ( 0.6030672727741701600, -12.36682345648149095, -46.49075153683468642 ) ) ;
#49550=B_SPLINE_CURVE_WITH_KNOTS ( 'NONE', 3,
 ( #59390, #16820, #54068, #25581, #44719, #35009, #16195, #21817, #2063, #49386, #15893, #20890, #58764, #35627, #40332, #50310, #45336, #1758, #7697 ),
 .UNSPECIFIED., .F., .F.,
 ( 4, 3, 3, 3, 3, 3, 4 ),
 ( 1.144439277862597989E-16, 0.0002618519381806255373, 0.0003927759815486000952, 0.0005237000248299464658, 0.0006546240681325001020, 0.0007855481115631326007, 0.0009699050456655100745 ),
 .UNSPECIFIED. ) ;
#49551=CARTESIAN_POINT ( 'NONE',  ( -6.015611763856276717, 2.465697960551318069, -18.68122482568277221 ) ) ;
#49554=CARTESIAN_POINT ( 'NONE',  ( 0.8751705887134423323, -47.79200036674284036, 5.393078191591890835 ) ) ;
#49556=CARTESIAN_POINT ( 'NONE',  ( 0.1073791018717483448, 41.52698815987167791, -11.62916352156108779 ) ) ;
#49563=CIRCLE ( 'NONE', #512, 42.92674063221959813 ) ;
#49568=CARTESIAN_POINT ( 'NONE',  ( 0.6031356755773454870, -41.66228085015309546, -24.05369945659519004 ) ) ;
#49573=CARTESIAN_POINT ( 'NONE',  ( -2.569797478183790229, -11.33042594333542041, -9.259773107243024270 ) ) ;
#49580=EDGE_CURVE ( 'NONE', #26668, #36895, #17489, .T. ) ;
#49583=CARTESIAN_POINT ( 'NONE',  ( -6.017396004339687465, 11.47005965438138375, 14.95000090562885475 ) ) ;
#49589=ADVANCED_FACE ( 'NONE', ( #59454 ), #9828, .F. ) ;
#49600=VERTEX_POINT ( 'NONE', #21568 ) ;
#49603=DIRECTION ( 'NONE',  ( 0.1024043820194936449, 0.7126273545981393065, 0.6940285268068333568 ) ) ;
#49608=CARTESIAN_POINT ( 'NONE',  ( 1.827326673878743701, 1.232746109312175431, -43.03225468313001301 ) ) ;
#49617=CARTESIAN_POINT ( 'NONE',  ( 2.301430502907644726, -47.77346269870103868, 4.990893951996192790 ) ) ;
#49618=ADVANCED_FACE ( 'NONE', ( #2442 ), #48140, .F. ) ;
#49620=AXIS2_PLACEMENT_3D ( 'NONE', #37455, #19266, #56526 ) ;
#49621=CARTESIAN_POINT ( 'NONE',  ( 0.8751705887134553219, 19.22545746485597817, 44.08562551107088723 ) ) ;
#49623=EDGE_CURVE ( 'NONE', #23536, #10336, #39964, .T. ) ;
#49629=ORIENTED_EDGE ( 'NONE', *, *, #21657, .F. ) ;
#49631=CARTESIAN_POINT ( 'NONE',  ( -6.015611763856276717, 9.427003116184401676, -16.31561949997065852 ) ) ;
#49633=CARTESIAN_POINT ( 'NONE',  ( 4.549368137175248350, 19.17571786012269541, 38.40568845698284406 ) ) ;
#49642=CARTESIAN_POINT ( 'NONE',  ( -2.569797478183783568, 14.62602397812941390, -0.4487456364277307430 ) ) ;
#49643=CARTESIAN_POINT ( 'NONE',  ( 0.6254087463353915632, -47.77987801197956941, -5.596276562478156080 ) ) ;
#49646=ADVANCED_FACE ( 'NONE', ( #198 ), #17766, .F. ) ;
#49648=CARTESIAN_POINT ( 'NONE',  ( 0.6254087463353924514, -5.596276562478680106, 47.77987801197951256 ) ) ;
#49653=CARTESIAN_POINT ( 'NONE',  ( 0.6030672727741701600, -41.70584815505905141, 23.97812608463460293 ) ) ;
#49655=CARTESIAN_POINT ( 'NONE',  ( -6.010958268070873523, 18.19761767765829674, 4.891065400978450661 ) ) ;
#49662=ORIENTED_EDGE ( 'NONE', *, *, #4351, .T. ) ;
#49664=VECTOR ( 'NONE', #39279, 999.9999999999998863 ) ;
#49666=CARTESIAN_POINT ( 'NONE',  ( 4.549368137175248350, 0.000000000000000000, 0.000000000000000000 ) ) ;
#49670=CARTESIAN_POINT ( 'NONE',  ( 1.827326673878743923, -31.30008222956402619, 29.55671596281155189 ) ) ;
#49673=( BOUNDED_SURFACE ( )  B_SPLINE_SURFACE ( 3, 1, ( 
 ( #29953, #49061 ),
 ( #38153, #19962 ),
 ( #19333, #25253 ),
 ( #58132, #34360 ) ),
 .UNSPECIFIED., .F., .F., .F. ) 
 B_SPLINE_SURFACE_WITH_KNOTS ( ( 4, 4 ),
 ( 2, 2 ),
 ( 0.000000000000000000, 1.000000000000000000 ),
 ( 0.000000000000000000, 1.000000000000000000 ),
 .UNSPECIFIED. ) 
 GEOMETRIC_REPRESENTATION_ITEM ( )  RATIONAL_B_SPLINE_SURFACE ( (
 ( 1.000000000000000000, 1.000000000000000000),
 ( 0.9953040768229013402, 0.8617119497784988535),
 ( 0.9953040768229013402, 0.8617119497784988535),
 ( 1.000000000000000000, 1.000000000000000000) ) ) 
 REPRESENTATION_ITEM ( '' )  SURFACE ( )  );
#49675=B_SPLINE_CURVE_WITH_KNOTS ( 'NONE', 3,
 ( #38242, #41710, #4664, #56687 ),
 .UNSPECIFIED., .F., .F.,
 ( 4, 4 ),
 ( 2.030441771438897272E-17, 0.004444306975806115896 ),
 .UNSPECIFIED. ) ;
#49678=CARTESIAN_POINT ( 'NONE',  ( 2.301430502907645170, -30.25184447737462179, 37.31003439265355581 ) ) ;
#49683=B_SPLINE_CURVE_WITH_KNOTS ( 'NONE', 3,
 ( #3351, #7752, #60991, #18099 ),
 .UNSPECIFIED., .F., .F.,
 ( 4, 4 ),
 ( 0.000000000000000000, 0.005014147105413699519 ),
 .UNSPECIFIED. ) ;
#49685=CARTESIAN_POINT ( 'NONE',  ( 0.1092565886968785427, 16.78938711553573881, 39.72209809039404149 ) ) ;
#49687=CARTESIAN_POINT ( 'NONE',  ( 0.7954190325252783467, 0.8690070772082590933, 48.09103420665682904 ) ) ;
#49688=CARTESIAN_POINT ( 'NONE',  ( 0.1100247026804066219, 41.69861001364773045, -10.99745200874652085 ) ) ;
#49695=VERTEX_POINT ( 'NONE', #23115 ) ;
#49698=EDGE_CURVE ( 'NONE', #36963, #19158, #9309, .T. ) ;
#49705=ORIENTED_EDGE ( 'NONE', *, *, #43575, .T. ) ;
#49707=EDGE_CURVE ( 'NONE', #11417, #60124, #19102, .T. ) ;
#49715=CARTESIAN_POINT ( 'NONE',  ( -5.995132425357893702, 7.203480333239078881, 17.41298668506973257 ) ) ;
#49717=CARTESIAN_POINT ( 'NONE',  ( 0.6041374136657475802, 44.51224464244998558, -18.24862627831490158 ) ) ;
#49729=VERTEX_POINT ( 'NONE', #14963 ) ;
#49740=CARTESIAN_POINT ( 'NONE',  ( 0.1102144999581333162, -5.503895401229690343, -42.77179372778541477 ) ) ;
#49742=CARTESIAN_POINT ( 'NONE',  ( -2.708315649062910779, -12.80362818457450125, 7.087851317223748282 ) ) ;
#49743=ORIENTED_EDGE ( 'NONE', *, *, #31277, .T. ) ;
#49746=CARTESIAN_POINT ( 'NONE',  ( -2.569797478183783568, -1.464172661884271198, 14.55946937464481117 ) ) ;
#49756=AXIS2_PLACEMENT_3D ( 'NONE', #30997, #40125, #16282 ) ;
#49767=VERTEX_POINT ( 'NONE', #38775 ) ;
#49768=B_SPLINE_CURVE_WITH_KNOTS ( 'NONE', 3,
 ( #35130, #11952, #30713, #30395, #26631, #16951 ),
 .UNSPECIFIED., .F., .F.,
 ( 4, 2, 4 ),
 ( 1.283058336952897787E-16, 0.0002450741128632365705, 0.0004901482257263447715 ),
 .UNSPECIFIED. ) ;
#49770=( BOUNDED_SURFACE ( )  B_SPLINE_SURFACE ( 3, 1, ( 
 ( #17866, #56052 ),
 ( #24095, #9369 ),
 ( #28475, #23472 ),
 ( #33203, #19109 ) ),
 .UNSPECIFIED., .F., .F., .F. ) 
 B_SPLINE_SURFACE_WITH_KNOTS ( ( 4, 4 ),
 ( 2, 2 ),
 ( 0.000000000000000000, 1.000000000000000000 ),
 ( 0.000000000000000000, 1.000000000000000000 ),
 .UNSPECIFIED. ) 
 GEOMETRIC_REPRESENTATION_ITEM ( )  RATIONAL_B_SPLINE_SURFACE ( (
 ( 1.000000000000000000, 1.000000000000000000),
 ( 0.9953040768229013402, 0.8617119497784988535),
 ( 0.9953040768229013402, 0.8617119497784988535),
 ( 1.000000000000000000, 1.000000000000000000) ) ) 
 REPRESENTATION_ITEM ( '' )  SURFACE ( )  );
#49771=DIRECTION ( 'NONE',  ( -0.000000000000000000, 0.000000000000000000, 1.000000000000000000 ) ) ;
#49774=CARTESIAN_POINT ( 'NONE',  ( 0.1095718737110178975, -41.72082389913624212, 10.91304379104990119 ) ) ;
#49778=AXIS2_PLACEMENT_3D ( 'NONE', #47837, #28097, #43452 ) ;
#49779=EDGE_CURVE ( 'NONE', #14890, #22780, #31356, .T. ) ;
#49781=VERTEX_POINT ( 'NONE', #34072 ) ;
#49791=EDGE_CURVE ( 'NONE', #38743, #37278, #12323, .T. ) ;
#49801=CARTESIAN_POINT ( 'NONE',  ( 0.6001305935487422083, 23.60027211631772204, 41.92422178329177029 ) ) ;
#49804=EDGE_CURVE ( 'NONE', #1146, #19605, #54893, .T. ) ;
#49828=AXIS2_PLACEMENT_3D ( 'NONE', #38528, #52277, #24717 ) ;
#49829=( NAMED_UNIT ( * ) SI_UNIT ( $, .STERADIAN. ) SOLID_ANGLE_UNIT ( ) );
#49832=VERTEX_POINT ( 'NONE', #34368 ) ;
#49833=CARTESIAN_POINT ( 'NONE',  ( 0.3622758884714730732, -25.58609868863794290, 34.70015533914785522 ) ) ;
#49835=CARTESIAN_POINT ( 'NONE',  ( 0.2885700199627510565, 6.424755504217665170, 42.63514063525628472 ) ) ;
#49842=B_SPLINE_CURVE_WITH_KNOTS ( 'NONE', 3,
 ( #19745, #4989, #43256, #5300 ),
 .UNSPECIFIED., .F., .F.,
 ( 4, 4 ),
 ( 2.165040709395311621E-17, 0.004444306975806115896 ),
 .UNSPECIFIED. ) ;
#49853=B_SPLINE_CURVE_WITH_KNOTS ( 'NONE', 3,
 ( #15455, #53630, #8654, #1633, #39588, #29849 ),
 .UNSPECIFIED., .F., .F.,
 ( 4, 2, 4 ),
 ( 1.823858501009600881E-17, 0.0002293319059085093849, 0.0004586638118170005009 ),
 .UNSPECIFIED. ) ;
#49858=FACE_OUTER_BOUND ( 'NONE', #49926, .T. ) ;
#49859=ADVANCED_FACE ( 'NONE', ( #25264 ), #52509, .F. ) ;
#49864=VERTEX_POINT ( 'NONE', #48758 ) ;
#49871=CARTESIAN_POINT ( 'NONE',  ( -2.569797478183790229, 1.464172661883968551, 14.55946937464484492 ) ) ;
#49879=CARTESIAN_POINT ( 'NONE',  ( 0.1102847568649952675, -30.42833243501171481, 30.55869130182056281 ) ) ;
#49880=AXIS2_PLACEMENT_3D ( 'NONE', #43704, #33986, #53061 ) ;
#49895=VERTEX_POINT ( 'NONE', #35612 ) ;
#49897=CARTESIAN_POINT ( 'NONE',  ( 0.8751705887134553219, 28.56654290188653178, -38.69254731947804515 ) ) ;
#49898=CARTESIAN_POINT ( 'NONE',  ( 0.8760168074887076939, -19.22870327415273550, -44.09317760313745538 ) ) ;
#49900=CARTESIAN_POINT ( 'NONE',  ( 0.1103878639767399417, 34.18336104662739672, -26.29099398937411536 ) ) ;
#49905=CARTESIAN_POINT ( 'NONE',  ( 0.6023143664670691511, 12.70384782338089558, -46.39980466492348654 ) ) ;
#49906=CARTESIAN_POINT ( 'NONE',  ( 0.6030672727741701600, -6.365785297725128800, 47.68443224372860101 ) ) ;
#49910=CARTESIAN_POINT ( 'NONE',  ( 0.2885700199627512785, -11.93479339212638379, -41.43179222486415370 ) ) ;
#49914=CARTESIAN_POINT ( 'NONE',  ( -2.708315649062916552, 14.54141329178160191, 1.648584381067091931 ) ) ;
#49915=CARTESIAN_POINT ( 'NONE',  ( 0.6023143664670691511, -6.019611522082996657, -47.72938193173970234 ) ) ;
#49920=CARTESIAN_POINT ( 'NONE',  ( 0.8760168074887090262, 47.56749362999713782, -7.161346975773206225 ) ) ;
#49923=CARTESIAN_POINT ( 'NONE',  ( 0.5980894510889457338, 46.65000524237070323, 11.77356634613333952 ) ) ;
#49925=CARTESIAN_POINT ( 'NONE',  ( 4.549368137175248350, 38.59302160394725689, 18.79584381673547711 ) ) ;
#49926=EDGE_LOOP ( 'NONE', ( #35676, #61627, #41896, #53452 ) ) ;
#49927=ORIENTED_EDGE ( 'NONE', *, *, #40170, .F. ) ;
#49929=CARTESIAN_POINT ( 'NONE',  ( 0.5980894510889457338, 33.52121017007826964, -34.51330645350367377 ) ) ;
#49933=ORIENTED_EDGE ( 'NONE', *, *, #21648, .T. ) ;
#49937=VECTOR ( 'NONE', #40956, 1000.000000000000000 ) ;
#49938=CARTESIAN_POINT ( 'NONE',  ( -2.569797478183790229, 14.24379821351257469, -3.352038560005768719 ) ) ;
#49939=CARTESIAN_POINT ( 'NONE',  ( -6.016104459813374383, 2.454244026261090283, 18.68271063303495794 ) ) ;
#49950=CARTESIAN_POINT ( 'NONE',  ( 3.680882792899936362, 44.99870212802617431, 16.63701193714004845 ) ) ;
#49952=ORIENTED_EDGE ( 'NONE', *, *, #46218, .F. ) ;
#49963=VERTEX_POINT ( 'NONE', #17109 ) ;
#49965=DIRECTION ( 'NONE',  ( 1.000000000000000000, 0.000000000000000000, 0.000000000000000000 ) ) ;
#49992=CARTESIAN_POINT ( 'NONE',  ( 0.6009452777970412107, 41.44251326863928853, -24.43074291040862533 ) ) ;
#49994=CARTESIAN_POINT ( 'NONE',  ( 0.2224561200757622370, -6.380320192202297847, 42.64482917976808096 ) ) ;
#49999=CIRCLE ( 'NONE', #54985, 42.92674063221959813 ) ;
#50009=CARTESIAN_POINT ( 'NONE',  ( 0.3622758884714600280, 37.74294673546586409, -20.83792692158932525 ) ) ;
#50013=CARTESIAN_POINT ( 'NONE',  ( 3.238741278300274917, -3.793425828152354295, -42.82436441900172497 ) ) ;
#50015=ORIENTED_EDGE ( 'NONE', *, *, #55853, .T. ) ;
#50016=CARTESIAN_POINT ( 'NONE',  ( 0.1081432562775997697, -0.4234896101214557507, 43.12249629849792854 ) ) ;
#50018=CARTESIAN_POINT ( 'NONE',  ( 0.8751705887134553219, -11.58504748649232496, 46.67919521768867241 ) ) ;
#50026=CARTESIAN_POINT ( 'NONE',  ( 0.5998501479064708430, 23.59887241503295741, 41.92175333043627461 ) ) ;
#50031=B_SPLINE_CURVE_WITH_KNOTS ( 'NONE', 3,
 ( #22930, #60192, #3478, #6385 ),
 .UNSPECIFIED., .F., .F.,
 ( 4, 4 ),
 ( 0.000000000000000000, 0.005014147105413695182 ),
 .UNSPECIFIED. ) ;
#50035=VERTEX_POINT ( 'NONE', #7678 ) ;
#50038=VERTEX_POINT ( 'NONE', #61229 ) ;
#50040=EDGE_LOOP ( 'NONE', ( #52401, #14973, #5194, #10833 ) ) ;
#50044=CARTESIAN_POINT ( 'NONE',  ( 0.1097557419366048670, -26.07515889977844026, 34.34829179474790095 ) ) ;
#50045=ORIENTED_EDGE ( 'NONE', *, *, #49263, .T. ) ;
#50046=CARTESIAN_POINT ( 'NONE',  ( -6.015611763856276717, 17.41126425312547710, -7.205255340944423992 ) ) ;
#50048=CARTESIAN_POINT ( 'NONE',  ( 4.322998006666179727, 39.32552843303813006, 27.50295597456465302 ) ) ;
#50054=CARTESIAN_POINT ( 'NONE',  ( 4.975801465491694664, 26.14269827151623105, 40.15204426031542795 ) ) ;
#50057=CARTESIAN_POINT ( 'NONE',  ( 4.549368137175248350, -8.582197505784124658, -42.06008734272393212 ) ) ;
#50059=CARTESIAN_POINT ( 'NONE',  ( 0.1092565886968784455, 37.19081526480825062, -21.83052579204423793 ) ) ;
#50062=EDGE_CURVE ( 'NONE', #52610, #30576, #24287, .T. ) ;
#50067=CARTESIAN_POINT ( 'NONE',  ( 4.975801465491695552, -9.906103548667894998, -46.87746200127453022 ) ) ;
#50081=CARTESIAN_POINT ( 'NONE',  ( 1.827326673878744590, -17.60663982372562941, 39.28486782721036263 ) ) ;
#50086=CARTESIAN_POINT ( 'NONE',  ( 0.1100053167205930910, 10.98799238780951271, -41.70112744323659371 ) ) ;
#50088=CARTESIAN_POINT ( 'NONE',  ( 0.1073791018717578927, 43.12183934961191056, 0.4849339620934667305 ) ) ;
#50091=CARTESIAN_POINT ( 'NONE',  ( 0.1092355843206037486, -41.73183925352188339, 10.87081649985017151 ) ) ;
#50092=ORIENTED_EDGE ( 'NONE', *, *, #3724, .F. ) ;
#50098=LINE ( 'NONE', #21591, #45890 ) ;
#50099=CARTESIAN_POINT ( 'NONE',  ( 0.6031356755773454870, -29.28593560184460287, 38.16621646312157878 ) ) ;
#50104=CARTESIAN_POINT ( 'NONE',  ( 0.1098349054025746507, -26.08296594991515960, -34.34238705454293950 ) ) ;
#50110=ORIENTED_EDGE ( 'NONE', *, *, #21779, .F. ) ;
#50113=VERTEX_POINT ( 'NONE', #4204 ) ;
#50117=CARTESIAN_POINT ( 'NONE',  ( 2.301430502907645614, -25.12309903330049110, 40.93949994354142063 ) ) ;
#50118=CARTESIAN_POINT ( 'NONE',  ( 0.1103744047535531458, -16.53879706351798973, 39.82693656558404882 ) ) ;
#50120=EDGE_LOOP ( 'NONE', ( #25695, #34007, #12125, #34481 ) ) ;
#50132=CARTESIAN_POINT ( 'NONE',  ( 0.8751705887134553219, -17.57879340691572878, 44.76769609654206050 ) ) ;
#50133=( BOUNDED_SURFACE ( )  B_SPLINE_SURFACE ( 3, 1, ( 
 ( #33247, #28515 ),
 ( #42963, #41728 ),
 ( #13209, #27604 ),
 ( #46729, #621 ) ),
 .UNSPECIFIED., .F., .F., .F. ) 
 B_SPLINE_SURFACE_WITH_KNOTS ( ( 4, 4 ),
 ( 2, 2 ),
 ( 0.000000000000000000, 1.000000000000000000 ),
 ( 0.000000000000000000, 1.000000000000000000 ),
 .UNSPECIFIED. ) 
 GEOMETRIC_REPRESENTATION_ITEM ( )  RATIONAL_B_SPLINE_SURFACE ( (
 ( 1.000000000000000000, 1.000000000000000000),
 ( 0.9953040768229005630, 0.8617119497784937465),
 ( 0.9953040768229005630, 0.8617119497784937465),
 ( 1.000000000000000000, 1.000000000000000000) ) ) 
 REPRESENTATION_ITEM ( '' )  SURFACE ( )  );
#50134=VERTEX_POINT ( 'NONE', #27415 ) ;
#50136=VERTEX_POINT ( 'NONE', #46545 ) ;
#50137=EDGE_CURVE ( 'NONE', #26923, #44899, #54626, .T. ) ;
#50143=ORIENTED_EDGE ( 'NONE', *, *, #30712, .F. ) ;
#50146=EDGE_CURVE ( 'NONE', #59804, #13656, #24261, .T. ) ;
#50147=CARTESIAN_POINT ( 'NONE',  ( 0.1310142868023675411, -39.59283406808317807, -17.08943085418572139 ) ) ;
#50150=CARTESIAN_POINT ( 'NONE',  ( 0.1101816497532063371, 21.44450189183869071, -37.41460501058194410 ) ) ;
#50151=EDGE_CURVE ( 'NONE', #55958, #9272, #59074, .T. ) ;
#50155=FACE_OUTER_BOUND ( 'NONE', #1785, .T. ) ;
#50156=LINE ( 'NONE', #21646, #13162 ) ;
#50167=CARTESIAN_POINT ( 'NONE',  ( 0.6031356755773454870, -12.45114731045998369, -46.46821530722335325 ) ) ;
#50168=VECTOR ( 'NONE', #5524, 1000.000000000000227 ) ;
#50169=VECTOR ( 'NONE', #38236, 1000.000000000000114 ) ;
#50170=EDGE_LOOP ( 'NONE', ( #4095, #59516, #24217, #48104 ) ) ;
#50173=ORIENTED_EDGE ( 'NONE', *, *, #1822, .T. ) ;
#50181=B_SPLINE_CURVE_WITH_KNOTS ( 'NONE', 3,
 ( #13050, #23053, #9243, #32144, #13979, #55608, #42180, #56542, #18360, #51222, #13659, #32764, #4214, #61539, #51841, #47172 ),
 .UNSPECIFIED., .F., .F.,
 ( 4, 3, 3, 3, 3, 4 ),
 ( 2.194378057379452319E-17, 0.0002618515315864391037, 0.0003927756766341941965, 0.0005236998216950568058, 0.0007855159896329857788, 0.001047349442285925268 ),
 .UNSPECIFIED. ) ;
#50188=VERTEX_POINT ( 'NONE', #28964 ) ;
#50192=CARTESIAN_POINT ( 'NONE',  ( 0.7246131072078578761, -47.79072675905350565, 5.464103862700703473 ) ) ;
#50198=VERTEX_POINT ( 'NONE', #53067 ) ;
#50201=CARTESIAN_POINT ( 'NONE',  ( 4.549368137175248350, 13.59764261105751793, -40.71620287708331176 ) ) ;
#50202=EDGE_CURVE ( 'NONE', #11373, #868, #5299, .T. ) ;
#50203=CARTESIAN_POINT ( 'NONE',  ( 0.6017666602106490625, 5.933006478840690434, -47.74032907933392522 ) ) ;
#50211=B_SPLINE_CURVE_WITH_KNOTS ( 'NONE', 3,
 ( #6008, #44286, #7250, #15450 ),
 .UNSPECIFIED., .F., .F.,
 ( 4, 4 ),
 ( 4.336808689942017736E-19, 0.005014147105413698652 ),
 .UNSPECIFIED. ) ;
#50222=CARTESIAN_POINT ( 'NONE',  ( -6.017396004339687465, 18.68180398134250453, 2.460690056887851807 ) ) ;
#50226=ORIENTED_EDGE ( 'NONE', *, *, #29909, .T. ) ;
#50230=CARTESIAN_POINT ( 'NONE',  ( 0.6001305935487315502, 46.60388846085706405, 11.94532529598394532 ) ) ;
#50232=FACE_OUTER_BOUND ( 'NONE', #6240, .T. ) ;
#50236=CARTESIAN_POINT ( 'NONE',  ( 0.3622758884714730732, 42.62881903538210793, -6.444611261694146442 ) ) ;
#50242=DIRECTION ( 'NONE',  ( -1.000000000000000000, 0.000000000000000000, 0.000000000000000000 ) ) ;
#50243=VERTEX_POINT ( 'NONE', #758 ) ;
#50245=AXIS2_PLACEMENT_3D ( 'NONE', #17633, #45239, #27028 ) ;
#50252=CARTESIAN_POINT ( 'NONE',  ( 0.6254311100348637353, 48.10157347124180660, 0.6881768005104212937 ) ) ;
#50256=CARTESIAN_POINT ( 'NONE',  ( 4.549368137175248350, -42.82045902618770583, -3.018832571116409014 ) ) ;
#50261=CARTESIAN_POINT ( 'NONE',  ( 0.6023142530420679819, 18.65157113320488236, 44.34465601638707000 ) ) ;
#50266=CARTESIAN_POINT ( 'NONE',  ( 0.1098349054025746785, 42.78286259078963383, -5.417317591399368304 ) ) ;
#50286=CARTESIAN_POINT ( 'NONE',  ( 2.301529144917015213, 1.287519423136602947, 48.01619158420459144 ) ) ;
#50288=CARTESIAN_POINT ( 'NONE',  ( -6.001507490154111224, 0.01557731607579719395, -18.84387066167321478 ) ) ;
#50292=CARTESIAN_POINT ( 'NONE',  ( -2.569797478183790229, 2.353985772484751049, -14.44232325624824398 ) ) ;
#50295=CARTESIAN_POINT ( 'NONE',  ( 0.8751705887134553219, -29.98056538504934210, -37.60752970653818039 ) ) ;
#50297=ORIENTED_EDGE ( 'NONE', *, *, #52677, .T. ) ;
#50301=CARTESIAN_POINT ( 'NONE',  ( 4.975801465491694664, -2.564218696447152279, -47.84403947906842092 ) ) ;
#50306=CARTESIAN_POINT ( 'NONE',  ( 0.7246131072078586532, 41.24126838495065783, 24.75818606403465338 ) ) ;
#50309=CARTESIAN_POINT ( 'NONE',  ( 0.8751705887134553219, -47.55935879196475469, 7.160166390003496417 ) ) ;
#50310=CARTESIAN_POINT ( 'NONE',  ( 0.1092355843206037486, -10.87081649985060849, -41.73183925352176971 ) ) ;
#50312=ORIENTED_EDGE ( 'NONE', *, *, #26338, .T. ) ;
#50326=CARTESIAN_POINT ( 'NONE',  ( -6.010958268070873523, 16.32616437357125250, -9.409153349053413606 ) ) ;
#50330=CARTESIAN_POINT ( 'NONE',  ( 0.1310142868023692897, -42.83311553787496706, 4.996535778098624370 ) ) ;
#50334=ORIENTED_EDGE ( 'NONE', *, *, #45068, .T. ) ;
#50339=CARTESIAN_POINT ( 'NONE',  ( 0.5988103564986355654, 44.21009236284883315, -18.96890181990844582 ) ) ;
#50346=AXIS2_PLACEMENT_3D ( 'NONE', #29265, #5439, #14888 ) ;
#50348=ORIENTED_EDGE ( 'NONE', *, *, #22030, .T. ) ;
#50352=CARTESIAN_POINT ( 'NONE',  ( 3.238931869106854489, -41.96286875554261542, -9.350562014685982248 ) ) ;
#50364=CARTESIAN_POINT ( 'NONE',  ( 0.6001305935487422083, 38.48510059944008077, 28.87057754790950881 ) ) ;
#50369=CARTESIAN_POINT ( 'NONE',  ( 0.6031356219577718170, 38.21934428970573094, 29.21669799774976184 ) ) ;
#50377=ADVANCED_FACE ( 'NONE', ( #7601 ), #16121, .F. ) ;
#50379=CONICAL_SURFACE ( 'NONE', #33368, 42.92674063221959813, 1.485477209440487556 ) ;
#50382=EDGE_LOOP ( 'NONE', ( #9236, #23000, #31997, #57 ) ) ;
#50384=CARTESIAN_POINT ( 'NONE',  ( 0.1087620492084206414, 43.12302841504342155, 0.3620418170788286538 ) ) ;
#50387=ORIENTED_EDGE ( 'NONE', *, *, #20645, .F. ) ;
#50391=VECTOR ( 'NONE', #28762, 1000.000000000000114 ) ;
#50397=ADVANCED_FACE ( 'NONE', ( #45864 ), #37354, .F. ) ;
#50404=CARTESIAN_POINT ( 'NONE',  ( 0.3622758884714600280, -42.84426538328734324, 4.808133778521152202 ) ) ;
#50405=EDGE_CURVE ( 'NONE', #15890, #5168, #27694, .T. ) ;
#50414=ORIENTED_EDGE ( 'NONE', *, *, #61568, .T. ) ;
#50415=CARTESIAN_POINT ( 'NONE',  ( 0.6041374136657476912, -34.14050483116115942, -33.89363087703035404 ) ) ;
#50430=B_SPLINE_CURVE_WITH_KNOTS ( 'NONE', 3,
 ( #50890, #18017, #37135, #32422, #36202, #54962 ),
 .UNSPECIFIED., .F., .F.,
 ( 4, 2, 4 ),
 ( 8.440430351524944310E-17, 0.0002293366620881469363, 0.0004586733241762094675 ),
 .UNSPECIFIED. ) ;
#50433=CARTESIAN_POINT ( 'NONE',  ( 0.1100053167205930632, -42.77858932361500877, -5.450899213259354781 ) ) ;
#50437=CARTESIAN_POINT ( 'NONE',  ( -6.010958268070873523, 13.33459572764776091, -13.31406649671948550 ) ) ;
#50439=EDGE_CURVE ( 'NONE', #57918, #48340, #14288, .T. ) ;
#50445=( LENGTH_UNIT ( ) NAMED_UNIT ( * ) SI_UNIT ( .MILLI., .METRE. ) );
#50447=CARTESIAN_POINT ( 'NONE',  ( 0.6254311100348655117, 37.74260849418455877, 29.82834996731709154 ) ) ;
#50449=DIRECTION ( 'NONE',  ( 1.000000000000000000, 0.000000000000000000, 0.000000000000000000 ) ) ;
#50455=CARTESIAN_POINT ( 'NONE',  ( 0.1310142868023692342, -0.6370537502139506092, 43.11885108606331585 ) ) ;
#50461=CARTESIAN_POINT ( 'NONE',  ( 4.549368137175248350, 13.99871866169365653, -40.58005590356676606 ) ) ;
#50468=CARTESIAN_POINT ( 'NONE',  ( 4.975801465491694664, 35.64402118370912120, 32.01766832630325155 ) ) ;
#50480=ADVANCED_FACE ( 'NONE', ( #51438 ), #46144, .F. ) ;
#50482=EDGE_CURVE ( 'NONE', #54850, #12765, #6808, .T. ) ;
#50483=( BOUNDED_SURFACE ( )  B_SPLINE_SURFACE ( 3, 1, ( 
 ( #16389, #17023 ),
 ( #31414, #50511 ),
 ( #7587, #1338 ),
 ( #20473, #39604 ) ),
 .UNSPECIFIED., .F., .F., .F. ) 
 B_SPLINE_SURFACE_WITH_KNOTS ( ( 4, 4 ),
 ( 2, 2 ),
 ( 0.000000000000000000, 1.000000000000000000 ),
 ( 0.000000000000000000, 1.000000000000000000 ),
 .UNSPECIFIED. ) 
 GEOMETRIC_REPRESENTATION_ITEM ( )  RATIONAL_B_SPLINE_SURFACE ( (
 ( 1.000000000000000000, 1.000000000000000000),
 ( 0.9953040768229005630, 0.8617119497784937465),
 ( 0.9953040768229005630, 0.8617119497784937465),
 ( 1.000000000000000000, 1.000000000000000000) ) ) 
 REPRESENTATION_ITEM ( '' )  SURFACE ( )  );
#50488=DIRECTION ( 'NONE',  ( 1.000000000000000000, 0.000000000000000000, -0.000000000000000000 ) ) ;
#50490=VERTEX_POINT ( 'NONE', #15985 ) ;
#50497=EDGE_CURVE ( 'NONE', #55102, #22212, #24439, .T. ) ;
#50498=FACE_OUTER_BOUND ( 'NONE', #46961, .T. ) ;
#50499=ORIENTED_EDGE ( 'NONE', *, *, #57069, .F. ) ;
#50505=ORIENTED_EDGE ( 'NONE', *, *, #54677, .T. ) ;
#50508=( BOUNDED_SURFACE ( )  B_SPLINE_SURFACE ( 3, 1, ( 
 ( #38054, #51175 ),
 ( #13298, #51477 ),
 ( #37741, #57101 ),
 ( #9199, #60570 ) ),
 .UNSPECIFIED., .F., .F., .F. ) 
 B_SPLINE_SURFACE_WITH_KNOTS ( ( 4, 4 ),
 ( 2, 2 ),
 ( 0.000000000000000000, 1.000000000000000000 ),
 ( 0.000000000000000000, 1.000000000000000000 ),
 .UNSPECIFIED. ) 
 GEOMETRIC_REPRESENTATION_ITEM ( )  RATIONAL_B_SPLINE_SURFACE ( (
 ( 1.000000000000000000, 1.000000000000000000),
 ( 0.7223157951917480446, 0.9931996967497186413),
 ( 0.7223157951917480446, 0.9931996967497186413),
 ( 1.000000000000000000, 1.000000000000000000) ) ) 
 REPRESENTATION_ITEM ( '' )  SURFACE ( )  );
#50510=CARTESIAN_POINT ( 'NONE',  ( 0.6029303876144825880, 6.409038528276127522, -47.67862422489726981 ) ) ;
#50511=CARTESIAN_POINT ( 'NONE',  ( 0.7048096507298635682, 37.64898672361954368, -29.95256433478687086 ) ) ;
#50513=CARTESIAN_POINT ( 'NONE',  ( 0.6028618097248862329, 12.28244208173060592, -46.51318640245703051 ) ) ;
#50515=B_SPLINE_CURVE_WITH_KNOTS ( 'NONE', 3,
 ( #24243, #29556, #53646, #10777, #48981, #10462, #30167, #53352, #6030, #58346, #416, #5720, #58045, #29865, #15170, #48665, #25167, #44009, #11087 ),
 .UNSPECIFIED., .F., .F.,
 ( 4, 3, 3, 3, 3, 3, 4 ),
 ( 1.128550957684774488E-16, 0.0002618519381806285731, 0.0003927759815486009626, 0.0005237000248299445142, 0.0006546240681324982588, 0.0007855481115631359618, 0.0009699050456655092071 ),
 .UNSPECIFIED. ) ;
#50519=AXIS2_PLACEMENT_3D ( 'NONE', #7327, #2642, #60264 ) ;
#50527=CARTESIAN_POINT ( 'NONE',  ( 0.6017666602106489515, 46.37677619531712025, -12.78804974226051705 ) ) ;
#50533=CARTESIAN_POINT ( 'NONE',  ( 0.5988103622719987973, 34.44344971428028401, -33.58571533649124774 ) ) ;
#50537=CARTESIAN_POINT ( 'NONE',  ( 0.5998501479064708430, 12.95623334615502387, -46.33007877220726556 ) ) ;
#50539=ORIENTED_EDGE ( 'NONE', *, *, #34041, .F. ) ;
#50541=CARTESIAN_POINT ( 'NONE',  ( 0.7048096507298635682, -33.41730025321778186, 34.61049487267002434 ) ) ;
#50543=ORIENTED_EDGE ( 'NONE', *, *, #7545, .F. ) ;
#50544=CARTESIAN_POINT ( 'NONE',  ( -6.016104459813371719, -2.454244026261222622, 18.68271063303494017 ) ) ;
#50545=DIRECTION ( 'NONE',  ( 0.1024043820194936449, -0.9946559125373960475, 0.01315135725336192239 ) ) ;
#50546=EDGE_CURVE ( 'NONE', #42276, #14894, #11278, .T. ) ;
#50558=CARTESIAN_POINT ( 'NONE',  ( 0.6009452777970410997, 33.70725232128892657, -34.32439724343003462 ) ) ;
#50559=EDGE_CURVE ( 'NONE', #6090, #24495, #57934, .T. ) ;
#50571=EDGE_CURVE ( 'NONE', #18458, #53617, #48658, .T. ) ;
#50575=CARTESIAN_POINT ( 'NONE',  ( 0.6031357023905875581, -41.68407605450330067, 24.01594909943193912 ) ) ;
#50578=CARTESIAN_POINT ( 'NONE',  ( 0.2885700199627512785, 42.63514063525626341, -6.424755504217793955 ) ) ;
#50580=CARTESIAN_POINT ( 'NONE',  ( 3.680974057930773924, -40.59247216052836649, -25.57193971028145540 ) ) ;
#50583=ORIENTED_EDGE ( 'NONE', *, *, #34078, .T. ) ;
#50584=CARTESIAN_POINT ( 'NONE',  ( 0.6001305935487422083, -5.760103278698371021, 47.76436356026957952 ) ) ;
#50594=CARTESIAN_POINT ( 'NONE',  ( 0.6030672727741701600, 41.70584815505888798, -23.97812608463489426 ) ) ;
#50595=DIRECTION ( 'NONE',  ( 0.000000000000000000, 0.000000000000000000, 1.000000000000000000 ) ) ;
#50597=ORIENTED_EDGE ( 'NONE', *, *, #28467, .F. ) ;
#50605=CARTESIAN_POINT ( 'NONE',  ( 0.1098349054025746924, 41.70974743324814682, -10.95525583467232700 ) ) ;
#50606=B_SPLINE_CURVE_WITH_KNOTS ( 'NONE', 3,
 ( #11913, #39256, #48623, #21592, #45120, #5680, #55092, #59801, #24829, #50099, #11587, #2776, #19835, #2468, #7465, #58305 ),
 .UNSPECIFIED., .F., .F.,
 ( 4, 3, 3, 3, 3, 4 ),
 ( 2.221635811791082109E-17, 0.0002618515315864383447, 0.0003927756766341984249, 0.0005236998216950556131, 0.0007855159896329916335, 0.001047349442285925268 ),
 .UNSPECIFIED. ) ;
#50607=ORIENTED_EDGE ( 'NONE', *, *, #28567, .F. ) ;
#50611=CARTESIAN_POINT ( 'NONE',  ( 0.1100247026804066219, -39.77655614012843444, -16.65964013375371877 ) ) ;
#50612=DIRECTION ( 'NONE',  ( -1.000000000000000000, -0.000000000000000000, -0.000000000000000000 ) ) ;
#50616=CARTESIAN_POINT ( 'NONE',  ( 0.3622758884714600280, -34.70015533914845918, 25.58609868863709380 ) ) ;
#50621=CARTESIAN_POINT ( 'NONE',  ( -6.001507490154111224, 18.68062548815625945, 2.475062734132503550 ) ) ;
#50623=CARTESIAN_POINT ( 'NONE',  ( 0.5998501479064699549, -47.76154736470754614, -5.759754759340617092 ) ) ;
#50624=CARTESIAN_POINT ( 'NONE',  ( 0.3622758884714730732, 34.70015533914794759, 25.58609868863780434 ) ) ;
#50625=EDGE_CURVE ( 'NONE', #50198, #31680, #2262, .T. ) ;
#50628=ORIENTED_EDGE ( 'NONE', *, *, #18407, .F. ) ;
#50631=CARTESIAN_POINT ( 'NONE',  ( 0.6031357023905874470, 44.46217339385169964, -18.36962560204173656 ) ) ;
#50635=CARTESIAN_POINT ( 'NONE',  ( -6.016761891674565099, 7.207804629151311815, 17.41015286184805078 ) ) ;
#50639=CARTESIAN_POINT ( 'NONE',  ( 0.7246131072078525470, -17.64706930304264176, -44.74808308960844272 ) ) ;
#50656=CARTESIAN_POINT ( 'NONE',  ( 0.3622758884714730732, 41.85013935980087751, 10.35929834645937397 ) ) ;
#50659=CARTESIAN_POINT ( 'NONE',  ( 0.1103310638050662013, 37.38800124003712000, -21.49083802119861630 ) ) ;
#50660=CARTESIAN_POINT ( 'NONE',  ( 4.322998006666179727, -47.25487450103542386, 8.359821156455678803 ) ) ;
#50661=VERTEX_POINT ( 'NONE', #50404 ) ;
#50663=CARTESIAN_POINT ( 'NONE',  ( -2.569797478183783568, 11.33042594333548436, -9.259773107242946111 ) ) ;
#50674=CARTESIAN_POINT ( 'NONE',  ( 0.8760168074886960365, 38.69913431881823129, -28.57146030081939969 ) ) ;
#50680=CARTESIAN_POINT ( 'NONE',  ( 0.1092355843206037486, 11.45151637801127542, -41.57624119012377406 ) ) ;
#50685=VECTOR ( 'NONE', #15752, 1000.000000000000114 ) ;
#50686=EDGE_LOOP ( 'NONE', ( #27897, #55481, #17140, #56366 ) ) ;
#50692=CARTESIAN_POINT ( 'NONE',  ( 3.238931869106854489, 7.419701784410564827, 42.34694073502593170 ) ) ;
#50700=EDGE_CURVE ( 'NONE', #47799, #19827, #52299, .T. ) ;
#50703=CARTESIAN_POINT ( 'NONE',  ( 0.1102144999581332885, -26.15241010113000542, -34.28951223307520735 ) ) ;
#50705=ORIENTED_EDGE ( 'NONE', *, *, #54052, .F. ) ;
#50718=CARTESIAN_POINT ( 'NONE',  ( 4.975801465491694664, -3.702618843597810905, 47.76942479135478692 ) ) ;
#50723=B_SPLINE_CURVE_WITH_KNOTS ( 'NONE', 3,
 ( #22919, #32626, #13520, #50252, #32943, #17064 ),
 .UNSPECIFIED., .F., .F.,
 ( 4, 2, 4 ),
 ( 1.267283937151336631E-16, 0.0002450741128632353237, 0.0004901482257263439042 ),
 .UNSPECIFIED. ) ;
#50731=CONICAL_SURFACE ( 'NONE', #26722, 42.92674063221959813, 1.485477209440487556 ) ;
#50735=CARTESIAN_POINT ( 'NONE',  ( 0.7048096507298635682, 38.67623024744010252, 28.61383451045712079 ) ) ;
#50738=CARTESIAN_POINT ( 'NONE',  ( 2.643462169533613793, 30.32726672320750438, 37.25264019563424256 ) ) ;
#50743=CARTESIAN_POINT ( 'NONE',  ( 0.1064266379913938465, 39.62374453032494870, -17.02047542254809187 ) ) ;
#50760=EDGE_LOOP ( 'NONE', ( #11692, #60099, #5551, #14770 ) ) ;
#50767=( BOUNDED_SURFACE ( )  B_SPLINE_SURFACE ( 3, 1, ( 
 ( #42941, #51996 ),
 ( #28191, #47312 ),
 ( #23494, #14425 ),
 ( #42624, #61685 ) ),
 .UNSPECIFIED., .F., .F., .F. ) 
 B_SPLINE_SURFACE_WITH_KNOTS ( ( 4, 4 ),
 ( 2, 2 ),
 ( 0.000000000000000000, 1.000000000000000000 ),
 ( 0.000000000000000000, 1.000000000000000000 ),
 .UNSPECIFIED. ) 
 GEOMETRIC_REPRESENTATION_ITEM ( )  RATIONAL_B_SPLINE_SURFACE ( (
 ( 1.000000000000000000, 1.000000000000000000),
 ( 0.9953040768229005630, 0.8617119497784937465),
 ( 0.9953040768229005630, 0.8617119497784937465),
 ( 1.000000000000000000, 1.000000000000000000) ) ) 
 REPRESENTATION_ITEM ( '' )  SURFACE ( )  );
#50775=CARTESIAN_POINT ( 'NONE',  ( 0.6031357023905875581, 29.25135304925229818, 38.19275261685284306 ) ) ;
#50777=EDGE_CURVE ( 'NONE', #32408, #33003, #33480, .T. ) ;
#50789=ORIENTED_EDGE ( 'NONE', *, *, #51528, .T. ) ;
#50796=DIRECTION ( 'NONE',  ( 0.000000000000000000, 0.000000000000000000, 1.000000000000000000 ) ) ;
#50806=CARTESIAN_POINT ( 'NONE',  ( 0.6001305935487315502, 46.60388846085722747, -11.94532529598329518 ) ) ;
#50808=CARTESIAN_POINT ( 'NONE',  ( 0.6031356219577719280, -41.70591683999489163, -23.97811961689673055 ) ) ;
#50809=CIRCLE ( 'NONE', #54826, 47.91270532121795611 ) ;
#50816=B_SPLINE_CURVE_WITH_KNOTS ( 'NONE', 3,
 ( #4198, #61523, #37774, #52136 ),
 .UNSPECIFIED., .F., .F.,
 ( 4, 4 ),
 ( 0.000000000000000000, 0.004445488388166994251 ),
 .UNSPECIFIED. ) ;
#50820=CARTESIAN_POINT ( 'NONE',  ( -6.001507490154110336, 2.475062734132436493, 18.68062548815627011 ) ) ;
#50824=EDGE_CURVE ( 'NONE', #60124, #16733, #38151, .T. ) ;
#50825=CARTESIAN_POINT ( 'NONE',  ( -2.708315649062916552, 1.648584381067041527, -14.54141329178160547 ) ) ;
#50826=CARTESIAN_POINT ( 'NONE',  ( 0.1092565886968783623, -21.29292791075612712, 37.50119754628571656 ) ) ;
#50831=CARTESIAN_POINT ( 'NONE',  ( 0.1073791018717483448, -0.4849339620930353534, -43.12183934961191056 ) ) ;
#50834=CARTESIAN_POINT ( 'NONE',  ( 0.6031357023905875581, 46.47951061918811178, -12.40899271757790423 ) ) ;
#50840=CARTESIAN_POINT ( 'NONE',  ( 0.2885697896453094380, 31.05173034173371960, -29.91358794843029401 ) ) ;
#50848=EDGE_LOOP ( 'NONE', ( #32193, #43265, #49092, #61058 ) ) ;
#50857=CARTESIAN_POINT ( 'NONE',  ( 0.5980894510889448457, 6.974827154144098706, -47.60453381548686025 ) ) ;
#50858=B_SPLINE_CURVE_WITH_KNOTS ( 'NONE', 3,
 ( #25493, #43720, #16115, #34607 ),
 .UNSPECIFIED., .F., .F.,
 ( 4, 4 ),
 ( 2.165040709395311621E-17, 0.004444306975806114161 ),
 .UNSPECIFIED. ) ;
#50859=CARTESIAN_POINT ( 'NONE',  ( 0.1092565886968784317, 21.83052579204411003, 37.19081526480832878 ) ) ;
#50867=CARTESIAN_POINT ( 'NONE',  ( -6.001507490154110336, -0.01557731607540145842, -18.84387066167321478 ) ) ;
#50868=CARTESIAN_POINT ( 'NONE',  ( 4.691466044806103852, 29.14742760351109396, -33.74235639413297605 ) ) ;
#50879=CARTESIAN_POINT ( 'NONE',  ( 0.1103878639767399972, 42.74915604780180445, -5.676988162228224333 ) ) ;
#50882=CARTESIAN_POINT ( 'NONE',  ( 0.1313383488274124378, 30.03864748494545722, -30.94058105930532321 ) ) ;
#50890=CARTESIAN_POINT ( 'NONE',  ( 0.3622758884714730732, -34.70015533914812522, -25.58609868863756276 ) ) ;
#50896=ORIENTED_EDGE ( 'NONE', *, *, #20645, .T. ) ;
#50899=CARTESIAN_POINT ( 'NONE',  ( 4.549368137175248350, 0.000000000000000000, 0.000000000000000000 ) ) ;
#50900=CARTESIAN_POINT ( 'NONE',  ( 4.975801465491695552, -3.702618843597113685, -47.76942479135485087 ) ) ;
#50901=CARTESIAN_POINT ( 'NONE',  ( 0.7954190325252773475, -28.58653703871186025, 38.68220061605119753 ) ) ;
#50902=CARTESIAN_POINT ( 'NONE',  ( 0.7954190325252807892, 17.60078418394994415, -44.76287681188613021 ) ) ;
#50906=LINE ( 'NONE', #41233, #25418 ) ;
#50914=CARTESIAN_POINT ( 'NONE',  ( 4.833616638992205949, -2.572717262757654666, -46.17873762321151077 ) ) ;
#50918=CARTESIAN_POINT ( 'NONE',  ( 0.1100247026804066219, 5.797046384219859405, -42.73303500775681130 ) ) ;
#50920=VERTEX_POINT ( 'NONE', #25291 ) ;
#50922=AXIS2_PLACEMENT_3D ( 'NONE', #1268, #29173, #35678 ) ;
#50927=B_SPLINE_CURVE_WITH_KNOTS ( 'NONE', 3,
 ( #21365, #26363, #59561, #45498, #35791, #17595 ),
 .UNSPECIFIED., .F., .F.,
 ( 4, 2, 4 ),
 ( 1.258037581941437391E-16, 0.0002450741128632354863, 0.0004901482257263450968 ),
 .UNSPECIFIED. ) ;
#50933=FACE_OUTER_BOUND ( 'NONE', #850, .T. ) ;
#50934=B_SPLINE_CURVE_WITH_KNOTS ( 'NONE', 3,
 ( #17488, #30964, #11886, #2750, #17799, #36609 ),
 .UNSPECIFIED., .F., .F.,
 ( 4, 2, 4 ),
 ( 8.609910155989501895E-17, 0.0002293366620881465297, 0.0004586733241762069738 ),
 .UNSPECIFIED. ) ;
#50935=EDGE_LOOP ( 'NONE', ( #836, #12854, #17655, #42049, #23751, #51782 ) ) ;
#50944=ORIENTED_EDGE ( 'NONE', *, *, #23218, .F. ) ;
#50947=B_SPLINE_CURVE_WITH_KNOTS ( 'NONE', 3,
 ( #21812, #54063, #50306, #30271, #59384, #7370 ),
 .UNSPECIFIED., .F., .F.,
 ( 4, 2, 4 ),
 ( 1.275615807185303638E-16, 0.0002450741128632367874, 0.0004901482257263460726 ),
 .UNSPECIFIED. ) ;
#50949=EDGE_CURVE ( 'NONE', #16942, #7371, #31353, .T. ) ;
#50954=CARTESIAN_POINT ( 'NONE',  ( 0.1073791018717483448, 16.05399293000815675, -40.02496097243042072 ) ) ;
#50965=CARTESIAN_POINT ( 'NONE',  ( 0.1095718737110178143, 26.45591486700756434, -34.05592812063355268 ) ) ;
#50968=CARTESIAN_POINT ( 'NONE',  ( 0.1087620492084206553, 37.52665900408519661, -21.24797679669920925 ) ) ;
#50971=ORIENTED_EDGE ( 'NONE', *, *, #22030, .F. ) ;
#50986=CARTESIAN_POINT ( 'NONE',  ( 0.7245667037590732829, -46.66865388241075863, -11.65533952568336318 ) ) ;
#50988=ADVANCED_FACE ( 'NONE', ( #11513 ), #13755, .F. ) ;
#50995=ADVANCED_FACE ( 'NONE', ( #54703 ), #32966, .F. ) ;
#50997=FACE_OUTER_BOUND ( 'NONE', #22980, .T. ) ;
#50998=CARTESIAN_POINT ( 'NONE',  ( -2.708315649062916552, -9.116606751444257029, -11.44805714186568579 ) ) ;
#51007=ORIENTED_EDGE ( 'NONE', *, *, #1817, .T. ) ;
#51009=CARTESIAN_POINT ( 'NONE',  ( -6.016104459813374383, -11.46679299034570398, -14.95258000663143960 ) ) ;
#51011=DIRECTION ( 'NONE',  ( 0.000000000000000000, 0.000000000000000000, 1.000000000000000000 ) ) ;
#51016=CARTESIAN_POINT ( 'NONE',  ( 4.691466044806104740, -42.11359095667501151, 14.64802401911153851 ) ) ;
#51017=CARTESIAN_POINT ( 'NONE',  ( 0.1073791018717578927, -16.05399293000789385, -40.02496097243051310 ) ) ;
#51020=CARTESIAN_POINT ( 'NONE',  ( 4.322998006666165516, -25.80712523194303287, 40.45864630878473633 ) ) ;
#51026=DIRECTION ( 'NONE',  ( -1.000000000000000000, -0.000000000000000000, -0.000000000000000000 ) ) ;
#51027=DIRECTION ( 'NONE',  ( 0.000000000000000000, -1.000000000000000000, 0.000000000000000000 ) ) ;
#51029=LINE ( 'NONE', #22543, #53667 ) ;
#51033=ORIENTED_EDGE ( 'NONE', *, *, #6390, .T. ) ;
#51040=DIRECTION ( 'NONE',  ( -0.1024043820194934507, 0.7971196296869377251, -0.5950744814819106665 ) ) ;
#51050=CARTESIAN_POINT ( 'NONE',  ( 0.1073791018717578927, 34.50606437925546999, -25.86618856530675714 ) ) ;
#51055=CARTESIAN_POINT ( 'NONE',  ( 0.1103744047535531458, -16.46720136312954708, -39.85659247569254404 ) ) ;
#51069=CARTESIAN_POINT ( 'NONE',  ( 0.8760168074887076939, -41.20610493656926820, 24.81951362746006495 ) ) ;
#51078=CARTESIAN_POINT ( 'NONE',  ( 0.6254087463353941168, 24.64672211239907185, 41.31312313681416271 ) ) ;
#51080=CARTESIAN_POINT ( 'NONE',  ( 0.6031356755773454870, 29.28597628606495462, 38.16618524502131748 ) ) ;
#51085=DIRECTION ( 'NONE',  ( 1.000000000000000000, 0.000000000000000000, 0.000000000000000000 ) ) ;
#51088=AXIS2_PLACEMENT_3D ( 'NONE', #12800, #21563, #46016 ) ;
#51096=EDGE_CURVE ( 'NONE', #55183, #5605, #44154, .T. ) ;
#51101=ORIENTED_EDGE ( 'NONE', *, *, #22156, .F. ) ;
#51104=CARTESIAN_POINT ( 'NONE',  ( 0.1073791018717483448, 11.62916352156094035, 41.52698815987171344 ) ) ;
#51111=ORIENTED_EDGE ( 'NONE', *, *, #54004, .T. ) ;
#51112=ORIENTED_EDGE ( 'NONE', *, *, #13583, .F. ) ;
#51117=( BOUNDED_SURFACE ( )  B_SPLINE_SURFACE ( 3, 1, ( 
 ( #51, #52366 ),
 ( #9462, #4734 ),
 ( #23882, #38932 ),
 ( #38311, #57063 ) ),
 .UNSPECIFIED., .F., .F., .F. ) 
 B_SPLINE_SURFACE_WITH_KNOTS ( ( 4, 4 ),
 ( 2, 2 ),
 ( 0.000000000000000000, 1.000000000000000000 ),
 ( 0.000000000000000000, 1.000000000000000000 ),
 .UNSPECIFIED. ) 
 GEOMETRIC_REPRESENTATION_ITEM ( )  RATIONAL_B_SPLINE_SURFACE ( (
 ( 1.000000000000000000, 1.000000000000000000),
 ( 0.7223157951917480446, 0.9931996967497186413),
 ( 0.7223157951917480446, 0.9931996967497186413),
 ( 1.000000000000000000, 1.000000000000000000) ) ) 
 REPRESENTATION_ITEM ( '' )  SURFACE ( )  );
#51123=CARTESIAN_POINT ( 'NONE',  ( 0.8760168074886960365, -5.394043284319175235, -47.80016357497247981 ) ) ;
#51135=AXIS2_PLACEMENT_3D ( 'NONE', #33134, #52518, #9301 ) ;
#51139=CARTESIAN_POINT ( 'NONE',  ( 2.301430502907646503, 25.12309903330020688, -40.93949994354160538 ) ) ;
#51147=ORIENTED_EDGE ( 'NONE', *, *, #22354, .F. ) ;
#51158=ORIENTED_EDGE ( 'NONE', *, *, #18827, .F. ) ;
#51159=CARTESIAN_POINT ( 'NONE',  ( 0.8751705887134553219, 24.81530984069150136, 41.19904111682516401 ) ) ;
#51165=EDGE_CURVE ( 'NONE', #4984, #22082, #6680, .T. ) ;
#51167=B_SPLINE_CURVE_WITH_KNOTS ( 'NONE', 3,
 ( #15065, #15991, #52945, #30069, #49179, #53857 ),
 .UNSPECIFIED., .F., .F.,
 ( 4, 2, 4 ),
 ( 8.551243849294126806E-17, 0.0002293366620881437108, 0.0004586733241762018781 ),
 .UNSPECIFIED. ) ;
#51172=CARTESIAN_POINT ( 'NONE',  ( 3.238931869106854489, 29.07925862215132184, -31.66562935062907513 ) ) ;
#51175=CARTESIAN_POINT ( 'NONE',  ( 0.8760168074886960365, 13.30888447662080409, -46.22580377597773094 ) ) ;
#51178=EDGE_CURVE ( 'NONE', #61214, #25486, #25398, .T. ) ;
#51184=EDGE_CURVE ( 'NONE', #56408, #19218, #29124, .T. ) ;
#51186=CARTESIAN_POINT ( 'NONE',  ( 0.6254311100348654007, 6.960804577576820584, -47.60023274471273425 ) ) ;
#51190=CARTESIAN_POINT ( 'NONE',  ( -6.016761891674564211, 18.84319130225482297, -0.003433883959849463787 ) ) ;
#51196=CARTESIAN_POINT ( 'NONE',  ( 0.7954196712028458460, -46.22745629466061956, -13.28627209367561335 ) ) ;
#51197=EDGE_CURVE ( 'NONE', #12367, #37726, #23393, .T. ) ;
#51202=CARTESIAN_POINT ( 'NONE',  ( -6.010958268070873523, -18.68034667844847618, -2.473955915502408676 ) ) ;
#51204=CARTESIAN_POINT ( 'NONE',  ( 3.680974057930774812, -4.423547572561986385, -47.77138393978994912 ) ) ;
#51206=CARTESIAN_POINT ( 'NONE',  ( 0.1092565886968785704, 42.79503959566645932, 5.321013289171810712 ) ) ;
#51208=CARTESIAN_POINT ( 'NONE',  ( 0.2885697896453102707, 36.93108635218666791, 22.25146201964156845 ) ) ;
#51217=DIRECTION ( 'NONE',  ( 0.000000000000000000, 0.000000000000000000, 1.000000000000000000 ) ) ;
#51222=CARTESIAN_POINT ( 'NONE',  ( 0.6031356755773454870, -44.44549206087170035, -18.40989784469844892 ) ) ;
#51227=ORIENTED_EDGE ( 'NONE', *, *, #47889, .F. ) ;
#51232=CARTESIAN_POINT ( 'NONE',  ( 0.7246131072078599855, -23.33689307364222998, -42.06185227555107531 ) ) ;
#51234=B_SPLINE_CURVE_WITH_KNOTS ( 'NONE', 3,
 ( #12877, #17258, #42007, #36381 ),
 .UNSPECIFIED., .F., .F.,
 ( 4, 4 ),
 ( 7.806255641895631925E-18, 0.005014147105413701254 ),
 .UNSPECIFIED. ) ;
#51238=CARTESIAN_POINT ( 'NONE',  ( 5.880360259849752858, -47.86623372148048361, -3.184717612777768547 ) ) ;
#51250=VERTEX_POINT ( 'NONE', #34326 ) ;
#51251=CARTESIAN_POINT ( 'NONE',  ( -6.017396004339686577, -2.460690056887663513, -18.68180398134252940 ) ) ;
#51258=DIRECTION ( 'NONE',  ( 0.000000000000000000, 0.000000000000000000, 1.000000000000000000 ) ) ;
#51268=DIRECTION ( 'NONE',  ( 0.000000000000000000, 0.000000000000000000, -1.000000000000000000 ) ) ;
#51273=EDGE_LOOP ( 'NONE', ( #18287, #29442, #25976, #10925 ) ) ;
#51275=CARTESIAN_POINT ( 'NONE',  ( 5.880360259849752858, -47.05949693022714087, 9.312491912827331575 ) ) ;
#51282=CARTESIAN_POINT ( 'NONE',  ( 0.5998501479064699549, -41.39809967730504781, 24.50586714782532027 ) ) ;
#51294=CARTESIAN_POINT ( 'NONE',  ( 3.680882792899937250, -44.99870212802630220, -16.63701193713973936 ) ) ;
#51298=ORIENTED_EDGE ( 'NONE', *, *, #13597, .T. ) ;
#51300=CARTESIAN_POINT ( 'NONE',  ( 5.880360259849739535, 31.59460303415982807, -36.09847387447826605 ) ) ;
#51305=B_SPLINE_CURVE_WITH_KNOTS ( 'NONE', 3,
 ( #30406, #11021, #53895, #30102 ),
 .UNSPECIFIED., .F., .F.,
 ( 4, 4 ),
 ( 0.000000000000000000, 0.005014147105413698652 ),
 .UNSPECIFIED. ) ;
#51312=CARTESIAN_POINT ( 'NONE',  ( 0.7048096507298635682, 29.95256433478676072, 37.64898672361963605 ) ) ;
#51313=CARTESIAN_POINT ( 'NONE',  ( 0.1073791018717483448, 21.98088480513615295, 37.10214135362896570 ) ) ;
#51316=CARTESIAN_POINT ( 'NONE',  ( 3.680974057930774812, 43.58300585207893363, 20.05478739720751236 ) ) ;
#51317=ORIENTED_EDGE ( 'NONE', *, *, #10559, .F. ) ;
#51319=CARTESIAN_POINT ( 'NONE',  ( -2.708315649062910779, 13.61924161399633526, -5.356004933109328014 ) ) ;
#51322=CARTESIAN_POINT ( 'NONE',  ( -5.995132425357893702, 9.414704407578033951, -16.32377331145310606 ) ) ;
#51324=EDGE_LOOP ( 'NONE', ( #1711, #21361, #10955, #60117 ) ) ;
#51345=CARTESIAN_POINT ( 'NONE',  ( 0.1100247026804066219, -34.31594964380199997, 26.11768802553187641 ) ) ;
#51346=CARTESIAN_POINT ( 'NONE',  ( 0.6001305935487422083, 41.92422178329168503, -23.60027211631787125 ) ) ;
#51351=CARTESIAN_POINT ( 'NONE',  ( 0.1073791018717483448, 33.91564619577807349, -26.63563652260133097 ) ) ;
#51355=SURFACE_STYLE_USAGE ( .BOTH. , #27564 ) ;
#51360=CARTESIAN_POINT ( 'NONE',  ( 0.1102847568649952675, 21.48234084756696305, -37.39286109091555943 ) ) ;
#51368=CARTESIAN_POINT ( 'NONE',  ( -6.010958268070873523, 14.95835081545489409, -11.45964880703811595 ) ) ;
#51379=CARTESIAN_POINT ( 'NONE',  ( -6.015611763856276717, 18.68122482568280063, 2.465697960551114232 ) ) ;
#51382=ORIENTED_EDGE ( 'NONE', *, *, #9451, .T. ) ;
#51383=CARTESIAN_POINT ( 'NONE',  ( 0.7246131072078553226, 46.24389631750668883, 13.24054562911141808 ) ) ;
#51385=VERTEX_POINT ( 'NONE', #57944 ) ;
#51394=EDGE_CURVE ( 'NONE', #10420, #11294, #23035, .T. ) ;
#51400=EDGE_CURVE ( 'NONE', #10739, #42739, #37417, .T. ) ;
#51414=ORIENTED_EDGE ( 'NONE', *, *, #35586, .F. ) ;
#51430=CARTESIAN_POINT ( 'NONE',  ( 2.643462169533613793, 17.09809940585662247, -44.89050350746133944 ) ) ;
#51433=CARTESIAN_POINT ( 'NONE',  ( 4.549368137175248350, 0.000000000000000000, 0.000000000000000000 ) ) ;
#51435=ADVANCED_FACE ( 'NONE', ( #13927 ), #34977, .F. ) ;
#51438=FACE_OUTER_BOUND ( 'NONE', #20750, .T. ) ;
#51444=ORIENTED_EDGE ( 'NONE', *, *, #21547, .T. ) ;
#51447=AXIS2_PLACEMENT_3D ( 'NONE', #7188, #59204, #16308 ) ;
#51448=CARTESIAN_POINT ( 'NONE',  ( 0.1073791018717578927, 21.14095454447508615, 37.58707531572213156 ) ) ;
#51449=B_SPLINE_CURVE_WITH_KNOTS ( 'NONE', 3,
 ( #40914, #59042, #36199, #59348 ),
 .UNSPECIFIED., .F., .F.,
 ( 4, 4 ),
 ( 5.553824967135426632E-18, 0.004566006591234645501 ),
 .UNSPECIFIED. ) ;
#51451=ORIENTED_EDGE ( 'NONE', *, *, #844, .F. ) ;
#51464=CARTESIAN_POINT ( 'NONE',  ( 0.1102847568649952675, 21.64199720113191105, 37.30068345220698944 ) ) ;
#51471=CARTESIAN_POINT ( 'NONE',  ( 4.691466044806102964, 14.64802401911229701, -42.11359095667474861 ) ) ;
#51477=CARTESIAN_POINT ( 'NONE',  ( 2.643462169533600914, 13.76277278785560654, -46.02269433264218179 ) ) ;
#51478=CARTESIAN_POINT ( 'NONE',  ( 0.5988103622719992414, 24.57719485303637796, -41.35593060299647306 ) ) ;
#51481=CARTESIAN_POINT ( 'NONE',  ( -6.016761891674565099, -18.68243340030204536, 2.456125503350645278 ) ) ;
#51484=CARTESIAN_POINT ( 'NONE',  ( 0.1097557419366048670, 42.72583172879053137, -5.849988371690637123 ) ) ;
#51491=PLANE ( 'NONE',  #26680 ) ;
#51493=EDGE_CURVE ( 'NONE', #10204, #32930, #21378, .T. ) ;
#51494=VECTOR ( 'NONE', #53693, 1000.000000000000114 ) ;
#51501=CARTESIAN_POINT ( 'NONE',  ( 0.8751705887134553219, 29.98056538504910051, 37.60752970653838645 ) ) ;
#51506=CARTESIAN_POINT ( 'NONE',  ( 0.1073791018717578927, -42.68962945260949482, -6.109314776652552403 ) ) ;
#51510=CARTESIAN_POINT ( 'NONE',  ( 0.1103310638050661735, 42.74468893497609656, 5.710544932889072278 ) ) ;
#51512=CARTESIAN_POINT ( 'NONE',  ( 3.680974057930773036, -22.36814223828938353, -42.44218549341202618 ) ) ;
#51521=CARTESIAN_POINT ( 'NONE',  ( 0.1102144999581332746, 39.79340763430485595, 16.61938362665564028 ) ) ;
#51524=VERTEX_POINT ( 'NONE', #21302 ) ;
#51528=EDGE_CURVE ( 'NONE', #593, #30431, #20686, .T. ) ;
#51532=EDGE_CURVE ( 'NONE', #5852, #18698, #54473, .T. ) ;
#51533=CIRCLE ( 'NONE', #10556, 42.92674063221959813 ) ;
#51535=CARTESIAN_POINT ( 'NONE',  ( 0.6023143664670691511, 41.53077189784229972, 24.28012784216892683 ) ) ;
#51542=CARTESIAN_POINT ( 'NONE',  ( 1.827326673878744145, 41.88502433275003511, -9.946825761454068271 ) ) ;
#51543=CARTESIAN_POINT ( 'NONE',  ( -6.016104459813374383, -18.84322058118302223, -0.005335450885264243250 ) ) ;
#51550=ORIENTED_EDGE ( 'NONE', *, *, #52464, .T. ) ;
#51557=DIRECTION ( 'NONE',  ( 0.000000000000000000, 0.000000000000000000, -1.000000000000000000 ) ) ;
#51558=ORIENTED_EDGE ( 'NONE', *, *, #1833, .F. ) ;
#51559=CARTESIAN_POINT ( 'NONE',  ( 0.8760168074886960365, 46.22580377597767409, 13.30888447662096397 ) ) ;
#51568=CARTESIAN_POINT ( 'NONE',  ( 0.6009452777970412107, -29.63106797105387713, -37.89911497740560975 ) ) ;
#51570=FACE_OUTER_BOUND ( 'NONE', #40591, .T. ) ;
#51572=CARTESIAN_POINT ( 'NONE',  ( 0.1102847568649952675, 26.17930421801151297, -34.26895182984672061 ) ) ;
#51575=( BOUNDED_SURFACE ( )  B_SPLINE_SURFACE ( 3, 1, ( 
 ( #42190, #61247 ),
 ( #23365, #42488 ),
 ( #23977, #61551 ),
 ( #43105, #37803 ) ),
 .UNSPECIFIED., .F., .F., .F. ) 
 B_SPLINE_SURFACE_WITH_KNOTS ( ( 4, 4 ),
 ( 2, 2 ),
 ( 0.000000000000000000, 1.000000000000000000 ),
 ( 0.000000000000000000, 1.000000000000000000 ),
 .UNSPECIFIED. ) 
 GEOMETRIC_REPRESENTATION_ITEM ( )  RATIONAL_B_SPLINE_SURFACE ( (
 ( 1.000000000000000000, 1.000000000000000000),
 ( 0.9953040768229005630, 0.8617119497784937465),
 ( 0.9953040768229005630, 0.8617119497784937465),
 ( 1.000000000000000000, 1.000000000000000000) ) ) 
 REPRESENTATION_ITEM ( '' )  SURFACE ( )  );
#51576=FACE_OUTER_BOUND ( 'NONE', #31395, .T. ) ;
#51581=CARTESIAN_POINT ( 'NONE',  ( 4.549368137175248350, 3.018832571116558672, -42.82045902618769873 ) ) ;
#51586=CARTESIAN_POINT ( 'NONE',  ( 0.3622758884714730732, -0.8252992914325094631, -43.10531414739105571 ) ) ;
#51592=CARTESIAN_POINT ( 'NONE',  ( 0.1101816497532063510, -5.494186916736032877, 42.77304337559933600 ) ) ;
#51593=ORIENTED_EDGE ( 'NONE', *, *, #34454, .T. ) ;
#51599=CARTESIAN_POINT ( 'NONE',  ( -2.708315649062910779, 7.544341609839976037, -12.54007339125007547 ) ) ;
#51608=EDGE_CURVE ( 'NONE', #58555, #24987, #44804, .T. ) ;
#51610=LINE ( 'NONE', #50998, #19551 ) ;
#51619=EDGE_CURVE ( 'NONE', #55695, #49511, #59814, .T. ) ;
#51621=VERTEX_POINT ( 'NONE', #41656 ) ;
#51623=CARTESIAN_POINT ( 'NONE',  ( 1.827326673878743923, -43.03225468313002011, -1.232746109312025329 ) ) ;
#51625=EDGE_LOOP ( 'NONE', ( #61805, #41473, #42715, #3695 ) ) ;
#51628=CARTESIAN_POINT ( 'NONE',  ( 0.1102847568649952675, 26.32556309315071275, 34.15672344772096380 ) ) ;
#51632=ORIENTED_EDGE ( 'NONE', *, *, #333, .F. ) ;
#51637=ORIENTED_EDGE ( 'NONE', *, *, #45096, .F. ) ;
#51649=EDGE_CURVE ( 'NONE', #34790, #9403, #374, .T. ) ;
#51656=CARTESIAN_POINT ( 'NONE',  ( 0.7245667037590743931, -34.58857005974929422, -33.42814706018009474 ) ) ;
#51661=CARTESIAN_POINT ( 'NONE',  ( -6.015611763856276717, -11.46610900684713030, -14.95313250337441424 ) ) ;
#51666=CARTESIAN_POINT ( 'NONE',  ( 0.1073791018717578927, -30.14884492832369745, -30.83464511437127697 ) ) ;
#51668=CARTESIAN_POINT ( 'NONE',  ( 0.3622758884714600280, 34.70015533914828865, -25.58609868863731407 ) ) ;
#51670=CIRCLE ( 'NONE', #41732, 47.91270532121795611 ) ;
#51682=CONICAL_SURFACE ( 'NONE', #12678, 42.92674063221959813, 1.485477209440487556 ) ;
#51693=AXIS2_PLACEMENT_3D ( 'NONE', #4648, #52909, #10013 ) ;
#51695=B_SPLINE_CURVE_WITH_KNOTS ( 'NONE', 3,
 ( #54868, #13218, #41432, #22612, #27613, #59887 ),
 .UNSPECIFIED., .F., .F.,
 ( 4, 2, 4 ),
 ( 1.275615807185303638E-16, 0.0002450741128632385221, 0.0004901482257263495420 ),
 .UNSPECIFIED. ) ;
#51701=CARTESIAN_POINT ( 'NONE',  ( 0.6029303876144825880, 29.18200390283997336, 38.24575311130009680 ) ) ;
#51711=CARTESIAN_POINT ( 'NONE',  ( 4.975801465491694664, 47.84403947906843513, -2.564218696446985302 ) ) ;
#51713=ORIENTED_EDGE ( 'NONE', *, *, #4216, .F. ) ;
#51716=CARTESIAN_POINT ( 'NONE',  ( 4.975801465491695552, -31.15993731089151808, 36.39623109580413285 ) ) ;
#51726=EDGE_CURVE ( 'NONE', #1315, #19675, #13151, .T. ) ;
#51738=B_SPLINE_CURVE_WITH_KNOTS ( 'NONE', 3,
 ( #19484, #5346, #338, #58905 ),
 .UNSPECIFIED., .F., .F.,
 ( 4, 4 ),
 ( 0.000000000000000000, 0.004445488388166992516 ),
 .UNSPECIFIED. ) ;
#51744=DIRECTION ( 'NONE',  ( 0.09835009131224567436, -0.5042575517176746125, 0.8579344853044256203 ) ) ;
#51758=DIRECTION ( 'NONE',  ( -1.000000000000000000, -0.000000000000000000, -0.000000000000000000 ) ) ;
#51759=CARTESIAN_POINT ( 'NONE',  ( -6.015611763856276717, 18.20278301740943405, -4.870987357967985432 ) ) ;
#51767=ORIENTED_EDGE ( 'NONE', *, *, #49394, .T. ) ;
#51768=EDGE_LOOP ( 'NONE', ( #51767, #41493, #24535, #16365 ) ) ;
#51778=CARTESIAN_POINT ( 'NONE',  ( 0.2230388203127611768, 15.79641846944918449, -40.12182516270784305 ) ) ;
#51781=CARTESIAN_POINT ( 'NONE',  ( 0.1102144999581333162, -30.40435207217207747, -30.58258619461911110 ) ) ;
#51782=ORIENTED_EDGE ( 'NONE', *, *, #41339, .F. ) ;
#51783=DIRECTION ( 'NONE',  ( 0.000000000000000000, 0.000000000000000000, 1.000000000000000000 ) ) ;
#51790=CARTESIAN_POINT ( 'NONE',  ( -6.010958268070873523, 17.40352239307067705, -7.224487401384108942 ) ) ;
#51791=CARTESIAN_POINT ( 'NONE',  ( -6.017396004339686577, -13.32329839588564369, 13.32495836419619728 ) ) ;
#51808=CARTESIAN_POINT ( 'NONE',  ( 0.5980894510889448457, -48.10766805928368939, -0.7015180096003186261 ) ) ;
#51813=CARTESIAN_POINT ( 'NONE',  ( 0.1313383488274136313, 42.66669366003522867, -6.260443365526930037 ) ) ;
#51814=CARTESIAN_POINT ( 'NONE',  ( 0.1073791018717578927, 42.81622261970994003, -5.147744207006430983 ) ) ;
#51816=CARTESIAN_POINT ( 'NONE',  ( -5.995132425357893702, 2.468096378288389570, -18.68182899165008592 ) ) ;
#51821=CARTESIAN_POINT ( 'NONE',  ( 0.6254311100348661778, -33.52633430496203459, -34.49956326955403796 ) ) ;
#51823=CARTESIAN_POINT ( 'NONE',  ( 0.6001305935487315502, 44.24520387813801392, 18.89378601236080257 ) ) ;
#51825=CARTESIAN_POINT ( 'NONE',  ( -6.010958268070873523, 18.84344976839986785, -0.01451635840169805507 ) ) ;
#51827=B_SPLINE_CURVE_WITH_KNOTS ( 'NONE', 3,
 ( #54329, #44991, #54029, #2338, #26159, #2027 ),
 .UNSPECIFIED., .F., .F.,
 ( 4, 2, 4 ),
 ( 8.440430351524944310E-17, 0.0002293366620881450118, 0.0004586733241762056185 ),
 .UNSPECIFIED. ) ;
#51837=EDGE_CURVE ( 'NONE', #27695, #37089, #41803, .T. ) ;
#51841=CARTESIAN_POINT ( 'NONE',  ( 0.6009452777970410997, -44.61081509289892466, -18.00606236585358033 ) ) ;
#51842=B_SPLINE_CURVE_WITH_KNOTS ( 'NONE', 3,
 ( #6343, #24881, #15182, #25480 ),
 .UNSPECIFIED., .F., .F.,
 ( 4, 4 ),
 ( 2.323236804244109875E-17, 0.004564976165746189446 ),
 .UNSPECIFIED. ) ;
#51844=VERTEX_POINT ( 'NONE', #9985 ) ;
#51853=CARTESIAN_POINT ( 'NONE',  ( 0.8751705887134553219, -17.57879340691572878, 44.76769609654206050 ) ) ;
#51859=ORIENTED_EDGE ( 'NONE', *, *, #17688, .F. ) ;
#51867=ORIENTED_EDGE ( 'NONE', *, *, #19576, .T. ) ;
#51868=ORIENTED_EDGE ( 'NONE', *, *, #51165, .F. ) ;
#51873=( BOUNDED_SURFACE ( )  B_SPLINE_SURFACE ( 3, 1, ( 
 ( #44532, #53876 ),
 ( #15392, #2177 ),
 ( #6554, #29465 ),
 ( #957, #49194 ) ),
 .UNSPECIFIED., .F., .F., .F. ) 
 B_SPLINE_SURFACE_WITH_KNOTS ( ( 4, 4 ),
 ( 2, 2 ),
 ( 0.000000000000000000, 1.000000000000000000 ),
 ( 0.000000000000000000, 1.000000000000000000 ),
 .UNSPECIFIED. ) 
 GEOMETRIC_REPRESENTATION_ITEM ( )  RATIONAL_B_SPLINE_SURFACE ( (
 ( 1.000000000000000000, 1.000000000000000000),
 ( 0.7223157951917480446, 0.9931996967497186413),
 ( 0.7223157951917480446, 0.9931996967497186413),
 ( 1.000000000000000000, 1.000000000000000000) ) ) 
 REPRESENTATION_ITEM ( '' )  SURFACE ( )  );
#51883=AXIS2_PLACEMENT_3D ( 'NONE', #32987, #18887, #60840 ) ;
#51889=CARTESIAN_POINT ( 'NONE',  ( -2.569797478183790229, 6.011723966604152203, -13.34095667500598736 ) ) ;
#51892=CARTESIAN_POINT ( 'NONE',  ( 0.1097557419366048670, 26.07515889977818446, -34.34829179474809280 ) ) ;
#51893=B_SPLINE_CURVE_WITH_KNOTS ( 'NONE', 3,
 ( #57763, #48693, #42480, #43408, #19281, #14278 ),
 .UNSPECIFIED., .F., .F.,
 ( 4, 2, 4 ),
 ( 1.474357996003774831E-17, 0.0002293319059085077857, 0.0004586638118170008262 ),
 .UNSPECIFIED. ) ;
#51894=CARTESIAN_POINT ( 'NONE',  ( -2.569797478183790229, -13.34095667500600868, -6.011723966604104241 ) ) ;
#51900=EDGE_LOOP ( 'NONE', ( #18685, #17760, #28881, #27794 ) ) ;
#51906=CARTESIAN_POINT ( 'NONE',  ( 0.1073791018717483448, 5.147744207006859973, -42.81622261970989030 ) ) ;
#51907=CARTESIAN_POINT ( 'NONE',  ( 5.880360259849739535, 47.87242051977161594, 3.090325311465030200 ) ) ;
#51918=CARTESIAN_POINT ( 'NONE',  ( -6.016489644550737204, -9.425415887801202430, 16.31649074174274361 ) ) ;
#51933=B_SPLINE_CURVE_WITH_KNOTS ( 'NONE', 3,
 ( #14598, #9563, #57453, #4229, #23366, #23978 ),
 .UNSPECIFIED., .F., .F.,
 ( 4, 2, 4 ),
 ( 8.525499192591780946E-17, 0.0002293366620881443342, 0.0004586733241762034501 ),
 .UNSPECIFIED. ) ;
#51936=CARTESIAN_POINT ( 'NONE',  ( -6.017396004339686577, 17.40836349643177527, -7.212050743683987797 ) ) ;
#51943=CARTESIAN_POINT ( 'NONE',  ( 1.827326673878742813, 22.58371678864582321, -36.65065268305635726 ) ) ;
#51945=ORIENTED_EDGE ( 'NONE', *, *, #22654, .T. ) ;
#51952=CARTESIAN_POINT ( 'NONE',  ( 0.6025881611877910160, -34.17105830828438684, 33.86250327239836366 ) ) ;
#51954=CARTESIAN_POINT ( 'NONE',  ( 0.1064266418746775134, 21.07422140941954680, 37.62465821955109391 ) ) ;
#51963=VERTEX_POINT ( 'NONE', #50954 ) ;
#51964=CARTESIAN_POINT ( 'NONE',  ( 0.1103744047535531458, -21.52865142340111504, -37.36621271144529999 ) ) ;
#51969=EDGE_CURVE ( 'NONE', #59715, #37650, #46896, .T. ) ;
#51971=ADVANCED_FACE ( 'NONE', ( #17765 ), #1272, .F. ) ;
#51972=CARTESIAN_POINT ( 'NONE',  ( 1.827119703190778877, -9.946884032291396949, 41.88501940447977745 ) ) ;
#51977=EDGE_CURVE ( 'NONE', #43585, #18698, #44676, .T. ) ;
#51980=ORIENTED_EDGE ( 'NONE', *, *, #14332, .T. ) ;
#51996=CARTESIAN_POINT ( 'NONE',  ( 0.8760168074887076939, 13.30888447662016461, 46.22580377597790147 ) ) ;
#52004=CARTESIAN_POINT ( 'NONE',  ( 0.8760168074886965917, -33.37827814204101173, -34.63873394077476320 ) ) ;
#52015=CARTESIAN_POINT ( 'NONE',  ( 4.549368137175248350, 3.018832571115968033, 42.82045902618773425 ) ) ;
#52016=B_SPLINE_CURVE_WITH_KNOTS ( 'NONE', 3,
 ( #16962, #45779, #31349, #31040, #7516, #50150, #51360, #36682, #2824, #13181, #21955, #60149, #32280, #31975, #8445, #27569, #46696, #3742, #22877 ),
 .UNSPECIFIED., .F., .F.,
 ( 4, 3, 3, 3, 3, 3, 4 ),
 ( 1.149162571898268292E-16, 0.0002618519381806238568, 0.0003927759815485961921, 0.0005237000248299452732, 0.0006546240681324992346, 0.0007855481115631317334, 0.0009699050456655165797 ),
 .UNSPECIFIED. ) ;
#52019=LINE ( 'NONE', #32320, #471 ) ;
#52024=B_SPLINE_CURVE_WITH_KNOTS ( 'NONE', 3,
 ( #48765, #9951, #842, #43480 ),
 .UNSPECIFIED., .F., .F.,
 ( 4, 4 ),
 ( 0.000000000000000000, 0.005014147105413699519 ),
 .UNSPECIFIED. ) ;
#52029=ORIENTED_EDGE ( 'NONE', *, *, #19449, .F. ) ;
#52041=ORIENTED_EDGE ( 'NONE', *, *, #23190, .T. ) ;
#52042=CARTESIAN_POINT ( 'NONE',  ( 3.238931869106855821, -27.59912060131749456, -32.96367555688102868 ) ) ;
#52045=CARTESIAN_POINT ( 'NONE',  ( -6.001507490154111224, -17.41542759839268939, 7.196845540359109172 ) ) ;
#52055=CARTESIAN_POINT ( 'NONE',  ( 4.833616638992208614, -35.06988470649548617, -30.15290813935891023 ) ) ;
#52058=CARTESIAN_POINT ( 'NONE',  ( 0.1102144999581333301, -21.67128446981406142, 37.28370465375319043 ) ) ;
#52073=AXIS2_PLACEMENT_3D ( 'NONE', #19220, #25128, #44270 ) ;
#52084=ORIENTED_EDGE ( 'NONE', *, *, #33294, .T. ) ;
#52087=B_SPLINE_CURVE_WITH_KNOTS ( 'NONE', 3,
 ( #50900, #51204, #18341, #17713 ),
 .UNSPECIFIED., .F., .F.,
 ( 4, 4 ),
 ( 0.000000000000000000, 0.004445488388166992516 ),
 .UNSPECIFIED. ) ;
#52088=CARTESIAN_POINT ( 'NONE',  ( 0.1101816497532063094, -30.58948775778066675, -30.39741055095849021 ) ) ;
#52093=FACE_OUTER_BOUND ( 'NONE', #615, .T. ) ;
#52103=DIRECTION ( 'NONE',  ( 0.000000000000000000, 0.000000000000000000, 1.000000000000000000 ) ) ;
#52107=CARTESIAN_POINT ( 'NONE',  ( 0.8751705887134423323, -48.08707113907595243, -0.8911681664086732457 ) ) ;
#52111=EDGE_CURVE ( 'NONE', #22443, #7371, #54023, .T. ) ;
#52113=ORIENTED_EDGE ( 'NONE', *, *, #51178, .T. ) ;
#52115=ADVANCED_FACE ( 'NONE', ( #58720 ), #58528, .F. ) ;
#52116=CARTESIAN_POINT ( 'NONE',  ( 0.8760168074886965917, -48.09529047980637273, -0.8912768426704601454 ) ) ;
#52124=CARTESIAN_POINT ( 'NONE',  ( 0.5988103564986353433, 29.76496605343795920, 37.79415694022867456 ) ) ;
#52135=B_SPLINE_CURVE_WITH_KNOTS ( 'NONE', 3,
 ( #35157, #16661, #7227, #11981 ),
 .UNSPECIFIED., .F., .F.,
 ( 4, 4 ),
 ( 2.230302957514598322E-17, 0.004564976165746185977 ),
 .UNSPECIFIED. ) ;
#52136=CARTESIAN_POINT ( 'NONE',  ( 0.8751705887134423323, 44.76769609654235893, -17.57879340691497561 ) ) ;
#52150=ORIENTED_EDGE ( 'NONE', *, *, #11544, .T. ) ;
#52151=CARTESIAN_POINT ( 'NONE',  ( 4.691466044806102076, 33.74235639413328158, -29.14742760351073869 ) ) ;
#52155=ORIENTED_EDGE ( 'NONE', *, *, #15281, .T. ) ;
#52178=CARTESIAN_POINT ( 'NONE',  ( 0.3622758884714600280, -42.84426538328734324, 4.808133778521152202 ) ) ;
#52182=EDGE_CURVE ( 'NONE', #25486, #47464, #10330, .T. ) ;
#52184=CARTESIAN_POINT ( 'NONE',  ( 0.6001305935487422083, -0.5236757026886095234, -48.10757715638248300 ) ) ;
#52194=CARTESIAN_POINT ( 'NONE',  ( 0.1073791018717483448, 26.63563652260123149, 33.91564619577815165 ) ) ;
#52195=CARTESIAN_POINT ( 'NONE',  ( 0.6030672727741701600, 29.35514790473150626, -38.11303703924438224 ) ) ;
#52205=CARTESIAN_POINT ( 'NONE',  ( 0.6001305935487422083, 37.84751346122816074, 29.70149728382448373 ) ) ;
#52206=B_SPLINE_CURVE_WITH_KNOTS ( 'NONE', 3,
 ( #36584, #8354, #27475, #42223, #27172, #22779, #32814, #46600, #61585, #18706, #61281, #47213, #46296, #56589, #4260, #42523 ),
 .UNSPECIFIED., .F., .F.,
 ( 4, 3, 3, 3, 3, 4 ),
 ( 1.995049841954898532E-17, 0.0002618515315864436031, 0.0003927756766342006475, 0.0005236998216950585405, 0.0007855159896329922840, 0.001047349442285930039 ),
 .UNSPECIFIED. ) ;
#52210=CARTESIAN_POINT ( 'NONE',  ( 1.827326673878745034, -25.21837361081565021, -34.89023127623411824 ) ) ;
#52214=CARTESIAN_POINT ( 'NONE',  ( -6.015611763856276717, 18.19956619163665223, -4.882992715191109667 ) ) ;
#52228=VERTEX_POINT ( 'NONE', #45291 ) ;
#52230=B_SPLINE_CURVE_WITH_KNOTS ( 'NONE', 3,
 ( #476, #9902, #38738, #38422, #10515, #57473, #9577, #33720, #10830, #24930, #47816, #4862, #14615, #19935, #43124, #52799, #57792, #14927, #27306 ),
 .UNSPECIFIED., .F., .F.,
 ( 4, 3, 3, 3, 3, 3, 4 ),
 ( 1.179660550279648157E-16, 0.0002618519381806238568, 0.0003927759815485961921, 0.0005237000248299418037, 0.0006546240681324958736, 0.0007855481115631319502, 0.0009699050456655096408 ),
 .UNSPECIFIED. ) ;
#52231=EDGE_CURVE ( 'NONE', #11294, #38025, #33465, .T. ) ;
#52239=CARTESIAN_POINT ( 'NONE',  ( 0.5998501479064699549, 34.38546660123250120, 33.64490850298857083 ) ) ;
#52241=CARTESIAN_POINT ( 'NONE',  ( 1.827119703190780653, 42.82501615430325614, 4.394694966566632388 ) ) ;
#52253=ADVANCED_FACE ( 'NONE', ( #30848 ), #41387, .F. ) ;
#52254=ORIENTED_EDGE ( 'NONE', *, *, #20545, .T. ) ;
#52260=CARTESIAN_POINT ( 'NONE',  ( -6.010958268070873523, 11.45964880703826339, 14.95835081545477863 ) ) ;
#52265=EDGE_CURVE ( 'NONE', #49895, #27049, #55848, .T. ) ;
#52270=CARTESIAN_POINT ( 'NONE',  ( -6.016489644550737204, -16.31649074174270808, -9.425415887801259274 ) ) ;
#52273=DIRECTION ( 'NONE',  ( 0.000000000000000000, 0.000000000000000000, -1.000000000000000000 ) ) ;
#52277=DIRECTION ( 'NONE',  ( 1.000000000000000000, 0.000000000000000000, 0.000000000000000000 ) ) ;
#52278=B_SPLINE_CURVE_WITH_KNOTS ( 'NONE', 3,
 ( #52866, #5235, #43497, #43187, #48183, #38184 ),
 .UNSPECIFIED., .F., .F.,
 ( 4, 2, 4 ),
 ( 1.764953265579307567E-18, 0.0002450742804987328209, 0.0004901485609974637987 ),
 .UNSPECIFIED. ) ;
#52285=CARTESIAN_POINT ( 'NONE',  ( 0.1102144999581333162, -16.38650952318882759, -39.88986724628629332 ) ) ;
#52290=CARTESIAN_POINT ( 'NONE',  ( 2.643462169533613793, -37.25264019563434914, 30.32726672320737293 ) ) ;
#52294=B_SPLINE_CURVE_WITH_KNOTS ( 'NONE', 3,
 ( #61925, #38175, #38791, #48174 ),
 .UNSPECIFIED., .F., .F.,
 ( 4, 4 ),
 ( 0.000000000000000000, 0.005014147105413700387 ),
 .UNSPECIFIED. ) ;
#52297=ORIENTED_EDGE ( 'NONE', *, *, #2185, .T. ) ;
#52299=B_SPLINE_CURVE_WITH_KNOTS ( 'NONE', 3,
 ( #51017, #8109, #3392, #60711, #17832, #24067 ),
 .UNSPECIFIED., .F., .F.,
 ( 4, 2, 4 ),
 ( 1.870559545977334001E-17, 0.0002293319059085106317, 0.0004586638118170025609 ),
 .UNSPECIFIED. ) ;
#52302=EDGE_CURVE ( 'NONE', #37338, #54112, #38685, .T. ) ;
#52307=CARTESIAN_POINT ( 'NONE',  ( 4.549368137175248350, -38.59302160394766901, 18.79584381673463866 ) ) ;
#52309=CARTESIAN_POINT ( 'NONE',  ( -6.016761891674564211, 2.462934516563804355, 18.68153697670642543 ) ) ;
#52313=CARTESIAN_POINT ( 'NONE',  ( 0.7954190325252770144, 33.39101560460801466, -34.61997719899450487 ) ) ;
#52317=EDGE_LOOP ( 'NONE', ( #38203, #7164, #43540, #48778 ) ) ;
#52321=CARTESIAN_POINT ( 'NONE',  ( 4.549368137175248350, -32.41327393324121431, -28.14399996863486209 ) ) ;
#52324=EDGE_CURVE ( 'NONE', #40762, #40551, #24453, .T. ) ;
#52326=B_SPLINE_CURVE_WITH_KNOTS ( 'NONE', 3,
 ( #20781, #16087, #44921, #35201, #54259, #25782 ),
 .UNSPECIFIED., .F., .F.,
 ( 4, 2, 4 ),
 ( 8.560751122900633232E-17, 0.0002293366620881449847, 0.0004586733241762043717 ),
 .UNSPECIFIED. ) ;
#52331=EDGE_LOOP ( 'NONE', ( #28370, #43144, #12310, #10102 ) ) ;
#52342=CARTESIAN_POINT ( 'NONE',  ( 0.1310142868023679297, -41.48473022063175364, -11.77532653407824270 ) ) ;
#52343=ORIENTED_EDGE ( 'NONE', *, *, #20383, .T. ) ;
#52344=CARTESIAN_POINT ( 'NONE',  ( 0.1073791018717483448, 6.109314776652144729, 42.68962945260955877 ) ) ;
#52359=CARTESIAN_POINT ( 'NONE',  ( 4.322998006666165516, 42.57894920390128135, -22.13465289016582460 ) ) ;
#52365=CARTESIAN_POINT ( 'NONE',  ( -2.569797478183790229, 14.44232325624823687, 2.353985772484800787 ) ) ;
#52366=CARTESIAN_POINT ( 'NONE',  ( 0.8760168074886960365, 47.80016357497249402, -5.394043284319009146 ) ) ;
#52369=DIRECTION ( 'NONE',  ( 0.000000000000000000, 8.881784197001252323E-16, 1.000000000000000000 ) ) ;
#52371=ORIENTED_EDGE ( 'NONE', *, *, #45503, .F. ) ;
#52380=CARTESIAN_POINT ( 'NONE',  ( 0.6017666602106489515, -38.37783452831185826, -29.00829887116056582 ) ) ;
#52387=EDGE_LOOP ( 'NONE', ( #61392, #37978, #54151, #38183 ) ) ;
#52389=VERTEX_POINT ( 'NONE', #38358 ) ;
#52395=LINE ( 'NONE', #9488, #15710 ) ;
#52396=B_SPLINE_CURVE_WITH_KNOTS ( 'NONE', 3,
 ( #60175, #17285, #3161, #36405, #18209, #37321, #51701, #31688, #50775, #51080, #56090, #7867, #46724, #46413, #17590, #13204 ),
 .UNSPECIFIED., .F., .F.,
 ( 4, 3, 3, 3, 3, 4 ),
 ( 2.221635811791082109E-17, 0.0002618515315864412721, 0.0003927756766341965818, 0.0005236998216950529026, 0.0007855159896329868630, 0.001047349442285927870 ),
 .UNSPECIFIED. ) ;
#52399=CARTESIAN_POINT ( 'NONE',  ( 0.5998501479064699549, -48.10473956285919428, 0.5236536531313263909 ) ) ;
#52401=ORIENTED_EDGE ( 'NONE', *, *, #56209, .F. ) ;
#52415=DIRECTION ( 'NONE',  ( 1.000000000000000000, 0.000000000000000000, 0.000000000000000000 ) ) ;
#52417=VERTEX_POINT ( 'NONE', #14545 ) ;
#52420=CARTESIAN_POINT ( 'NONE',  ( -6.015611763856276717, 18.84324252354755203, -0.006214430185207123029 ) ) ;
#52423=LINE ( 'NONE', #57115, #16553 ) ;
#52424=LINE ( 'NONE', #13945, #59457 ) ;
#52428=CARTESIAN_POINT ( 'NONE',  ( 4.975801465491695552, 0.000000000000000000, 0.000000000000000000 ) ) ;
#52429=CARTESIAN_POINT ( 'NONE',  ( 0.7246131072078515478, 19.16331062551085651, -44.12003537001155706 ) ) ;
#52432=VERTEX_POINT ( 'NONE', #35192 ) ;
#52437=CARTESIAN_POINT ( 'NONE',  ( -4.908599999999998964, 0.000000000000000000, 0.000000000000000000 ) ) ;
#52438=AXIS2_PLACEMENT_3D ( 'NONE', #17528, #51026, #17842 ) ;
#52445=CARTESIAN_POINT ( 'NONE',  ( -6.017396004339687465, 4.875835690939179123, 18.20140164570670649 ) ) ;
#52449=EDGE_LOOP ( 'NONE', ( #54280, #33005, #19017, #38251 ) ) ;
#52459=VERTEX_POINT ( 'NONE', #11371 ) ;
#52463=CARTESIAN_POINT ( 'NONE',  ( -6.001507490154110336, 11.45906331631453234, -14.95933060264861858 ) ) ;
#52464=EDGE_CURVE ( 'NONE', #29811, #32714, #7989, .T. ) ;
#52470=CARTESIAN_POINT ( 'NONE',  ( 0.7048096507298635682, 19.18768066167060127, 44.11842270945980715 ) ) ;
#52473=ORIENTED_EDGE ( 'NONE', *, *, #2414, .F. ) ;
#52474=CARTESIAN_POINT ( 'NONE',  ( 4.691466044806103852, -44.46979273209137773, 3.249105306917663416 ) ) ;
#52480=DIRECTION ( 'NONE',  ( 0.09835009131224567436, 0.9592125346408684194, 0.2650256080583793250 ) ) ;
#52482=ADVANCED_FACE ( 'NONE', ( #40520 ), #9333, .F. ) ;
#52485=VERTEX_POINT ( 'NONE', #22624 ) ;
#52504=CARTESIAN_POINT ( 'NONE',  ( 0.6023142530420679819, 29.07781306567101609, -38.32506243004162627 ) ) ;
#52506=CARTESIAN_POINT ( 'NONE',  ( 0.1095718737110178698, 16.74012863188504596, -39.74279513315657653 ) ) ;
#52508=CARTESIAN_POINT ( 'NONE',  ( -5.995132425357893702, 14.95525565067274876, 11.46484027925372828 ) ) ;
#52509=( BOUNDED_SURFACE ( )  B_SPLINE_SURFACE ( 3, 1, ( 
 ( #39700, #19655 ),
 ( #24965, #5212 ),
 ( #53443, #40015 ),
 ( #59067, #514 ) ),
 .UNSPECIFIED., .F., .F., .F. ) 
 B_SPLINE_SURFACE_WITH_KNOTS ( ( 4, 4 ),
 ( 2, 2 ),
 ( 0.000000000000000000, 1.000000000000000000 ),
 ( 0.000000000000000000, 1.000000000000000000 ),
 .UNSPECIFIED. ) 
 GEOMETRIC_REPRESENTATION_ITEM ( )  RATIONAL_B_SPLINE_SURFACE ( (
 ( 1.000000000000000000, 1.000000000000000000),
 ( 0.7223157951917480446, 0.9931996967497186413),
 ( 0.7223157951917480446, 0.9931996967497186413),
 ( 1.000000000000000000, 1.000000000000000000) ) ) 
 REPRESENTATION_ITEM ( '' )  SURFACE ( )  );
#52512=( BOUNDED_SURFACE ( )  B_SPLINE_SURFACE ( 3, 1, ( 
 ( #56187, #28306 ),
 ( #22688, #41818 ),
 ( #23308, #8571 ),
 ( #28004, #3866 ) ),
 .UNSPECIFIED., .F., .F., .F. ) 
 B_SPLINE_SURFACE_WITH_KNOTS ( ( 4, 4 ),
 ( 2, 2 ),
 ( 0.000000000000000000, 1.000000000000000000 ),
 ( 0.000000000000000000, 1.000000000000000000 ),
 .UNSPECIFIED. ) 
 GEOMETRIC_REPRESENTATION_ITEM ( )  RATIONAL_B_SPLINE_SURFACE ( (
 ( 1.000000000000000000, 1.000000000000000000),
 ( 0.9751682680413298332, 0.9999560080971552356),
 ( 0.9751682680413298332, 0.9999560080971552356),
 ( 1.000000000000000000, 1.000000000000000000) ) ) 
 REPRESENTATION_ITEM ( '' )  SURFACE ( )  );
#52517=CARTESIAN_POINT ( 'NONE',  ( -6.015611763856276717, 9.416239407363303116, 16.32183393015600004 ) ) ;
#52518=DIRECTION ( 'NONE',  ( -1.000000000000000000, -0.000000000000000000, -0.000000000000000000 ) ) ;
#52521=CARTESIAN_POINT ( 'NONE',  ( 0.6009452777970409887, 47.75105029762383424, 5.846392105360695091 ) ) ;
#52522=CARTESIAN_POINT ( 'NONE',  ( 2.643462169533600914, -46.73820883660214065, 11.09243630552451876 ) ) ;
#52524=CARTESIAN_POINT ( 'NONE',  ( 0.2224561200757616264, -26.84793396061007087, 33.74134531362587097 ) ) ;
#52525=CARTESIAN_POINT ( 'NONE',  ( 0.6001305935487315502, 23.60027211631829402, -41.92422178329146476 ) ) ;
#52527=ORIENTED_EDGE ( 'NONE', *, *, #12879, .T. ) ;
#52528=VECTOR ( 'NONE', #40485, 1000.000000000000114 ) ;
#52541=ORIENTED_EDGE ( 'NONE', *, *, #46846, .T. ) ;
#52547=FACE_OUTER_BOUND ( 'NONE', #1381, .T. ) ;
#52556=EDGE_CURVE ( 'NONE', #16923, #47251, #2399, .T. ) ;
#52570=CARTESIAN_POINT ( 'NONE',  ( 4.975801465491695552, 39.51822597168496287, -27.09127437476339395 ) ) ;
#52576=ORIENTED_EDGE ( 'NONE', *, *, #18746, .T. ) ;
#52579=CARTESIAN_POINT ( 'NONE',  ( 0.7246131072078558777, 47.57651137777903472, 7.091231226024960144 ) ) ;
#52592=DIRECTION ( 'NONE',  ( 0.000000000000000000, 0.000000000000000000, -1.000000000000000000 ) ) ;
#52599=CARTESIAN_POINT ( 'NONE',  ( 3.238931869106854489, 35.19033040238034005, 24.69728751010298495 ) ) ;
#52601=DIRECTION ( 'NONE',  ( 0.09835009131224567436, -0.5996571005210353800, -0.7941905447268796658 ) ) ;
#52610=VERTEX_POINT ( 'NONE', #56119 ) ;
#52614=CARTESIAN_POINT ( 'NONE',  ( 3.680974057930773924, -44.99871514631803393, 16.63696281867780868 ) ) ;
#52617=ORIENTED_EDGE ( 'NONE', *, *, #46004, .F. ) ;
#52618=CARTESIAN_POINT ( 'NONE',  ( 0.8760168074887076939, 47.80016357497242296, 5.394043284319666398 ) ) ;
#52625=ORIENTED_EDGE ( 'NONE', *, *, #34083, .T. ) ;
#52632=CARTESIAN_POINT ( 'NONE',  ( 0.8751705887134423323, -34.63284514348608667, 33.37254303619495488 ) ) ;
#52638=CARTESIAN_POINT ( 'NONE',  ( 4.549368137175248350, 42.82045902618768451, 3.018832571116707442 ) ) ;
#52646=CARTESIAN_POINT ( 'NONE',  ( 0.6001305935487315502, -46.33281397023053927, -12.95698906763794334 ) ) ;
#52653=AXIS2_PLACEMENT_3D ( 'NONE', #27144, #61560, #23373 ) ;
#52654=VERTEX_POINT ( 'NONE', #25085 ) ;
#52655=LINE ( 'NONE', #39527, #40987 ) ;
#52656=AXIS2_PLACEMENT_3D ( 'NONE', #35881, #49965, #30847 ) ;
#52665=CIRCLE ( 'NONE', #10657, 47.91270532121795611 ) ;
#52668=DIRECTION ( 'NONE',  ( 0.09835009131224552170, 0.7091251765523974848, 0.6981896185982745529 ) ) ;
#52669=CARTESIAN_POINT ( 'NONE',  ( 0.6017667736363750963, 48.10631678344240925, 0.3491025323182196938 ) ) ;
#52670=CARTESIAN_POINT ( 'NONE',  ( -2.708315649062916552, 11.44805714186571777, -9.116606751444216172 ) ) ;
#52672=AXIS2_PLACEMENT_3D ( 'NONE', #6120, #25261, #53138 ) ;
#52675=CARTESIAN_POINT ( 'NONE',  ( 0.7048096507298579061, 47.80151517212785706, -5.442192462018969223 ) ) ;
#52677=EDGE_CURVE ( 'NONE', #29523, #4, #4301, .T. ) ;
#52696=ORIENTED_EDGE ( 'NONE', *, *, #30109, .T. ) ;
#52701=CARTESIAN_POINT ( 'NONE',  ( -5.995132425357893702, 11.47834865841095642, 14.94489030678155572 ) ) ;
#52702=EDGE_CURVE ( 'NONE', #28193, #4544, #48379, .T. ) ;
#52706=CARTESIAN_POINT ( 'NONE',  ( 0.1084644655670281566, 0.3976617192052402938, 43.12277244437006374 ) ) ;
#52710=ORIENTED_EDGE ( 'NONE', *, *, #32483, .T. ) ;
#52720=DIRECTION ( 'NONE',  ( -1.000000000000000000, -0.000000000000000000, -0.000000000000000000 ) ) ;
#52724=CARTESIAN_POINT ( 'NONE',  ( -6.016489644550736315, 18.19999694163070814, -4.881234076340183137 ) ) ;
#52728=VERTEX_POINT ( 'NONE', #38910 ) ;
#52733=CARTESIAN_POINT ( 'NONE',  ( 0.8760168074887076939, -24.81951362746049838, -41.20610493656901241 ) ) ;
#52737=CARTESIAN_POINT ( 'NONE',  ( 0.2230388203127650348, -17.20066002792390236, -39.54016926433967427 ) ) ;
#52741=CARTESIAN_POINT ( 'NONE',  ( -5.995132425357893702, -13.33084941932916756, 13.31880955509722497 ) ) ;
#52742=ADVANCED_FACE ( 'NONE', ( #11006 ), #33512, .F. ) ;
#52743=CARTESIAN_POINT ( 'NONE',  ( 0.5980894510889448457, -44.17723055703940105, -19.05812566676491215 ) ) ;
#52745=AXIS2_PLACEMENT_3D ( 'NONE', #7720, #22145, #37821 ) ;
#52748=CARTESIAN_POINT ( 'NONE',  ( 0.1104177457020372732, -34.21590786699023568, -26.24862037251720537 ) ) ;
#52751=CARTESIAN_POINT ( 'NONE',  ( 0.6028618097248863439, -23.90242650600305296, 41.74935807801004017 ) ) ;
#52754=CARTESIAN_POINT ( 'NONE',  ( 4.549368137175248350, -42.06008734272390370, -8.582197505784284530 ) ) ;
#52758=EDGE_CURVE ( 'NONE', #5676, #33419, #61768, .T. ) ;
#52764=CARTESIAN_POINT ( 'NONE',  ( 0.1064266418746777076, -37.62465821955116496, 21.07422140941941180 ) ) ;
#52766=CARTESIAN_POINT ( 'NONE',  ( 0.1073791018717578927, -21.14095454447534550, -37.58707531572198235 ) ) ;
#52771=VECTOR ( 'NONE', #30624, 1000.000000000000114 ) ;
#52775=CARTESIAN_POINT ( 'NONE',  ( 0.1064266418746776244, 17.02047513535232071, -39.62374465289877890 ) ) ;
#52779=ADVANCED_FACE ( 'NONE', ( #40156 ), #2446, .F. ) ;
#52782=EDGE_CURVE ( 'NONE', #53617, #59362, #34979, .T. ) ;
#52785=VERTEX_POINT ( 'NONE', #4257 ) ;
#52792=CARTESIAN_POINT ( 'NONE',  ( 0.6023143664670691511, 46.39980466492342970, 12.70384782338105545 ) ) ;
#52799=CARTESIAN_POINT ( 'NONE',  ( 0.1092355843206037486, -37.19569459163120229, -21.82203846347315590 ) ) ;
#52803=ORIENTED_EDGE ( 'NONE', *, *, #52815, .T. ) ;
#52804=FACE_OUTER_BOUND ( 'NONE', #25946, .T. ) ;
#52808=ORIENTED_EDGE ( 'NONE', *, *, #50405, .F. ) ;
#52810=CARTESIAN_POINT ( 'NONE',  ( 0.5980894510889448457, -42.01322166096935007, 23.44630161211513197 ) ) ;
#52811=CARTESIAN_POINT ( 'NONE',  ( 4.549368137175248350, -23.67244292351614376, -35.80950303116092925 ) ) ;
#52813=CIRCLE ( 'NONE', #54770, 47.91270532121795611 ) ;
#52815=EDGE_CURVE ( 'NONE', #30127, #34543, #8662, .T. ) ;
#52819=DIRECTION ( 'NONE',  ( 1.000000000000000000, 0.000000000000000000, 0.000000000000000000 ) ) ;
#52820=CARTESIAN_POINT ( 'NONE',  ( -6.010958268070873523, -2.445171577615640857, -18.68413620842266454 ) ) ;
#52834=CARTESIAN_POINT ( 'NONE',  ( 0.8760168074887076939, 44.77533136581857320, 17.58183840866416148 ) ) ;
#52839=CARTESIAN_POINT ( 'NONE',  ( 0.6031356755852232965, 4.336951783013129340E-16, 48.10744332413860747 ) ) ;
#52841=CARTESIAN_POINT ( 'NONE',  ( 0.1064266418746774440, -25.80493189480207761, -34.55203617814582628 ) ) ;
#52844=ORIENTED_EDGE ( 'NONE', *, *, #31836, .F. ) ;
#52852=ORIENTED_EDGE ( 'NONE', *, *, #14099, .T. ) ;
#52854=B_SPLINE_CURVE_WITH_KNOTS ( 'NONE', 3,
 ( #22789, #4269, #37216, #32506 ),
 .UNSPECIFIED., .F., .F.,
 ( 4, 4 ),
 ( 0.000000000000000000, 0.005014147105413709060 ),
 .UNSPECIFIED. ) ;
#52866=CARTESIAN_POINT ( 'NONE',  ( 0.5998501479064699549, -12.95623334615470057, -46.33007877220734372 ) ) ;
#52873=B_SPLINE_CURVE_WITH_KNOTS ( 'NONE', 3,
 ( #3659, #22482, #47527, #13716, #46615, #56290 ),
 .UNSPECIFIED., .F., .F.,
 ( 4, 2, 4 ),
 ( 2.032850612904068153E-17, 0.0002293319059085106046, 0.0004586638118170008804 ),
 .UNSPECIFIED. ) ;
#52877=CARTESIAN_POINT ( 'NONE',  ( 0.1313383488274104394, 21.00709374781539651, -37.66088038379817249 ) ) ;
#52882=VECTOR ( 'NONE', #17891, 1000.000000000000227 ) ;
#52886=CARTESIAN_POINT ( 'NONE',  ( -6.001507490154111224, -7.196845540359040783, -17.41542759839272136 ) ) ;
#52887=CARTESIAN_POINT ( 'NONE',  ( 4.549368137175248350, -24.02461520945298545, 35.57418903283073064 ) ) ;
#52888=( BOUNDED_SURFACE ( )  B_SPLINE_SURFACE ( 3, 1, ( 
 ( #5477, #24613 ),
 ( #28688, #47814 ),
 ( #57472, #43750 ),
 ( #797, #20230 ) ),
 .UNSPECIFIED., .F., .F., .F. ) 
 B_SPLINE_SURFACE_WITH_KNOTS ( ( 4, 4 ),
 ( 2, 2 ),
 ( 0.000000000000000000, 1.000000000000000000 ),
 ( 0.000000000000000000, 1.000000000000000000 ),
 .UNSPECIFIED. ) 
 GEOMETRIC_REPRESENTATION_ITEM ( )  RATIONAL_B_SPLINE_SURFACE ( (
 ( 1.000000000000000000, 1.000000000000000000),
 ( 0.9751682680413298332, 0.9999560080971552356),
 ( 0.9751682680413298332, 0.9999560080971552356),
 ( 1.000000000000000000, 1.000000000000000000) ) ) 
 REPRESENTATION_ITEM ( '' )  SURFACE ( )  );
#52891=EDGE_CURVE ( 'NONE', #24440, #40711, #57339, .T. ) ;
#52894=CARTESIAN_POINT ( 'NONE',  ( 0.3622758884714600280, -26.89560658783410574, 33.69533458712297147 ) ) ;
#52898=CIRCLE ( 'NONE', #19927, 42.92674063221959813 ) ;
#52899=ORIENTED_EDGE ( 'NONE', *, *, #42743, .T. ) ;
#52903=CARTESIAN_POINT ( 'NONE',  ( 1.827119703190778877, -12.32825544177808119, -41.24693285842924695 ) ) ;
#52909=DIRECTION ( 'NONE',  ( 1.000000000000000000, 0.000000000000000000, 0.000000000000000000 ) ) ;
#52918=VERTEX_POINT ( 'NONE', #4562 ) ;
#52921=CARTESIAN_POINT ( 'NONE',  ( 0.1102847568649952675, 37.39286109091547416, 21.48234084756709095 ) ) ;
#52930=ORIENTED_EDGE ( 'NONE', *, *, #6269, .T. ) ;
#52931=CARTESIAN_POINT ( 'NONE',  ( 4.691466044806102076, -42.32811009116564804, 14.01607102724468490 ) ) ;
#52936=ORIENTED_EDGE ( 'NONE', *, *, #41327, .T. ) ;
#52937=CARTESIAN_POINT ( 'NONE',  ( 0.8760168074887090262, -44.09317760313766144, 19.22870327415225233 ) ) ;
#52944=CARTESIAN_POINT ( 'NONE',  ( -2.708315649062910779, 5.842990691604599718, -13.41752550814504907 ) ) ;
#52945=CARTESIAN_POINT ( 'NONE',  ( 0.2230388203127619540, 33.74101226470666859, -26.84831060237808131 ) ) ;
#52952=CARTESIAN_POINT ( 'NONE',  ( -6.016761891674565099, 9.418621820384494470, 16.32039929810260048 ) ) ;
#52965=CARTESIAN_POINT ( 'NONE',  ( 0.6041374136657475802, 47.67304777898691270, 6.452348380036067255 ) ) ;
#52967=ADVANCED_FACE ( 'NONE', ( #810 ), #35911, .F. ) ;
#52970=DIRECTION ( 'NONE',  ( -0.1024043820194934645, 0.9946559125373960475, 0.01315135725336188596 ) ) ;
#52971=ADVANCED_FACE ( 'NONE', ( #19633 ), #54710, .F. ) ;
#52980=CARTESIAN_POINT ( 'NONE',  ( 0.2885700199627508344, -36.93108631019309485, 22.25146206940400972 ) ) ;
#52981=CARTESIAN_POINT ( 'NONE',  ( 0.6023143664670691511, 48.10676742339276046, 0.2618215695309267232 ) ) ;
#52984=CARTESIAN_POINT ( 'NONE',  ( 0.6001305935487422083, 44.64600790884030346, 17.92615948558555417 ) ) ;
#52985=B_SPLINE_CURVE_WITH_KNOTS ( 'NONE', 3,
 ( #43142, #48135, #47836, #19026, #39065, #14322, #15242, #52195, #495, #814, #14943, #34051, #52504, #28396, #178, #5492 ),
 .UNSPECIFIED., .F., .F.,
 ( 4, 3, 3, 3, 3, 4 ),
 ( 1.962735358247463844E-17, 0.0002618515315864417600, 0.0003927756766342021112, 0.0005236998216950595163, 0.0007855159896329960787, 0.001047349442285930039 ),
 .UNSPECIFIED. ) ;
#52991=CARTESIAN_POINT ( 'NONE',  ( 4.549368137175248350, 0.000000000000000000, 0.000000000000000000 ) ) ;
#52993=CARTESIAN_POINT ( 'NONE',  ( 4.549368137175248350, 28.14399996863453168, 32.41327393324149853 ) ) ;
#52999=CARTESIAN_POINT ( 'NONE',  ( -5.995132425357893702, 4.869002713216572076, 18.20425902871269486 ) ) ;
#53008=DIRECTION ( 'NONE',  ( 1.000000000000000000, 0.000000000000000000, 0.000000000000000000 ) ) ;
#53011=CARTESIAN_POINT ( 'NONE',  ( 0.8760168074886960365, -46.22580377597776646, -13.30888447662064067 ) ) ;
#53013=CARTESIAN_POINT ( 'NONE',  ( 0.7245667037590795001, -44.74806999162976240, -17.64710816761245482 ) ) ;
#53014=CLOSED_SHELL ( 'NONE', ( #53057, #32979, #5442, #29041, #4109, #31631, #45732, #27651, #19537, #7113, #48103, #58247, #27164, #37097, #40500, #20078, #54870, #13932, #58024, #53732, #34986, #54273, #6318, #43101, #56356, #32608, #36724, #28753, #1836, #12953, #50988, #48827, #8140, #5773, #18486, #37004, #31067, #45433, #37122, #7909, #54793, #22706, #44033, #11669, #8154, #31833, #25670, #15687, #16178, #40413, #12686, #41982, #42677, #25091, #7924, #41146, #7584, #26962, #42975, #51971, #2449, #46770, #30524, #6047, #54203, #56559, #33019, #11323, #19913, #47450, #29373, #45916, #37823, #24056, #24704, #16692, #39946, #57537, #2206, #20497, #9729, #18463, #35593, #27865, #18670, #26066, #17969, #30547, #58338, #15864, #5287, #10638, #24425, #3020, #53577, #59775, #42924, #56155, #29401, #37507, #39493, #50480, #7933, #32467, #14667, #52482, #57121, #6231, #32388, #20193, #6281, #4424, #7299, #58882, #12524, #38601, #48490, #24787, #24267, #44121, #25970, #24390, #61526, #32082, #26811, #18333, #9127, #33613, #56851, #24088, #57203, #2119, #54351, #23539, #16328, #40084, #6972, #3439, #37983, #43653, #44024, #4146, #40836, #314, #33201, #37908, #48171, #2055, #19987, #7771, #6129, #10143, #20727, #34645, #50377, #8992, #50397, #1184, #17973, #3121, #58593, #49435, #54083, #40216, #13908, #49618, #42184, #24814, #26898, #22833, #21119, #25050, #18265, #10321, #53720, #9914, #24666, #30261, #4377, #1682, #12221, #19849, #61442, #54133, #16768, #15655, #37913, #36288, #49084, #4149, #56132, #42390, #32855, #1081, #5585, #28231, #12701, #49646, #6694, #32977, #45638, #49859, #52967, #45484, #2668, #52779, #55500, #42632, #43222, #52253, #53211, #30098, #727, #18856, #25503, #16788, #53230, #19330, #28984, #46773, #40052, #26523, #38170, #28132, #44802, #27782, #37738, #5415, #51435, #52742, #14505, #22133, #34308, #1302, #58857, #49589, #31673, #57665, #54759, #26713, #50995, #12270, #39134, #40100, #35952, #47820, #19651, #1557, #32713, #913, #16487, #39359, #42882, #59909, #58935, #9463, #39579, #553, #61862, #20116, #24560, #37576, #5965, #14379, #13383, #18181, #20653, #36739, #60240, #52115, #41560, #11465, #27505, #53436, #46416, #4499, #36372, #28954, #9307, #60072, #36097, #7541, #23597, #14130, #12477, #4157, #30577, #59010, #6460, #47084, #25154, #42802, #52971, #59850, #9578, #11335, #36947, #54988, #17048, #37036 ) ) ;
#53016=ORIENTED_EDGE ( 'NONE', *, *, #15091, .F. ) ;
#53017=EDGE_CURVE ( 'NONE', #55454, #47659, #6401, .T. ) ;
#53019=CARTESIAN_POINT ( 'NONE',  ( -6.015611763856276717, 14.94556629257441038, -11.47596948473795919 ) ) ;
#53020=VECTOR ( 'NONE', #26038, 999.9999999999998863 ) ;
#53030=CARTESIAN_POINT ( 'NONE',  ( -6.016761891674565099, -2.462934516563935805, 18.68153697670640767 ) ) ;
#53037=ORIENTED_EDGE ( 'NONE', *, *, #32895, .T. ) ;
#53038=ORIENTED_EDGE ( 'NONE', *, *, #10599, .F. ) ;
#53041=EDGE_CURVE ( 'NONE', #38521, #19675, #31066, .T. ) ;
#53046=CARTESIAN_POINT ( 'NONE',  ( -6.010958268070873523, -2.473955915502343395, 18.68034667844848329 ) ) ;
#53050=CARTESIAN_POINT ( 'NONE',  ( 0.6027935024548037868, -18.24855952726199604, -44.51201578381220259 ) ) ;
#53052=ORIENTED_EDGE ( 'NONE', *, *, #21493, .T. ) ;
#53056=CARTESIAN_POINT ( 'NONE',  ( -6.016489644550736315, -0.004404229197644145798, -18.84320342686341121 ) ) ;
#53057=ADVANCED_FACE ( 'NONE', ( #22390 ), #16456, .F. ) ;
#53061=DIRECTION ( 'NONE',  ( 0.000000000000000000, 0.000000000000000000, -1.000000000000000000 ) ) ;
#53062=AXIS2_PLACEMENT_3D ( 'NONE', #42717, #27987, #61776 ) ;
#53065=CARTESIAN_POINT ( 'NONE',  ( 4.833616638992205949, -45.44786513329603395, 8.578242093414962355 ) ) ;
#53066=CARTESIAN_POINT ( 'NONE',  ( 4.549368137175248350, 28.14399996863497577, -32.41327393324110773 ) ) ;
#53067=CARTESIAN_POINT ( 'NONE',  ( 0.1073791018717483448, -26.63563652260144821, -33.91564619577798823 ) ) ;
#53077=ORIENTED_EDGE ( 'NONE', *, *, #44512, .F. ) ;
#53108=ORIENTED_EDGE ( 'NONE', *, *, #61708, .F. ) ;
#53114=CARTESIAN_POINT ( 'NONE',  ( -6.016489644550736315, 16.31649074174290703, -9.425415887800916437 ) ) ;
#53121=LINE ( 'NONE', #48432, #38810 ) ;
#53127=CARTESIAN_POINT ( 'NONE',  ( 1.827326673878741481, 29.55671596281165847, 31.30008222956393027 ) ) ;
#53135=CARTESIAN_POINT ( 'NONE',  ( 0.5988103622719989083, 17.84821742497932462, 44.67429504351065361 ) ) ;
#53136=( BOUNDED_SURFACE ( )  B_SPLINE_SURFACE ( 3, 1, ( 
 ( #34727, #19698 ),
 ( #48203, #15006 ),
 ( #49418, #11221 ),
 ( #25617, #39437 ) ),
 .UNSPECIFIED., .F., .F., .F. ) 
 B_SPLINE_SURFACE_WITH_KNOTS ( ( 4, 4 ),
 ( 2, 2 ),
 ( 0.000000000000000000, 1.000000000000000000 ),
 ( 0.000000000000000000, 1.000000000000000000 ),
 .UNSPECIFIED. ) 
 GEOMETRIC_REPRESENTATION_ITEM ( )  RATIONAL_B_SPLINE_SURFACE ( (
 ( 1.000000000000000000, 1.000000000000000000),
 ( 0.7223157951917476005, 0.9931996967497186413),
 ( 0.7223157951917476005, 0.9931996967497186413),
 ( 1.000000000000000000, 1.000000000000000000) ) ) 
 REPRESENTATION_ITEM ( '' )  SURFACE ( )  );
#53138=DIRECTION ( 'NONE',  ( 0.000000000000000000, 0.000000000000000000, 1.000000000000000000 ) ) ;
#53139=CARTESIAN_POINT ( 'NONE',  ( 0.1310142868023689289, -26.75450212504347292, 33.82067078731299858 ) ) ;
#53143=CARTESIAN_POINT ( 'NONE',  ( 4.975801465491694664, -43.22084481528235500, 20.67815041659062913 ) ) ;
#53151=VECTOR ( 'NONE', #15652, 1000.000000000000114 ) ;
#53162=B_SPLINE_CURVE_WITH_KNOTS ( 'NONE', 3,
 ( #35078, #30653, #30978, #11896, #26269, #7449, #10958, #44798, #25972, #39796, #40402, #16262, #49460, #21268, #12202, #59463, #50384, #25349, #50088 ),
 .UNSPECIFIED., .F., .F.,
 ( 4, 3, 3, 3, 3, 3, 4 ),
 ( 1.157434093048479169E-16, 0.0002618519381806257000, 0.0003927759815485975473, 0.0005237000248299427795, 0.0006546240681324977167, 0.0007855481115631319502, 0.0009699050456655103998 ),
 .UNSPECIFIED. ) ;
#53168=EDGE_CURVE ( 'NONE', #42991, #11351, #52424, .T. ) ;
#53187=CARTESIAN_POINT ( 'NONE',  ( 0.1073791018717578927, -21.14095454447534550, -37.58707531572198235 ) ) ;
#53188=ORIENTED_EDGE ( 'NONE', *, *, #45632, .T. ) ;
#53192=ORIENTED_EDGE ( 'NONE', *, *, #46972, .T. ) ;
#53196=CARTESIAN_POINT ( 'NONE',  ( 0.5980894510889448457, 5.583794302584615288, 47.78766676462078067 ) ) ;
#53204=CARTESIAN_POINT ( 'NONE',  ( 0.6023143664670691511, 12.19804739160196938, 46.53533348214995868 ) ) ;
#53208=CARTESIAN_POINT ( 'NONE',  ( 4.975801465491694664, 43.22084481528220579, -20.67815041659094888 ) ) ;
#53210=DIRECTION ( 'NONE',  ( 0.09835009131224567436, 0.9855991218957013134, 0.1375559175655325372 ) ) ;
#53211=ADVANCED_FACE ( 'NONE', ( #32421 ), #10286, .F. ) ;
#53215=CARTESIAN_POINT ( 'NONE',  ( -2.708315649062916552, -10.53288422393049473, -10.16016146078285054 ) ) ;
#53217=DIRECTION ( 'NONE',  ( 0.1024043820194936311, 0.6159418278945496539, 0.7811075516170142841 ) ) ;
#53226=ORIENTED_EDGE ( 'NONE', *, *, #36977, .T. ) ;
#53230=ADVANCED_FACE ( 'NONE', ( #43372 ), #14323, .F. ) ;
#53234=CARTESIAN_POINT ( 'NONE',  ( 0.2885700199627522222, -31.05173037893222343, -29.91358789498772097 ) ) ;
#53235=EDGE_CURVE ( 'NONE', #55695, #11438, #7191, .T. ) ;
#53237=ORIENTED_EDGE ( 'NONE', *, *, #20241, .T. ) ;
#53244=CARTESIAN_POINT ( 'NONE',  ( 4.549368137175248350, 0.000000000000000000, 0.000000000000000000 ) ) ;
#53246=ORIENTED_EDGE ( 'NONE', *, *, #61568, .F. ) ;
#53250=CARTESIAN_POINT ( 'NONE',  ( -2.708315649062916552, 7.544341609839809948, 12.54007339125017317 ) ) ;
#53276=B_SPLINE_CURVE_WITH_KNOTS ( 'NONE', 3,
 ( #29347, #48452, #39090, #1140 ),
 .UNSPECIFIED., .F., .F.,
 ( 4, 4 ),
 ( 2.226610509583310728E-17, 0.004564976165746187711 ),
 .UNSPECIFIED. ) ;
#53278=CARTESIAN_POINT ( 'NONE',  ( -6.015611763856276717, 0.006214430185141332774, 18.84324252354755203 ) ) ;
#53287=CARTESIAN_POINT ( 'NONE',  ( -6.016489644550736315, 4.881234076340374095, 18.19999694163065840 ) ) ;
#53290=AXIS2_PLACEMENT_3D ( 'NONE', #31437, #7609, #60232 ) ;
#53293=ORIENTED_EDGE ( 'NONE', *, *, #26769, .F. ) ;
#53296=CARTESIAN_POINT ( 'NONE',  ( 0.7954196712028466232, 28.58653687859115067, 38.68220069891179946 ) ) ;
#53302=CARTESIAN_POINT ( 'NONE',  ( 4.322998006666179727, -14.45630056002908503, -45.75942687572293011 ) ) ;
#53307=EDGE_CURVE ( 'NONE', #46926, #38023, #14503, .T. ) ;
#53317=B_SPLINE_CURVE_WITH_KNOTS ( 'NONE', 3,
 ( #29662, #38789, #57849, #38174, #14976, #34087 ),
 .UNSPECIFIED., .F., .F.,
 ( 4, 2, 4 ),
 ( 8.525499192591780946E-17, 0.0002293366620881460689, 0.0004586733241762069196 ),
 .UNSPECIFIED. ) ;
#53322=CARTESIAN_POINT ( 'NONE',  ( 0.1313383488274121880, 41.48452234694097740, -11.77600546273727034 ) ) ;
#53334=ORIENTED_EDGE ( 'NONE', *, *, #35814, .F. ) ;
#53337=DIRECTION ( 'NONE',  ( 0.000000000000000000, 0.000000000000000000, -1.000000000000000000 ) ) ;
#53339=EDGE_LOOP ( 'NONE', ( #1232, #44531, #50607, #24399 ) ) ;
#53342=CARTESIAN_POINT ( 'NONE',  ( 50.00005079999999680, 0.000000000000000000, 3.000000000000000000 ) ) ;
#53346=CARTESIAN_POINT ( 'NONE',  ( 0.6041374136657475802, 29.42442150067197204, -38.05989626241401425 ) ) ;
#53347=CARTESIAN_POINT ( 'NONE',  ( 2.643462169533613793, 4.896978544602148098, -47.78621045426870495 ) ) ;
#53350=EDGE_CURVE ( 'NONE', #13656, #28634, #28513, .T. ) ;
#53352=CARTESIAN_POINT ( 'NONE',  ( 0.1103878639767399417, 30.45925431905113356, -30.52789484587422564 ) ) ;
#53353=CARTESIAN_POINT ( 'NONE',  ( -6.016104459813371719, 17.41090761020836553, 7.206059014950146668 ) ) ;
#53355=CARTESIAN_POINT ( 'NONE',  ( 4.975801465491694664, 36.39623109580467997, -31.15993731089085017 ) ) ;
#53356=CARTESIAN_POINT ( 'NONE',  ( 4.975801465491694664, 45.55012473237754023, -14.85979367497125381 ) ) ;
#53359=CARTESIAN_POINT ( 'NONE',  ( 2.301529144917016101, -46.71331407887430487, -11.18385659262662024 ) ) ;
#53360=CARTESIAN_POINT ( 'NONE',  ( 0.5998501479064699549, -46.33007877220747872, 12.95623334615421740 ) ) ;
#53366=CARTESIAN_POINT ( 'NONE',  ( 0.8760168074886965917, -13.30888447662113094, 46.22580377597762435 ) ) ;
#53367=CARTESIAN_POINT ( 'NONE',  ( 2.301430502907645170, -43.86847929982172900, -19.56449039932716616 ) ) ;
#53379=CARTESIAN_POINT ( 'NONE',  ( -6.016104459813374383, 17.40682403289248370, 7.215917642689130496 ) ) ;
#53382=CARTESIAN_POINT ( 'NONE',  ( 0.6031357023905875581, -24.01594909943237610, -41.68407605450304487 ) ) ;
#53386=CARTESIAN_POINT ( 'NONE',  ( 0.5998501479064699549, -46.33007877220747872, 12.95623334615421740 ) ) ;
#53388=EDGE_CURVE ( 'NONE', #33185, #2469, #37642, .T. ) ;
#53397=ORIENTED_EDGE ( 'NONE', *, *, #17377, .F. ) ;
#53398=CARTESIAN_POINT ( 'NONE',  ( -6.010958268070873523, -13.31406649671971998, 13.33459572764752998 ) ) ;
#53411=CARTESIAN_POINT ( 'NONE',  ( -6.016761891674564211, 18.20023637398605842, -4.880293656734773222 ) ) ;
#53422=CARTESIAN_POINT ( 'NONE',  ( 4.975801465491695552, 0.000000000000000000, 0.000000000000000000 ) ) ;
#53423=CARTESIAN_POINT ( 'NONE',  ( 0.2230388203127658953, -20.89822698305293613, 37.71673103297332119 ) ) ;
#53424=CARTESIAN_POINT ( 'NONE',  ( -6.010958268070873523, -2.445171577615893987, 18.68413620842263612 ) ) ;
#53430=EDGE_CURVE ( 'NONE', #45197, #9105, #18428, .T. ) ;
#53435=CARTESIAN_POINT ( 'NONE',  ( 0.6023143664670691511, 38.32505149877513162, -29.07782746490714487 ) ) ;
#53436=ADVANCED_FACE ( 'NONE', ( #9408 ), #48329, .F. ) ;
#53443=CARTESIAN_POINT ( 'NONE',  ( -6.001507490154110336, -7.196845540359293913, 17.41542759839262189 ) ) ;
#53450=CARTESIAN_POINT ( 'NONE',  ( 0.2230388203127621483, 17.20066002792360038, 39.54016926433980927 ) ) ;
#53451=CARTESIAN_POINT ( 'NONE',  ( 0.8751705887134553219, 11.58504748649199811, -46.67919521768876479 ) ) ;
#53452=ORIENTED_EDGE ( 'NONE', *, *, #15524, .F. ) ;
#53456=CARTESIAN_POINT ( 'NONE',  ( -6.015611763856276717, 11.47596948473832690, -14.94556629257413327 ) ) ;
#53462=EDGE_CURVE ( 'NONE', #12539, #43595, #418, .T. ) ;
#53468=DIRECTION ( 'NONE',  ( -1.000000000000000000, -0.000000000000000000, -0.000000000000000000 ) ) ;
#53476=CARTESIAN_POINT ( 'NONE',  ( -2.569797478183790229, 0.4487456364278817333, -14.62602397812940858 ) ) ;
#53477=CARTESIAN_POINT ( 'NONE',  ( 0.6031356755773454870, -2.564066905512520764E-05, -48.10744332413212021 ) ) ;
#53478=EDGE_LOOP ( 'NONE', ( #3625, #41964, #7824, #2849 ) ) ;
#53482=ORIENTED_EDGE ( 'NONE', *, *, #8152, .T. ) ;
#53485=CARTESIAN_POINT ( 'NONE',  ( 0.1064266418746776799, -21.07422140941981326, -37.62465821955093759 ) ) ;
#53488=CARTESIAN_POINT ( 'NONE',  ( 4.833616638992208614, -15.29495699393695674, -43.64812679991114663 ) ) ;
#53493=CARTESIAN_POINT ( 'NONE',  ( 0.7048096507298579061, 5.442192462018821786, 47.80151517212787837 ) ) ;
#53498=VECTOR ( 'NONE', #14162, 1000.000000000000114 ) ;
#53499=VERTEX_POINT ( 'NONE', #30672 ) ;
#53508=CARTESIAN_POINT ( 'NONE',  ( 4.975801465491695552, -36.39623109580445259, -31.15993731089111662 ) ) ;
#53513=CARTESIAN_POINT ( 'NONE',  ( 3.238931869106854489, -42.95312220797016067, 1.828840280769237658 ) ) ;
#53517=CARTESIAN_POINT ( 'NONE',  ( -2.569797478183783568, 12.44213550320653461, -7.701637110048551449 ) ) ;
#53526=CARTESIAN_POINT ( 'NONE',  ( 0.1084644655670283647, 37.54424727804272521, 21.21700107124061674 ) ) ;
#53527=CARTESIAN_POINT ( 'NONE',  ( 0.6041374136657476912, 12.61972904329536505, 46.42299778158159995 ) ) ;
#53542=CARTESIAN_POINT ( 'NONE',  ( 4.322998006666179727, -43.48102276965716584, 20.30542865297572064 ) ) ;
#53545=CARTESIAN_POINT ( 'NONE',  ( 0.6254087463353918963, 41.31312313681408455, -24.64672211239920330 ) ) ;
#53546=ORIENTED_EDGE ( 'NONE', *, *, #34459, .T. ) ;
#53556=CARTESIAN_POINT ( 'NONE',  ( 0.6031357023905875581, 24.01594909943208123, 41.68407605450320830 ) ) ;
#53559=CARTESIAN_POINT ( 'NONE',  ( 4.833616638992208614, -14.43699082351744600, 43.93936707042075085 ) ) ;
#53560=CARTESIAN_POINT ( 'NONE',  ( 4.322998006666165516, -42.57894920390143056, 22.13465289016552973 ) ) ;
#53564=DIRECTION ( 'NONE',  ( 0.000000000000000000, -1.000000000000000000, 0.000000000000000000 ) ) ;
#53567=DIRECTION ( 'NONE',  ( -1.000000000000000000, -0.000000000000000000, -0.000000000000000000 ) ) ;
#53577=ADVANCED_FACE ( 'NONE', ( #26916 ), #13842, .F. ) ;
#53578=( BOUNDED_SURFACE ( )  B_SPLINE_SURFACE ( 3, 1, ( 
 ( #56475, #373 ),
 ( #14519, #9179 ),
 ( #32385, #61471 ),
 ( #52701, #9799 ) ),
 .UNSPECIFIED., .F., .F., .F. ) 
 B_SPLINE_SURFACE_WITH_KNOTS ( ( 4, 4 ),
 ( 2, 2 ),
 ( 0.000000000000000000, 1.000000000000000000 ),
 ( 0.000000000000000000, 1.000000000000000000 ),
 .UNSPECIFIED. ) 
 GEOMETRIC_REPRESENTATION_ITEM ( )  RATIONAL_B_SPLINE_SURFACE ( (
 ( 1.000000000000000000, 1.000000000000000000),
 ( 0.7223157951917480446, 0.9931996967497186413),
 ( 0.7223157951917480446, 0.9931996967497186413),
 ( 1.000000000000000000, 1.000000000000000000) ) ) 
 REPRESENTATION_ITEM ( '' )  SURFACE ( )  );
#53584=CARTESIAN_POINT ( 'NONE',  ( -6.016489644550737204, 9.425415887801317893, -16.31649074174267255 ) ) ;
#53597=CARTESIAN_POINT ( 'NONE',  ( 4.549368137175248350, 38.59302160394725689, 18.79584381673547711 ) ) ;
#53598=CARTESIAN_POINT ( 'NONE',  ( 0.2230388203127605384, -39.54016926433985901, 17.20066002792346538 ) ) ;
#53601=FACE_OUTER_BOUND ( 'NONE', #38698, .T. ) ;
#53606=CARTESIAN_POINT ( 'NONE',  ( 0.1100247026804066219, 10.99745200874637518, 41.69861001364777309 ) ) ;
#53612=ORIENTED_EDGE ( 'NONE', *, *, #53812, .F. ) ;
#53616=AXIS2_PLACEMENT_3D ( 'NONE', #3787, #55801, #50796 ) ;
#53617=VERTEX_POINT ( 'NONE', #36953 ) ;
#53618=CARTESIAN_POINT ( 'NONE',  ( 0.6031356755773454870, -18.40989784469888946, 44.44549206087150850 ) ) ;
#53622=CARTESIAN_POINT ( 'NONE',  ( 0.2885697896453111588, 0.8047882042606538944, -43.10898998017122352 ) ) ;
#53623=EDGE_LOOP ( 'NONE', ( #44832, #45348, #35082, #55854 ) ) ;
#53624=CARTESIAN_POINT ( 'NONE',  ( 0.5998501479064699549, -11.94461217097501837, 46.60114184914296942 ) ) ;
#53626=CARTESIAN_POINT ( 'NONE',  ( 4.322998006666179727, 42.57894920390098292, 22.13465289016641790 ) ) ;
#53630=CARTESIAN_POINT ( 'NONE',  ( 0.1064266418746774856, 42.67882141624136239, 6.185136754498480549 ) ) ;
#53633=ORIENTED_EDGE ( 'NONE', *, *, #40745, .F. ) ;
#53636=CARTESIAN_POINT ( 'NONE',  ( 0.6001305935487315502, -34.38748867424737199, 33.64689939321881695 ) ) ;
#53639=CARTESIAN_POINT ( 'NONE',  ( 0.1073791018717483448, 33.91564619577807349, -26.63563652260133097 ) ) ;
#53642=LINE ( 'NONE', #29862, #11018 ) ;
#53644=CARTESIAN_POINT ( 'NONE',  ( 4.833616638992208614, -43.93936707042090717, -14.43699082351698415 ) ) ;
#53646=CARTESIAN_POINT ( 'NONE',  ( 0.1092565886968785149, 30.27341312544114160, -30.71235995742708980 ) ) ;
#53649=EDGE_CURVE ( 'NONE', #17098, #55047, #11657, .T. ) ;
#53653=CARTESIAN_POINT ( 'NONE',  ( -6.016761891674565099, -17.41015286184807209, 7.207804629151251419 ) ) ;
#53654=B_SPLINE_CURVE_WITH_KNOTS ( 'NONE', 3,
 ( #24387, #49118, #53488, #58190 ),
 .UNSPECIFIED., .F., .F.,
 ( 4, 4 ),
 ( 0.000000000000000000, 0.005014147105413705591 ),
 .UNSPECIFIED. ) ;
#53655=CARTESIAN_POINT ( 'NONE',  ( 0.6031356219577718170, -23.97811961689716753, 41.70591683999463584 ) ) ;
#53657=CARTESIAN_POINT ( 'NONE',  ( 0.7954190325252784577, 23.29293489839735187, -42.08256085583550288 ) ) ;
#53659=DIRECTION ( 'NONE',  ( 0.000000000000000000, 0.000000000000000000, -1.000000000000000000 ) ) ;
#53660=CIRCLE ( 'NONE', #19674, 42.92674063221959813 ) ;
#53667=VECTOR ( 'NONE', #12538, 1000.000000000000227 ) ;
#53669=CARTESIAN_POINT ( 'NONE',  ( 0.5988103564986356764, -48.10388392110853317, 0.6065102550371687107 ) ) ;
#53671=VERTEX_POINT ( 'NONE', #20000 ) ;
#53674=CARTESIAN_POINT ( 'NONE',  ( 0.1073791018717483448, 43.12183934961191056, -0.4849339620928847516 ) ) ;
#53679=VERTEX_POINT ( 'NONE', #47879 ) ;
#53683=CARTESIAN_POINT ( 'NONE',  ( 0.5988103564986355654, 18.96890181990826463, 44.21009236284890420 ) ) ;
#53691=CARTESIAN_POINT ( 'NONE',  ( 4.975801465491694664, 45.18341283946434572, 15.94009207553066787 ) ) ;
#53692=ORIENTED_EDGE ( 'NONE', *, *, #49097, .F. ) ;
#53693=DIRECTION ( 'NONE',  ( 0.09835009131224549395, -0.5996571005210464822, 0.7941905447268713392 ) ) ;
#53697=ORIENTED_EDGE ( 'NONE', *, *, #23190, .F. ) ;
#53698=CARTESIAN_POINT ( 'NONE',  ( 0.1073791018717578927, 5.147744207006301309, 42.81622261970996135 ) ) ;
#53706=ORIENTED_EDGE ( 'NONE', *, *, #43944, .T. ) ;
#53711=ORIENTED_EDGE ( 'NONE', *, *, #579, .F. ) ;
#53717=CARTESIAN_POINT ( 'NONE',  ( 0.1073791018717578927, 16.95003405440313315, -39.65380858626198091 ) ) ;
#53720=ADVANCED_FACE ( 'NONE', ( #43820 ), #16687, .F. ) ;
#53731=CARTESIAN_POINT ( 'NONE',  ( 0.1064266379913941241, -0.5615183164814757655, -43.12102052820964104 ) ) ;
#53732=ADVANCED_FACE ( 'NONE', ( #24371 ), #20529, .F. ) ;
#53750=ORIENTED_EDGE ( 'NONE', *, *, #39290, .T. ) ;
#53755=VECTOR ( 'NONE', #43282, 1000.000000000000000 ) ;
#53756=CARTESIAN_POINT ( 'NONE',  ( 4.691466044806102076, -9.025781474741773280, 43.66525414675626848 ) ) ;
#53760=EDGE_LOOP ( 'NONE', ( #11721, #36093, #14385, #32539 ) ) ;
#53776=ORIENTED_EDGE ( 'NONE', *, *, #52111, .F. ) ;
#53779=CARTESIAN_POINT ( 'NONE',  ( 0.8751705887134423323, 41.19904111682474479, 24.81530984069222256 ) ) ;
#53792=ORIENTED_EDGE ( 'NONE', *, *, #23207, .F. ) ;
#53793=CARTESIAN_POINT ( 'NONE',  ( 4.975801465491694664, 47.10002938642141856, -8.787181743659651545 ) ) ;
#53795=CARTESIAN_POINT ( 'NONE',  ( 3.238931869106854045, 24.69728751010286061, -35.19033040238042531 ) ) ;
#53808=DIRECTION ( 'NONE',  ( 0.000000000000000000, 0.000000000000000000, -1.000000000000000000 ) ) ;
#53810=CARTESIAN_POINT ( 'NONE',  ( 4.975801465491695552, -21.70134120755170315, -42.71626295676257001 ) ) ;
#53811=CARTESIAN_POINT ( 'NONE',  ( 3.238931869106853600, 32.96367555688112105, -27.59912060131738087 ) ) ;
#53812=EDGE_CURVE ( 'NONE', #9480, #37185, #57108, .T. ) ;
#53817=CARTESIAN_POINT ( 'NONE',  ( -6.015611763856276717, -17.40650793417848519, 7.216738110653220239 ) ) ;
#53821=DIRECTION ( 'NONE',  ( 0.000000000000000000, 0.000000000000000000, -1.000000000000000000 ) ) ;
#53824=CARTESIAN_POINT ( 'NONE',  ( 0.5998501479064708430, 11.94461217097404493, 46.60114184914321811 ) ) ;
#53827=CONICAL_SURFACE ( 'NONE', #32859, 42.92674063221959813, 1.485477209440487556 ) ;
#53831=CARTESIAN_POINT ( 'NONE',  ( 0.1313383488274142974, -30.03864748494565973, 30.94058105930509939 ) ) ;
#53834=LINE ( 'NONE', #14429, #43317 ) ;
#53850=ORIENTED_EDGE ( 'NONE', *, *, #14683, .F. ) ;
#53854=EDGE_CURVE ( 'NONE', #60939, #7367, #18319, .T. ) ;
#53855=CARTESIAN_POINT ( 'NONE',  ( 0.1064266379913942490, -41.50637574965957555, 11.70292640078081803 ) ) ;
#53857=CARTESIAN_POINT ( 'NONE',  ( 0.1073791018717483448, 33.91564619577807349, -26.63563652260133097 ) ) ;
#53863=VECTOR ( 'NONE', #9144, 1000.000000000000000 ) ;
#53864=CARTESIAN_POINT ( 'NONE',  ( 0.6023143664670691511, 23.82663958122378389, 41.79259346737330816 ) ) ;
#53866=ORIENTED_EDGE ( 'NONE', *, *, #11057, .T. ) ;
#53876=CARTESIAN_POINT ( 'NONE',  ( 0.8760168074886960365, -33.37827814204101173, -34.63873394077476320 ) ) ;
#53881=CARTESIAN_POINT ( 'NONE',  ( 4.549368137175248350, 0.000000000000000000, 0.000000000000000000 ) ) ;
#53895=CARTESIAN_POINT ( 'NONE',  ( 4.833616638992208614, 34.47248434257912919, -30.83411269743528038 ) ) ;
#53899=CARTESIAN_POINT ( 'NONE',  ( 0.5980894510889448457, -11.77356634613285813, -46.65000524237083113 ) ) ;
#53918=B_SPLINE_CURVE_WITH_KNOTS ( 'NONE', 3,
 ( #19778, #29157, #636, #34184 ),
 .UNSPECIFIED., .F., .F.,
 ( 4, 4 ),
 ( 2.330832950083589181E-17, 0.004564976165746187711 ),
 .UNSPECIFIED. ) ;
#53919=ORIENTED_EDGE ( 'NONE', *, *, #38793, .T. ) ;
#53920=ORIENTED_EDGE ( 'NONE', *, *, #21945, .F. ) ;
#53926=EDGE_CURVE ( 'NONE', #2469, #56932, #29497, .T. ) ;
#53931=ORIENTED_EDGE ( 'NONE', *, *, #50777, .F. ) ;
#53942=B_SPLINE_CURVE_WITH_KNOTS ( 'NONE', 3,
 ( #7510, #8145, #21949, #13480, #32586, #7200 ),
 .UNSPECIFIED., .F., .F.,
 ( 4, 2, 4 ),
 ( 1.268633296668913999E-16, 0.0002450741128632347816, 0.0004901482257263427116 ),
 .UNSPECIFIED. ) ;
#53945=CARTESIAN_POINT ( 'NONE',  ( -6.017396004339686577, -2.458362590802920522, 18.68211039806562823 ) ) ;
#53951=AXIS2_PLACEMENT_3D ( 'NONE', #34427, #9999, #25019 ) ;
#53954=CARTESIAN_POINT ( 'NONE',  ( 0.5980894510889448457, -34.51330645350425641, 33.52121017007767279 ) ) ;
#53962=CARTESIAN_POINT ( 'NONE',  ( 0.5998501479064699549, -18.89267974119636406, -44.24259072156078787 ) ) ;
#53963=DIRECTION ( 'NONE',  ( 1.000000000000000000, 0.000000000000000000, 0.000000000000000000 ) ) ;
#53965=CARTESIAN_POINT ( 'NONE',  ( 2.301529144917015213, 37.31001381748733792, -30.25186323939234612 ) ) ;
#53967=LINE ( 'NONE', #11091, #15042 ) ;
#53968=CARTESIAN_POINT ( 'NONE',  ( 5.880360259849752858, -15.46489389606785281, 45.41096578730621047 ) ) ;
#53974=EDGE_CURVE ( 'NONE', #47464, #38885, #45955, .T. ) ;
#53980=ORIENTED_EDGE ( 'NONE', *, *, #25662, .F. ) ;
#53986=CARTESIAN_POINT ( 'NONE',  ( 0.1102847568649952675, -11.07236323260782207, 41.67876919128903523 ) ) ;
#53987=CARTESIAN_POINT ( 'NONE',  ( 0.6001305935487315502, 33.64689939321941381, -34.38748867424678224 ) ) ;
#53988=CARTESIAN_POINT ( 'NONE',  ( 0.1102144999581333162, -37.40973521037476957, 21.45299314243928990 ) ) ;
#53993=CIRCLE ( 'NONE', #14063, 10.00000000000000000 ) ;
#53995=CARTESIAN_POINT ( 'NONE',  ( 50.00005079999999680, 0.000000000000000000, 0.000000000000000000 ) ) ;
#53998=CARTESIAN_POINT ( 'NONE',  ( 0.8760168074887076939, -48.09529047980637273, 0.8912768426704632541 ) ) ;
#54001=EDGE_CURVE ( 'NONE', #22293, #19553, #44520, .T. ) ;
#54004=EDGE_CURVE ( 'NONE', #12663, #30079, #60522, .T. ) ;
#54007=ORIENTED_EDGE ( 'NONE', *, *, #56055, .T. ) ;
#54008=CARTESIAN_POINT ( 'NONE',  ( 4.322998006666165516, 35.39923696759012017, -32.40067585697761388 ) ) ;
#54011=CARTESIAN_POINT ( 'NONE',  ( 4.975801465491695552, 0.000000000000000000, 0.000000000000000000 ) ) ;
#54020=CARTESIAN_POINT ( 'NONE',  ( 0.5998501479064699549, -47.76154736470754614, -5.759754759340617092 ) ) ;
#54021=ORIENTED_EDGE ( 'NONE', *, *, #56554, .F. ) ;
#54022=CARTESIAN_POINT ( 'NONE',  ( 4.549368137175248350, -42.82045902618770583, -3.018832571116409014 ) ) ;
#54023=LINE ( 'NONE', #10216, #18433 ) ;
#54027=CARTESIAN_POINT ( 'NONE',  ( -6.015611763856276717, 16.31561949997088945, -9.427003116184000220 ) ) ;
#54029=CARTESIAN_POINT ( 'NONE',  ( 0.2230388203127642022, 25.64246103889296435, -34.66629317821146117 ) ) ;
#54047=B_SPLINE_CURVE_WITH_KNOTS ( 'NONE', 3,
 ( #47159, #51512, #38384, #61223 ),
 .UNSPECIFIED., .F., .F.,
 ( 4, 4 ),
 ( 0.000000000000000000, 0.004445488388166995118 ),
 .UNSPECIFIED. ) ;
#54049=CARTESIAN_POINT ( 'NONE',  ( 0.5998501479064699549, 17.92509395669108585, -44.64337787626229925 ) ) ;
#54052=EDGE_CURVE ( 'NONE', #47393, #47251, #10886, .T. ) ;
#54054=CARTESIAN_POINT ( 'NONE',  ( 0.5998501479064699549, -29.69975237324587169, -37.84527566984847624 ) ) ;
#54055=CARTESIAN_POINT ( 'NONE',  ( 4.975801465491695552, 0.000000000000000000, 0.000000000000000000 ) ) ;
#54056=VERTEX_POINT ( 'NONE', #38413 ) ;
#54060=CARTESIAN_POINT ( 'NONE',  ( 0.1102144999581333162, 16.38650952318852916, 39.88986724628640701 ) ) ;
#54063=CARTESIAN_POINT ( 'NONE',  ( 0.7954196712028472893, 41.21355366240430840, 24.79809944608789252 ) ) ;
#54067=FACE_OUTER_BOUND ( 'NONE', #57326, .T. ) ;
#54068=CARTESIAN_POINT ( 'NONE',  ( 0.1092565886968785843, -11.46097737058334864, -41.57372480460681174 ) ) ;
#54074=AXIS2_PLACEMENT_3D ( 'NONE', #54857, #51085, #2551 ) ;
#54079=DIRECTION ( 'NONE',  ( 0.09835009131224566048, 0.007732607185430591737, -0.9951218349151970122 ) ) ;
#54083=ADVANCED_FACE ( 'NONE', ( #21135 ), #12308, .F. ) ;
#54088=CARTESIAN_POINT ( 'NONE',  ( 0.6023143664670691511, 44.54505257464859369, -18.16777128831346033 ) ) ;
#54090=CARTESIAN_POINT ( 'NONE',  ( 0.8751705887134553219, 47.79200036674271956, 5.393078191592866055 ) ) ;
#54091=ORIENTED_EDGE ( 'NONE', *, *, #333, .T. ) ;
#54106=CARTESIAN_POINT ( 'NONE',  ( 3.680882792899939915, 40.59250320379013033, -25.57189948075143704 ) ) ;
#54107=CARTESIAN_POINT ( 'NONE',  ( 0.1081432562775997558, -5.208748643066400064, -42.80885385101080942 ) ) ;
#54109=CARTESIAN_POINT ( 'NONE',  ( -6.017396004339686577, 14.94857180792008577, -11.47192209077572045 ) ) ;
#54112=VERTEX_POINT ( 'NONE', #29914 ) ;
#54122=CARTESIAN_POINT ( 'NONE',  ( -6.016489644550736315, -17.40716454747933284, 7.215050741357980080 ) ) ;
#54125=CARTESIAN_POINT ( 'NONE',  ( 0.7048096507298635682, 46.24547838151369916, -13.26491767067467542 ) ) ;
#54126=CARTESIAN_POINT ( 'NONE',  ( 4.975801465491694664, 45.18341283946434572, 15.94009207553066787 ) ) ;
#54128=CARTESIAN_POINT ( 'NONE',  ( 0.5998501479064699549, -37.84527566984877467, 29.69975237324549155 ) ) ;
#54133=ADVANCED_FACE ( 'NONE', ( #15217 ), #33528, .F. ) ;
#54139=CARTESIAN_POINT ( 'NONE',  ( 0.1101816497532063371, -41.61967362528563541, 11.29256821151141388 ) ) ;
#54141=( BOUNDED_SURFACE ( )  B_SPLINE_SURFACE ( 3, 1, ( 
 ( #34270, #52733 ),
 ( #38981, #33354 ),
 ( #5105, #5416 ),
 ( #61811, #9835 ) ),
 .UNSPECIFIED., .F., .F., .F. ) 
 B_SPLINE_SURFACE_WITH_KNOTS ( ( 4, 4 ),
 ( 2, 2 ),
 ( 0.000000000000000000, 1.000000000000000000 ),
 ( 0.000000000000000000, 1.000000000000000000 ),
 .UNSPECIFIED. ) 
 GEOMETRIC_REPRESENTATION_ITEM ( )  RATIONAL_B_SPLINE_SURFACE ( (
 ( 1.000000000000000000, 1.000000000000000000),
 ( 0.9953040768229005630, 0.8617119497784937465),
 ( 0.9953040768229005630, 0.8617119497784937465),
 ( 1.000000000000000000, 1.000000000000000000) ) ) 
 REPRESENTATION_ITEM ( '' )  SURFACE ( )  );
#54151=ORIENTED_EDGE ( 'NONE', *, *, #31072, .T. ) ;
#54153=EDGE_CURVE ( 'NONE', #55407, #25265, #790, .T. ) ;
#54166=CARTESIAN_POINT ( 'NONE',  ( -4.908599999999998964, 0.000000000000000000, 0.000000000000000000 ) ) ;
#54172=EDGE_CURVE ( 'NONE', #4129, #41115, #30514, .T. ) ;
#54188=CARTESIAN_POINT ( 'NONE',  ( 4.975801465491695552, 27.09127437476327671, 39.51822597168504814 ) ) ;
#54190=SHAPE_REPRESENTATION_RELATIONSHIP ( 'NONE' , 'NONE' ,  #8803, #25822 ) ;
#54192=DIRECTION ( 'NONE',  ( -0.1024043820194934507, 0.3927886084231760888, -0.9139094329506565195 ) ) ;
#54203=ADVANCED_FACE ( 'NONE', ( #32399 ), #7892, .F. ) ;
#54211=DIRECTION ( 'NONE',  ( 0.1024043820194936172, -0.5950744814819302064, 0.7971196296869232922 ) ) ;
#54213=( BOUNDED_SURFACE ( )  B_SPLINE_SURFACE ( 3, 1, ( 
 ( #138, #42792 ),
 ( #5145, #9557 ),
 ( #52463, #14285 ),
 ( #28665, #58081 ) ),
 .UNSPECIFIED., .F., .F., .F. ) 
 B_SPLINE_SURFACE_WITH_KNOTS ( ( 4, 4 ),
 ( 2, 2 ),
 ( 0.000000000000000000, 1.000000000000000000 ),
 ( 0.000000000000000000, 1.000000000000000000 ),
 .UNSPECIFIED. ) 
 GEOMETRIC_REPRESENTATION_ITEM ( )  RATIONAL_B_SPLINE_SURFACE ( (
 ( 1.000000000000000000, 1.000000000000000000),
 ( 0.7223157951917480446, 0.9931996967497186413),
 ( 0.7223157951917480446, 0.9931996967497186413),
 ( 1.000000000000000000, 1.000000000000000000) ) ) 
 REPRESENTATION_ITEM ( '' )  SURFACE ( )  );
#54214=CARTESIAN_POINT ( 'NONE',  ( 0.6023143664670691511, -12.19804739160229623, -46.53533348214987342 ) ) ;
#54217=B_SPLINE_CURVE_WITH_KNOTS ( 'NONE', 3,
 ( #18960, #3271, #37772, #51821, #56215, #46532 ),
 .UNSPECIFIED., .F., .F.,
 ( 4, 2, 4 ),
 ( 1.268664800107929448E-16, 0.0002450741128632330469, 0.0004901482257263392421 ),
 .UNSPECIFIED. ) ;
#54221=CARTESIAN_POINT ( 'NONE',  ( 0.8760168074886960365, -38.69913431881841603, 28.57146030081915100 ) ) ;
#54235=CARTESIAN_POINT ( 'NONE',  ( 0.6031356219577718170, -18.32926896140859441, 44.47888959008666632 ) ) ;
#54243=CARTESIAN_POINT ( 'NONE',  ( 0.1102847568649952675, 41.67876919128907076, 11.07236323260767641 ) ) ;
#54259=CARTESIAN_POINT ( 'NONE',  ( 0.1064266379913941102, -43.12102052820963394, 0.5615183164816264227 ) ) ;
#54263=CARTESIAN_POINT ( 'NONE',  ( 0.2885700199627515561, -6.424755504217940505, -42.63514063525625630 ) ) ;
#54264=CARTESIAN_POINT ( 'NONE',  ( 0.6023142530420679819, -6.019593586345654224, 47.72938419887608319 ) ) ;
#54265=CARTESIAN_POINT ( 'NONE',  ( 0.1073791018717578927, -40.02496097243069784, 16.05399293000745686 ) ) ;
#54268=CARTESIAN_POINT ( 'NONE',  ( 0.5980894510889457338, 44.17723055703951474, -19.05812566676460307 ) ) ;
#54270=CARTESIAN_POINT ( 'NONE',  ( 0.6028618097248863439, -34.14037999462347983, -33.89350006451816455 ) ) ;
#54273=ADVANCED_FACE ( 'NONE', ( #43045 ), #46705, .F. ) ;
#54278=EDGE_CURVE ( 'NONE', #2911, #52228, #48155, .T. ) ;
#54280=ORIENTED_EDGE ( 'NONE', *, *, #29200, .T. ) ;
#54287=EDGE_LOOP ( 'NONE', ( #17608, #8697, #51111, #31051 ) ) ;
#54289=CARTESIAN_POINT ( 'NONE',  ( -6.015611763856276717, -13.32857883366842700, 13.31979030221794424 ) ) ;
#54290=CARTESIAN_POINT ( 'NONE',  ( 0.6031356219577718170, 6.365832241665933644, 47.68448279784256982 ) ) ;
#54293=EDGE_LOOP ( 'NONE', ( #7381, #32707, #52041, #18204 ) ) ;
#54296=CARTESIAN_POINT ( 'NONE',  ( 0.6041374136657475802, 46.51335992032618805, -12.28249295041999289 ) ) ;
#54300=ORIENTED_EDGE ( 'NONE', *, *, #61518, .F. ) ;
#54305=ORIENTED_EDGE ( 'NONE', *, *, #55723, .T. ) ;
#54307=CARTESIAN_POINT ( 'NONE',  ( 0.7246131072078527691, 44.74808308960848535, -17.64706930304248900 ) ) ;
#54323=ORIENTED_EDGE ( 'NONE', *, *, #31967, .T. ) ;
#54324=CARTESIAN_POINT ( 'NONE',  ( 0.8751705887134553219, 42.09020928323342758, 23.27176129838440488 ) ) ;
#54329=CARTESIAN_POINT ( 'NONE',  ( 0.3622758884714730732, 25.58609868863768355, -34.70015533914803285 ) ) ;
#54331=CARTESIAN_POINT ( 'NONE',  ( 0.6017667736363749853, -41.83584368312207857, 23.75082673020790835 ) ) ;
#54336=CARTESIAN_POINT ( 'NONE',  ( 5.880360259849739535, 9.312491912828125606, -47.05949693022697744 ) ) ;
#54337=CARTESIAN_POINT ( 'NONE',  ( 0.1098349054025746785, -41.59932877996191536, -11.36734385883990406 ) ) ;
#54339=CARTESIAN_POINT ( 'NONE',  ( 1.827119703190778877, -40.22835835992454179, -15.32887915442582205 ) ) ;
#54342=CARTESIAN_POINT ( 'NONE',  ( 2.301529144917016101, 34.86298839095284308, 33.04216096093416155 ) ) ;
#54343=DIRECTION ( 'NONE',  ( 0.000000000000000000, 0.000000000000000000, 1.000000000000000000 ) ) ;
#54347=CARTESIAN_POINT ( 'NONE',  ( 0.5988103564986354543, -28.80261217992950762, 38.53259703935783165 ) ) ;
#54350=CARTESIAN_POINT ( 'NONE',  ( 0.2230388203127639524, -41.84042374003691833, -10.42432885623869510 ) ) ;
#54351=ADVANCED_FACE ( 'NONE', ( #34865 ), #48229, .F. ) ;
#54354=CARTESIAN_POINT ( 'NONE',  ( 0.6029303876144825880, 0.1308990448395709882, -48.10727438003475953 ) ) ;
#54357=ORIENTED_EDGE ( 'NONE', *, *, #36217, .F. ) ;
#54360=CARTESIAN_POINT ( 'NONE',  ( -6.016761891674565099, 0.003433883960047550993, -18.84319130225482297 ) ) ;
#54362=CARTESIAN_POINT ( 'NONE',  ( 0.1073791018717483448, 16.95003405440257893, 39.65380858626220828 ) ) ;
#54366=CARTESIAN_POINT ( 'NONE',  ( 0.1102847568649952675, 41.63105453442837245, -11.25043675627755135 ) ) ;
#54372=CARTESIAN_POINT ( 'NONE',  ( 0.1073791018717578927, -39.65380858626204486, -16.95003405440299460 ) ) ;
#54394=CARTESIAN_POINT ( 'NONE',  ( 0.6001305935487422083, 44.24520387813827682, -18.89378601236018795 ) ) ;
#54402=ORIENTED_EDGE ( 'NONE', *, *, #18596, .T. ) ;
#54411=( BOUNDED_SURFACE ( )  B_SPLINE_SURFACE ( 3, 1, ( 
 ( #26625, #22858 ),
 ( #41991, #3723 ),
 ( #3120, #61057 ),
 ( #2502, #51346 ) ),
 .UNSPECIFIED., .F., .F., .F. ) 
 B_SPLINE_SURFACE_WITH_KNOTS ( ( 4, 4 ),
 ( 2, 2 ),
 ( 0.000000000000000000, 1.000000000000000000 ),
 ( 0.000000000000000000, 1.000000000000000000 ),
 .UNSPECIFIED. ) 
 GEOMETRIC_REPRESENTATION_ITEM ( )  RATIONAL_B_SPLINE_SURFACE ( (
 ( 1.000000000000000000, 1.000000000000000000),
 ( 0.9751682680413298332, 0.9999560080971552356),
 ( 0.9751682680413298332, 0.9999560080971552356),
 ( 1.000000000000000000, 1.000000000000000000) ) ) 
 REPRESENTATION_ITEM ( '' )  SURFACE ( )  );
#54415=CARTESIAN_POINT ( 'NONE',  ( 0.1103310638050662151, -5.547176740493243052, -42.76619676553134042 ) ) ;
#54418=CARTESIAN_POINT ( 'NONE',  ( 0.6001305935487422083, -37.84751346122875759, 29.70149728382373056 ) ) ;
#54423=LINE ( 'NONE', #11875, #23376 ) ;
#54431=CARTESIAN_POINT ( 'NONE',  ( 0.6001305935487315502, -46.33281397023073112, 12.95698906763729852 ) ) ;
#54440=CARTESIAN_POINT ( 'NONE',  ( 0.5988103622719985752, 11.86435782853368970, 46.62176011478425863 ) ) ;
#54448=CARTESIAN_POINT ( 'NONE',  ( 0.1102144999581333301, -41.68747259405357397, 11.03964818279701632 ) ) ;
#54453=B_SPLINE_CURVE_WITH_KNOTS ( 'NONE', 3,
 ( #10625, #48830, #2118, #31267, #17479, #21254 ),
 .UNSPECIFIED., .F., .F.,
 ( 4, 2, 4 ),
 ( 1.764953265579307567E-18, 0.0002450742804987340677, 0.0004901485609974662924 ),
 .UNSPECIFIED. ) ;
#54457=CARTESIAN_POINT ( 'NONE',  ( 4.549368137175248350, 42.84816078363926550, 2.596185425822091553 ) ) ;
#54462=ORIENTED_EDGE ( 'NONE', *, *, #5425, .F. ) ;
#54464=ORIENTED_EDGE ( 'NONE', *, *, #19048, .T. ) ;
#54465=ORIENTED_EDGE ( 'NONE', *, *, #33601, .F. ) ;
#54466=DIRECTION ( 'NONE',  ( 0.000000000000000000, 0.000000000000000000, 1.000000000000000000 ) ) ;
#54470=ORIENTED_EDGE ( 'NONE', *, *, #59184, .F. ) ;
#54471=EDGE_LOOP ( 'NONE', ( #37940, #21214, #56503, #33918 ) ) ;
#54473=LINE ( 'NONE', #1866, #56377 ) ;
#54484=VERTEX_POINT ( 'NONE', #35487 ) ;
#54493=( BOUNDED_SURFACE ( )  B_SPLINE_SURFACE ( 3, 1, ( 
 ( #6660, #16110 ),
 ( #30802, #54594 ),
 ( #11724, #49923 ),
 ( #21416, #50230 ) ),
 .UNSPECIFIED., .F., .F., .F. ) 
 B_SPLINE_SURFACE_WITH_KNOTS ( ( 4, 4 ),
 ( 2, 2 ),
 ( 0.000000000000000000, 1.000000000000000000 ),
 ( 0.000000000000000000, 1.000000000000000000 ),
 .UNSPECIFIED. ) 
 GEOMETRIC_REPRESENTATION_ITEM ( )  RATIONAL_B_SPLINE_SURFACE ( (
 ( 1.000000000000000000, 1.000000000000000000),
 ( 0.9953040768229005630, 0.8617119497784937465),
 ( 0.9953040768229005630, 0.8617119497784937465),
 ( 1.000000000000000000, 1.000000000000000000) ) ) 
 REPRESENTATION_ITEM ( '' )  SURFACE ( )  );
#54494=VERTEX_POINT ( 'NONE', #18226 ) ;
#54500=VECTOR ( 'NONE', #17417, 1000.000000000000227 ) ;
#54508=CARTESIAN_POINT ( 'NONE',  ( 0.7048096507298635682, -23.32077812596911315, 42.08020459959941206 ) ) ;
#54510=CARTESIAN_POINT ( 'NONE',  ( 0.1064266418746774995, -0.5615180042403685734, 43.12102053154801951 ) ) ;
#54515=ORIENTED_EDGE ( 'NONE', *, *, #46271, .T. ) ;
#54528=CARTESIAN_POINT ( 'NONE',  ( 0.5980894510889457338, 34.51330645350356008, 33.52121017007839043 ) ) ;
#54535=ORIENTED_EDGE ( 'NONE', *, *, #49277, .T. ) ;
#54537=CARTESIAN_POINT ( 'NONE',  ( 0.6001305935487422083, -41.40054608060277275, -24.50730504006441635 ) ) ;
#54539=LINE ( 'NONE', #40199, #14721 ) ;
#54547=EDGE_CURVE ( 'NONE', #17218, #50038, #52019, .T. ) ;
#54548=B_SPLINE_CURVE_WITH_KNOTS ( 'NONE', 3,
 ( #57868, #19688, #29379, #29078 ),
 .UNSPECIFIED., .F., .F.,
 ( 4, 4 ),
 ( 6.254634441385501517E-18, 0.004566006591234647236 ),
 .UNSPECIFIED. ) ;
#54549=ORIENTED_EDGE ( 'NONE', *, *, #49779, .T. ) ;
#54555=ORIENTED_EDGE ( 'NONE', *, *, #45813, .F. ) ;
#54565=CARTESIAN_POINT ( 'NONE',  ( 0.6254087463353922294, 28.73645667569951101, -38.58044986685661826 ) ) ;
#54566=CARTESIAN_POINT ( 'NONE',  ( 0.1098349054025746646, -39.92296693299719124, 16.30574661324300223 ) ) ;
#54567=AXIS2_PLACEMENT_3D ( 'NONE', #11080, #49272, #39289 ) ;
#54589=CARTESIAN_POINT ( 'NONE',  ( 0.5998501479064708430, 46.60114184914316837, -11.94461217097420658 ) ) ;
#54591=CARTESIAN_POINT ( 'NONE',  ( -6.016761891674565099, -18.68243340030204536, 2.456125503350645278 ) ) ;
#54594=CARTESIAN_POINT ( 'NONE',  ( 0.7048096507298635682, 46.68221792389225300, 11.63498350884352739 ) ) ;
#54596=CARTESIAN_POINT ( 'NONE',  ( 4.691466044806103852, 40.13652286047866369, 19.42108863068394342 ) ) ;
#54597=ORIENTED_EDGE ( 'NONE', *, *, #31890, .T. ) ;
#54603=B_SPLINE_CURVE_WITH_KNOTS ( 'NONE', 3,
 ( #34194, #5336, #19788, #57040 ),
 .UNSPECIFIED., .F., .F.,
 ( 4, 4 ),
 ( 4.670885906470169154E-18, 0.004566006591234645501 ),
 .UNSPECIFIED. ) ;
#54613=CARTESIAN_POINT ( 'NONE',  ( 0.6254087463353902310, -24.64672211239934541, -41.31312313681398507 ) ) ;
#54617=CARTESIAN_POINT ( 'NONE',  ( 4.549368137175248350, 38.40568845698277300, -19.17571786012283042 ) ) ;
#54626=B_SPLINE_CURVE_WITH_KNOTS ( 'NONE', 3,
 ( #56838, #33071, #9234, #28343 ),
 .UNSPECIFIED., .F., .F.,
 ( 4, 4 ),
 ( 0.000000000000000000, 0.004445488388166992516 ),
 .UNSPECIFIED. ) ;
#54627=ORIENTED_EDGE ( 'NONE', *, *, #10261, .T. ) ;
#54630=EDGE_CURVE ( 'NONE', #50134, #52459, #33182, .T. ) ;
#54640=ORIENTED_EDGE ( 'NONE', *, *, #57907, .T. ) ;
#54641=CARTESIAN_POINT ( 'NONE',  ( -2.708315649062916552, 5.356004933109461241, -13.61924161399628730 ) ) ;
#54659=VECTOR ( 'NONE', #12156, 1000.000000000000227 ) ;
#54662=CARTESIAN_POINT ( 'NONE',  ( 4.691466044806103852, 2.583163953528483159, -44.51344083442436528 ) ) ;
#54664=CARTESIAN_POINT ( 'NONE',  ( 4.549368137175248350, -32.13400537129945178, 28.46244473166616729 ) ) ;
#54668=CARTESIAN_POINT ( 'NONE',  ( 0.6023142530420679819, 41.53076277789742932, -24.28014345169125932 ) ) ;
#54670=CARTESIAN_POINT ( 'NONE',  ( 0.1073791018717578927, -6.109314776653017809, 42.68962945260943087 ) ) ;
#54675=CARTESIAN_POINT ( 'NONE',  ( 4.975801465491695552, -8.787181743660504196, 47.10002938642126935 ) ) ;
#54677=EDGE_CURVE ( 'NONE', #45978, #39651, #33556, .T. ) ;
#54685=CARTESIAN_POINT ( 'NONE',  ( 0.1103310638050661735, -39.81020119244070798, -16.57910240621627906 ) ) ;
#54689=CARTESIAN_POINT ( 'NONE',  ( 0.1100247026804066219, -0.1696715072120354439, 43.12411436000287779 ) ) ;
#54692=CARTESIAN_POINT ( 'NONE',  ( 4.549368137175248350, -8.582197505784124658, -42.06008734272393212 ) ) ;
#54697=DIRECTION ( 'NONE',  ( -1.000000000000000000, -0.000000000000000000, -0.000000000000000000 ) ) ;
#54699=ORIENTED_EDGE ( 'NONE', *, *, #12532, .T. ) ;
#54703=FACE_OUTER_BOUND ( 'NONE', #13446, .T. ) ;
#54708=ORIENTED_EDGE ( 'NONE', *, *, #19225, .T. ) ;
#54710=( BOUNDED_SURFACE ( )  B_SPLINE_SURFACE ( 3, 1, ( 
 ( #6100, #15852 ),
 ( #59045, #24629 ),
 ( #20249, #39364 ),
 ( #58420, #34968 ) ),
 .UNSPECIFIED., .F., .F., .F. ) 
 B_SPLINE_SURFACE_WITH_KNOTS ( ( 4, 4 ),
 ( 2, 2 ),
 ( 0.000000000000000000, 1.000000000000000000 ),
 ( 0.000000000000000000, 1.000000000000000000 ),
 .UNSPECIFIED. ) 
 GEOMETRIC_REPRESENTATION_ITEM ( )  RATIONAL_B_SPLINE_SURFACE ( (
 ( 1.000000000000000000, 1.000000000000000000),
 ( 0.7223157951917476005, 0.9931996967497186413),
 ( 0.7223157951917476005, 0.9931996967497186413),
 ( 1.000000000000000000, 1.000000000000000000) ) ) 
 REPRESENTATION_ITEM ( '' )  SURFACE ( )  );
#54711=EDGE_LOOP ( 'NONE', ( #23286, #13749, #22765, #41969 ) ) ;
#54712=CARTESIAN_POINT ( 'NONE',  ( 4.975801465491695552, 40.15204426031497320, 26.14269827151694514 ) ) ;
#54719=ORIENTED_EDGE ( 'NONE', *, *, #10675, .F. ) ;
#54728=CARTESIAN_POINT ( 'NONE',  ( 0.8751705887134423323, -44.08562551107069538, -19.22545746485646490 ) ) ;
#54738=CARTESIAN_POINT ( 'NONE',  ( -2.569797478183783568, -5.182550149005390239, 13.68441171582007598 ) ) ;
#54752=B_SPLINE_CURVE_WITH_KNOTS ( 'NONE', 3,
 ( #34406, #42349, #15607, #53477, #870, #29996, #14149, #43827, #13840, #20302 ),
 .UNSPECIFIED., .F., .F.,
 ( 4, 3, 3, 4 ),
 ( 0.0005236741812375312905, 0.0005236998216949950062, 0.0007855159896329595411, 0.001047349442285928738 ),
 .UNSPECIFIED. ) ;
#54753=VECTOR ( 'NONE', #14145, 1000.000000000000114 ) ;
#54759=ADVANCED_FACE ( 'NONE', ( #55957 ), #59106, .F. ) ;
#54761=CARTESIAN_POINT ( 'NONE',  ( 0.1103878639767399694, 11.11454059769200420, -41.66755962011269077 ) ) ;
#54770=AXIS2_PLACEMENT_3D ( 'NONE', #52428, #23942, #9218 ) ;
#54771=( BOUNDED_SURFACE ( )  B_SPLINE_SURFACE ( 3, 1, ( 
 ( #26221, #25926 ),
 ( #7407, #26536 ),
 ( #45363, #17452 ),
 ( #11853, #45061 ) ),
 .UNSPECIFIED., .F., .F., .F. ) 
 B_SPLINE_SURFACE_WITH_KNOTS ( ( 4, 4 ),
 ( 2, 2 ),
 ( 0.000000000000000000, 1.000000000000000000 ),
 ( 0.000000000000000000, 1.000000000000000000 ),
 .UNSPECIFIED. ) 
 GEOMETRIC_REPRESENTATION_ITEM ( )  RATIONAL_B_SPLINE_SURFACE ( (
 ( 1.000000000000000000, 1.000000000000000000),
 ( 0.9751682680413298332, 0.9999560080971552356),
 ( 0.9751682680413298332, 0.9999560080971552356),
 ( 1.000000000000000000, 1.000000000000000000) ) ) 
 REPRESENTATION_ITEM ( '' )  SURFACE ( )  );
#54782=ORIENTED_EDGE ( 'NONE', *, *, #61708, .T. ) ;
#54784=CARTESIAN_POINT ( 'NONE',  ( 0.1101816497532063094, -26.36013219694247667, -34.13008584880283536 ) ) ;
#54785=ORIENTED_EDGE ( 'NONE', *, *, #3737, .F. ) ;
#54786=ORIENTED_EDGE ( 'NONE', *, *, #1861, .T. ) ;
#54789=VERTEX_POINT ( 'NONE', #17152 ) ;
#54790=CARTESIAN_POINT ( 'NONE',  ( 0.1097557419366048670, 11.37678103520278583, 41.59672960874316061 ) ) ;
#54793=ADVANCED_FACE ( 'NONE', ( #36888 ), #5854, .F. ) ;
#54797=AXIS2_PLACEMENT_3D ( 'NONE', #530, #19667, #17134 ) ;
#54798=CARTESIAN_POINT ( 'NONE',  ( 0.1103878639767399417, -16.45816205842789515, 39.86034920885558108 ) ) ;
#54799=CARTESIAN_POINT ( 'NONE',  ( 0.5998501479064699549, 44.64337787626223530, 17.92509395669123862 ) ) ;
#54807=CARTESIAN_POINT ( 'NONE',  ( 0.5998501479064699549, -23.59887241503383493, 41.92175333043579144 ) ) ;
#54812=DIRECTION ( 'NONE',  ( 0.000000000000000000, 0.000000000000000000, -1.000000000000000000 ) ) ;
#54816=ORIENTED_EDGE ( 'NONE', *, *, #48886, .F. ) ;
#54826=AXIS2_PLACEMENT_3D ( 'NONE', #18251, #56436, #35592 ) ;
#54827=FACE_OUTER_BOUND ( 'NONE', #10572, .T. ) ;
#54838=VECTOR ( 'NONE', #12492, 1000.000000000000000 ) ;
#54840=CARTESIAN_POINT ( 'NONE',  ( -6.015611763856276717, 18.68284711750061788, -2.453375430803879986 ) ) ;
#54847=ORIENTED_EDGE ( 'NONE', *, *, #28467, .T. ) ;
#54849=CARTESIAN_POINT ( 'NONE',  ( -6.016489644550736315, 13.32727118274438105, 13.32104266208103738 ) ) ;
#54850=VERTEX_POINT ( 'NONE', #38426 ) ;
#54857=CARTESIAN_POINT ( 'NONE',  ( 4.549368137175248350, 0.000000000000000000, 0.000000000000000000 ) ) ;
#54866=CARTESIAN_POINT ( 'NONE',  ( 0.1100247026804066219, -30.61332956994603194, 30.37337782329838376 ) ) ;
#54868=CARTESIAN_POINT ( 'NONE',  ( 0.8751705887134423323, -41.19904111682490822, -24.81530984069193480 ) ) ;
#54870=ADVANCED_FACE ( 'NONE', ( #28692 ), #43863, .F. ) ;
#54880=CARTESIAN_POINT ( 'NONE',  ( 0.8760168074886960365, 28.57146030081928245, 38.69913431881832366 ) ) ;
#54887=CARTESIAN_POINT ( 'NONE',  ( 0.1073791018717483448, 34.50606437925512182, 25.86618856530722610 ) ) ;
#54893=B_SPLINE_CURVE_WITH_KNOTS ( 'NONE', 3,
 ( #48447, #6424, #19971, #29961 ),
 .UNSPECIFIED., .F., .F.,
 ( 4, 4 ),
 ( 0.000000000000000000, 0.005014147105413703856 ),
 .UNSPECIFIED. ) ;
#54895=CARTESIAN_POINT ( 'NONE',  ( -6.010958268070873523, -18.19761767765826477, -4.891065400978576783 ) ) ;
#54906=CARTESIAN_POINT ( 'NONE',  ( -6.016761891674565099, 18.68153697670641833, 2.462934516563870080 ) ) ;
#54908=CARTESIAN_POINT ( 'NONE',  ( 5.880360259849752858, 47.05949693022707692, -9.312491912827638885 ) ) ;
#54921=ORIENTED_EDGE ( 'NONE', *, *, #17771, .F. ) ;
#54930=CARTESIAN_POINT ( 'NONE',  ( 0.7246131072078524360, -19.16331062551114428, 44.12003537001145048 ) ) ;
#54931=CARTESIAN_POINT ( 'NONE',  ( 0.8751705887134553219, -24.81530984069179269, -41.19904111682499348 ) ) ;
#54936=DIRECTION ( 'NONE',  ( -0.1024043820194934645, 0.5087173657443641028, -0.8548216096550907972 ) ) ;
#54945=CARTESIAN_POINT ( 'NONE',  ( 0.6025881611877910160, 18.20817581200352819, 44.52856035602914631 ) ) ;
#54951=CARTESIAN_POINT ( 'NONE',  ( 0.1092565886968784872, 42.71401356099878655, -5.936467125236589482 ) ) ;
#54953=CARTESIAN_POINT ( 'NONE',  ( 0.7245667037590751702, 42.06183421678296241, 23.33692989609125945 ) ) ;
#54962=CARTESIAN_POINT ( 'NONE',  ( 0.1073791018717483448, -34.50606437925530656, -25.86618856530698451 ) ) ;
#54971=CARTESIAN_POINT ( 'NONE',  ( 4.322998006666179727, -10.36018990813345653, 46.85697641700690497 ) ) ;
#54985=AXIS2_PLACEMENT_3D ( 'NONE', #31893, #60672, #8071 ) ;
#54986=DIRECTION ( 'NONE',  ( 0.1024043820194936449, 0.9878630899050855341, 0.1167898032637372935 ) ) ;
#54988=ADVANCED_FACE ( 'NONE', ( #7020 ), #26151, .T. ) ;
#54989=ORIENTED_EDGE ( 'NONE', *, *, #4482, .F. ) ;
#54992=CARTESIAN_POINT ( 'NONE',  ( 0.8751705887134553219, -46.21789262997766201, 13.30665218149281870 ) ) ;
#54993=EDGE_CURVE ( 'NONE', #2725, #47783, #30845, .T. ) ;
#54998=EDGE_CURVE ( 'NONE', #5168, #33426, #1099, .T. ) ;
#55000=CARTESIAN_POINT ( 'NONE',  ( 0.3622758884714600280, -4.808133778521581192, -42.84426538328729350 ) ) ;
#55006=B_SPLINE_CURVE_WITH_KNOTS ( 'NONE', 3,
 ( #26334, #61069, #3433, #41388 ),
 .UNSPECIFIED., .F., .F.,
 ( 4, 4 ),
 ( 5.818439421673297140E-18, 0.004566006591234645501 ),
 .UNSPECIFIED. ) ;
#55024=CIRCLE ( 'NONE', #34049, 47.91270532121795611 ) ;
#55025=EDGE_LOOP ( 'NONE', ( #50896, #31668, #55967, #16918, #4247, #55152, #32002, #2602, #48351, #31325, #37084, #12376, #54323, #12153, #59621, #34162, #51444, #37082, #20431, #18149, #6216, #45476, #20450, #37696, #43511, #19711, #24068, #38746, #49342, #20389, #6159, #7286, #41679, #6055, #13928, #15082, #44721, #9323, #54305, #13324, #33397, #26546, #48158, #4159, #14022, #6125, #20013, #3797, #12438, #31135, #60722, #15502, #47921, #2611, #44388, #61162, #29506, #44824, #28075, #50297, #5921, #12054, #25120, #48107, #10107, #33227, #32384, #16620, #58001, #21331, #36047, #34611, #22608, #58334, #920, #46988, #47804, #23348, #14521, #28527, #5617, #23974, #14844, #38777, #52710, #50499, #11920, #53866, #27174, #20925, #40892, #35326, #3236, #54847, #57251, #17606, #22872, #50092, #8236, #33928, #32, #25753, #16114, #15108, #11917, #11520, #35959, #35258, #33175, #59304, #9544, #19435, #60847, #40644, #24073, #7055, #53706, #17287, #21222, #8974, #7263, #55478, #56844, #48617, #23516, #26946, #26917, #2285, #16490, #30126, #50045, #48201, #19932, #7648, #40726, #9329, #36770, #47825, #5133, #943, #48122, #36550, #9589, #5447, #36710, #15358, #4393, #21606 ) ) ;
#55028=CARTESIAN_POINT ( 'NONE',  ( 0.3622758884714600280, 41.42293301073608802, 11.95365414648511582 ) ) ;
#55031=CARTESIAN_POINT ( 'NONE',  ( 0.3622758884714600280, -20.83792692158946025, -37.74294673546579304 ) ) ;
#55035=LINE ( 'NONE', #6171, #29904 ) ;
#55039=VERTEX_POINT ( 'NONE', #40905 ) ;
#55044=CARTESIAN_POINT ( 'NONE',  ( 0.3622758884714730732, -41.85013935980095567, -10.35929834645908265 ) ) ;
#55046=CARTESIAN_POINT ( 'NONE',  ( 0.2230388203127606772, 41.84042374003679043, 10.42432885623897043 ) ) ;
#55047=VERTEX_POINT ( 'NONE', #46510 ) ;
#55049=CARTESIAN_POINT ( 'NONE',  ( 3.680974057930773036, -46.78530430706945253, 10.62112035260160603 ) ) ;
#55054=CARTESIAN_POINT ( 'NONE',  ( 0.7048096507298579061, -47.80151517212789969, 5.442192462018654808 ) ) ;
#55058=CARTESIAN_POINT ( 'NONE',  ( 0.6031357023905875581, 38.13964912630292758, 29.32055886552335977 ) ) ;
#55068=EDGE_CURVE ( 'NONE', #39264, #32330, #42070, .T. ) ;
#55071=EDGE_CURVE ( 'NONE', #50920, #2500, #15525, .T. ) ;
#55072=VECTOR ( 'NONE', #45088, 1000.000000000000000 ) ;
#55087=EDGE_CURVE ( 'NONE', #35404, #49963, #47252, .T. ) ;
#55089=CARTESIAN_POINT ( 'NONE',  ( 0.3622758884714730732, 41.85013935980087751, 10.35929834645937397 ) ) ;
#55090=ORIENTED_EDGE ( 'NONE', *, *, #11187, .F. ) ;
#55091=FACE_OUTER_BOUND ( 'NONE', #60657, .T. ) ;
#55092=CARTESIAN_POINT ( 'NONE',  ( 0.6029303876144825880, -29.38970229176932136, 38.08638053211486607 ) ) ;
#55102=VERTEX_POINT ( 'NONE', #9508 ) ;
#55104=CARTESIAN_POINT ( 'NONE',  ( 0.6001305935487422083, -34.38748867424691014, -33.64689939321930012 ) ) ;
#55109=ORIENTED_EDGE ( 'NONE', *, *, #37925, .F. ) ;
#55117=CARTESIAN_POINT ( 'NONE',  ( 0.1310142868023736751, -33.82067078731331122, -26.75450212504311764 ) ) ;
#55118=CARTESIAN_POINT ( 'NONE',  ( 2.643462169533600914, -7.637863311827957524, 47.42536612906414462 ) ) ;
#55121=ORIENTED_EDGE ( 'NONE', *, *, #2471, .F. ) ;
#55122=CARTESIAN_POINT ( 'NONE',  ( -2.569797478183790229, -13.68441171582019855, 5.182550149005058948 ) ) ;
#55125=CARTESIAN_POINT ( 'NONE',  ( -6.016761891674565099, -14.94721834528406923, -11.47373234755518823 ) ) ;
#55134=CARTESIAN_POINT ( 'NONE',  ( 0.1101816497532063371, -16.62841624476650182, -39.78963561881059263 ) ) ;
#55136=CARTESIAN_POINT ( 'NONE',  ( 0.7954190325252783467, -44.09776758977486111, 19.20649988843040745 ) ) ;
#55141=( BOUNDED_SURFACE ( )  B_SPLINE_SURFACE ( 3, 1, ( 
 ( #3324, #42508 ),
 ( #32169, #46584 ),
 ( #51251, #33105 ),
 ( #14002, #33411 ) ),
 .UNSPECIFIED., .F., .F., .F. ) 
 B_SPLINE_SURFACE_WITH_KNOTS ( ( 4, 4 ),
 ( 2, 2 ),
 ( 0.000000000000000000, 1.000000000000000000 ),
 ( 0.000000000000000000, 1.000000000000000000 ),
 .UNSPECIFIED. ) 
 GEOMETRIC_REPRESENTATION_ITEM ( )  RATIONAL_B_SPLINE_SURFACE ( (
 ( 1.000000000000000000, 1.000000000000000000),
 ( 0.9751682680413298332, 0.9999560080971552356),
 ( 0.9751682680413298332, 0.9999560080971552356),
 ( 1.000000000000000000, 1.000000000000000000) ) ) 
 REPRESENTATION_ITEM ( '' )  SURFACE ( )  );
#55144=CARTESIAN_POINT ( 'NONE',  ( 0.2224561200757615431, 33.74134531362598466, 26.84793396060992876 ) ) ;
#55152=ORIENTED_EDGE ( 'NONE', *, *, #14631, .T. ) ;
#55157=CARTESIAN_POINT ( 'NONE',  ( 0.3622758884714600280, -42.84426538328734324, 4.808133778521152202 ) ) ;
#55178=CARTESIAN_POINT ( 'NONE',  ( 0.7954196712028469562, 5.415566793624693176, 47.79303691884135219 ) ) ;
#55183=VERTEX_POINT ( 'NONE', #37425 ) ;
#55187=CARTESIAN_POINT ( 'NONE',  ( 0.1073791018717578927, -41.77800844988522755, 10.69234304549982895 ) ) ;
#55190=CARTESIAN_POINT ( 'NONE',  ( -6.016489644550736315, -18.19999694163067616, 4.881234076340310146 ) ) ;
#55196=CARTESIAN_POINT ( 'NONE',  ( 0.1098349054025746369, 34.08267426123924082, 26.42143025180000748 ) ) ;
#55198=CARTESIAN_POINT ( 'NONE',  ( 0.6031356219577718170, 6.192730535896147970, -47.70727206974379442 ) ) ;
#55203=CARTESIAN_POINT ( 'NONE',  ( 4.549368137175248350, 32.13400537129925283, -28.46244473166639111 ) ) ;
#55204=B_SPLINE_CURVE_WITH_KNOTS ( 'NONE', 3,
 ( #59920, #31423, #16713, #7920, #2901, #45243, #22032, #59295, #46160, #11712, #44932, #54270, #36451, #41462, #55519, #41155 ),
 .UNSPECIFIED., .F., .F.,
 ( 4, 3, 3, 3, 3, 4 ),
 ( 1.962735358247463844E-17, 0.0002618515315864471810, 0.0003927756766342011354, 0.0005236998216950600584, 0.0007855159896329930429, 0.001047349442285932641 ),
 .UNSPECIFIED. ) ;
#55208=LINE ( 'NONE', #50825, #24062 ) ;
#55212=CARTESIAN_POINT ( 'NONE',  ( 0.6028618097248862329, -6.452328974163289210, -47.67286800277441472 ) ) ;
#55213=CARTESIAN_POINT ( 'NONE',  ( 0.1101816497532063094, -0.1358190954552562779, -43.12424935764384060 ) ) ;
#55216=CARTESIAN_POINT ( 'NONE',  ( 0.6031356755773454870, 46.46821530722340299, -12.45114731045982026 ) ) ;
#55219=ORIENTED_EDGE ( 'NONE', *, *, #30534, .F. ) ;
#55222=CARTESIAN_POINT ( 'NONE',  ( 0.7246131072078578761, 34.58859703353080306, -33.42811616637882821 ) ) ;
#55224=VERTEX_POINT ( 'NONE', #35189 ) ;
#55231=CARTESIAN_POINT ( 'NONE',  ( -6.016104459813374383, 13.32794178585016098, -13.32039631884670250 ) ) ;
#55236=B_SPLINE_CURVE_WITH_KNOTS ( 'NONE', 3,
 ( #16247, #44474, #39771, #19716 ),
 .UNSPECIFIED., .F., .F.,
 ( 4, 4 ),
 ( 0.000000000000000000, 0.004445488388166989914 ),
 .UNSPECIFIED. ) ;
#55239=CARTESIAN_POINT ( 'NONE',  ( 0.1081432562775997974, 21.19449538864506266, 37.55692207416033312 ) ) ;
#55240=ORIENTED_EDGE ( 'NONE', *, *, #7224, .F. ) ;
#55243=VERTEX_POINT ( 'NONE', #6623 ) ;
#55246=CARTESIAN_POINT ( 'NONE',  ( 4.549368137175248350, 28.14399996863497577, -32.41327393324110773 ) ) ;
#55252=B_SPLINE_CURVE_WITH_KNOTS ( 'NONE', 3,
 ( #14128, #52614, #9711, #34155 ),
 .UNSPECIFIED., .F., .F.,
 ( 4, 4 ),
 ( 0.000000000000000000, 0.004445488388166995118 ),
 .UNSPECIFIED. ) ;
#55253=CARTESIAN_POINT ( 'NONE',  ( 0.6254311100348652896, 29.82834996731695298, -37.74260849418467956 ) ) ;
#55254=( BOUNDED_SURFACE ( )  B_SPLINE_SURFACE ( 3, 1, ( 
 ( #6603, #43651 ),
 ( #24832, #1007 ),
 ( #16355, #35481 ),
 ( #20141, #54537 ) ),
 .UNSPECIFIED., .F., .F., .F. ) 
 B_SPLINE_SURFACE_WITH_KNOTS ( ( 4, 4 ),
 ( 2, 2 ),
 ( 0.000000000000000000, 1.000000000000000000 ),
 ( 0.000000000000000000, 1.000000000000000000 ),
 .UNSPECIFIED. ) 
 GEOMETRIC_REPRESENTATION_ITEM ( )  RATIONAL_B_SPLINE_SURFACE ( (
 ( 1.000000000000000000, 1.000000000000000000),
 ( 0.9751682680413298332, 0.9999560080971552356),
 ( 0.9751682680413298332, 0.9999560080971552356),
 ( 1.000000000000000000, 1.000000000000000000) ) ) 
 REPRESENTATION_ITEM ( '' )  SURFACE ( )  );
#55255=CARTESIAN_POINT ( 'NONE',  ( 0.6001305935487315502, 47.62765676940944104, -6.798494447611730607 ) ) ;
#55258=CARTESIAN_POINT ( 'NONE',  ( 0.1103310638050662290, 42.76619676553136173, -5.547176740493094727 ) ) ;
#55259=CARTESIAN_POINT ( 'NONE',  ( 0.3622758884714730732, -4.808133778522197588, 42.84426538328723666 ) ) ;
#55284=CARTESIAN_POINT ( 'NONE',  ( 0.6031357023905875581, -44.46217339385183465, 18.36962560204140615 ) ) ;
#55291=CARTESIAN_POINT ( 'NONE',  ( 0.3622758884714730732, 6.444611261694017657, 42.62881903538212924 ) ) ;
#55300=CARTESIAN_POINT ( 'NONE',  ( 0.1103878639767399555, 41.64243544356628490, -11.20830530106149325 ) ) ;
#55305=PLANE ( 'NONE',  #58307 ) ;
#55306=CARTESIAN_POINT ( 'NONE',  ( 0.1102144999581333162, -39.79340763430497674, -16.61938362665535962 ) ) ;
#55308=ORIENTED_EDGE ( 'NONE', *, *, #35446, .F. ) ;
#55317=CARTESIAN_POINT ( 'NONE',  ( 4.322998006666179727, -47.80838462754062590, -4.155494336618541062 ) ) ;
#55345=CARTESIAN_POINT ( 'NONE',  ( 0.5988103564986357874, -37.79415694022880245, 29.76496605343782420 ) ) ;
#55346=CARTESIAN_POINT ( 'NONE',  ( 0.8751705887134423323, -24.81530984069236823, 41.19904111682465242 ) ) ;
#55348=CARTESIAN_POINT ( 'NONE',  ( 0.1098349054025746646, 30.34240357440793190, 30.64407294528958658 ) ) ;
#55349=CARTESIAN_POINT ( 'NONE',  ( 0.1073791018717483448, 16.95003405440257893, 39.65380858626220828 ) ) ;
#55351=EDGE_CURVE ( 'NONE', #17692, #10204, #7895, .T. ) ;
#55352=CARTESIAN_POINT ( 'NONE',  ( 0.1097557419366048670, 37.23482781437645173, -21.75515245866085934 ) ) ;
#55357=CARTESIAN_POINT ( 'NONE',  ( 0.3622758884714600280, 40.13994584881781691, -15.73321244754812298 ) ) ;
#55364=CARTESIAN_POINT ( 'NONE',  ( 0.6030672727741701600, 38.11303703924428277, 29.35514790473164126 ) ) ;
#55367=EDGE_CURVE ( 'NONE', #52228, #17050, #17615, .T. ) ;
#55392=B_SPLINE_CURVE_WITH_KNOTS ( 'NONE', 3,
 ( #54670, #1431, #12114, #49994, #10870, #7052 ),
 .UNSPECIFIED., .F., .F.,
 ( 4, 2, 4 ),
 ( 1.823789517034659149E-17, 0.0002293319059085093578, 0.0004586638118170004467 ),
 .UNSPECIFIED. ) ;
#55393=CARTESIAN_POINT ( 'NONE',  ( 1.827119703190780653, 41.88501940447980587, 9.946884032291251287 ) ) ;
#55395=CARTESIAN_POINT ( 'NONE',  ( 2.643462169533613793, 48.01657676222237114, -1.382267876917960381 ) ) ;
#55397=EDGE_LOOP ( 'NONE', ( #45965, #27369, #52113, #29962 ) ) ;
#55398=CARTESIAN_POINT ( 'NONE',  ( 0.6001305935487422083, 18.89378601236001742, 44.24520387813834787 ) ) ;
#55401=CARTESIAN_POINT ( 'NONE',  ( 0.1095718737110178420, -26.04820588677170079, -34.36877422440991126 ) ) ;
#55403=CARTESIAN_POINT ( 'NONE',  ( 0.8760168074886960365, -24.81951362746106682, 41.20610493656867135 ) ) ;
#55406=ORIENTED_EDGE ( 'NONE', *, *, #4601, .T. ) ;
#55407=VERTEX_POINT ( 'NONE', #26386 ) ;
#55410=CARTESIAN_POINT ( 'NONE',  ( 0.8751705887134553219, -5.393078191593054349, 47.79200036674269825 ) ) ;
#55412=CARTESIAN_POINT ( 'NONE',  ( 0.6028618097248863439, 44.51207924874651667, 18.24855319618761840 ) ) ;
#55431=CARTESIAN_POINT ( 'NONE',  ( -6.016104459813371719, -18.68271063303493307, -2.454244026261287015 ) ) ;
#55433=EDGE_CURVE ( 'NONE', #37278, #40338, #25612, .T. ) ;
#55438=FACE_OUTER_BOUND ( 'NONE', #48498, .T. ) ;
#55444=CARTESIAN_POINT ( 'NONE',  ( 0.2224561200757602386, -39.54039348282969257, -17.20021002050910042 ) ) ;
#55449=CARTESIAN_POINT ( 'NONE',  ( -6.001507490154110336, -7.225628667346451373, -17.40350523682702999 ) ) ;
#55454=VERTEX_POINT ( 'NONE', #52344 ) ;
#55456=DIRECTION ( 'NONE',  ( -1.000000000000000000, -0.000000000000000000, -0.000000000000000000 ) ) ;
#55457=ORIENTED_EDGE ( 'NONE', *, *, #18346, .F. ) ;
#55460=EDGE_CURVE ( 'NONE', #31073, #31157, #46614, .T. ) ;
#55462=B_SPLINE_CURVE_WITH_KNOTS ( 'NONE', 3,
 ( #20525, #30217, #59643, #20225, #59025, #39341 ),
 .UNSPECIFIED., .F., .F.,
 ( 4, 2, 4 ),
 ( 0.000000000000000000, 0.0002450742804987318451, 0.0004901485609974636903 ),
 .UNSPECIFIED. ) ;
#55465=EDGE_CURVE ( 'NONE', #58167, #28193, #33844, .T. ) ;
#55466=CARTESIAN_POINT ( 'NONE',  ( 0.8760168074887076939, 34.63873394077442214, 33.37827814204136700 ) ) ;
#55478=ORIENTED_EDGE ( 'NONE', *, *, #35086, .F. ) ;
#55481=ORIENTED_EDGE ( 'NONE', *, *, #21394, .T. ) ;
#55484=CARTESIAN_POINT ( 'NONE',  ( 0.5998501479064708430, 17.92509395669044636, 44.64337787626254794 ) ) ;
#55496=CARTESIAN_POINT ( 'NONE',  ( -6.015611763856276717, -4.882992715191171840, -18.19956619163663447 ) ) ;
#55499=CARTESIAN_POINT ( 'NONE',  ( 0.6025881611877910160, -41.55278713510066524, -24.24244696985793723 ) ) ;
#55500=ADVANCED_FACE ( 'NONE', ( #11003 ), #5493, .F. ) ;
#55508=B_SPLINE_CURVE_WITH_KNOTS ( 'NONE', 3,
 ( #11146, #30230, #35266, #54953, #6392, #54324 ),
 .UNSPECIFIED., .F., .F.,
 ( 4, 2, 4 ),
 ( 0.000000000000000000, 0.0002450742804987325499, 0.0004901485609974650997 ),
 .UNSPECIFIED. ) ;
#55511=VECTOR ( 'NONE', #53564, 1000.000000000000000 ) ;
#55519=CARTESIAN_POINT ( 'NONE',  ( 0.6009452777970412107, -34.32439724343015541, -33.70725232128880577 ) ) ;
#55520=CARTESIAN_POINT ( 'NONE',  ( -6.016104459813374383, 14.94608397322084414, 11.47525878590921344 ) ) ;
#55531=ORIENTED_EDGE ( 'NONE', *, *, #9615, .F. ) ;
#55533=CARTESIAN_POINT ( 'NONE',  ( 1.827119703190778877, 42.50321986945169073, -6.838980420687535755 ) ) ;
#55544=CARTESIAN_POINT ( 'NONE',  ( 4.549368137175248350, -28.46244473166695954, 32.13400537129875545 ) ) ;
#55548=VERTEX_POINT ( 'NONE', #59201 ) ;
#55558=AXIS2_PLACEMENT_3D ( 'NONE', #43290, #8824, #61120 ) ;
#55572=EDGE_CURVE ( 'NONE', #45423, #1146, #58554, .T. ) ;
#55583=EDGE_CURVE ( 'NONE', #15737, #61648, #41280, .T. ) ;
#55585=CARTESIAN_POINT ( 'NONE',  ( -6.017396004339686577, 2.458362590803059078, -18.68211039806561047 ) ) ;
#55593=CARTESIAN_POINT ( 'NONE',  ( 0.6017666602106489515, -44.31084100715266061, 18.73203020817283004 ) ) ;
#55595=CARTESIAN_POINT ( 'NONE',  ( 4.549368137175248350, 32.41327393324100825, 28.14399996863509301 ) ) ;
#55608=CARTESIAN_POINT ( 'NONE',  ( 0.6027935024548037868, -44.37842839362961911, -18.57106801640284033 ) ) ;
#55609=B_SPLINE_CURVE_WITH_KNOTS ( 'NONE', 3,
 ( #29644, #48754, #54350, #14960, #43469, #24961 ),
 .UNSPECIFIED., .F., .F.,
 ( 4, 2, 4 ),
 ( 8.571645052368668133E-17, 0.0002293366620881447950, 0.0004586733241762038838 ),
 .UNSPECIFIED. ) ;
#55625=VERTEX_POINT ( 'NONE', #7821 ) ;
#55627=CARTESIAN_POINT ( 'NONE',  ( 0.2230388203127593727, 34.66629317821133327, 25.64246103889307449 ) ) ;
#55638=EDGE_CURVE ( 'NONE', #28532, #4, #26944, .T. ) ;
#55639=CIRCLE ( 'NONE', #53616, 42.92674063221959813 ) ;
#55643=VECTOR ( 'NONE', #43116, 1000.000000000000114 ) ;
#55651=B_SPLINE_CURVE_WITH_KNOTS ( 'NONE', 3,
 ( #54020, #49337, #49643, #40290, #11765, #59342 ),
 .UNSPECIFIED., .F., .F.,
 ( 4, 2, 4 ),
 ( 1.764953265579307567E-18, 0.0002450742804987336341, 0.0004901485609974654250 ),
 .UNSPECIFIED. ) ;
#55657=CARTESIAN_POINT ( 'NONE',  ( 0.1103744047535531458, 26.28322091066875998, -34.18931094755013333 ) ) ;
#55659=CARTESIAN_POINT ( 'NONE',  ( 4.833616638992208614, -9.466882727841817058, -45.27110352095245815 ) ) ;
#55662=CARTESIAN_POINT ( 'NONE',  ( 0.1101816497532062678, 37.27878591512674689, -21.67974746580510725 ) ) ;
#55667=EDGE_CURVE ( 'NONE', #11266, #33185, #48682, .T. ) ;
#55671=CARTESIAN_POINT ( 'NONE',  ( 0.5998501479064699549, 38.48283596221989455, 28.86886762351138103 ) ) ;
#55681=ORIENTED_EDGE ( 'NONE', *, *, #42455, .T. ) ;
#55693=CARTESIAN_POINT ( 'NONE',  ( 0.6017667736363749853, 24.35549005323416694, -41.48674115080378755 ) ) ;
#55695=VERTEX_POINT ( 'NONE', #60134 ) ;
#55708=AXIS2_PLACEMENT_3D ( 'NONE', #48153, #39084, #34366 ) ;
#55710=CARTESIAN_POINT ( 'NONE',  ( -6.001507490154110336, 9.408444979392550422, -16.32705935667497243 ) ) ;
#55711=ORIENTED_EDGE ( 'NONE', *, *, #53854, .T. ) ;
#55712=CARTESIAN_POINT ( 'NONE',  ( -6.001507490154111224, -0.01557731607566560997, 18.84387066167321478 ) ) ;
#55713=ORIENTED_EDGE ( 'NONE', *, *, #15986, .F. ) ;
#55716=CARTESIAN_POINT ( 'NONE',  ( 0.5988103564986357874, 34.44345003622203905, 33.58571500783070718 ) ) ;
#55720=CARTESIAN_POINT ( 'NONE',  ( 0.6001305935487315502, 41.40054608060258801, 24.50730504006472543 ) ) ;
#55723=EDGE_CURVE ( 'NONE', #4004, #55102, #45711, .T. ) ;
#55727=EDGE_CURVE ( 'NONE', #49695, #24433, #37506, .T. ) ;
#55736=ORIENTED_EDGE ( 'NONE', *, *, #400, .F. ) ;
#55737=CIRCLE ( 'NONE', #21725, 42.92674063221959813 ) ;
#55739=AXIS2_PLACEMENT_3D ( 'NONE', #46276, #45354, #59414 ) ;
#55743=B_SPLINE_CURVE_WITH_KNOTS ( 'NONE', 3,
 ( #6737, #40322, #59377, #16485, #7056, #45325 ),
 .UNSPECIFIED., .F., .F.,
 ( 4, 2, 4 ),
 ( 1.964907063297894324E-17, 0.0002293319059085105775, 0.0004586638118170014767 ),
 .UNSPECIFIED. ) ;
#55748=ORIENTED_EDGE ( 'NONE', *, *, #14871, .T. ) ;
#55749=CARTESIAN_POINT ( 'NONE',  ( 4.975801465491695552, 5.867614121011992532E-15, -47.91270532121795611 ) ) ;
#55751=CARTESIAN_POINT ( 'NONE',  ( 0.1073791018717578927, -39.65380858626204486, -16.95003405440299460 ) ) ;
#55766=CARTESIAN_POINT ( 'NONE',  ( -6.016489644550737204, 16.32089497094074559, -9.417787539062077329 ) ) ;
#55767=ORIENTED_EDGE ( 'NONE', *, *, #22412, .T. ) ;
#55771=EDGE_CURVE ( 'NONE', #38633, #5563, #60650, .T. ) ;
#55773=ORIENTED_EDGE ( 'NONE', *, *, #35173, .F. ) ;
#55777=CARTESIAN_POINT ( 'NONE',  ( 4.691466044806102076, -8.371234562541538082, -43.79545162262305524 ) ) ;
#55781=CARTESIAN_POINT ( 'NONE',  ( 4.975801465491695552, 31.15993731089124097, -36.39623109580435312 ) ) ;
#55783=CONICAL_SURFACE ( 'NONE', #32785, 42.92674063221959813, 1.485477209440487556 ) ;
#55785=ORIENTED_EDGE ( 'NONE', *, *, #18590, .T. ) ;
#55787=ORIENTED_EDGE ( 'NONE', *, *, #27621, .T. ) ;
#55790=CARTESIAN_POINT ( 'NONE',  ( -2.569797478183783568, 13.68441171582009019, 5.182550149005350271 ) ) ;
#55798=CARTESIAN_POINT ( 'NONE',  ( 50.00005079999999680, 12.80000000000000071, -3.000000000000000000 ) ) ;
#55801=DIRECTION ( 'NONE',  ( -1.000000000000000000, -0.000000000000000000, -0.000000000000000000 ) ) ;
#55805=EDGE_CURVE ( 'NONE', #33185, #44510, #41944, .T. ) ;
#55816=ORIENTED_EDGE ( 'NONE', *, *, #13547, .F. ) ;
#55819=CARTESIAN_POINT ( 'NONE',  ( 4.975801465491694664, -9.906103548668557579, 46.87746200127438101 ) ) ;
#55820=CARTESIAN_POINT ( 'NONE',  ( 4.549368137175248350, 38.59302160394752690, -18.79584381673492288 ) ) ;
#55839=CARTESIAN_POINT ( 'NONE',  ( 0.5998501479064699549, 46.33007877220738635, -12.95623334615453892 ) ) ;
#55842=ORIENTED_EDGE ( 'NONE', *, *, #30133, .T. ) ;
#55846=CARTESIAN_POINT ( 'NONE',  ( 0.8751705887134423323, -46.67919521768896374, 11.58504748649118810 ) ) ;
#55848=B_SPLINE_CURVE_WITH_KNOTS ( 'NONE', 3,
 ( #40595, #7331, #56807, #51186, #61802, #56195 ),
 .UNSPECIFIED., .F., .F.,
 ( 4, 2, 4 ),
 ( 1.274743298368305687E-16, 0.0002450741128632353779, 0.0004901482257263433621 ),
 .UNSPECIFIED. ) ;
#55849=EDGE_CURVE ( 'NONE', #58618, #5670, #3072, .T. ) ;
#55850=ORIENTED_EDGE ( 'NONE', *, *, #22208, .F. ) ;
#55853=EDGE_CURVE ( 'NONE', #41784, #32640, #27719, .T. ) ;
#55854=ORIENTED_EDGE ( 'NONE', *, *, #56222, .F. ) ;
#55858=EDGE_CURVE ( 'NONE', #58483, #7638, #59882, .T. ) ;
#55867=CARTESIAN_POINT ( 'NONE',  ( 0.1100247026804066219, 21.41511734445746740, 37.43141430507378686 ) ) ;
#55868=ORIENTED_EDGE ( 'NONE', *, *, #7352, .T. ) ;
#55887=CARTESIAN_POINT ( 'NONE',  ( 0.5998501479064699549, 34.38546660123250120, 33.64490850298857083 ) ) ;
#55892=CARTESIAN_POINT ( 'NONE',  ( -6.016104459813371719, 18.84322058118302579, -0.005335450885131768489 ) ) ;
#55920=CARTESIAN_POINT ( 'NONE',  ( 4.691466044806102076, -2.583163953528165635, -44.51344083442437949 ) ) ;
#55923=CARTESIAN_POINT ( 'NONE',  ( 0.7245667037590732829, -38.65590879674368807, -28.62745028382802914 ) ) ;
#55925=CARTESIAN_POINT ( 'NONE',  ( -6.001507490154110336, -13.33564355450099015, -13.31361390284173929 ) ) ;
#55933=CARTESIAN_POINT ( 'NONE',  ( 0.6001305935487315502, 46.33281397023046111, 12.95698906763826841 ) ) ;
#55934=CARTESIAN_POINT ( 'NONE',  ( 0.6009452777970412107, 41.87890062806003755, 23.67489783211108900 ) ) ;
#55950=ORIENTED_EDGE ( 'NONE', *, *, #58901, .T. ) ;
#55957=FACE_OUTER_BOUND ( 'NONE', #35570, .T. ) ;
#55958=VERTEX_POINT ( 'NONE', #18326 ) ;
#55959=CARTESIAN_POINT ( 'NONE',  ( -6.015611763856276717, -18.20278301740933102, -4.870987357968367348 ) ) ;
#55967=ORIENTED_EDGE ( 'NONE', *, *, #16129, .T. ) ;
#55973=CARTESIAN_POINT ( 'NONE',  ( 0.8751705887134423323, -11.58504748649167837, -46.67919521768883584 ) ) ;
#55975=CARTESIAN_POINT ( 'NONE',  ( 0.1104177457020373010, 37.34442418285502896, -21.56646482560092792 ) ) ;
#55985=CARTESIAN_POINT ( 'NONE',  ( 4.322998006666165516, 47.94177812210861589, 2.120302895116446873 ) ) ;
#56009=DIRECTION ( 'NONE',  ( 0.000000000000000000, 0.000000000000000000, 1.000000000000000000 ) ) ;
#56010=B_SPLINE_CURVE_WITH_KNOTS ( 'NONE', 3,
 ( #38896, #29459, #53559, #10676 ),
 .UNSPECIFIED., .F., .F.,
 ( 4, 4 ),
 ( 0.000000000000000000, 0.005014147105413699519 ),
 .UNSPECIFIED. ) ;
#56012=ORIENTED_EDGE ( 'NONE', *, *, #17487, .F. ) ;
#56017=CARTESIAN_POINT ( 'NONE',  ( 0.7048096507298635682, -46.68221792389232405, -11.63498350884320232 ) ) ;
#56018=EDGE_LOOP ( 'NONE', ( #20615, #59646, #29511, #27227 ) ) ;
#56023=CARTESIAN_POINT ( 'NONE',  ( 0.1103878639767399555, -26.29099398937423615, -34.18336104662730435 ) ) ;
#56026=CARTESIAN_POINT ( 'NONE',  ( 0.8751705887134553219, -42.09020928323357680, -23.27176129838411001 ) ) ;
#56033=CARTESIAN_POINT ( 'NONE',  ( 3.680882792899938138, -4.423598386734752808, 47.77138407787914787 ) ) ;
#56035=CARTESIAN_POINT ( 'NONE',  ( -6.015611763856276717, -16.32183393015590056, -9.416239407363475422 ) ) ;
#56042=CARTESIAN_POINT ( 'NONE',  ( 0.6041374136657475802, -48.10739871142803992, -0.1745662470642904973 ) ) ;
#56045=EDGE_CURVE ( 'NONE', #34317, #17061, #52423, .T. ) ;
#56046=CARTESIAN_POINT ( 'NONE',  ( 0.1095718737110178836, -34.36877422441016705, 26.04820588677135618 ) ) ;
#56052=CARTESIAN_POINT ( 'NONE',  ( 0.6001305935487315502, 37.84751346122814653, 29.70149728382449794 ) ) ;
#56055=EDGE_CURVE ( 'NONE', #32395, #39423, #39725, .T. ) ;
#56061=CARTESIAN_POINT ( 'NONE',  ( 0.09136607875274982415, 12.80000000000000071, -3.000000000000000000 ) ) ;
#56063=CARTESIAN_POINT ( 'NONE',  ( 0.5998501479064699549, 46.33007877220738635, -12.95623334615453892 ) ) ;
#56078=CARTESIAN_POINT ( 'NONE',  ( 0.7048096507298635682, -41.23648859290943847, 24.78213711671527619 ) ) ;
#56084=EDGE_CURVE ( 'NONE', #33948, #53671, #33355, .T. ) ;
#56085=ORIENTED_EDGE ( 'NONE', *, *, #30924, .T. ) ;
#56090=CARTESIAN_POINT ( 'NONE',  ( 0.6031356219577718170, 29.35521383643406779, 38.11305734842073178 ) ) ;
#56099=AXIS2_PLACEMENT_3D ( 'NONE', #43969, #53008, #20140 ) ;
#56103=ORIENTED_EDGE ( 'NONE', *, *, #13395, .T. ) ;
#56110=ORIENTED_EDGE ( 'NONE', *, *, #9876, .T. ) ;
#56115=ORIENTED_EDGE ( 'NONE', *, *, #50146, .T. ) ;
#56116=DIRECTION ( 'NONE',  ( 0.09835009131224552170, 0.9592125346408720832, -0.2650256080583662799 ) ) ;
#56117=CARTESIAN_POINT ( 'NONE',  ( -6.016761891674564211, -18.20023637398602290, 4.880293656734900232 ) ) ;
#56119=CARTESIAN_POINT ( 'NONE',  ( 0.5998501479064708430, -46.33007877220729398, -12.95623334615486222 ) ) ;
#56124=CARTESIAN_POINT ( 'NONE',  ( 0.6001305935487422083, 41.40054608060260222, 24.50730504006470767 ) ) ;
#56125=CARTESIAN_POINT ( 'NONE',  ( 0.6001305935487422083, -47.62765676940948367, 6.798494447611420632 ) ) ;
#56132=ADVANCED_FACE ( 'NONE', ( #61812 ), #4747, .F. ) ;
#56137=CARTESIAN_POINT ( 'NONE',  ( 0.1102847568649952675, -21.48234084756722240, 37.39286109091540311 ) ) ;
#56146=( BOUNDED_SURFACE ( )  B_SPLINE_SURFACE ( 3, 1, ( 
 ( #12831, #41958 ),
 ( #31607, #18439 ),
 ( #61023, #55395 ),
 ( #46044, #3689 ) ),
 .UNSPECIFIED., .F., .F., .F. ) 
 B_SPLINE_SURFACE_WITH_KNOTS ( ( 4, 4 ),
 ( 2, 2 ),
 ( 0.000000000000000000, 1.000000000000000000 ),
 ( 0.000000000000000000, 1.000000000000000000 ),
 .UNSPECIFIED. ) 
 GEOMETRIC_REPRESENTATION_ITEM ( )  RATIONAL_B_SPLINE_SURFACE ( (
 ( 1.000000000000000000, 1.000000000000000000),
 ( 0.7223157951917476005, 0.9931996967497186413),
 ( 0.7223157951917476005, 0.9931996967497186413),
 ( 1.000000000000000000, 1.000000000000000000) ) ) 
 REPRESENTATION_ITEM ( '' )  SURFACE ( )  );
#56152=CARTESIAN_POINT ( 'NONE',  ( 4.549368137175248350, 0.000000000000000000, 0.000000000000000000 ) ) ;
#56154=CARTESIAN_POINT ( 'NONE',  ( 4.549368137175248350, -35.57418903283098643, -24.02461520945259466 ) ) ;
#56155=ADVANCED_FACE ( 'NONE', ( #9837 ), #40583, .F. ) ;
#56157=VERTEX_POINT ( 'NONE', #57727 ) ;
#56174=EDGE_CURVE ( 'NONE', #32390, #26300, #49459, .T. ) ;
#56175=B_SPLINE_CURVE_WITH_KNOTS ( 'NONE', 3,
 ( #2672, #40014, #45321, #29960 ),
 .UNSPECIFIED., .F., .F.,
 ( 4, 4 ),
 ( 0.000000000000000000, 0.005014147105413695182 ),
 .UNSPECIFIED. ) ;
#56176=CARTESIAN_POINT ( 'NONE',  ( 0.1103878639767399555, 21.60424693647505023, 37.32258098927775336 ) ) ;
#56178=ORIENTED_EDGE ( 'NONE', *, *, #48950, .F. ) ;
#56180=EDGE_LOOP ( 'NONE', ( #31236, #25487, #15992, #35793 ) ) ;
#56181=CARTESIAN_POINT ( 'NONE',  ( -6.017396004339686577, 4.875835690939434919, -18.20140164570664254 ) ) ;
#56186=ORIENTED_EDGE ( 'NONE', *, *, #24479, .F. ) ;
#56187=CARTESIAN_POINT ( 'NONE',  ( -6.016761891674565099, 9.424569481870481269, -16.31696541414262214 ) ) ;
#56189=CARTESIAN_POINT ( 'NONE',  ( 4.833616638992208614, 26.07076047129084273, 38.20222678111946379 ) ) ;
#56190=CARTESIAN_POINT ( 'NONE',  ( -6.016104459813374383, -18.68271063303496504, 2.454244026261025446 ) ) ;
#56195=CARTESIAN_POINT ( 'NONE',  ( 0.5998501479064708430, 6.798102206414135651, -47.62484632993681544 ) ) ;
#56198=CARTESIAN_POINT ( 'NONE',  ( -6.016104459813374383, 14.95258000663147691, -11.46679299034565247 ) ) ;
#56205=LINE ( 'NONE', #18331, #5750 ) ;
#56208=FACE_OUTER_BOUND ( 'NONE', #1461, .T. ) ;
#56209=EDGE_CURVE ( 'NONE', #37177, #4442, #6575, .T. ) ;
#56215=CARTESIAN_POINT ( 'NONE',  ( 0.5988103622719990193, -33.58571533649136143, -34.44344971428014901 ) ) ;
#56222=EDGE_CURVE ( 'NONE', #49600, #42216, #52326, .T. ) ;
#56228=CARTESIAN_POINT ( 'NONE',  ( 0.1101816497532062955, -43.12424935764384060, 0.1358190954554068519 ) ) ;
#56234=CARTESIAN_POINT ( 'NONE',  ( -5.995132425357893702, -13.33084941932897927, -13.31880955509740971 ) ) ;
#56237=ORIENTED_EDGE ( 'NONE', *, *, #14631, .F. ) ;
#56240=CARTESIAN_POINT ( 'NONE',  ( 4.549368137175248350, -13.59764261105721950, -40.71620287708339703 ) ) ;
#56249=CARTESIAN_POINT ( 'NONE',  ( 0.5980894510889457338, 48.10766805928369649, -0.7015180095999885568 ) ) ;
#56257=CARTESIAN_POINT ( 'NONE',  ( -6.015611763856276717, -11.47596948473821321, 14.94556629257421498 ) ) ;
#56259=CARTESIAN_POINT ( 'NONE',  ( 0.1073791018717578927, 25.86618856530665767, 34.50606437925554815 ) ) ;
#56261=ORIENTED_EDGE ( 'NONE', *, *, #23690, .F. ) ;
#56272=EDGE_CURVE ( 'NONE', #24504, #2547, #59773, .T. ) ;
#56278=CARTESIAN_POINT ( 'NONE',  ( 0.1081432562775997697, 26.58728936586516767, -33.95357233988202239 ) ) ;
#56280=ORIENTED_EDGE ( 'NONE', *, *, #50151, .F. ) ;
#56282=CARTESIAN_POINT ( 'NONE',  ( -6.015611763856276717, -9.427003116184058840, -16.31561949997086103 ) ) ;
#56290=CARTESIAN_POINT ( 'NONE',  ( 0.3622758884714600280, -11.95365414648526148, 41.42293301073604539 ) ) ;
#56292=CARTESIAN_POINT ( 'NONE',  ( 2.643462169533600914, 48.01657676222235693, 1.382267876918626959 ) ) ;
#56297=CARTESIAN_POINT ( 'NONE',  ( 4.549368137175248350, 0.000000000000000000, 0.000000000000000000 ) ) ;
#56298=CARTESIAN_POINT ( 'NONE',  ( 4.975801465491695552, -46.87746200127462970, 9.906103548667402947 ) ) ;
#56299=CARTESIAN_POINT ( 'NONE',  ( 0.1098349054025746369, -5.840292671757984166, 42.72717686504319801 ) ) ;
#56305=CARTESIAN_POINT ( 'NONE',  ( 0.3622758884714600280, 26.89560658783384994, -33.69533458712316332 ) ) ;
#56315=CARTESIAN_POINT ( 'NONE',  ( 0.6027935024548037868, 24.20473723001696698, -41.57475399306895980 ) ) ;
#56325=CARTESIAN_POINT ( 'NONE',  ( 0.1100053167205931048, 26.39466280306222856, 34.10339839758293579 ) ) ;
#56326=EDGE_LOOP ( 'NONE', ( #7955, #18094, #7447, #57566 ) ) ;
#56342=VERTEX_POINT ( 'NONE', #47949 ) ;
#56349=LINE ( 'NONE', #32575, #41828 ) ;
#56351=CARTESIAN_POINT ( 'NONE',  ( 0.7954190325252785687, -34.61997719899462567, -33.39101560460790097 ) ) ;
#56354=EDGE_LOOP ( 'NONE', ( #16003, #36192, #53052, #36942 ) ) ;
#56356=ADVANCED_FACE ( 'NONE', ( #5604 ), #31130, .F. ) ;
#56357=CARTESIAN_POINT ( 'NONE',  ( 5.880360259849752858, 31.59460303415934845, 36.09847387447869238 ) ) ;
#56363=CARTESIAN_POINT ( 'NONE',  ( 0.5998501479064708430, 48.10473956285918717, 0.5236536531316605680 ) ) ;
#56366=ORIENTED_EDGE ( 'NONE', *, *, #25159, .T. ) ;
#56369=CARTESIAN_POINT ( 'NONE',  ( 2.643462169533600914, 25.20536747735779315, -40.89244134039086020 ) ) ;
#56377=VECTOR ( 'NONE', #39822, 1000.000000000000227 ) ;
#56386=CARTESIAN_POINT ( 'NONE',  ( 4.549368137175248350, 8.582197505783829783, 42.06008734272398897 ) ) ;
#56388=ORIENTED_EDGE ( 'NONE', *, *, #35314, .T. ) ;
#56392=CARTESIAN_POINT ( 'NONE',  ( 4.975801465491694664, -8.787181743659814970, -47.10002938642139014 ) ) ;
#56393=VERTEX_POINT ( 'NONE', #27185 ) ;
#56394=CARTESIAN_POINT ( 'NONE',  ( 4.322998006666165516, -39.32552843303867718, 27.50295597456385366 ) ) ;
#56401=AXIS2_PLACEMENT_3D ( 'NONE', #49666, #6722, #40309 ) ;
#56408=VERTEX_POINT ( 'NONE', #17481 ) ;
#56414=FACE_OUTER_BOUND ( 'NONE', #61873, .T. ) ;
#56422=EDGE_LOOP ( 'NONE', ( #52617, #38815, #3993, #52808 ) ) ;
#56423=CARTESIAN_POINT ( 'NONE',  ( 4.975801465491695552, 14.85979367497174408, -45.55012473237738391 ) ) ;
#56424=CARTESIAN_POINT ( 'NONE',  ( -6.015611763856276717, -18.19956619163661671, 4.882992715191235789 ) ) ;
#56430=CARTESIAN_POINT ( 'NONE',  ( 4.549368137175248350, 40.71620287708344677, -13.59764261105707739 ) ) ;
#56431=EDGE_CURVE ( 'NONE', #56955, #34923, #31896, .T. ) ;
#56432=CARTESIAN_POINT ( 'NONE',  ( 5.880360259849752858, 43.04573319267444731, -21.17507050419470715 ) ) ;
#56436=DIRECTION ( 'NONE',  ( -1.000000000000000000, -0.000000000000000000, -0.000000000000000000 ) ) ;
#56438=CARTESIAN_POINT ( 'NONE',  ( 0.6041374136657475802, -29.14743607025058125, -38.27243465845331372 ) ) ;
#56439=CARTESIAN_POINT ( 'NONE',  ( -2.569797478183790229, 11.33042594333535646, 9.259773107243104207 ) ) ;
#56441=CARTESIAN_POINT ( 'NONE',  ( 0.1073791018717578927, -21.98088480513690968, 37.10214135362851096 ) ) ;
#56453=ORIENTED_EDGE ( 'NONE', *, *, #51493, .T. ) ;
#56457=DIRECTION ( 'NONE',  ( 1.000000000000000000, 0.000000000000000000, 0.000000000000000000 ) ) ;
#56466=CARTESIAN_POINT ( 'NONE',  ( 0.6029303876144825880, -38.08638053211517871, -29.38970229176890570 ) ) ;
#56469=VERTEX_POINT ( 'NONE', #50067 ) ;
#56475=CARTESIAN_POINT ( 'NONE',  ( -6.015611763856276717, 11.47596948473810841, 14.94556629257429492 ) ) ;
#56477=CARTESIAN_POINT ( 'NONE',  ( 0.1092565886968784594, -30.71235995742719993, -30.27341312544103857 ) ) ;
#56480=CARTESIAN_POINT ( 'NONE',  ( 0.6029303876144825880, -48.10727438003475953, -0.1308990448394030115 ) ) ;
#56481=ORIENTED_EDGE ( 'NONE', *, *, #45193, .T. ) ;
#56485=ORIENTED_EDGE ( 'NONE', *, *, #24150, .F. ) ;
#56487=CARTESIAN_POINT ( 'NONE',  ( 0.8760168074886960365, -0.8912768426709578584, 48.09529047980636562 ) ) ;
#56489=CARTESIAN_POINT ( 'NONE',  ( 0.7048096507298635682, -29.95256433478701297, -37.64898672361943710 ) ) ;
#56492=DIRECTION ( 'NONE',  ( -1.000000000000000000, -0.000000000000000000, -0.000000000000000000 ) ) ;
#56494=CARTESIAN_POINT ( 'NONE',  ( 3.680974057930773036, 36.90739001595131441, 30.65154904503192412 ) ) ;
#56503=ORIENTED_EDGE ( 'NONE', *, *, #13597, .F. ) ;
#56506=CARTESIAN_POINT ( 'NONE',  ( 0.1104177457020373010, -42.75487793940128256, 5.633723015004153289 ) ) ;
#56511=CARTESIAN_POINT ( 'NONE',  ( 5.880360259849752858, 9.405269135695244032, -47.04104239318758118 ) ) ;
#56526=DIRECTION ( 'NONE',  ( 0.000000000000000000, 0.000000000000000000, 1.000000000000000000 ) ) ;
#56529=B_SPLINE_CURVE_WITH_KNOTS ( 'NONE', 3,
 ( #50309, #21195, #40331, #40638 ),
 .UNSPECIFIED., .F., .F.,
 ( 4, 4 ),
 ( 2.012794395885733147E-17, 0.004444306975806115029 ),
 .UNSPECIFIED. ) ;
#56536=CARTESIAN_POINT ( 'NONE',  ( 0.1098349054025746785, 39.75970464594242060, 16.69989664087468739 ) ) ;
#56542=CARTESIAN_POINT ( 'NONE',  ( 0.6030672727741701600, -44.41203814406394912, -18.49051564326117969 ) ) ;
#56543=ORIENTED_EDGE ( 'NONE', *, *, #19728, .T. ) ;
#56547=DIRECTION ( 'NONE',  ( -0.1024043820194934368, -0.9878630899050870884, 0.1167898032637235545 ) ) ;
#56552=VECTOR ( 'NONE', #56116, 1000.000000000000114 ) ;
#56554=EDGE_CURVE ( 'NONE', #32580, #35399, #11986, .T. ) ;
#56559=ADVANCED_FACE ( 'NONE', ( #23110 ), #60379, .F. ) ;
#56564=EDGE_CURVE ( 'NONE', #24212, #5544, #48563, .T. ) ;
#56567=CARTESIAN_POINT ( 'NONE',  ( 4.833616638992208614, 45.44786513329586342, 8.578242093415909153 ) ) ;
#56574=ORIENTED_EDGE ( 'NONE', *, *, #23189, .F. ) ;
#56576=VERTEX_POINT ( 'NONE', #49064 ) ;
#56583=DIRECTION ( 'NONE',  ( 0.09835009131224552170, 0.9855991218957030897, -0.1375559175655191035 ) ) ;
#56585=ORIENTED_EDGE ( 'NONE', *, *, #40745, .T. ) ;
#56589=CARTESIAN_POINT ( 'NONE',  ( 0.6017666602106488405, 47.64919188470828715, -6.625262199740582503 ) ) ;
#56590=CARTESIAN_POINT ( 'NONE',  ( 0.1073791018717483448, 41.77800844988500018, 10.69234304550068337 ) ) ;
#56592=CARTESIAN_POINT ( 'NONE',  ( -6.001507490154110336, 14.95933060264873937, 11.45906331631436359 ) ) ;
#56598=CIRCLE ( 'NONE', #29591, 42.92674063221959813 ) ;
#56601=CARTESIAN_POINT ( 'NONE',  ( 4.975801465491695552, -39.51822597168514051, 27.09127437476313816 ) ) ;
#56609=VECTOR ( 'NONE', #54192, 1000.000000000000000 ) ;
#56610=CARTESIAN_POINT ( 'NONE',  ( 0.1073791018717578927, -6.109314776653017809, 42.68962945260943087 ) ) ;
#56612=CARTESIAN_POINT ( 'NONE',  ( 0.8760168074887076939, 0.8912768426699595459, 48.09529047980637984 ) ) ;
#56628=VERTEX_POINT ( 'NONE', #11169 ) ;
#56633=CARTESIAN_POINT ( 'NONE',  ( 0.6001305935487422083, -44.24520387813841893, 18.89378601235986110 ) ) ;
#56634=CARTESIAN_POINT ( 'NONE',  ( 0.3622758884714730732, 22.26738722580116558, 36.91764744403329246 ) ) ;
#56638=CARTESIAN_POINT ( 'NONE',  ( -6.017396004339686577, -7.212050743684049081, -17.40836349643175041 ) ) ;
#56649=ORIENTED_EDGE ( 'NONE', *, *, #13147, .F. ) ;
#56657=ORIENTED_EDGE ( 'NONE', *, *, #57961, .F. ) ;
#56660=CARTESIAN_POINT ( 'NONE',  ( 0.7954196712028470673, 47.56618050291064748, 7.138712347928350077 ) ) ;
#56671=EDGE_CURVE ( 'NONE', #55548, #56965, #39606, .T. ) ;
#56679=EDGE_CURVE ( 'NONE', #37474, #11351, #14193, .T. ) ;
#56681=FACE_OUTER_BOUND ( 'NONE', #43382, .T. ) ;
#56687=CARTESIAN_POINT ( 'NONE',  ( 4.975801465491694664, 39.51822597168457918, 27.09127437476394817 ) ) ;
#56688=CARTESIAN_POINT ( 'NONE',  ( 2.301430502907645614, 47.43735983879643214, 7.543848632415379285 ) ) ;
#56690=LINE ( 'NONE', #24118, #34315 ) ;
#56693=ORIENTED_EDGE ( 'NONE', *, *, #38057, .F. ) ;
#56697=CARTESIAN_POINT ( 'NONE',  ( 0.5988103564986354543, 24.57719524907183839, 41.35593036885941132 ) ) ;
#56702=ORIENTED_EDGE ( 'NONE', *, *, #60792, .F. ) ;
#56720=AXIS2_PLACEMENT_3D ( 'NONE', #944, #20987, #54466 ) ;
#56736=CARTESIAN_POINT ( 'NONE',  ( 4.322998006666165516, 27.50295597456399577, 39.32552843303859191 ) ) ;
#56752=CARTESIAN_POINT ( 'NONE',  ( 0.6001305935487422083, 28.87057754790887643, 38.48510059944056394 ) ) ;
#56776=EDGE_CURVE ( 'NONE', #57783, #24396, #47800, .T. ) ;
#56779=ORIENTED_EDGE ( 'NONE', *, *, #7018, .T. ) ;
#56784=ORIENTED_EDGE ( 'NONE', *, *, #50949, .T. ) ;
#56796=CARTESIAN_POINT ( 'NONE',  ( 0.1102847568649952675, 5.720244683738028968, 42.74337176234131164 ) ) ;
#56798=EDGE_CURVE ( 'NONE', #32640, #4311, #27587, .T. ) ;
#56806=CARTESIAN_POINT ( 'NONE',  ( 0.1073791018717483448, -37.58707531572191840, -21.14095454447545919 ) ) ;
#56807=CARTESIAN_POINT ( 'NONE',  ( 0.7246131072078552116, 7.091231226024794054, -47.57651137777907735 ) ) ;
#56810=ORIENTED_EDGE ( 'NONE', *, *, #601, .F. ) ;
#56814=DIRECTION ( 'NONE',  ( 0.09835009131224567436, 0.9164135549743729348, 0.3879606369183669079 ) ) ;
#56818=CARTESIAN_POINT ( 'NONE',  ( 0.2885697896453118805, 40.13549262224777436, -15.75356890148114886 ) ) ;
#56826=CARTESIAN_POINT ( 'NONE',  ( 0.8760168074886965917, 23.27577685234539118, 42.09738177923962610 ) ) ;
#56828=FACE_OUTER_BOUND ( 'NONE', #44847, .T. ) ;
#56829=CARTESIAN_POINT ( 'NONE',  ( 0.7048096507298579061, -37.64898672361932341, -29.95256433478712310 ) ) ;
#56838=CARTESIAN_POINT ( 'NONE',  ( 4.975801465491695552, 3.702618843596801934, 47.76942479135487218 ) ) ;
#56844=ORIENTED_EDGE ( 'NONE', *, *, #30518, .T. ) ;
#56847=CARTESIAN_POINT ( 'NONE',  ( 4.322998006666165516, 32.40067585697750729, 35.39923696759023386 ) ) ;
#56851=ADVANCED_FACE ( 'NONE', ( #13640 ), #5127, .F. ) ;
#56858=CARTESIAN_POINT ( 'NONE',  ( -6.016489644550737204, -7.206912786933163062, -17.41053539857207610 ) ) ;
#56861=ORIENTED_EDGE ( 'NONE', *, *, #55465, .T. ) ;
#56862=CARTESIAN_POINT ( 'NONE',  ( -6.015611763856276717, -9.427003116184289766, 16.31561949997072958 ) ) ;
#56865=CARTESIAN_POINT ( 'NONE',  ( 3.680974057930773924, 16.63696281867796500, 44.99871514631797709 ) ) ;
#56876=PRODUCT_DEFINITION_FORMATION_WITH_SPECIFIED_SOURCE ( 'ANY', '', #27294, .NOT_KNOWN. ) ;
#56889=CARTESIAN_POINT ( 'NONE',  ( 4.549368137175248350, 19.17571786012324608, -38.40568845698256695 ) ) ;
#56891=CARTESIAN_POINT ( 'NONE',  ( 2.301529144917014769, 42.22700141647010952, 22.89307126380001378 ) ) ;
#56892=CARTESIAN_POINT ( 'NONE',  ( 0.1084644655670283508, 16.13497904887303847, -39.99242539812098585 ) ) ;
#56893=ORIENTED_EDGE ( 'NONE', *, *, #56679, .T. ) ;
#56899=CIRCLE ( 'NONE', #15881, 47.91270532121795611 ) ;
#56912=CARTESIAN_POINT ( 'NONE',  ( 0.6031357023905874470, 47.69018446756500396, 6.322524267548747190 ) ) ;
#56917=CARTESIAN_POINT ( 'NONE',  ( 0.1102144999581333162, -5.753800096706359390, 42.73889315046709925 ) ) ;
#56925=ORIENTED_EDGE ( 'NONE', *, *, #30224, .T. ) ;
#56927=EDGE_CURVE ( 'NONE', #43595, #26311, #18620, .T. ) ;
#56932=VERTEX_POINT ( 'NONE', #1971 ) ;
#56938=AXIS2_PLACEMENT_3D ( 'NONE', #60386, #37246, #56009 ) ;
#56943=CARTESIAN_POINT ( 'NONE',  ( 0.6031356219577718170, 34.07882816221574274, 33.95537057546196991 ) ) ;
#56948=CARTESIAN_POINT ( 'NONE',  ( 4.549368137175248350, 23.67244292351640667, -35.80950303116076583 ) ) ;
#56949=EDGE_CURVE ( 'NONE', #42739, #49695, #55204, .T. ) ;
#56950=ORIENTED_EDGE ( 'NONE', *, *, #60314, .T. ) ;
#56955=VERTEX_POINT ( 'NONE', #7595 ) ;
#56965=VERTEX_POINT ( 'NONE', #45856 ) ;
#56967=CARTESIAN_POINT ( 'NONE',  ( 0.8751705887134553219, -48.08707113907594533, 0.8911681664086766874 ) ) ;
#56968=CARTESIAN_POINT ( 'NONE',  ( 0.5998501479064708430, 47.62484632993678701, 6.798102206414301740 ) ) ;
#56970=CARTESIAN_POINT ( 'NONE',  ( 0.1310142868023688456, -42.66681113736510866, -6.259743112235379492 ) ) ;
#56976=CARTESIAN_POINT ( 'NONE',  ( -6.001507490154111224, -11.45906331631421438, -14.95933060264885484 ) ) ;
#56981=CARTESIAN_POINT ( 'NONE',  ( 0.6031356219577718170, 0.08729769678243670672, 48.10744328000515679 ) ) ;
#56993=CARTESIAN_POINT ( 'NONE',  ( 4.322998006666165516, 16.38761975793144288, 45.10383234877038916 ) ) ;
#56996=CARTESIAN_POINT ( 'NONE',  ( 0.8760168074887090262, -37.61398439004553751, 29.98565522133282713 ) ) ;
#56998=VECTOR ( 'NONE', #4891, 1000.000000000000227 ) ;
#57004=CARTESIAN_POINT ( 'NONE',  ( 4.975801465491695552, 0.000000000000000000, 0.000000000000000000 ) ) ;
#57015=ORIENTED_EDGE ( 'NONE', *, *, #34378, .T. ) ;
#57017=CARTESIAN_POINT ( 'NONE',  ( -6.010958268070873523, 17.41463273278779056, 7.197664668556505774 ) ) ;
#57036=CARTESIAN_POINT ( 'NONE',  ( 0.2230388203127602886, 11.89247826311217260, 41.44703429209689460 ) ) ;
#57040=CARTESIAN_POINT ( 'NONE',  ( 0.3622758884714730732, 15.73321244754854753, -40.13994584881767480 ) ) ;
#57043=ORIENTED_EDGE ( 'NONE', *, *, #31890, .F. ) ;
#57048=CARTESIAN_POINT ( 'NONE',  ( 0.8751705887134423323, -29.98056538504989277, 37.60752970653777538 ) ) ;
#57063=CARTESIAN_POINT ( 'NONE',  ( 5.880360259849739535, 47.86623372148050493, -3.184717612777442142 ) ) ;
#57069=EDGE_CURVE ( 'NONE', #49359, #34393, #56598, .T. ) ;
#57072=VERTEX_POINT ( 'NONE', #42386 ) ;
#57075=ORIENTED_EDGE ( 'NONE', *, *, #18770, .F. ) ;
#57078=B_SPLINE_CURVE_WITH_KNOTS ( 'NONE', 3,
 ( #25825, #26133, #54613, #30507, #2308, #54931 ),
 .UNSPECIFIED., .F., .F.,
 ( 4, 2, 4 ),
 ( 0.000000000000000000, 0.0002450742804987323330, 0.0004901485609974646660 ),
 .UNSPECIFIED. ) ;
#57080=VERTEX_POINT ( 'NONE', #8219 ) ;
#57081=CARTESIAN_POINT ( 'NONE',  ( 4.549368137175248350, 38.59302160394725689, 18.79584381673547711 ) ) ;
#57084=LINE ( 'NONE', #8877, #21101 ) ;
#57087=CARTESIAN_POINT ( 'NONE',  ( 0.5988103564986357874, -44.67429521517320978, -17.84821699813467077 ) ) ;
#57092=EDGE_LOOP ( 'NONE', ( #36111, #54300, #51227, #34176 ) ) ;
#57093=ORIENTED_EDGE ( 'NONE', *, *, #42674, .T. ) ;
#57100=ORIENTED_EDGE ( 'NONE', *, *, #21356, .T. ) ;
#57101=CARTESIAN_POINT ( 'NONE',  ( 4.322998006666165516, 14.45630056002939945, -45.75942687572284484 ) ) ;
#57107=CARTESIAN_POINT ( 'NONE',  ( 0.6254087463353906751, 38.58044986685651878, 28.73645667569962825 ) ) ;
#57108=B_SPLINE_CURVE_WITH_KNOTS ( 'NONE', 3,
 ( #2076, #20902, #11510, #45048, #10583, #50026 ),
 .UNSPECIFIED., .F., .F.,
 ( 4, 2, 4 ),
 ( 1.269856260368691521E-16, 0.0002450741128632377090, 0.0004901482257263484578 ),
 .UNSPECIFIED. ) ;
#57112=CARTESIAN_POINT ( 'NONE',  ( 0.1102144999581333440, -42.77179372778547162, 5.503895401229260465 ) ) ;
#57115=CARTESIAN_POINT ( 'NONE',  ( -2.708315649062910779, 5.356004933109274724, 13.61924161399635658 ) ) ;
#57117=CIRCLE ( 'NONE', #10100, 10.00000000000000000 ) ;
#57118=CARTESIAN_POINT ( 'NONE',  ( 0.8751705887134553219, -29.98056538504934210, -37.60752970653818039 ) ) ;
#57119=CARTESIAN_POINT ( 'NONE',  ( 4.975801465491694664, -14.85979367497141546, -45.55012473237748338 ) ) ;
#57121=ADVANCED_FACE ( 'NONE', ( #27645 ), #24364, .F. ) ;
#57132=CARTESIAN_POINT ( 'NONE',  ( 0.3622758884714730732, 29.89648521331631414, -31.06363466427696807 ) ) ;
#57135=CARTESIAN_POINT ( 'NONE',  ( 3.238741278300273141, 42.34697043723801357, 7.419593128524208936 ) ) ;
#57137=ORIENTED_EDGE ( 'NONE', *, *, #52782, .T. ) ;
#57141=CARTESIAN_POINT ( 'NONE',  ( 0.1084644655670282676, 39.99242539812092190, 16.13497904887317347 ) ) ;
#57142=EDGE_CURVE ( 'NONE', #13269, #35477, #12638, .T. ) ;
#57143=ORIENTED_EDGE ( 'NONE', *, *, #37947, .F. ) ;
#57146=CARTESIAN_POINT ( 'NONE',  ( 0.6001305935487315502, -44.64600790884043846, -17.92615948558525218 ) ) ;
#57158=ORIENTED_EDGE ( 'NONE', *, *, #35466, .F. ) ;
#57167=ORIENTED_EDGE ( 'NONE', *, *, #58114, .F. ) ;
#57168=ORIENTED_EDGE ( 'NONE', *, *, #36316, .F. ) ;
#57175=CARTESIAN_POINT ( 'NONE',  ( 0.6041374136657476912, -33.89363087703070931, 34.14050483116080414 ) ) ;
#57177=CARTESIAN_POINT ( 'NONE',  ( 0.1313383488274130484, -26.75504982351785088, -33.82021892231536953 ) ) ;
#57179=ORIENTED_EDGE ( 'NONE', *, *, #46004, .T. ) ;
#57186=CARTESIAN_POINT ( 'NONE',  ( 0.1073791018717578927, 10.69234304549997105, 41.77800844988518492 ) ) ;
#57187=DIRECTION ( 'NONE',  ( 0.000000000000000000, 0.000000000000000000, -1.000000000000000000 ) ) ;
#57188=CARTESIAN_POINT ( 'NONE',  ( 0.1092565886968784317, 16.21587544131324421, -39.95965440403629998 ) ) ;
#57191=CARTESIAN_POINT ( 'NONE',  ( 4.975801465491695552, 0.000000000000000000, 0.000000000000000000 ) ) ;
#57203=ADVANCED_FACE ( 'NONE', ( #39539 ), #23996, .F. ) ;
#57206=CARTESIAN_POINT ( 'NONE',  ( 0.3622758884714600280, -26.89560658783410574, 33.69533458712297147 ) ) ;
#57207=CARTESIAN_POINT ( 'NONE',  ( 0.1087620492084206414, -5.987629195158126194, 42.70684898916385208 ) ) ;
#57210=CARTESIAN_POINT ( 'NONE',  ( -6.016104459813374383, 0.005335450885330034372, -18.84322058118302223 ) ) ;
#57217=B_SPLINE_CURVE_WITH_KNOTS ( 'NONE', 3,
 ( #35904, #50286, #7351, #26478 ),
 .UNSPECIFIED., .F., .F.,
 ( 4, 4 ),
 ( 2.033478910116247305E-17, 0.004444306975806114161 ),
 .UNSPECIFIED. ) ;
#57228=CARTESIAN_POINT ( 'NONE',  ( 0.7048096507298579061, 33.41730025321705710, 34.61049487267071356 ) ) ;
#57232=CARTESIAN_POINT ( 'NONE',  ( -2.569797478183783568, -14.55946937464482893, -1.464172661884112214 ) ) ;
#57241=CARTESIAN_POINT ( 'NONE',  ( -2.569797478183790229, 9.259773107243065127, -11.33042594333538666 ) ) ;
#57248=CARTESIAN_POINT ( 'NONE',  ( 0.6029303876144825880, -34.10953954078163974, 33.92442033626723941 ) ) ;
#57251=ORIENTED_EDGE ( 'NONE', *, *, #16280, .T. ) ;
#57255=CARTESIAN_POINT ( 'NONE',  ( 4.975801465491694664, -36.39623109580487892, 31.15993731089061924 ) ) ;
#57260=CARTESIAN_POINT ( 'NONE',  ( 0.1101816497532062955, 30.58948775778045004, 30.39741055095869982 ) ) ;
#57261=CARTESIAN_POINT ( 'NONE',  ( 0.1102847568649952675, -34.15672344772105617, 26.32556309315059551 ) ) ;
#57266=B_SPLINE_CURVE_WITH_KNOTS ( 'NONE', 3,
 ( #31566, #21863, #36589, #41004 ),
 .UNSPECIFIED., .F., .F.,
 ( 4, 4 ),
 ( 4.670885906470169924E-18, 0.004566006591234647236 ),
 .UNSPECIFIED. ) ;
#57268=CARTESIAN_POINT ( 'NONE',  ( 3.238741278300274029, -42.34697043723806331, -7.419593128523912284 ) ) ;
#57270=CARTESIAN_POINT ( 'NONE',  ( -4.908599999999998964, 1.224646799147353256E-15, -10.00000000000000000 ) ) ;
#57275=CARTESIAN_POINT ( 'NONE',  ( 1.827119703190780653, -42.50321986945174046, 6.838980420687256867 ) ) ;
#57279=CARTESIAN_POINT ( 'NONE',  ( -6.001507490154110336, -9.408444979392434959, 16.32705935667504349 ) ) ;
#57281=LINE ( 'NONE', #19419, #38248 ) ;
#57282=EDGE_CURVE ( 'NONE', #11449, #43871, #612, .T. ) ;
#57284=CIRCLE ( 'NONE', #3317, 47.91270532121795611 ) ;
#57286=B_SPLINE_CURVE_WITH_KNOTS ( 'NONE', 3,
 ( #25276, #58454, #24044, #15581, #47866, #58154 ),
 .UNSPECIFIED., .F., .F.,
 ( 4, 2, 4 ),
 ( 1.736958732247374613E-17, 0.0002293319059085089783, 0.0004586638118170005551 ),
 .UNSPECIFIED. ) ;
#57296=VECTOR ( 'NONE', #25367, 1000.000000000000114 ) ;
#57321=ORIENTED_EDGE ( 'NONE', *, *, #18929, .F. ) ;
#57324=CARTESIAN_POINT ( 'NONE',  ( 0.8751705887134423323, -13.30665218149394669, 46.21789262997734227 ) ) ;
#57326=EDGE_LOOP ( 'NONE', ( #56453, #57937 ) ) ;
#57339=B_SPLINE_CURVE_WITH_KNOTS ( 'NONE', 3,
 ( #29020, #47832, #28092, #48132, #27784, #14017 ),
 .UNSPECIFIED., .F., .F.,
 ( 4, 2, 4 ),
 ( 1.269611854458016711E-16, 0.0002450741128632354863, 0.0004901482257263440126 ),
 .UNSPECIFIED. ) ;
#57340=EDGE_LOOP ( 'NONE', ( #18, #53016, #21831, #51158 ) ) ;
#57341=FACE_OUTER_BOUND ( 'NONE', #61617, .T. ) ;
#57343=CARTESIAN_POINT ( 'NONE',  ( 0.8751705887134553219, -19.22545746485630502, -44.08562551107074512 ) ) ;
#57353=CARTESIAN_POINT ( 'NONE',  ( 0.6030672727741701600, 48.10738703097480595, 0.08725775308938291119 ) ) ;
#57354=EDGE_CURVE ( 'NONE', #30576, #29913, #58861, .T. ) ;
#57378=ORIENTED_EDGE ( 'NONE', *, *, #22659, .T. ) ;
#57381=VECTOR ( 'NONE', #31940, 1000.000000000000114 ) ;
#57382=CARTESIAN_POINT ( 'NONE',  ( 4.322998006666165516, -45.75942687572288037, -14.45630056002923780 ) ) ;
#57386=CARTESIAN_POINT ( 'NONE',  ( 0.6023142530420679819, -48.10676733004997629, 0.2618396477465863015 ) ) ;
#57388=VERTEX_POINT ( 'NONE', #47236 ) ;
#57396=CARTESIAN_POINT ( 'NONE',  ( 0.8751705887134423323, -13.30665218149394669, 46.21789262997734227 ) ) ;
#57399=CARTESIAN_POINT ( 'NONE',  ( 0.6023143664670691511, -12.70384782338121887, 46.39980466492338707 ) ) ;
#57402=B_SPLINE_CURVE_WITH_KNOTS ( 'NONE', 3,
 ( #5358, #33912, #34216, #10403 ),
 .UNSPECIFIED., .F., .F.,
 ( 4, 4 ),
 ( 0.000000000000000000, 0.004445488388166995118 ),
 .UNSPECIFIED. ) ;
#57403=ORIENTED_EDGE ( 'NONE', *, *, #59318, .T. ) ;
#57411=CARTESIAN_POINT ( 'NONE',  ( 0.2224561200757604607, 37.71651051365630281, -20.89867881469728772 ) ) ;
#57417=DIRECTION ( 'NONE',  ( 0.09835009131224552170, -0.9951218349151971232, 0.007732607185427432805 ) ) ;
#57423=CARTESIAN_POINT ( 'NONE',  ( 0.1073791018717578927, 16.95003405440313315, -39.65380858626198091 ) ) ;
#57424=ORIENTED_EDGE ( 'NONE', *, *, #40535, .F. ) ;
#57431=CARTESIAN_POINT ( 'NONE',  ( 0.1102144999581333024, 42.73889315046712056, 5.753800096706190637 ) ) ;
#57432=CARTESIAN_POINT ( 'NONE',  ( -5.995132425357893702, 18.84415457712583475, -0.008513469642872414228 ) ) ;
#57436=CARTESIAN_POINT ( 'NONE',  ( 3.238741278300275361, 27.59904135366535272, -32.96375560769470781 ) ) ;
#57437=CARTESIAN_POINT ( 'NONE',  ( 0.6023143664670691511, -46.39980466492352917, -12.70384782338073215 ) ) ;
#57442=ORIENTED_EDGE ( 'NONE', *, *, #5123, .T. ) ;
#57445=FACE_OUTER_BOUND ( 'NONE', #12239, .T. ) ;
#57449=CARTESIAN_POINT ( 'NONE',  ( 4.549368137175248350, 35.80950303116068056, 23.67244292351653101 ) ) ;
#57450=CARTESIAN_POINT ( 'NONE',  ( 0.8751705887134553219, -29.98056538504934210, -37.60752970653818039 ) ) ;
#57453=CARTESIAN_POINT ( 'NONE',  ( 0.2230388203127597058, 10.42432885623882122, -41.84042374003681886 ) ) ;
#57459=ORIENTED_EDGE ( 'NONE', *, *, #6313, .F. ) ;
#57465=CARTESIAN_POINT ( 'NONE',  ( 4.549368137175248350, 35.80950303116100741, -23.67244292351601942 ) ) ;
#57468=VECTOR ( 'NONE', #4684, 1000.000000000000000 ) ;
#57472=CARTESIAN_POINT ( 'NONE',  ( -6.017396004339686577, 17.40926186480779592, 7.209881890566617102 ) ) ;
#57473=CARTESIAN_POINT ( 'NONE',  ( 0.1101816497532063233, -37.41460501058200094, -21.44450189183855571 ) ) ;
#57478=CARTESIAN_POINT ( 'NONE',  ( -6.001507490154110336, 9.435425682280817128, 16.31148204059951112 ) ) ;
#57480=EDGE_CURVE ( 'NONE', #27859, #47737, #8690, .T. ) ;
#57483=CARTESIAN_POINT ( 'NONE',  ( -5.995132425357893702, 16.32377331145320554, 9.414704407577861645 ) ) ;
#57486=B_SPLINE_CURVE_WITH_KNOTS ( 'NONE', 3,
 ( #31509, #4828, #52151, #23969 ),
 .UNSPECIFIED., .F., .F.,
 ( 4, 4 ),
 ( 0.000000000000000000, 0.005014147105413699519 ),
 .UNSPECIFIED. ) ;
#57488=CARTESIAN_POINT ( 'NONE',  ( 0.6031356755773454870, -29.28597628606519976, -38.16618524502111853 ) ) ;
#57489=CARTESIAN_POINT ( 'NONE',  ( 4.691466044806102076, 20.01963481131660672, -39.84135254923116065 ) ) ;
#57490=CARTESIAN_POINT ( 'NONE',  ( 4.549368137175248350, 42.82045902618768451, 3.018832571116707442 ) ) ;
#57493=CARTESIAN_POINT ( 'NONE',  ( -6.001507490154111224, -2.444174634178017946, -18.68469198366099349 ) ) ;
#57500=DIRECTION ( 'NONE',  ( -0.9990097760809876215, 5.448601141171616265E-18, -0.04449120468828354769 ) ) ;
#57502=CARTESIAN_POINT ( 'NONE',  ( 3.680974057930773036, -27.71659654258268546, -39.15945827951701119 ) ) ;
#57514=CARTESIAN_POINT ( 'NONE',  ( -6.016104459813374383, -9.426230926598757165, 16.31603998697566738 ) ) ;
#57516=VERTEX_POINT ( 'NONE', #23117 ) ;
#57521=DIRECTION ( 'NONE',  ( 0.09835009131224564660, 0.5042575517176685063, -0.8579344853044291730 ) ) ;
#57531=ORIENTED_EDGE ( 'NONE', *, *, #9876, .F. ) ;
#57537=ADVANCED_FACE ( 'NONE', ( #47543 ), #17978, .F. ) ;
#57540=CARTESIAN_POINT ( 'NONE',  ( 0.6001305935487315502, -46.60388846085714931, -11.94532529598361847 ) ) ;
#57542=CARTESIAN_POINT ( 'NONE',  ( 0.8760168074887090262, 41.20610493656909767, -24.81951362746034917 ) ) ;
#57555=CARTESIAN_POINT ( 'NONE',  ( 0.6017666602106489515, -33.76944145963998523, 34.26316403931501497 ) ) ;
#57565=B_SPLINE_CURVE_WITH_KNOTS ( 'NONE', 3,
 ( #29443, #51196, #27098, #60906, #3887, #42157 ),
 .UNSPECIFIED., .F., .F.,
 ( 4, 2, 4 ),
 ( 1.266794085606387986E-16, 0.0002450741128632359200, 0.0004901482257263450968 ),
 .UNSPECIFIED. ) ;
#57566=ORIENTED_EDGE ( 'NONE', *, *, #32118, .F. ) ;
#57568=CARTESIAN_POINT ( 'NONE',  ( 0.5998501479064699549, 6.798102206413494386, 47.62484632993690781 ) ) ;
#57573=CARTESIAN_POINT ( 'NONE',  ( 0.6009452777970412107, 12.87217382175429137, 46.35353542372327951 ) ) ;
#57602=VECTOR ( 'NONE', #30960, 1000.000000000000227 ) ;
#57606=CARTESIAN_POINT ( 'NONE',  ( 0.5998501479064708430, -44.64337787626261189, 17.92509395669028649 ) ) ;
#57612=B_SPLINE_CURVE_WITH_KNOTS ( 'NONE', 3,
 ( #12151, #31231, #50330, #7400, #47500, #52178 ),
 .UNSPECIFIED., .F., .F.,
 ( 4, 2, 4 ),
 ( 1.823789517034659149E-17, 0.0002293319059085092764, 0.0004586638118170002841 ),
 .UNSPECIFIED. ) ;
#57616=ORIENTED_EDGE ( 'NONE', *, *, #54278, .T. ) ;
#57618=CARTESIAN_POINT ( 'NONE',  ( 0.3622758884714730732, 40.13994584881760375, 15.73321244754868964 ) ) ;
#57628=CARTESIAN_POINT ( 'NONE',  ( -2.569797478183783568, 11.87678401312183141, 8.547745408040835713 ) ) ;
#57630=CARTESIAN_POINT ( 'NONE',  ( 0.6041374136657475802, -23.90252055111294283, -41.74951251761564919 ) ) ;
#57641=CARTESIAN_POINT ( 'NONE',  ( -6.017396004339687465, -18.68180398134248676, -2.460690056887981925 ) ) ;
#57643=VECTOR ( 'NONE', #29315, 999.9999999999998863 ) ;
#57649=CARTESIAN_POINT ( 'NONE',  ( -6.015611763856276717, -18.84324252354755203, 0.006214430185075541652 ) ) ;
#57651=FACE_OUTER_BOUND ( 'NONE', #51768, .T. ) ;
#57652=CARTESIAN_POINT ( 'NONE',  ( 3.238741278300274473, 7.419593128524060610, -42.34697043723804200 ) ) ;
#57664=EDGE_CURVE ( 'NONE', #55047, #15365, #41862, .T. ) ;
#57665=ADVANCED_FACE ( 'NONE', ( #35616 ), #3130, .F. ) ;
#57680=EDGE_CURVE ( 'NONE', #26613, #55183, #35779, .T. ) ;
#57687=ORIENTED_EDGE ( 'NONE', *, *, #12532, .F. ) ;
#57691=CARTESIAN_POINT ( 'NONE',  ( 0.8751705887134423323, 47.79200036674280483, -5.393078191592203474 ) ) ;
#57701=CARTESIAN_POINT ( 'NONE',  ( 0.7048096507298579061, -38.67623024744067095, 28.61383451045632853 ) ) ;
#57703=CARTESIAN_POINT ( 'NONE',  ( -6.001507490154110336, 17.40350523682705486, -7.225628667346390976 ) ) ;
#57727=CARTESIAN_POINT ( 'NONE',  ( 4.549368137175248350, 38.40568845698250300, 19.17571786012337753 ) ) ;
#57729=CARTESIAN_POINT ( 'NONE',  ( 3.680882792899937694, -30.65151321162973730, -36.90742604464114152 ) ) ;
#57732=VECTOR ( 'NONE', #52480, 1000.000000000000114 ) ;
#57733=CARTESIAN_POINT ( 'NONE',  ( 0.6023143664670691511, -18.16777128831361665, -44.54505257464852264 ) ) ;
#57740=CARTESIAN_POINT ( 'NONE',  ( 0.1092355843206037486, -34.02913268098572530, -26.49036028133769705 ) ) ;
#57745=CARTESIAN_POINT ( 'NONE',  ( 0.6031357023905874470, -46.47951061918818993, 12.40899271757757916 ) ) ;
#57751=EDGE_CURVE ( 'NONE', #9105, #16525, #39488, .T. ) ;
#57757=CARTESIAN_POINT ( 'NONE',  ( 0.3622758884714600280, -37.74294673546600620, 20.83792692158906235 ) ) ;
#57763=CARTESIAN_POINT ( 'NONE',  ( 0.1073791018717578927, -30.14884492832369745, -30.83464511437127697 ) ) ;
#57769=DIRECTION ( 'NONE',  ( 0.09835009131224552170, -0.6119264800004727833, -0.7847759187265520575 ) ) ;
#57783=VERTEX_POINT ( 'NONE', #8937 ) ;
#57785=CARTESIAN_POINT ( 'NONE',  ( 0.1313383488274140198, 37.66088038379816538, 21.00709374781555283 ) ) ;
#57786=CARTESIAN_POINT ( 'NONE',  ( 0.7048096507298579061, -23.32077812596851629, -42.08020459959973181 ) ) ;
#57788=ORIENTED_EDGE ( 'NONE', *, *, #61535, .T. ) ;
#57792=CARTESIAN_POINT ( 'NONE',  ( 0.1087620492084206830, -37.16461718700651318, -21.87505161834403822 ) ) ;
#57798=ORIENTED_EDGE ( 'NONE', *, *, #774, .F. ) ;
#57799=CARTESIAN_POINT ( 'NONE',  ( -5.995132425357893702, -18.20425902871264512, -4.869002713216763034 ) ) ;
#57802=ORIENTED_EDGE ( 'NONE', *, *, #53388, .F. ) ;
#57803=CARTESIAN_POINT ( 'NONE',  ( 0.6041374136657476912, 12.28249295042045475, -46.51335992032606725 ) ) ;
#57804=CARTESIAN_POINT ( 'NONE',  ( 0.6029303876144825880, -47.71279573267363361, 6.149480157545783143 ) ) ;
#57809=DIRECTION ( 'NONE',  ( -1.000000000000000000, -0.000000000000000000, -0.000000000000000000 ) ) ;
#57810=CARTESIAN_POINT ( 'NONE',  ( 4.549368137175248350, 0.000000000000000000, 0.000000000000000000 ) ) ;
#57811=CARTESIAN_POINT ( 'NONE',  ( 4.549368137175248350, -8.582197505784124658, -42.06008734272393212 ) ) ;
#57817=EDGE_LOOP ( 'NONE', ( #19294, #34939, #267, #33877 ) ) ;
#57830=VECTOR ( 'NONE', #28678, 1000.000000000000114 ) ;
#57833=DIRECTION ( 'NONE',  ( 0.000000000000000000, 0.000000000000000000, 1.000000000000000000 ) ) ;
#57844=VERTEX_POINT ( 'NONE', #6661 ) ;
#57849=CARTESIAN_POINT ( 'NONE',  ( 0.2230388203127620650, -10.42432885623912320, 41.84042374003679043 ) ) ;
#57858=CARTESIAN_POINT ( 'NONE',  ( -6.016489644550736315, -13.32727118274428513, -13.32104266208113152 ) ) ;
#57859=DIRECTION ( 'NONE',  ( 0.000000000000000000, 0.000000000000000000, 1.000000000000000000 ) ) ;
#57868=CARTESIAN_POINT ( 'NONE',  ( 4.549368137175248350, -35.80950303116117794, 23.67244292351576718 ) ) ;
#57871=ORIENTED_EDGE ( 'NONE', *, *, #39428, .F. ) ;
#57874=AXIS2_PLACEMENT_3D ( 'NONE', #56152, #51758, #38015 ) ;
#57876=B_SPLINE_CURVE_WITH_KNOTS ( 'NONE', 3,
 ( #61293, #37530, #12564, #50447, #36998, #32276 ),
 .UNSPECIFIED., .F., .F.,
 ( 4, 2, 4 ),
 ( 1.267602517345562747E-16, 0.0002450741128632351611, 0.0004901482257263435789 ),
 .UNSPECIFIED. ) ;
#57896=DIRECTION ( 'NONE',  ( 0.09835009131224552170, 0.2650256080583628382, 0.9592125346408729714 ) ) ;
#57897=CARTESIAN_POINT ( 'NONE',  ( 2.301529144917014769, 43.86846428170459689, -19.56451384728999088 ) ) ;
#57900=( BOUNDED_SURFACE ( )  B_SPLINE_SURFACE ( 3, 1, ( 
 ( #24164, #34204 ),
 ( #4411, #658 ),
 ( #18551, #14787 ),
 ( #14177, #23548 ) ),
 .UNSPECIFIED., .F., .F., .F. ) 
 B_SPLINE_SURFACE_WITH_KNOTS ( ( 4, 4 ),
 ( 2, 2 ),
 ( 0.000000000000000000, 1.000000000000000000 ),
 ( 0.000000000000000000, 1.000000000000000000 ),
 .UNSPECIFIED. ) 
 GEOMETRIC_REPRESENTATION_ITEM ( )  RATIONAL_B_SPLINE_SURFACE ( (
 ( 1.000000000000000000, 1.000000000000000000),
 ( 0.9953040768229005630, 0.8617119497784937465),
 ( 0.9953040768229005630, 0.8617119497784937465),
 ( 1.000000000000000000, 1.000000000000000000) ) ) 
 REPRESENTATION_ITEM ( '' )  SURFACE ( )  );
#57901=CARTESIAN_POINT ( 'NONE',  ( -6.016489644550736315, 2.455165042130005304, -18.68257207665193675 ) ) ;
#57906=CARTESIAN_POINT ( 'NONE',  ( 0.3622758884714730732, 0.8252992914322084816, 43.10531414739106282 ) ) ;
#57907=EDGE_CURVE ( 'NONE', #52728, #40342, #8061, .T. ) ;
#57914=CARTESIAN_POINT ( 'NONE',  ( 3.238741278300275361, 3.793425828152074519, 42.82436441900174628 ) ) ;
#57917=DIRECTION ( 'NONE',  ( -1.000000000000000000, -0.000000000000000000, -0.000000000000000000 ) ) ;
#57918=VERTEX_POINT ( 'NONE', #22343 ) ;
#57934=LINE ( 'NONE', #939, #57296 ) ;
#57935=ORIENTED_EDGE ( 'NONE', *, *, #37708, .F. ) ;
#57937=ORIENTED_EDGE ( 'NONE', *, *, #18929, .T. ) ;
#57944=CARTESIAN_POINT ( 'NONE',  ( 4.975801465491694664, 45.18341283946434572, 15.94009207553066787 ) ) ;
#57947=CARTESIAN_POINT ( 'NONE',  ( 4.975801465491694664, 39.51822597168457918, 27.09127437476394817 ) ) ;
#57952=CARTESIAN_POINT ( 'NONE',  ( 2.301430502907645170, 38.87758534782506814, -28.20897229937363093 ) ) ;
#57956=CARTESIAN_POINT ( 'NONE',  ( -6.015611763856276717, 18.20278301740936655, 4.870987357968240339 ) ) ;
#57958=ORIENTED_EDGE ( 'NONE', *, *, #1180, .T. ) ;
#57959=CARTESIAN_POINT ( 'NONE',  ( 0.8760168074886965917, 13.30888447662080942, -46.22580377597773094 ) ) ;
#57961=EDGE_CURVE ( 'NONE', #58675, #24495, #5813, .T. ) ;
#57967=CARTESIAN_POINT ( 'NONE',  ( 4.975801465491694664, 14.85979367497109571, 45.55012473237758996 ) ) ;
#57974=CARTESIAN_POINT ( 'NONE',  ( 0.2230388203127596225, 6.380812898000993272, 42.64472907182732797 ) ) ;
#57976=DIRECTION ( 'NONE',  ( 0.09835009131224566048, 0.9951218349151971232, 0.007732607185434067255 ) ) ;
#57978=CARTESIAN_POINT ( 'NONE',  ( 0.5988103622719990193, -41.96244039798807535, 23.52668907282270894 ) ) ;
#57979=CARTESIAN_POINT ( 'NONE',  ( 0.6031356219577718170, 48.10744328000515679, -0.08729769678260468346 ) ) ;
#57989=CARTESIAN_POINT ( 'NONE',  ( 0.6001305935487422083, 23.60027211631829047, -41.92422178329146476 ) ) ;
#57994=ORIENTED_EDGE ( 'NONE', *, *, #42455, .F. ) ;
#57997=CARTESIAN_POINT ( 'NONE',  ( -6.001507490154111224, 4.862106078787924446, 18.20581304543299339 ) ) ;
#58001=ORIENTED_EDGE ( 'NONE', *, *, #10726, .T. ) ;
#58019=CARTESIAN_POINT ( 'NONE',  ( 4.833616638992205949, 20.04871863793747622, 41.67905425467714053 ) ) ;
#58024=ADVANCED_FACE ( 'NONE', ( #61451 ), #43974, .F. ) ;
#58028=EDGE_LOOP ( 'NONE', ( #31876, #49307, #12917, #56237 ) ) ;
#58031=EDGE_CURVE ( 'NONE', #22299, #45571, #47541, .T. ) ;
#58032=CARTESIAN_POINT ( 'NONE',  ( -2.708315649062916552, -10.16016146078295890, 10.53288422393038992 ) ) ;
#58035=ORIENTED_EDGE ( 'NONE', *, *, #51096, .F. ) ;
#58038=CARTESIAN_POINT ( 'NONE',  ( -6.016761891674565099, 7.207804629151311815, 17.41015286184805078 ) ) ;
#58043=DIRECTION ( 'NONE',  ( 0.000000000000000000, 0.000000000000000000, -1.000000000000000000 ) ) ;
#58045=CARTESIAN_POINT ( 'NONE',  ( 0.1100247026804066219, 30.61332956994582233, -30.37337782329859692 ) ) ;
#58049=B_SPLINE_CURVE_WITH_KNOTS ( 'NONE', 3,
 ( #51581, #27797, #4890, #24023 ),
 .UNSPECIFIED., .F., .F.,
 ( 4, 4 ),
 ( 5.818439421673296370E-18, 0.004566006591234647236 ),
 .UNSPECIFIED. ) ;
#58054=CARTESIAN_POINT ( 'NONE',  ( 4.975801465491694664, -42.71626295676247764, -21.70134120755185947 ) ) ;
#58059=CARTESIAN_POINT ( 'NONE',  ( 4.833616638992205949, -45.27110352095240131, -9.466882727841984035 ) ) ;
#58065=CARTESIAN_POINT ( 'NONE',  ( 0.3622758884714600280, 42.62881903538200845, 6.444611261694737081 ) ) ;
#58071=CARTESIAN_POINT ( 'NONE',  ( 4.549368137175248350, -32.41327393324159800, 28.14399996863441800 ) ) ;
#58080=CARTESIAN_POINT ( 'NONE',  ( 0.6029303876144825880, -23.94027529185524017, -41.72757124235813819 ) ) ;
#58081=CARTESIAN_POINT ( 'NONE',  ( 5.880360259849739535, -31.59460303416009808, 36.09847387447805289 ) ) ;
#58083=CARTESIAN_POINT ( 'NONE',  ( 2.643462169533613793, 13.76277278785496350, 46.02269433264237364 ) ) ;
#58086=CARTESIAN_POINT ( 'NONE',  ( 0.5998501479064699549, -5.759754759341138453, 47.76154736470748219 ) ) ;
#58093=CARTESIAN_POINT ( 'NONE',  ( -2.708315649062910779, 8.698422600176970221, 11.76894112707814877 ) ) ;
#58094=CARTESIAN_POINT ( 'NONE',  ( -2.708315649062916552, 7.087851317223962333, -12.80362818457438578 ) ) ;
#58098=ORIENTED_EDGE ( 'NONE', *, *, #6670, .F. ) ;
#58109=CARTESIAN_POINT ( 'NONE',  ( 0.5998501479064699549, 48.10473956285920138, -0.5236536531309904374 ) ) ;
#58114=EDGE_CURVE ( 'NONE', #51844, #10899, #4328, .T. ) ;
#58115=CARTESIAN_POINT ( 'NONE',  ( 0.6031356219577719280, -47.68448279784259114, 6.365832241665767555 ) ) ;
#58132=CARTESIAN_POINT ( 'NONE',  ( -6.015611763856276717, -7.216738110653151850, -17.40650793417851361 ) ) ;
#58134=CARTESIAN_POINT ( 'NONE',  ( 0.6029303876144825880, 38.24575311130000443, -29.18200390284009060 ) ) ;
#58136=CARTESIAN_POINT ( 'NONE',  ( 4.975801465491694664, 32.01766832630313075, -35.64402118370923489 ) ) ;
#58139=CARTESIAN_POINT ( 'NONE',  ( 3.238931869106855377, -38.11291514434428507, -19.89273896137469677 ) ) ;
#58144=CARTESIAN_POINT ( 'NONE',  ( 0.1084644655670281288, 16.86976209534724092, 39.68806829486954513 ) ) ;
#58150=AXIS2_PLACEMENT_3D ( 'NONE', #23397, #57809, #14630 ) ;
#58154=CARTESIAN_POINT ( 'NONE',  ( 0.3622758884714600280, -4.808133778521581192, -42.84426538328729350 ) ) ;
#58167=VERTEX_POINT ( 'NONE', #35773 ) ;
#58174=CARTESIAN_POINT ( 'NONE',  ( -6.017396004339686577, -17.40836349643172198, 7.212050743684117471 ) ) ;
#58187=ORIENTED_EDGE ( 'NONE', *, *, #18770, .T. ) ;
#58190=CARTESIAN_POINT ( 'NONE',  ( 4.975801465491695552, -15.94009207553018648, -45.18341283946452336 ) ) ;
#58198=CARTESIAN_POINT ( 'NONE',  ( 0.1103878639767399555, 30.52789484587411550, 30.45925431905124015 ) ) ;
#58200=CARTESIAN_POINT ( 'NONE',  ( -6.016761891674565099, 14.95139917749719949, -11.46828378093544210 ) ) ;
#58206=CARTESIAN_POINT ( 'NONE',  ( -6.010958268070873523, -17.41463273278773372, -7.197664668556627454 ) ) ;
#58214=CARTESIAN_POINT ( 'NONE',  ( 4.549368137175248350, -35.80950303116083688, -23.67244292351627521 ) ) ;
#58230=CARTESIAN_POINT ( 'NONE',  ( 4.833616638992205949, -43.93936707042109902, 14.43699082351635532 ) ) ;
#58232=EDGE_LOOP ( 'NONE', ( #37645, #32168, #50505, #20920 ) ) ;
#58233=CARTESIAN_POINT ( 'NONE',  ( 0.1064266418746773052, -17.02047513535257295, 39.62374465289867942 ) ) ;
#58234=EDGE_LOOP ( 'NONE', ( #47318, #55121, #6164, #39567 ) ) ;
#58236=VERTEX_POINT ( 'NONE', #50461 ) ;
#58247=ADVANCED_FACE ( 'NONE', ( #7529 ), #41218, .F. ) ;
#58253=VERTEX_POINT ( 'NONE', #21654 ) ;
#58264=ORIENTED_EDGE ( 'NONE', *, *, #17089, .F. ) ;
#58267=CARTESIAN_POINT ( 'NONE',  ( 0.6254311100348650676, 13.11433105842141345, -46.28443883864382968 ) ) ;
#58275=CARTESIAN_POINT ( 'NONE',  ( 0.8760168074887090262, -38.69913431881803945, -28.57146030081966614 ) ) ;
#58277=B_SPLINE_CURVE_WITH_KNOTS ( 'NONE', 3,
 ( #5330, #24459, #57952, #48572 ),
 .UNSPECIFIED., .F., .F.,
 ( 4, 4 ),
 ( 0.000000000000000000, 0.004445488388166994251 ),
 .UNSPECIFIED. ) ;
#58280=CARTESIAN_POINT ( 'NONE',  ( 0.6001305935487315502, -23.60027211631858535, 41.92422178329128712 ) ) ;
#58283=CARTESIAN_POINT ( 'NONE',  ( -2.708315649062910779, 10.16016146078274573, 10.53288422393059243 ) ) ;
#58295=VERTEX_POINT ( 'NONE', #46711 ) ;
#58305=CARTESIAN_POINT ( 'NONE',  ( 0.5998501479064699549, -28.86886762351154090, 38.48283596221978797 ) ) ;
#58307=AXIS2_PLACEMENT_3D ( 'NONE', #40954, #25893, #12424 ) ;
#58314=ORIENTED_EDGE ( 'NONE', *, *, #4918, .F. ) ;
#58317=CARTESIAN_POINT ( 'NONE',  ( 0.1098349054025746507, -30.64407294528969672, 30.34240357440782887 ) ) ;
#58322=ORIENTED_EDGE ( 'NONE', *, *, #60609, .T. ) ;
#58324=CARTESIAN_POINT ( 'NONE',  ( -6.001507490154110336, 0.01557731607553304240, 18.84387066167321478 ) ) ;
#58326=CARTESIAN_POINT ( 'NONE',  ( -2.569797478183790229, -10.02484965418634033, -10.65947181927836063 ) ) ;
#58334=ORIENTED_EDGE ( 'NONE', *, *, #55460, .F. ) ;
#58336=DIRECTION ( 'NONE',  ( 1.000000000000000000, 0.000000000000000000, 0.000000000000000000 ) ) ;
#58338=ADVANCED_FACE ( 'NONE', ( #5899 ), #9536, .F. ) ;
#58340=B_SPLINE_CURVE_WITH_KNOTS ( 'NONE', 3,
 ( #15471, #43692, #53644, #9522 ),
 .UNSPECIFIED., .F., .F.,
 ( 4, 4 ),
 ( 0.000000000000000000, 0.005014147105413706458 ),
 .UNSPECIFIED. ) ;
#58343=DIRECTION ( 'NONE',  ( 0.1024043820194936311, 0.1167898032637338518, -0.9878630899050858671 ) ) ;
#58344=CARTESIAN_POINT ( 'NONE',  ( 4.975801465491695552, 0.000000000000000000, 0.000000000000000000 ) ) ;
#58346=CARTESIAN_POINT ( 'NONE',  ( 0.1103744047535531458, 30.52096488484627201, -30.46616790811190256 ) ) ;
#58347=CARTESIAN_POINT ( 'NONE',  ( 0.6017666602106490625, -5.933006478841043929, 47.74032907933387548 ) ) ;
#58355=CARTESIAN_POINT ( 'NONE',  ( 0.6031357023905875581, -24.09149424676645168, 41.64046004335374818 ) ) ;
#58368=CARTESIAN_POINT ( 'NONE',  ( 0.1100247026804066219, -43.12411436000287779, -0.1696715072115837497 ) ) ;
#58369=CARTESIAN_POINT ( 'NONE',  ( 0.5998501479064699549, -48.10473956285919428, 0.5236536531313263909 ) ) ;
#58372=VERTEX_POINT ( 'NONE', #39167 ) ;
#58382=CARTESIAN_POINT ( 'NONE',  ( 0.6041374136657476912, 46.42299778158155732, -12.61972904329552847 ) ) ;
#58385=CARTESIAN_POINT ( 'NONE',  ( 0.7954190325252783467, -46.22745637125051132, 13.28627193046288468 ) ) ;
#58393=CARTESIAN_POINT ( 'NONE',  ( 4.833616638992205949, 2.572717262757331813, 46.17873762321152498 ) ) ;
#58394=FACE_OUTER_BOUND ( 'NONE', #47969, .T. ) ;
#58397=CARTESIAN_POINT ( 'NONE',  ( 0.1103936448916665869, 5.228610780659758526E-15, -43.12443171339897674 ) ) ;
#58408=ORIENTED_EDGE ( 'NONE', *, *, #45718, .T. ) ;
#58412=CARTESIAN_POINT ( 'NONE',  ( -6.015611763856276717, 9.427003116184170750, 16.31561949997079353 ) ) ;
#58416=FACE_OUTER_BOUND ( 'NONE', #51900, .T. ) ;
#58420=CARTESIAN_POINT ( 'NONE',  ( -6.015611763856276717, 18.84324252354755203, 0.006214430185208092740 ) ) ;
#58429=VERTEX_POINT ( 'NONE', #40109 ) ;
#58435=CARTESIAN_POINT ( 'NONE',  ( 0.6023142530420679819, 38.00626667377522239, -29.49327578399148209 ) ) ;
#58437=( BOUNDED_SURFACE ( )  B_SPLINE_SURFACE ( 3, 1, ( 
 ( #14632, #42524 ),
 ( #57493, #14021 ),
 ( #52820, #13707 ),
 ( #43143, #28711 ) ),
 .UNSPECIFIED., .F., .F., .F. ) 
 B_SPLINE_SURFACE_WITH_KNOTS ( ( 4, 4 ),
 ( 2, 2 ),
 ( 0.000000000000000000, 1.000000000000000000 ),
 ( 0.000000000000000000, 1.000000000000000000 ),
 .UNSPECIFIED. ) 
 GEOMETRIC_REPRESENTATION_ITEM ( )  RATIONAL_B_SPLINE_SURFACE ( (
 ( 1.000000000000000000, 1.000000000000000000),
 ( 0.7223157951917476005, 0.9931996967497186413),
 ( 0.7223157951917476005, 0.9931996967497186413),
 ( 1.000000000000000000, 1.000000000000000000) ) ) 
 REPRESENTATION_ITEM ( '' )  SURFACE ( )  );
#58441=ORIENTED_EDGE ( 'NONE', *, *, #51394, .F. ) ;
#58442=ORIENTED_EDGE ( 'NONE', *, *, #8249, .F. ) ;
#58454=CARTESIAN_POINT ( 'NONE',  ( 0.1064266418746776105, -5.071708474752946394, -42.82540703015429528 ) ) ;
#58457=EDGE_CURVE ( 'NONE', #50198, #59362, #51610, .T. ) ;
#58461=CARTESIAN_POINT ( 'NONE',  ( 0.2885700199627528884, 36.93108631019295274, -22.25146206940426907 ) ) ;
#58466=ORIENTED_EDGE ( 'NONE', *, *, #9034, .T. ) ;
#58479=CARTESIAN_POINT ( 'NONE',  ( 0.2885700199627524998, 20.85752789928062612, -37.73587457854645777 ) ) ;
#58481=ORIENTED_EDGE ( 'NONE', *, *, #46258, .F. ) ;
#58483=VERTEX_POINT ( 'NONE', #19594 ) ;
#58490=DIRECTION ( 'NONE',  ( 0.000000000000000000, 0.000000000000000000, -1.000000000000000000 ) ) ;
#58495=DIRECTION ( 'NONE',  ( 0.09835009131224567436, 0.1375559175655290955, -0.9855991218957017574 ) ) ;
#58496=CARTESIAN_POINT ( 'NONE',  ( 2.301529144917015213, 40.93948199333333093, -25.12312032040467003 ) ) ;
#58500=CARTESIAN_POINT ( 'NONE',  ( 0.6001305935487422083, -38.48510059944066342, 28.87057754790874142 ) ) ;
#58511=CARTESIAN_POINT ( 'NONE',  ( 3.680974057930773924, -36.90739001595152047, -30.65154904503166122 ) ) ;
#58519=DIRECTION ( 'NONE',  ( -1.000000000000000000, -0.000000000000000000, -0.000000000000000000 ) ) ;
#58522=DIRECTION ( 'NONE',  ( 0.09835009131224566048, -0.7941905447268856610, 0.5996571005210273864 ) ) ;
#58528=( BOUNDED_SURFACE ( )  B_SPLINE_SURFACE ( 3, 1, ( 
 ( #11147, #44373 ),
 ( #33729, #34960 ),
 ( #24306, #9910 ),
 ( #25535, #43442 ) ),
 .UNSPECIFIED., .F., .F., .F. ) 
 B_SPLINE_SURFACE_WITH_KNOTS ( ( 4, 4 ),
 ( 2, 2 ),
 ( 0.000000000000000000, 1.000000000000000000 ),
 ( 0.000000000000000000, 1.000000000000000000 ),
 .UNSPECIFIED. ) 
 GEOMETRIC_REPRESENTATION_ITEM ( )  RATIONAL_B_SPLINE_SURFACE ( (
 ( 1.000000000000000000, 1.000000000000000000),
 ( 0.9953040768229005630, 0.8617119497784937465),
 ( 0.9953040768229005630, 0.8617119497784937465),
 ( 1.000000000000000000, 1.000000000000000000) ) ) 
 REPRESENTATION_ITEM ( '' )  SURFACE ( )  );
#58530=CARTESIAN_POINT ( 'NONE',  ( -6.017396004339686577, -4.878103249820940235, -18.20079405513554960 ) ) ;
#58532=CARTESIAN_POINT ( 'NONE',  ( 0.5988103564986357874, -23.52668867203678715, 41.96244062389610008 ) ) ;
#58534=VERTEX_POINT ( 'NONE', #59317 ) ;
#58546=DIRECTION ( 'NONE',  ( 0.000000000000000000, 0.000000000000000000, 1.000000000000000000 ) ) ;
#58554=CIRCLE ( 'NONE', #32571, 42.92674063221959813 ) ;
#58555=VERTEX_POINT ( 'NONE', #15199 ) ;
#58562=CARTESIAN_POINT ( 'NONE',  ( 0.6009453534118438522, 44.27682103112805123, 18.81239552213000010 ) ) ;
#58570=EDGE_CURVE ( 'NONE', #24298, #49021, #23011, .T. ) ;
#58572=EDGE_LOOP ( 'NONE', ( #34797, #784, #45672, #51637 ) ) ;
#58573=CARTESIAN_POINT ( 'NONE',  ( 0.6001305935487315502, 12.95698906763810676, -46.33281397023051085 ) ) ;
#58579=CARTESIAN_POINT ( 'NONE',  ( -2.708315649062916552, -14.63219292706382824, 0.2635547933243125862 ) ) ;
#58580=B_SPLINE_CURVE_WITH_KNOTS ( 'NONE', 3,
 ( #4566, #56892, #57188, #37841, #18400, #61587, #9291, #18708, #33123, #28398, #47519, #14324, #19324, #33431, #52506, #9595, #24015, #179, #53717 ),
 .UNSPECIFIED., .F., .F.,
 ( 4, 3, 3, 3, 3, 3, 4 ),
 ( 1.153344816771540786E-16, 0.0002618519381806248868, 0.0003927759815485954873, 0.0005237000248299407195, 0.0006546240681324947894, 0.0007855481115631294566, 0.0009699050456655082314 ),
 .UNSPECIFIED. ) ;
#58586=CARTESIAN_POINT ( 'NONE',  ( 4.975801465491695552, -15.94009207553018648, -45.18341283946452336 ) ) ;
#58593=ADVANCED_FACE ( 'NONE', ( #30201 ), #1112, .F. ) ;
#58598=ORIENTED_EDGE ( 'NONE', *, *, #12343, .T. ) ;
#58602=CARTESIAN_POINT ( 'NONE',  ( 0.8751705887134423323, 28.56654290188602019, 38.69254731947842885 ) ) ;
#58607=( BOUNDED_SURFACE ( )  B_SPLINE_SURFACE ( 3, 1, ( 
 ( #54906, #40546 ),
 ( #50222, #26411 ),
 ( #59926, #3514 ),
 ( #21719, #37078 ) ),
 .UNSPECIFIED., .F., .F., .F. ) 
 B_SPLINE_SURFACE_WITH_KNOTS ( ( 4, 4 ),
 ( 2, 2 ),
 ( 0.000000000000000000, 1.000000000000000000 ),
 ( 0.000000000000000000, 1.000000000000000000 ),
 .UNSPECIFIED. ) 
 GEOMETRIC_REPRESENTATION_ITEM ( )  RATIONAL_B_SPLINE_SURFACE ( (
 ( 1.000000000000000000, 1.000000000000000000),
 ( 0.9751682680413298332, 0.9999560080971552356),
 ( 0.9751682680413298332, 0.9999560080971552356),
 ( 1.000000000000000000, 1.000000000000000000) ) ) 
 REPRESENTATION_ITEM ( '' )  SURFACE ( )  );
#58608=VERTEX_POINT ( 'NONE', #2925 ) ;
#58609=ORIENTED_EDGE ( 'NONE', *, *, #34083, .F. ) ;
#58616=CARTESIAN_POINT ( 'NONE',  ( 0.1103310638050661596, 11.08182869403236381, 41.67627416617918357 ) ) ;
#58618=VERTEX_POINT ( 'NONE', #22665 ) ;
#58620=CARTESIAN_POINT ( 'NONE',  ( 0.1073791018717483448, -42.68962945260958008, 6.109314776651994627 ) ) ;
#58621=VERTEX_POINT ( 'NONE', #27056 ) ;
#58624=ORIENTED_EDGE ( 'NONE', *, *, #38427, .F. ) ;
#58628=CIRCLE ( 'NONE', #52653, 47.91270532121795611 ) ;
#58633=ORIENTED_EDGE ( 'NONE', *, *, #4093, .F. ) ;
#58634=CARTESIAN_POINT ( 'NONE',  ( 4.549368137175248350, 19.17571786012269541, 38.40568845698284406 ) ) ;
#58635=CARTESIAN_POINT ( 'NONE',  ( 0.1103310638050661596, 41.63362651001249759, 11.24099191367013617 ) ) ;
#58636=CARTESIAN_POINT ( 'NONE',  ( -5.995132425357893702, -16.31525984181026701, -9.429450169548125871 ) ) ;
#58639=CARTESIAN_POINT ( 'NONE',  ( 4.549368137175248350, -32.13400537129904677, -28.46244473166662559 ) ) ;
#58640=ORIENTED_EDGE ( 'NONE', *, *, #15565, .F. ) ;
#58649=DIRECTION ( 'NONE',  ( 0.000000000000000000, 0.000000000000000000, -1.000000000000000000 ) ) ;
#58651=FACE_OUTER_BOUND ( 'NONE', #9412, .T. ) ;
#58656=CARTESIAN_POINT ( 'NONE',  ( 0.3622758884714600280, 31.06363466427727360, -29.89648521331598729 ) ) ;
#58659=CARTESIAN_POINT ( 'NONE',  ( 0.6009452777970410997, -18.81240106508496979, -44.27681866781098563 ) ) ;
#58663=CARTESIAN_POINT ( 'NONE',  ( 2.643462169533600914, 37.25264019563373097, 30.32726672320812966 ) ) ;
#58670=AXIS2_PLACEMENT_3D ( 'NONE', #23321, #32107, #23622 ) ;
#58675=VERTEX_POINT ( 'NONE', #41177 ) ;
#58676=CARTESIAN_POINT ( 'NONE',  ( 0.1095718737110178143, -43.12372487139541732, -0.2569529612656323847 ) ) ;
#58685=CARTESIAN_POINT ( 'NONE',  ( 0.6023143664670691511, 6.019611522082684907, 47.72938193173974497 ) ) ;
#58691=CARTESIAN_POINT ( 'NONE',  ( -5.995132425357893702, -4.869002713216444178, -18.20425902871272683 ) ) ;
#58698=CARTESIAN_POINT ( 'NONE',  ( -6.016489644550736315, -7.206912786933415305, 17.41053539857196952 ) ) ;
#58700=ORIENTED_EDGE ( 'NONE', *, *, #61796, .T. ) ;
#58702=CARTESIAN_POINT ( 'NONE',  ( 2.643462169533613793, 25.20536747735722471, 40.89244134039119416 ) ) ;
#58706=CARTESIAN_POINT ( 'NONE',  ( 0.6031357023905875581, 46.45693331047441887, 12.49325238079554268 ) ) ;
#58708=ORIENTED_EDGE ( 'NONE', *, *, #7545, .T. ) ;
#58716=AXIS2_PLACEMENT_3D ( 'NONE', #53244, #25366, #618 ) ;
#58720=FACE_OUTER_BOUND ( 'NONE', #35771, .T. ) ;
#58721=EDGE_LOOP ( 'NONE', ( #45772, #22440, #59988, #20685 ) ) ;
#58723=CARTESIAN_POINT ( 'NONE',  ( 0.6001305935487315502, -41.92422178329186266, 23.60027211631755861 ) ) ;
#58724=CARTESIAN_POINT ( 'NONE',  ( 1.827119703190779765, 1.232688548475426193, 43.03226500438895386 ) ) ;
#58725=B_SPLINE_CURVE_WITH_KNOTS ( 'NONE', 3,
 ( #28560, #47683, #52669, #52981, #42, #19190, #38304, #57353, #14486, #48295, #57979, #9766, #47997, #5045, #43311, #344 ),
 .UNSPECIFIED., .F., .F.,
 ( 4, 3, 3, 3, 3, 4 ),
 ( 2.027574016683678720E-17, 0.0002618515315864419768, 0.0003927756766341985875, 0.0005236998216950574563, 0.0007855159896329904409, 0.001047349442285928304 ),
 .UNSPECIFIED. ) ;
#58727=CARTESIAN_POINT ( 'NONE',  ( 0.6041374136657476912, 18.24862627831534923, -44.51224464244982215 ) ) ;
#58732=CARTESIAN_POINT ( 'NONE',  ( 4.691466044806103852, 19.42108863068380842, -40.13652286047873474 ) ) ;
#58739=DIRECTION ( 'NONE',  ( 0.09835009131224563272, -0.9164135549743757103, -0.3879606369183604686 ) ) ;
#58740=FACE_OUTER_BOUND ( 'NONE', #60558, .T. ) ;
#58742=LINE ( 'NONE', #34064, #26105 ) ;
#58743=CARTESIAN_POINT ( 'NONE',  ( 0.6009452777970412107, 37.89911497740571633, -29.63106797105374568 ) ) ;
#58755=EDGE_CURVE ( 'NONE', #20011, #53671, #4218, .T. ) ;
#58760=ORIENTED_EDGE ( 'NONE', *, *, #57354, .T. ) ;
#58764=CARTESIAN_POINT ( 'NONE',  ( 0.1100247026804066219, -10.99745200874666651, -41.69861001364769493 ) ) ;
#58767=VERTEX_POINT ( 'NONE', #13899 ) ;
#58771=ORIENTED_EDGE ( 'NONE', *, *, #10922, .T. ) ;
#58773=EDGE_LOOP ( 'NONE', ( #7543, #40767, #42361, #2366 ) ) ;
#58776=CARTESIAN_POINT ( 'NONE',  ( 0.3622758884714600280, 29.89648521331588071, 31.06363466427737663 ) ) ;
#58779=CARTESIAN_POINT ( 'NONE',  ( 3.680882792899936362, -25.57189948075158270, -40.59250320379004506 ) ) ;
#58782=CARTESIAN_POINT ( 'NONE',  ( 0.1064266418746775550, 43.12102053154801240, 0.5615180042402182492 ) ) ;
#58786=DIRECTION ( 'NONE',  ( -1.000000000000000000, -0.000000000000000000, -0.000000000000000000 ) ) ;
#58789=VERTEX_POINT ( 'NONE', #28581 ) ;
#58803=DIRECTION ( 'NONE',  ( -0.1024043820194934507, 0.01315135725337230471, -0.9946559125373959365 ) ) ;
#58809=( BOUNDED_SURFACE ( )  B_SPLINE_SURFACE ( 3, 1, ( 
 ( #28469, #23467 ),
 ( #18789, #28784 ),
 ( #52270, #9365 ),
 ( #19400, #42915 ) ),
 .UNSPECIFIED., .F., .F., .F. ) 
 B_SPLINE_SURFACE_WITH_KNOTS ( ( 4, 4 ),
 ( 2, 2 ),
 ( 0.000000000000000000, 1.000000000000000000 ),
 ( 0.000000000000000000, 1.000000000000000000 ),
 .UNSPECIFIED. ) 
 GEOMETRIC_REPRESENTATION_ITEM ( )  RATIONAL_B_SPLINE_SURFACE ( (
 ( 1.000000000000000000, 1.000000000000000000),
 ( 0.9953040768229005630, 0.8617119497784937465),
 ( 0.9953040768229005630, 0.8617119497784937465),
 ( 1.000000000000000000, 1.000000000000000000) ) ) 
 REPRESENTATION_ITEM ( '' )  SURFACE ( )  );
#58813=CARTESIAN_POINT ( 'NONE',  ( 0.1073791018717483448, 25.86618856530710531, -34.50606437925521419 ) ) ;
#58815=CARTESIAN_POINT ( 'NONE',  ( 0.6041374136657476912, -38.05989626241449031, 29.42442150067134676 ) ) ;
#58826=CARTESIAN_POINT ( 'NONE',  ( 0.6041374136657476912, -41.57494627055160663, 24.20487816031449668 ) ) ;
#58836=CARTESIAN_POINT ( 'NONE',  ( 5.880360259849739535, 39.86101557989670852, -26.69116321728528973 ) ) ;
#58838=CARTESIAN_POINT ( 'NONE',  ( -5.995132425357893702, -18.19985213254575740, 4.885449473615266491 ) ) ;
#58839=DIRECTION ( 'NONE',  ( -1.000000000000000000, 0.000000000000000000, 0.000000000000000000 ) ) ;
#58840=CARTESIAN_POINT ( 'NONE',  ( 4.975801465491695552, -9.906103548667894998, -46.87746200127453022 ) ) ;
#58857=ADVANCED_FACE ( 'NONE', ( #53601 ), #47603, .F. ) ;
#58861=B_SPLINE_CURVE_WITH_KNOTS ( 'NONE', 3,
 ( #3669, #60371, #12810, #50986, #27193, #3359 ),
 .UNSPECIFIED., .F., .F.,
 ( 4, 2, 4 ),
 ( 1.764953265579307567E-18, 0.0002450742804987336341, 0.0004901485609974654250 ),
 .UNSPECIFIED. ) ;
#58862=VECTOR ( 'NONE', #59153, 1000.000000000000114 ) ;
#58866=ORIENTED_EDGE ( 'NONE', *, *, #11055, .T. ) ;
#58868=CARTESIAN_POINT ( 'NONE',  ( 0.7245667037590730608, 41.24129124474298180, -24.75815201345804084 ) ) ;
#58869=ORIENTED_EDGE ( 'NONE', *, *, #15910, .F. ) ;
#58879=CARTESIAN_POINT ( 'NONE',  ( 0.6023142530420679819, 24.28014345169111365, 41.53076277789750037 ) ) ;
#58882=ADVANCED_FACE ( 'NONE', ( #44263 ), #7138, .F. ) ;
#58892=CARTESIAN_POINT ( 'NONE',  ( 0.8751705887134553219, 5.393078191592700854, -47.79200036674274088 ) ) ;
#58901=EDGE_CURVE ( 'NONE', #20774, #58429, #21980, .T. ) ;
#58904=( NAMED_UNIT ( * ) PLANE_ANGLE_UNIT ( ) SI_UNIT ( $, .RADIAN. ) );
#58905=CARTESIAN_POINT ( 'NONE',  ( 0.8751705887134423323, 19.22545746485661766, -44.08562551107063143 ) ) ;
#58917=CARTESIAN_POINT ( 'NONE',  ( 0.7048096507298579061, 28.61383451045646353, 38.67623024744057858 ) ) ;
#58918=CONICAL_SURFACE ( 'NONE', #10933, 42.92674063221959813, 1.485477209440487556 ) ;
#58925=CARTESIAN_POINT ( 'NONE',  ( 0.6041374136657476912, 23.90252055111321638, -41.74951251761550708 ) ) ;
#58926=VERTEX_POINT ( 'NONE', #12592 ) ;
#58927=CARTESIAN_POINT ( 'NONE',  ( 4.975801465491694664, -21.70134120755230711, 42.71626295676225027 ) ) ;
#58932=ORIENTED_EDGE ( 'NONE', *, *, #38288, .T. ) ;
#58935=ADVANCED_FACE ( 'NONE', ( #49858 ), #45982, .F. ) ;
#58937=VERTEX_POINT ( 'NONE', #52307 ) ;
#58952=AXIS2_PLACEMENT_3D ( 'NONE', #2387, #20593, #16509 ) ;
#58955=CARTESIAN_POINT ( 'NONE',  ( 0.3622758884714600280, 0.8252992914328071139, -43.10531414739104861 ) ) ;
#58960=CARTESIAN_POINT ( 'NONE',  ( -6.015611763856276717, -16.31561949997069405, -9.427003116184344833 ) ) ;
#58967=CARTESIAN_POINT ( 'NONE',  ( 0.5998501479064699549, -41.92175333043603302, -23.59887241503339439 ) ) ;
#58970=ORIENTED_EDGE ( 'NONE', *, *, #18167, .T. ) ;
#58974=CARTESIAN_POINT ( 'NONE',  ( 4.975801465491694664, 43.22084481528220579, -20.67815041659094888 ) ) ;
#58977=CARTESIAN_POINT ( 'NONE',  ( 0.1087620492084205998, 34.43219573047432647, -25.96440931622094439 ) ) ;
#58978=CARTESIAN_POINT ( 'NONE',  ( 0.1073791018717578927, -6.109314776653017809, 42.68962945260943087 ) ) ;
#58980=B_SPLINE_CURVE_WITH_KNOTS ( 'NONE', 3,
 ( #57906, #35692, #41023, #15955, #35069, #1828 ),
 .UNSPECIFIED., .F., .F.,
 ( 4, 2, 4 ),
 ( 8.560751122900633232E-17, 0.0002293366620881450389, 0.0004586733241762044801 ),
 .UNSPECIFIED. ) ;
#58982=DIRECTION ( 'NONE',  ( 0.000000000000000000, 0.000000000000000000, -1.000000000000000000 ) ) ;
#58987=LINE ( 'NONE', #2272, #49056 ) ;
#58989=CARTESIAN_POINT ( 'NONE',  ( 0.6017667736363748743, -46.55748817282783847, 12.11362382130055515 ) ) ;
#58993=CARTESIAN_POINT ( 'NONE',  ( 0.1103936448916665869, 5.228610780659758526E-15, -43.12443171339897674 ) ) ;
#59003=ORIENTED_EDGE ( 'NONE', *, *, #57142, .F. ) ;
#59007=CARTESIAN_POINT ( 'NONE',  ( 0.6027935024548037868, 6.106197519200845747, 47.71838037711336256 ) ) ;
#59010=ADVANCED_FACE ( 'NONE', ( #37024 ), #45599, .F. ) ;
#59011=CARTESIAN_POINT ( 'NONE',  ( 0.6023142530420679819, -24.28014345169140498, -41.53076277789733695 ) ) ;
#59015=ORIENTED_EDGE ( 'NONE', *, *, #40897, .F. ) ;
#59025=CARTESIAN_POINT ( 'NONE',  ( 0.7954190325252775695, 44.76287681188606626, 17.60078418395009336 ) ) ;
#59042=CARTESIAN_POINT ( 'NONE',  ( 3.238931869106854489, -19.89273896137509823, 38.11291514434407901 ) ) ;
#59045=CARTESIAN_POINT ( 'NONE',  ( -6.001507490154111224, 18.84387066167321478, 0.01557731607559981711 ) ) ;
#59049=CARTESIAN_POINT ( 'NONE',  ( 4.975801465491695552, 20.67815041659141784, -43.22084481528199973 ) ) ;
#59067=CARTESIAN_POINT ( 'NONE',  ( -5.995132425357893702, -7.203480333239202338, 17.41298668506968284 ) ) ;
#59069=ORIENTED_EDGE ( 'NONE', *, *, #30924, .F. ) ;
#59074=B_SPLINE_CURVE_WITH_KNOTS ( 'NONE', 3,
 ( #38697, #33993, #34598, #24887, #29882, #15187 ),
 .UNSPECIFIED., .F., .F.,
 ( 4, 2, 4 ),
 ( 1.764953265579307567E-18, 0.0002450742804987336341, 0.0004901485609974654250 ),
 .UNSPECIFIED. ) ;
#59075=ORIENTED_EDGE ( 'NONE', *, *, #58901, .F. ) ;
#59078=CARTESIAN_POINT ( 'NONE',  ( 0.6001305935487422083, 37.84751346122855864, -29.70149728382397569 ) ) ;
#59083=CARTESIAN_POINT ( 'NONE',  ( 0.1100053167205930493, -39.91014771056767074, -16.33707796615692587 ) ) ;
#59088=CARTESIAN_POINT ( 'NONE',  ( 0.7954190325252775695, -11.60747917225617165, 46.67728753507120842 ) ) ;
#59096=DIRECTION ( 'NONE',  ( 0.000000000000000000, 0.000000000000000000, 1.000000000000000000 ) ) ;
#59097=VERTEX_POINT ( 'NONE', #4672 ) ;
#59102=CARTESIAN_POINT ( 'NONE',  ( 4.549368137175248350, 0.000000000000000000, 0.000000000000000000 ) ) ;
#59103=CARTESIAN_POINT ( 'NONE',  ( 0.6030672727741701600, 44.47882233696923038, -18.32928433899707343 ) ) ;
#59105=CARTESIAN_POINT ( 'NONE',  ( 4.975801465491695552, -42.71626295676279028, 21.70134120755125906 ) ) ;
#59106=( BOUNDED_SURFACE ( )  B_SPLINE_SURFACE ( 3, 1, ( 
 ( #50635, #41581 ),
 ( #27772, #12772 ),
 ( #26847, #32799 ),
 ( #7725, #60045 ) ),
 .UNSPECIFIED., .F., .F., .F. ) 
 B_SPLINE_SURFACE_WITH_KNOTS ( ( 4, 4 ),
 ( 2, 2 ),
 ( 0.000000000000000000, 1.000000000000000000 ),
 ( 0.000000000000000000, 1.000000000000000000 ),
 .UNSPECIFIED. ) 
 GEOMETRIC_REPRESENTATION_ITEM ( )  RATIONAL_B_SPLINE_SURFACE ( (
 ( 1.000000000000000000, 1.000000000000000000),
 ( 0.9751682680413298332, 0.9999560080971552356),
 ( 0.9751682680413298332, 0.9999560080971552356),
 ( 1.000000000000000000, 1.000000000000000000) ) ) 
 REPRESENTATION_ITEM ( '' )  SURFACE ( )  );
#59119=B_SPLINE_CURVE_WITH_KNOTS ( 'NONE', 3,
 ( #40792, #26653, #21966, #46098, #60156, #8158 ),
 .UNSPECIFIED., .F., .F.,
 ( 4, 2, 4 ),
 ( 1.268664800107929448E-16, 0.0002450741128632350527, 0.0004901482257263432537 ),
 .UNSPECIFIED. ) ;
#59125=CARTESIAN_POINT ( 'NONE',  ( 0.1092565886968785704, -5.936467125236737807, -42.71401356099877233 ) ) ;
#59130=CARTESIAN_POINT ( 'NONE',  ( 3.680882792899938138, 14.19444521819966631, 45.82784180332843249 ) ) ;
#59136=B_SPLINE_CURVE_WITH_KNOTS ( 'NONE', 3,
 ( #51159, #46490, #12987, #8242 ),
 .UNSPECIFIED., .F., .F.,
 ( 4, 4 ),
 ( 2.069917718005272729E-17, 0.004444306975806117631 ),
 .UNSPECIFIED. ) ;
#59139=CARTESIAN_POINT ( 'NONE',  ( -2.708315649062910779, 14.47261168455366942, 2.171184472130732956 ) ) ;
#59143=CARTESIAN_POINT ( 'NONE',  ( 4.975801465491694664, 20.67815041659077835, 43.22084481528228395 ) ) ;
#59144=CARTESIAN_POINT ( 'NONE',  ( -6.016761891674565099, -18.20201388312099056, 4.873659902332302174 ) ) ;
#59151=ORIENTED_EDGE ( 'NONE', *, *, #44542, .F. ) ;
#59153=DIRECTION ( 'NONE',  ( 0.09835009131224567436, -0.9632152266566440524, 0.2500873580884542813 ) ) ;
#59156=CARTESIAN_POINT ( 'NONE',  ( 0.1100053167205930910, -41.60823192620016187, 11.33468317718483753 ) ) ;
#59158=EDGE_CURVE ( 'NONE', #2547, #11109, #49842, .T. ) ;
#59160=DIRECTION ( 'NONE',  ( 0.1024043820194936449, -0.3927886084231637098, -0.9139094329506617376 ) ) ;
#59169=ORIENTED_EDGE ( 'NONE', *, *, #5891, .T. ) ;
#59184=EDGE_CURVE ( 'NONE', #8307, #50661, #7458, .T. ) ;
#59190=FACE_OUTER_BOUND ( 'NONE', #12563, .T. ) ;
#59201=CARTESIAN_POINT ( 'NONE',  ( 0.5998501479064708430, 38.48283596222029956, -28.86886762351084812 ) ) ;
#59204=DIRECTION ( 'NONE',  ( 1.000000000000000000, 0.000000000000000000, 0.000000000000000000 ) ) ;
#59205=ORIENTED_EDGE ( 'NONE', *, *, #25338, .T. ) ;
#59206=FACE_OUTER_BOUND ( 'NONE', #9350, .T. ) ;
#59208=CARTESIAN_POINT ( 'NONE',  ( 1.827119703190779765, 31.30004882613801698, 29.55676396270195738 ) ) ;
#59220=CARTESIAN_POINT ( 'NONE',  ( 0.2885697896453111588, -0.8047882042609548758, 43.10898998017122352 ) ) ;
#59227=ORIENTED_EDGE ( 'NONE', *, *, #1822, .F. ) ;
#59232=CARTESIAN_POINT ( 'NONE',  ( 0.6017666602106489515, -12.78804974226068047, -46.37677619531707762 ) ) ;
#59234=ORIENTED_EDGE ( 'NONE', *, *, #61962, .F. ) ;
#59235=CARTESIAN_POINT ( 'NONE',  ( 4.833616638992205949, 34.47248434257868865, 30.83411269743576355 ) ) ;
#59241=EDGE_CURVE ( 'NONE', #37177, #45673, #13244, .T. ) ;
#59255=CARTESIAN_POINT ( 'NONE',  ( 0.6028618097248863439, -18.24855319618775340, 44.51207924874646693 ) ) ;
#59258=CARTESIAN_POINT ( 'NONE',  ( 0.1097557419366048670, -30.33543403792258886, 30.65094619415014776 ) ) ;
#59266=CARTESIAN_POINT ( 'NONE',  ( 0.3622758884714600280, -41.85013935980108357, 10.35929834645850001 ) ) ;
#59271=CARTESIAN_POINT ( 'NONE',  ( 0.6028618097248863439, -41.74935807801029597, -23.90242650600261598 ) ) ;
#59272=VERTEX_POINT ( 'NONE', #40115 ) ;
#59275=CARTESIAN_POINT ( 'NONE',  ( 0.1073791018717578927, 33.91564619577771111, 26.63563652260178927 ) ) ;
#59276=( BOUNDED_SURFACE ( )  B_SPLINE_SURFACE ( 3, 1, ( 
 ( #52309, #23504 ),
 ( #9399, #8172 ),
 ( #27595, #27908 ),
 ( #32929, #46721 ) ),
 .UNSPECIFIED., .F., .F., .F. ) 
 B_SPLINE_SURFACE_WITH_KNOTS ( ( 4, 4 ),
 ( 2, 2 ),
 ( 0.000000000000000000, 1.000000000000000000 ),
 ( 0.000000000000000000, 1.000000000000000000 ),
 .UNSPECIFIED. ) 
 GEOMETRIC_REPRESENTATION_ITEM ( )  RATIONAL_B_SPLINE_SURFACE ( (
 ( 1.000000000000000000, 1.000000000000000000),
 ( 0.9953040768229013402, 0.8617119497784988535),
 ( 0.9953040768229013402, 0.8617119497784988535),
 ( 1.000000000000000000, 1.000000000000000000) ) ) 
 REPRESENTATION_ITEM ( '' )  SURFACE ( )  );
#59277=CARTESIAN_POINT ( 'NONE',  ( -6.016489644550737204, 7.206912786933291848, 17.41053539857202281 ) ) ;
#59280=CARTESIAN_POINT ( 'NONE',  ( 0.1103310638050662151, 34.26302445194747293, -26.18709435931489793 ) ) ;
#59283=B_SPLINE_CURVE_WITH_KNOTS ( 'NONE', 3,
 ( #2897, #22028, #41152, #60214 ),
 .UNSPECIFIED., .F., .F.,
 ( 4, 4 ),
 ( 2.297383214701471906E-17, 0.004564976165746187711 ),
 .UNSPECIFIED. ) ;
#59289=CARTESIAN_POINT ( 'NONE',  ( 0.6031356755773454870, -6.279255973231697929, 47.69588082432145626 ) ) ;
#59293=CARTESIAN_POINT ( 'NONE',  ( 0.5998501479064699549, 5.759754759340783181, -47.76154736470751772 ) ) ;
#59295=CARTESIAN_POINT ( 'NONE',  ( 0.6030672727741701600, -33.95535904584762932, -34.07876014368848416 ) ) ;
#59296=CARTESIAN_POINT ( 'NONE',  ( 0.7954190325252775695, -19.20649988843089417, -44.09776758977464084 ) ) ;
#59298=CARTESIAN_POINT ( 'NONE',  ( 0.6025881611877909050, -6.062907795289036450, -47.72390913208162999 ) ) ;
#59300=CARTESIAN_POINT ( 'NONE',  ( -6.016104459813371719, 4.871830707673312055, -18.20253432612961575 ) ) ;
#59304=ORIENTED_EDGE ( 'NONE', *, *, #966, .F. ) ;
#59306=CARTESIAN_POINT ( 'NONE',  ( 0.1073791018717578927, 30.83464511437137645, -30.14884492832358731 ) ) ;
#59312=CARTESIAN_POINT ( 'NONE',  ( 0.1073791018717483448, -37.10214135362904386, 21.98088480513601795 ) ) ;
#59317=CARTESIAN_POINT ( 'NONE',  ( 0.1073791018717578927, 10.69234304549997105, 41.77800844988518492 ) ) ;
#59318=EDGE_CURVE ( 'NONE', #30492, #16733, #51533, .T. ) ;
#59320=CARTESIAN_POINT ( 'NONE',  ( 3.680974057930773924, -47.77138393978999176, 4.423547572561508545 ) ) ;
#59328=ORIENTED_EDGE ( 'NONE', *, *, #2414, .T. ) ;
#59332=CARTESIAN_POINT ( 'NONE',  ( -6.001507490154111224, -18.20581304543301471, 4.862106078787861385 ) ) ;
#59334=CARTESIAN_POINT ( 'NONE',  ( 0.1073791018717483448, 42.68962945260953035, -6.109314776652274404 ) ) ;
#59342=CARTESIAN_POINT ( 'NONE',  ( 0.8751705887134553219, -47.79200036674276220, -5.393078191592532988 ) ) ;
#59348=CARTESIAN_POINT ( 'NONE',  ( 0.3622758884714730732, -20.83792692158999316, 37.74294673546550172 ) ) ;
#59353=( BOUNDED_SURFACE ( )  B_SPLINE_SURFACE ( 3, 1, ( 
 ( #27949, #18246 ),
 ( #18546, #37674 ),
 ( #14782, #28545 ),
 ( #33894, #23861 ) ),
 .UNSPECIFIED., .F., .F., .F. ) 
 B_SPLINE_SURFACE_WITH_KNOTS ( ( 4, 4 ),
 ( 2, 2 ),
 ( 0.000000000000000000, 1.000000000000000000 ),
 ( 0.000000000000000000, 1.000000000000000000 ),
 .UNSPECIFIED. ) 
 GEOMETRIC_REPRESENTATION_ITEM ( )  RATIONAL_B_SPLINE_SURFACE ( (
 ( 1.000000000000000000, 1.000000000000000000),
 ( 0.7223157951917480446, 0.9931996967497186413),
 ( 0.7223157951917480446, 0.9931996967497186413),
 ( 1.000000000000000000, 1.000000000000000000) ) ) 
 REPRESENTATION_ITEM ( '' )  SURFACE ( )  );
#59354=DIRECTION ( 'NONE',  ( 0.000000000000000000, 0.000000000000000000, 1.000000000000000000 ) ) ;
#59362=VERTEX_POINT ( 'NONE', #3079 ) ;
#59373=CARTESIAN_POINT ( 'NONE',  ( 0.6025881611877910160, 0.2181813582438441590, -48.10699274197334319 ) ) ;
#59376=ORIENTED_EDGE ( 'NONE', *, *, #23311, .F. ) ;
#59377=CARTESIAN_POINT ( 'NONE',  ( 0.1310142868023677909, -34.59629828998431122, 25.74368468368876606 ) ) ;
#59384=CARTESIAN_POINT ( 'NONE',  ( 0.5988103622719989083, 41.35593060299636647, 24.57719485303652007 ) ) ;
#59389=CARTESIAN_POINT ( 'NONE',  ( -6.015611763856276717, 7.216738110653281524, 17.40650793417846032 ) ) ;
#59390=CARTESIAN_POINT ( 'NONE',  ( 0.1073791018717483448, -11.62916352156123168, -41.52698815987163528 ) ) ;
#59392=ORIENTED_EDGE ( 'NONE', *, *, #14908, .F. ) ;
#59396=CARTESIAN_POINT ( 'NONE',  ( 0.1095718737110178004, -0.2569529612660841345, 43.12372487139541732 ) ) ;
#59411=EDGE_CURVE ( 'NONE', #19272, #8059, #32540, .T. ) ;
#59413=EDGE_LOOP ( 'NONE', ( #52625, #18276, #41903, #37419, #25921, #39558, #16598, #14578, #27630, #45495, #55406, #26021, #13922, #56085, #22227, #34379, #46274, #60806, #9029, #40757, #39117, #7398, #30458, #39518, #49168, #41341, #54535, #3627, #21364, #16331, #16570, #16949, #4326, #18531, #45686, #1669, #23314, #10744, #35119, #20123, #43355, #21666, #1805, #53750, #58466, #56543, #58771, #32105, #13753, #44835, #40904, #49662, #5868, #46047, #12993, #54549, #56950, #1617, #184, #45333, #21730, #18898, #22014, #59169, #17421, #53237, #4030, #41187, #34624, #14350, #39146, #26577, #32478, #32697, #15458, #16148, #9719, #41707, #33931, #38548, #7297, #38208, #29697, #18178, #16689, #20990, #29893, #44085, #53546, #31011, #56481, #35661, #14563, #19162, #59438, #36169, #48175, #39838, #58932, #57958, #10992, #27675, #28685, #17410, #31557, #16577, #27548, #27063, #24138, #44648, #772, #28316, #32465, #11959, #22537, #1024, #55767, #38163, #17601, #4745, #33619, #17925, #19972, #1237, #554, #44803, #32376, #61544, #42107, #2940, #15830, #56893, #10725, #10249, #56861, #7079, #2924, #36517, #39701, #11836, #50348, #8899, #25912, #31503, #13691, #5000, #12746, #20667 ) ) ;
#59414=DIRECTION ( 'NONE',  ( 0.000000000000000000, 0.000000000000000000, 1.000000000000000000 ) ) ;
#59420=ORIENTED_EDGE ( 'NONE', *, *, #36641, .F. ) ;
#59421=FACE_OUTER_BOUND ( 'NONE', #50935, .T. ) ;
#59423=CARTESIAN_POINT ( 'NONE',  ( 0.1073791018717483448, -25.86618856530736466, 34.50606437925502945 ) ) ;
#59434=CARTESIAN_POINT ( 'NONE',  ( 0.1104177457020372871, -5.633723015004581391, -42.75487793940121861 ) ) ;
#59435=EDGE_CURVE ( 'NONE', #16733, #57918, #27311, .T. ) ;
#59438=ORIENTED_EDGE ( 'NONE', *, *, #46258, .T. ) ;
#59443=CARTESIAN_POINT ( 'NONE',  ( 0.5998501479064699549, -41.92175333043603302, -23.59887241503339439 ) ) ;
#59451=CARTESIAN_POINT ( 'NONE',  ( -6.016104459813371719, -17.40682403289253344, 7.215917642689006151 ) ) ;
#59454=FACE_OUTER_BOUND ( 'NONE', #29754, .T. ) ;
#59457=VECTOR ( 'NONE', #42449, 1000.000000000000000 ) ;
#59458=LINE ( 'NONE', #28566, #43510 ) ;
#59462=CARTESIAN_POINT ( 'NONE',  ( 0.1092565886968784178, 10.86136484717969886, -41.73439049602441031 ) ) ;
#59463=CARTESIAN_POINT ( 'NONE',  ( 0.1092355843206037486, 43.12343565949664992, 0.3005923759135379902 ) ) ;
#59466=CARTESIAN_POINT ( 'NONE',  ( 0.1087620492084204887, -41.74735017127137837, 10.81135549499707871 ) ) ;
#59470=CARTESIAN_POINT ( 'NONE',  ( 0.3622758884714730732, 43.10531414739106282, -0.8252992914323589169 ) ) ;
#59473=ORIENTED_EDGE ( 'NONE', *, *, #29485, .F. ) ;
#59477=CARTESIAN_POINT ( 'NONE',  ( 0.3622758884714730732, 17.25816669464937902, 39.50828911767005280 ) ) ;
#59479=CARTESIAN_POINT ( 'NONE',  ( 0.8751705887134423323, 34.63284514348585930, -33.37254303619518225 ) ) ;
#59496=AXIS2_PLACEMENT_3D ( 'NONE', #33301, #56457, #52369 ) ;
#59498=CARTESIAN_POINT ( 'NONE',  ( 0.5998501479064708430, 23.59887241503295741, 41.92175333043627461 ) ) ;
#59499=CARTESIAN_POINT ( 'NONE',  ( 4.975801465491694664, -47.84403947906841381, 2.564218696447319257 ) ) ;
#59513=CARTESIAN_POINT ( 'NONE',  ( 0.6029303876144825880, -29.18200390284022205, -38.24575311129990496 ) ) ;
#59515=CARTESIAN_POINT ( 'NONE',  ( 0.8760168074886965917, 47.56749362999704545, 7.161346975773871470 ) ) ;
#59516=ORIENTED_EDGE ( 'NONE', *, *, #1180, .F. ) ;
#59522=PRESENTATION_STYLE_ASSIGNMENT (( #25713 ) ) ;
#59526=CARTESIAN_POINT ( 'NONE',  ( 4.833616638992208614, 43.64812679991120348, -15.29495699393680219 ) ) ;
#59545=ORIENTED_EDGE ( 'NONE', *, *, #634, .F. ) ;
#59550=CARTESIAN_POINT ( 'NONE',  ( 0.6009452777970410997, -12.87217382175461822, -46.35353542372318714 ) ) ;
#59561=CARTESIAN_POINT ( 'NONE',  ( 0.7246131072078570989, 42.06185227555113926, -23.33689307364207721 ) ) ;
#59567=CARTESIAN_POINT ( 'NONE',  ( -6.016104459813374383, 2.464823636987713673, -18.68131780085928995 ) ) ;
#59572=CARTESIAN_POINT ( 'NONE',  ( 0.1103744047535531458, -30.52096488484648518, 30.46616790811169295 ) ) ;
#59573=CARTESIAN_POINT ( 'NONE',  ( 0.6254087463353930065, 13.11428234126299053, 46.28445368454758579 ) ) ;
#59574=VERTEX_POINT ( 'NONE', #6757 ) ;
#59591=CARTESIAN_POINT ( 'NONE',  ( 0.3622758884714600280, 11.95365414648497193, -41.42293301073613776 ) ) ;
#59597=EDGE_CURVE ( 'NONE', #17218, #12553, #4880, .T. ) ;
#59598=CARTESIAN_POINT ( 'NONE',  ( 0.6031356755773454870, 12.45109777649109617, -46.46822857981031518 ) ) ;
#59603=CARTESIAN_POINT ( 'NONE',  ( -6.016489644550737204, -17.41053539857204768, 7.206912786933230564 ) ) ;
#59608=CARTESIAN_POINT ( 'NONE',  ( 0.1084644655670282121, -0.3976617192055414418, -43.12277244437005663 ) ) ;
#59609=EDGE_CURVE ( 'NONE', #38461, #50490, #41537, .T. ) ;
#59613=VERTEX_POINT ( 'NONE', #39718 ) ;
#59621=ORIENTED_EDGE ( 'NONE', *, *, #32413, .T. ) ;
#59623=CARTESIAN_POINT ( 'NONE',  ( 0.6009453534118440743, 5.846398087358736895, 47.75104957283900831 ) ) ;
#59624=EDGE_CURVE ( 'NONE', #50243, #24298, #60920, .T. ) ;
#59632=CARTESIAN_POINT ( 'NONE',  ( 0.3622758884714730732, 40.13994584881760375, 15.73321244754868964 ) ) ;
#59635=B_SPLINE_CURVE_WITH_KNOTS ( 'NONE', 3,
 ( #4290, #14051, #61313, #27504 ),
 .UNSPECIFIED., .F., .F.,
 ( 4, 4 ),
 ( 2.256078575551061230E-17, 0.004564976165746191181 ),
 .UNSPECIFIED. ) ;
#59639=CARTESIAN_POINT ( 'NONE',  ( 1.827326673878744367, 42.82501343454095633, -4.394636550976192879 ) ) ;
#59640=CARTESIAN_POINT ( 'NONE',  ( 5.880360259849752858, -21.25991003419982661, 43.00389496650577570 ) ) ;
#59642=CARTESIAN_POINT ( 'NONE',  ( 0.6001305935487422083, -11.94532529598410520, 46.60388846085702852 ) ) ;
#59643=CARTESIAN_POINT ( 'NONE',  ( 0.6254087463353924514, 44.70339519268190998, 17.77193046492968520 ) ) ;
#59644=CARTESIAN_POINT ( 'NONE',  ( 0.6009452777970412107, 46.57942614304341333, 12.02913818029328930 ) ) ;
#59646=ORIENTED_EDGE ( 'NONE', *, *, #30346, .T. ) ;
#59648=CARTESIAN_POINT ( 'NONE',  ( 0.6029303876144825880, 18.28892193312799819, 44.49541906039135597 ) ) ;
#59656=CARTESIAN_POINT ( 'NONE',  ( 4.975801465491695552, 15.94009207552985252, 45.18341283946464415 ) ) ;
#59659=CARTESIAN_POINT ( 'NONE',  ( 0.1101816497532063094, -42.73758747687833903, 5.763501205266392091 ) ) ;
#59661=B_SPLINE_CURVE_WITH_KNOTS ( 'NONE', 3,
 ( #14936, #487, #38749, #44379, #19629, #1405, #57804, #25233, #11150, #39670, #58115, #34045, #49344, #43765, #5487, #5180 ),
 .UNSPECIFIED., .F., .F.,
 ( 4, 3, 3, 3, 3, 4 ),
 ( 1.995049841954898532E-17, 0.0002618515315864414347, 0.0003927756766341999970, 0.0005236998216950569142, 0.0007855159896329919587, 0.001047349442285928304 ),
 .UNSPECIFIED. ) ;
#59685=CARTESIAN_POINT ( 'NONE',  ( 0.5998501479064708430, -44.64337787626261189, 17.92509395669028649 ) ) ;
#59696=CARTESIAN_POINT ( 'NONE',  ( 0.7954190325252787908, -38.68220061605148885, -28.58653703871143037 ) ) ;
#59697=CARTESIAN_POINT ( 'NONE',  ( 0.6041374136657475802, 38.27243465845341319, -29.14743607025044980 ) ) ;
#59715=VERTEX_POINT ( 'NONE', #782 ) ;
#59719=VERTEX_POINT ( 'NONE', #58086 ) ;
#59720=VECTOR ( 'NONE', #12294, 1000.000000000000114 ) ;
#59724=CARTESIAN_POINT ( 'NONE',  ( 4.322998006666179727, -20.30542865297618960, -43.48102276965694557 ) ) ;
#59725=B_SPLINE_CURVE_WITH_KNOTS ( 'NONE', 3,
 ( #2214, #26977, #45797, #26049 ),
 .UNSPECIFIED., .F., .F.,
 ( 4, 4 ),
 ( 0.000000000000000000, 0.004445488388166995118 ),
 .UNSPECIFIED. ) ;
#59731=( BOUNDED_SURFACE ( )  B_SPLINE_SURFACE ( 3, 1, ( 
 ( #40879, #36167 ),
 ( #55231, #50541 ),
 ( #7619, #22054 ),
 ( #12666, #3228 ) ),
 .UNSPECIFIED., .F., .F., .F. ) 
 B_SPLINE_SURFACE_WITH_KNOTS ( ( 4, 4 ),
 ( 2, 2 ),
 ( 0.000000000000000000, 1.000000000000000000 ),
 ( 0.000000000000000000, 1.000000000000000000 ),
 .UNSPECIFIED. ) 
 GEOMETRIC_REPRESENTATION_ITEM ( )  RATIONAL_B_SPLINE_SURFACE ( (
 ( 1.000000000000000000, 1.000000000000000000),
 ( 0.9953040768229005630, 0.8617119497784937465),
 ( 0.9953040768229005630, 0.8617119497784937465),
 ( 1.000000000000000000, 1.000000000000000000) ) ) 
 REPRESENTATION_ITEM ( '' )  SURFACE ( )  );
#59732=ORIENTED_EDGE ( 'NONE', *, *, #43622, .F. ) ;
#59734=ORIENTED_EDGE ( 'NONE', *, *, #19124, .F. ) ;
#59735=LINE ( 'NONE', #41279, #54659 ) ;
#59741=CARTESIAN_POINT ( 'NONE',  ( 4.975801465491694664, -36.39623109580487892, 31.15993731089061924 ) ) ;
#59755=AXIS2_PLACEMENT_3D ( 'NONE', #51433, #42388, #8527 ) ;
#59756=CARTESIAN_POINT ( 'NONE',  ( 3.680974057930773924, 46.78530430706938859, -10.62112035260193288 ) ) ;
#59770=CARTESIAN_POINT ( 'NONE',  ( -6.016489644550737204, 18.20227673842151361, -4.872725758886001124 ) ) ;
#59773=B_SPLINE_CURVE_WITH_KNOTS ( 'NONE', 3,
 ( #18836, #4681, #24436, #5306, #52313, #14747 ),
 .UNSPECIFIED., .F., .F.,
 ( 4, 2, 4 ),
 ( 0.000000000000000000, 0.0002450742804987339593, 0.0004901485609974679187 ),
 .UNSPECIFIED. ) ;
#59774=CARTESIAN_POINT ( 'NONE',  ( 2.643462169533600914, 44.89050350746150997, -17.09809940585614996 ) ) ;
#59775=ADVANCED_FACE ( 'NONE', ( #61552 ), #26367, .F. ) ;
#59781=EDGE_CURVE ( 'NONE', #23596, #25998, #51933, .T. ) ;
#59784=CARTESIAN_POINT ( 'NONE',  ( 4.549368137175248350, -18.79584381673559079, 38.59302160394720005 ) ) ;
#59786=CARTESIAN_POINT ( 'NONE',  ( 0.1073791018717483448, 10.69234304550053949, -41.77800844988504991 ) ) ;
#59791=ORIENTED_EDGE ( 'NONE', *, *, #34749, .F. ) ;
#59800=CARTESIAN_POINT ( 'NONE',  ( -6.015611763856276717, 4.870987357968431297, -18.20278301740931681 ) ) ;
#59801=CARTESIAN_POINT ( 'NONE',  ( 0.6030672727741701600, -29.35514790473179403, 38.11303703924417619 ) ) ;
#59804=VERTEX_POINT ( 'NONE', #9884 ) ;
#59809=ORIENTED_EDGE ( 'NONE', *, *, #51394, .T. ) ;
#59810=CARTESIAN_POINT ( 'NONE',  ( 4.322998006666179727, -2.120302895115950381, -47.94177812210863721 ) ) ;
#59813=CARTESIAN_POINT ( 'NONE',  ( -6.017396004339686577, -9.422598049764511430, -16.31807101179380126 ) ) ;
#59814=LINE ( 'NONE', #46060, #44439 ) ;
#59823=ORIENTED_EDGE ( 'NONE', *, *, #54630, .F. ) ;
#59824=CARTESIAN_POINT ( 'NONE',  ( -6.016761891674565099, 18.84319130225482297, 0.003433883959850178927 ) ) ;
#59828=CARTESIAN_POINT ( 'NONE',  ( 0.6254087463353910081, -34.49952850220948619, -33.52637152047068980 ) ) ;
#59834=CARTESIAN_POINT ( 'NONE',  ( -6.015611763856276717, -14.94556629257417590, -11.47596948473826650 ) ) ;
#59845=CARTESIAN_POINT ( 'NONE',  ( 4.691466044806103852, -3.249105306918109726, -44.46979273209134220 ) ) ;
#59846=CARTESIAN_POINT ( 'NONE',  ( 0.1073791018717483448, -16.95003405440287381, -39.65380858626208038 ) ) ;
#59848=CARTESIAN_POINT ( 'NONE',  ( 0.5988103564986355654, -44.21009236284897526, 18.96890181990811186 ) ) ;
#59850=ADVANCED_FACE ( 'NONE', ( #11125 ), #2760, .F. ) ;
#59857=CARTESIAN_POINT ( 'NONE',  ( -6.016761891674565099, 18.68243340030205957, -2.456125503350522710 ) ) ;
#59859=ORIENTED_EDGE ( 'NONE', *, *, #42724, .T. ) ;
#59861=CARTESIAN_POINT ( 'NONE',  ( 0.2885700199627517781, -39.51953436244184559, 17.24062365614525305 ) ) ;
#59866=ORIENTED_EDGE ( 'NONE', *, *, #51532, .F. ) ;
#59870=ORIENTED_EDGE ( 'NONE', *, *, #24358, .F. ) ;
#59872=ORIENTED_EDGE ( 'NONE', *, *, #50497, .T. ) ;
#59881=EDGE_LOOP ( 'NONE', ( #45943, #10652, #7363, #5923 ) ) ;
#59882=B_SPLINE_CURVE_WITH_KNOTS ( 'NONE', 3,
 ( #6483, #38832, #10932, #49128, #6180, #25626 ),
 .UNSPECIFIED., .F., .F.,
 ( 4, 2, 4 ),
 ( 1.474357996003774831E-17, 0.0002293319059085075146, 0.0004586638118170002841 ),
 .UNSPECIFIED. ) ;
#59885=CARTESIAN_POINT ( 'NONE',  ( 0.8751705887134423323, 5.393078191592057813, 47.79200036674281904 ) ) ;
#59887=CARTESIAN_POINT ( 'NONE',  ( 0.5998501479064708430, -41.39809967730470674, -24.50586714782589937 ) ) ;
#59888=EDGE_LOOP ( 'NONE', ( #32519, #26073, #33016, #15878 ) ) ;
#59891=CARTESIAN_POINT ( 'NONE',  ( 3.680974057930773924, -1.849713332884082684, 47.94008194857087091 ) ) ;
#59897=CARTESIAN_POINT ( 'NONE',  ( 0.6023142530420679819, -41.79260242564383532, -23.82662387835852158 ) ) ;
#59904=CARTESIAN_POINT ( 'NONE',  ( 0.1103310638050662429, 34.16271402810833280, 26.31782144882252439 ) ) ;
#59907=CARTESIAN_POINT ( 'NONE',  ( 0.6041374136657476912, -47.67304777898703350, 6.452348380035114239 ) ) ;
#59909=ADVANCED_FACE ( 'NONE', ( #5760 ), #48594, .F. ) ;
#59913=CARTESIAN_POINT ( 'NONE',  ( 0.6030672727741701600, 12.53539249098714770, -46.44558360017000354 ) ) ;
#59920=CARTESIAN_POINT ( 'NONE',  ( 0.5998501479064708430, -33.64490850298820845, -34.38546660123286358 ) ) ;
#59923=DIRECTION ( 'NONE',  ( 1.000000000000000000, 0.000000000000000000, 0.000000000000000000 ) ) ;
#59926=CARTESIAN_POINT ( 'NONE',  ( -6.017396004339686577, 18.68211039806563534, 2.458362590802854797 ) ) ;
#59928=CARTESIAN_POINT ( 'NONE',  ( 0.6001305935487422083, 47.76436356026967900, -5.760103278697539686 ) ) ;
#59933=CARTESIAN_POINT ( 'NONE',  ( -2.708315649062916552, -12.80362818457440710, -7.087851317223917036 ) ) ;
#59943=AXIS2_PLACEMENT_3D ( 'NONE', #29855, #10140, #28933 ) ;
#59950=CARTESIAN_POINT ( 'NONE',  ( 0.7954196712028475114, -19.20650004025030100, 44.09776749253649086 ) ) ;
#59952=CARTESIAN_POINT ( 'NONE',  ( 0.1092355843206037486, 0.3005923759133873885, -43.12343565949664992 ) ) ;
#59961=CARTESIAN_POINT ( 'NONE',  ( 0.6031357023905875581, 34.04794059289648800, -33.98625823839265081 ) ) ;
#59962=CARTESIAN_POINT ( 'NONE',  ( 0.6031356755773454870, 46.46822857981026544, 12.45109777649125782 ) ) ;
#59966=CARTESIAN_POINT ( 'NONE',  ( -2.708315649062910779, -7.087851317223882397, -12.80362818457442842 ) ) ;
#59967=CARTESIAN_POINT ( 'NONE',  ( 0.7246131072078549895, 29.92944207473653506, -37.65685186358364689 ) ) ;
#59970=CARTESIAN_POINT ( 'NONE',  ( 0.1104177457020372732, 42.75487793940123993, -5.633723015004433066 ) ) ;
#59973=CARTESIAN_POINT ( 'NONE',  ( 0.3622758884714730732, 29.89648521331631414, -31.06363466427696807 ) ) ;
#59974=EDGE_CURVE ( 'NONE', #49600, #40342, #12989, .T. ) ;
#59975=VERTEX_POINT ( 'NONE', #42122 ) ;
#59977=EDGE_CURVE ( 'NONE', #53499, #61466, #39208, .T. ) ;
#59978=CARTESIAN_POINT ( 'NONE',  ( -2.708315649062916552, 12.54007339125014830, -7.544341609839853469 ) ) ;
#59982=CARTESIAN_POINT ( 'NONE',  ( 4.322998006666165516, 40.45864630878482870, 25.80712523194289432 ) ) ;
#59985=CARTESIAN_POINT ( 'NONE',  ( 0.1101816497532063094, -41.68997876247040324, -11.03018586750479990 ) ) ;
#59988=ORIENTED_EDGE ( 'NONE', *, *, #57069, .T. ) ;
#59989=CARTESIAN_POINT ( 'NONE',  ( -6.016761891674565099, 2.462934516564073917, -18.68153697670638991 ) ) ;
#60005=CARTESIAN_POINT ( 'NONE',  ( 2.301430502907644726, -7.543848632415566691, 47.43735983879639662 ) ) ;
#60008=CARTESIAN_POINT ( 'NONE',  ( 0.5998501479064699549, 12.95623334615437550, 46.33007877220744319 ) ) ;
#60011=ORIENTED_EDGE ( 'NONE', *, *, #33911, .F. ) ;
#60013=CARTESIAN_POINT ( 'NONE',  ( 0.6001305935487315502, -17.92615948558509231, -44.64600790884048820 ) ) ;
#60014=CARTESIAN_POINT ( 'NONE',  ( 0.1102847568649952675, -39.87696813145917929, -16.41780866919029336 ) ) ;
#60017=EDGE_CURVE ( 'NONE', #1398, #34923, #30180, .T. ) ;
#60026=ORIENTED_EDGE ( 'NONE', *, *, #41598, .F. ) ;
#60029=FACE_OUTER_BOUND ( 'NONE', #14981, .T. ) ;
#60031=ORIENTED_EDGE ( 'NONE', *, *, #12674, .F. ) ;
#60033=EDGE_CURVE ( 'NONE', #43892, #56469, #1579, .T. ) ;
#60036=CARTESIAN_POINT ( 'NONE',  ( 2.643462169533613793, -40.89244134039129364, 25.20536747735708261 ) ) ;
#60041=CARTESIAN_POINT ( 'NONE',  ( 0.1313383488274136590, 42.83318330237617744, 4.995828979989608065 ) ) ;
#60045=CARTESIAN_POINT ( 'NONE',  ( 0.6001305935487422083, -17.92615948558511008, -44.64600790884048109 ) ) ;
#60046=VERTEX_POINT ( 'NONE', #35860 ) ;
#60047=CARTESIAN_POINT ( 'NONE',  ( 0.1310142868023686513, 41.48473022063163995, 11.77532653407853047 ) ) ;
#60048=CARTESIAN_POINT ( 'NONE',  ( 0.5980894510889457338, -17.76188940524976800, 44.71414919659875409 ) ) ;
#60051=CARTESIAN_POINT ( 'NONE',  ( 0.1104177457020372871, -26.24862037251758196, 34.21590786698995856 ) ) ;
#60052=ORIENTED_EDGE ( 'NONE', *, *, #47462, .T. ) ;
#60053=CARTESIAN_POINT ( 'NONE',  ( 0.6001305935487315502, -44.24520387813841893, 18.89378601235985755 ) ) ;
#60056=ORIENTED_EDGE ( 'NONE', *, *, #56174, .F. ) ;
#60062=CARTESIAN_POINT ( 'NONE',  ( 4.549368137175248350, -35.80950303116083688, -23.67244292351627521 ) ) ;
#60063=CARTESIAN_POINT ( 'NONE',  ( 0.5998501479064708430, -37.84527566984837677, -29.69975237324600315 ) ) ;
#60065=CARTESIAN_POINT ( 'NONE',  ( 0.1073791018717483448, 37.10214135362888754, -21.98088480513627729 ) ) ;
#60070=CARTESIAN_POINT ( 'NONE',  ( 4.549368137175248350, 40.58005590356690817, -13.99871866169321599 ) ) ;
#60072=ADVANCED_FACE ( 'NONE', ( #40884 ), #45246, .F. ) ;
#60084=FACE_OUTER_BOUND ( 'NONE', #2099, .T. ) ;
#60086=CARTESIAN_POINT ( 'NONE',  ( 0.8751705887134553219, -37.60752970653848593, 29.98056538504896906 ) ) ;
#60091=CARTESIAN_POINT ( 'NONE',  ( 0.8760168074886960365, 29.98565522133346306, -37.61398439004503302 ) ) ;
#60099=ORIENTED_EDGE ( 'NONE', *, *, #40135, .T. ) ;
#60101=CARTESIAN_POINT ( 'NONE',  ( 1.827326673878744145, 43.03225468313000590, 1.232746109312326199 ) ) ;
#60103=EDGE_CURVE ( 'NONE', #58608, #5237, #14825, .T. ) ;
#60106=ORIENTED_EDGE ( 'NONE', *, *, #37223, .T. ) ;
#60117=ORIENTED_EDGE ( 'NONE', *, *, #42104, .T. ) ;
#60123=CARTESIAN_POINT ( 'NONE',  ( 4.833616638992205949, -46.17873762321150366, 2.572717262757815870 ) ) ;
#60124=VERTEX_POINT ( 'NONE', #5386 ) ;
#60129=VECTOR ( 'NONE', #37147, 1000.000000000000000 ) ;
#60134=CARTESIAN_POINT ( 'NONE',  ( 0.1073791018717578927, -43.12183934961191056, -0.4849339620931655825 ) ) ;
#60149=CARTESIAN_POINT ( 'NONE',  ( 0.1102144999581333024, 21.67128446981380208, -37.28370465375335385 ) ) ;
#60153=CARTESIAN_POINT ( 'NONE',  ( -6.015611763856276717, -7.216738110653151850, -17.40650793417851361 ) ) ;
#60156=CARTESIAN_POINT ( 'NONE',  ( 0.5988103622719989083, 33.58571533649112695, 34.44344971428038349 ) ) ;
#60171=EDGE_CURVE ( 'NONE', #20018, #10739, #21991, .T. ) ;
#60175=CARTESIAN_POINT ( 'NONE',  ( 0.5998501479064708430, 28.86886762351073088, 38.48283596222038483 ) ) ;
#60180=ORIENTED_EDGE ( 'NONE', *, *, #49357, .T. ) ;
#60183=CARTESIAN_POINT ( 'NONE',  ( -5.995132425357893702, 16.31525984181033095, 9.429450169548012184 ) ) ;
#60192=CARTESIAN_POINT ( 'NONE',  ( 4.833616638992205949, -30.15290813935876812, -35.06988470649558565 ) ) ;
#60196=CARTESIAN_POINT ( 'NONE',  ( 0.8751705887134553219, 47.55935879196470495, -7.160166390003808168 ) ) ;
#60199=FACE_OUTER_BOUND ( 'NONE', #37053, .T. ) ;
#60201=CARTESIAN_POINT ( 'NONE',  ( 0.5998501479064708430, -41.39809967730470674, -24.50586714782589937 ) ) ;
#60202=VERTEX_POINT ( 'NONE', #58620 ) ;
#60203=ORIENTED_EDGE ( 'NONE', *, *, #49623, .F. ) ;
#60214=CARTESIAN_POINT ( 'NONE',  ( 4.549368137175248350, -13.99871866169335810, -40.58005590356685843 ) ) ;
#60219=CARTESIAN_POINT ( 'NONE',  ( 0.5998501479064708430, -5.759754759340450114, -47.76154736470756745 ) ) ;
#60220=CARTESIAN_POINT ( 'NONE',  ( 0.1102847568649952675, -0.09217763870870740450, -43.12433804869904463 ) ) ;
#60222=CARTESIAN_POINT ( 'NONE',  ( 4.549368137175248350, 8.166781970325731166, -42.14271863032826104 ) ) ;
#60223=CARTESIAN_POINT ( 'NONE',  ( 4.322998006666179727, 47.25487450103535991, -8.359821156455987889 ) ) ;
#60229=CARTESIAN_POINT ( 'NONE',  ( -6.010958268070873523, -13.31406649671953168, -13.33459572764771650 ) ) ;
#60232=DIRECTION ( 'NONE',  ( 0.000000000000000000, 0.000000000000000000, 1.000000000000000000 ) ) ;
#60240=ADVANCED_FACE ( 'NONE', ( #5682 ), #55254, .F. ) ;
#60246=AXIS2_PLACEMENT_3D ( 'NONE', #55798, #18227, #50488 ) ;
#60248=CARTESIAN_POINT ( 'NONE',  ( 0.1101816497532063094, 21.67974746580497580, 37.27878591512682505 ) ) ;
#60249=VERTEX_POINT ( 'NONE', #10738 ) ;
#60262=( BOUNDED_SURFACE ( )  B_SPLINE_SURFACE ( 3, 1, ( 
 ( #46531, #3270 ),
 ( #13636, #45607 ),
 ( #51202, #8284 ),
 ( #22715, #40926 ) ),
 .UNSPECIFIED., .F., .F., .F. ) 
 B_SPLINE_SURFACE_WITH_KNOTS ( ( 4, 4 ),
 ( 2, 2 ),
 ( 0.000000000000000000, 1.000000000000000000 ),
 ( 0.000000000000000000, 1.000000000000000000 ),
 .UNSPECIFIED. ) 
 GEOMETRIC_REPRESENTATION_ITEM ( )  RATIONAL_B_SPLINE_SURFACE ( (
 ( 1.000000000000000000, 1.000000000000000000),
 ( 0.7223157951917476005, 0.9931996967497186413),
 ( 0.7223157951917476005, 0.9931996967497186413),
 ( 1.000000000000000000, 1.000000000000000000) ) ) 
 REPRESENTATION_ITEM ( '' )  SURFACE ( )  );
#60264=DIRECTION ( 'NONE',  ( 0.000000000000000000, 0.000000000000000000, 1.000000000000000000 ) ) ;
#60268=ORIENTED_EDGE ( 'NONE', *, *, #10922, .F. ) ;
#60269=B_SPLINE_CURVE_WITH_KNOTS ( 'NONE', 3,
 ( #45684, #59756, #17783, #8062 ),
 .UNSPECIFIED., .F., .F.,
 ( 4, 4 ),
 ( 0.000000000000000000, 0.004445488388166995118 ),
 .UNSPECIFIED. ) ;
#60270=CARTESIAN_POINT ( 'NONE',  ( 0.5998501479064708430, 34.38546660123297727, -33.64490850298808056 ) ) ;
#60274=CARTESIAN_POINT ( 'NONE',  ( 0.6031356755773454870, -41.66225520948420780, 24.05374386753643989 ) ) ;
#60287=LINE ( 'NONE', #60596, #39026 ) ;
#60290=EDGE_CURVE ( 'NONE', #13776, #55407, #6970, .T. ) ;
#60297=VERTEX_POINT ( 'NONE', #37888 ) ;
#60305=CARTESIAN_POINT ( 'NONE',  ( 0.1102144999581332885, 5.753800096706042311, -42.73889315046714188 ) ) ;
#60310=EDGE_CURVE ( 'NONE', #32695, #6090, #42981, .T. ) ;
#60311=CARTESIAN_POINT ( 'NONE',  ( -6.015611763856276717, -18.20278301740933102, -4.870987357968367348 ) ) ;
#60314=EDGE_CURVE ( 'NONE', #22780, #27827, #17559, .T. ) ;
#60318=CARTESIAN_POINT ( 'NONE',  ( 0.3622758884714730732, -26.89560658783362612, -33.69533458712334806 ) ) ;
#60337=DIRECTION ( 'NONE',  ( -1.000000000000000000, -0.000000000000000000, -0.000000000000000000 ) ) ;
#60340=CARTESIAN_POINT ( 'NONE',  ( -6.016104459813374383, 7.215917642689303690, -17.40682403289241265 ) ) ;
#60341=CARTESIAN_POINT ( 'NONE',  ( 0.1081432562775997697, -26.58728936586542346, 33.95357233988183054 ) ) ;
#60342=ORIENTED_EDGE ( 'NONE', *, *, #29200, .F. ) ;
#60346=AXIS2_PLACEMENT_3D ( 'NONE', #54055, #20567, #57833 ) ;
#60351=CARTESIAN_POINT ( 'NONE',  ( 0.1103878639767399417, 26.21398130517517444, -34.24245495762994551 ) ) ;
#60352=CARTESIAN_POINT ( 'NONE',  ( 0.8751705887134553219, -0.8911681664085087107, -48.08707113907594533 ) ) ;
#60355=CARTESIAN_POINT ( 'NONE',  ( -6.001507490154111224, 18.68469198366100059, -2.444174634177952665 ) ) ;
#60361=CARTESIAN_POINT ( 'NONE',  ( 0.3622758884714730732, -0.8252992914325094631, -43.10531414739105571 ) ) ;
#60371=CARTESIAN_POINT ( 'NONE',  ( 0.5988103564986357874, -46.62176022926377783, -11.86435738293427100 ) ) ;
#60376=CARTESIAN_POINT ( 'NONE',  ( 0.2224561200757580182, 26.84793396060980797, -33.74134531362606282 ) ) ;
#60378=EDGE_CURVE ( 'NONE', #11845, #22472, #19782, .T. ) ;
#60379=( BOUNDED_SURFACE ( )  B_SPLINE_SURFACE ( 3, 1, ( 
 ( #4581, #14034 ),
 ( #14646, #29038 ),
 ( #33135, #48150 ),
 ( #5203, #41926 ) ),
 .UNSPECIFIED., .F., .F., .F. ) 
 B_SPLINE_SURFACE_WITH_KNOTS ( ( 4, 4 ),
 ( 2, 2 ),
 ( 0.000000000000000000, 1.000000000000000000 ),
 ( 0.000000000000000000, 1.000000000000000000 ),
 .UNSPECIFIED. ) 
 GEOMETRIC_REPRESENTATION_ITEM ( )  RATIONAL_B_SPLINE_SURFACE ( (
 ( 1.000000000000000000, 1.000000000000000000),
 ( 0.9953040768229005630, 0.8617119497784937465),
 ( 0.9953040768229005630, 0.8617119497784937465),
 ( 1.000000000000000000, 1.000000000000000000) ) ) 
 REPRESENTATION_ITEM ( '' )  SURFACE ( )  );
#60383=CARTESIAN_POINT ( 'NONE',  ( 5.880360259849739535, -47.05949693022701297, -9.312491912827962182 ) ) ;
#60386=CARTESIAN_POINT ( 'NONE',  ( 4.549368137175248350, 0.000000000000000000, 0.000000000000000000 ) ) ;
#60389=ORIENTED_EDGE ( 'NONE', *, *, #24991, .T. ) ;
#60395=CARTESIAN_POINT ( 'NONE',  ( 0.6041374136657475802, 18.24862627831472750, 44.51224464245006374 ) ) ;
#60396=CARTESIAN_POINT ( 'NONE',  ( 0.1102144999581333162, 26.15241010112978515, 34.28951223307537788 ) ) ;
#60401=B_SPLINE_CURVE_WITH_KNOTS ( 'NONE', 3,
 ( #34349, #24945, #53423, #44083, #1111, #20253 ),
 .UNSPECIFIED., .F., .F.,
 ( 4, 2, 4 ),
 ( 8.492412771929966223E-17, 0.0002293366620881452558, 0.0004586733241762056185 ),
 .UNSPECIFIED. ) ;
#60414=CARTESIAN_POINT ( 'NONE',  ( -6.016761891674564211, -16.32039929810250456, -9.418621820384668553 ) ) ;
#60421=ORIENTED_EDGE ( 'NONE', *, *, #51608, .F. ) ;
#60432=CARTESIAN_POINT ( 'NONE',  ( 0.8760168074887090262, 29.98565522133295502, 37.61398439004543803 ) ) ;
#60436=EDGE_CURVE ( 'NONE', #29055, #35054, #16782, .T. ) ;
#60438=( NAMED_UNIT ( * ) SI_UNIT ( $, .STERADIAN. ) SOLID_ANGLE_UNIT ( ) );
#60445=CARTESIAN_POINT ( 'NONE',  ( 0.1104177457020373426, -16.50753524010271889, -39.83992599038879945 ) ) ;
#60469=CARTESIAN_POINT ( 'NONE',  ( -6.016104459813374383, -13.32039631884674868, -13.32794178585011480 ) ) ;
#60478=ORIENTED_EDGE ( 'NONE', *, *, #43963, .T. ) ;
#60481=ORIENTED_EDGE ( 'NONE', *, *, #21779, .T. ) ;
#60488=CARTESIAN_POINT ( 'NONE',  ( 0.5998501479064699549, 46.33007877220738635, -12.95623334615453892 ) ) ;
#60489=DIRECTION ( 'NONE',  ( 0.000000000000000000, 0.000000000000000000, 1.000000000000000000 ) ) ;
#60492=ORIENTED_EDGE ( 'NONE', *, *, #844, .T. ) ;
#60493=CARTESIAN_POINT ( 'NONE',  ( 0.8751705887134423323, -0.8911681664091769539, 48.08707113907594533 ) ) ;
#60496=CARTESIAN_POINT ( 'NONE',  ( 0.1310142868023668195, -41.81449350725036851, 10.54463319394661447 ) ) ;
#60507=CARTESIAN_POINT ( 'NONE',  ( 1.827326673878743035, 12.32830836993820967, -41.24690799101795591 ) ) ;
#60510=CARTESIAN_POINT ( 'NONE',  ( 0.6028618097248862329, 6.106174977919045510, -47.71844004092982772 ) ) ;
#60521=DIRECTION ( 'NONE',  ( 0.09835009131224552170, 0.1222230102475009711, -0.9876177374393962927 ) ) ;
#60522=CIRCLE ( 'NONE', #3507, 42.92674063221959813 ) ;
#60523=CARTESIAN_POINT ( 'NONE',  ( 0.1103744047535531458, -21.59576373962443085, 37.32746539760782412 ) ) ;
#60525=DIRECTION ( 'NONE',  ( -1.000000000000000000, -0.000000000000000000, -0.000000000000000000 ) ) ;
#60534=ORIENTED_EDGE ( 'NONE', *, *, #4992, .T. ) ;
#60537=CARTESIAN_POINT ( 'NONE',  ( 0.2224561200757594337, 31.02237548791951838, -29.94832483818005642 ) ) ;
#60538=CARTESIAN_POINT ( 'NONE',  ( 0.5980894510889448457, -47.60453381548688156, -6.974827154143931729 ) ) ;
#60542=LINE ( 'NONE', #30493, #36345 ) ;
#60548=CARTESIAN_POINT ( 'NONE',  ( 0.5998501479064699549, 46.60114184914301205, 11.94461217097485672 ) ) ;
#60556=CARTESIAN_POINT ( 'NONE',  ( 0.1097557419366048670, 21.75515245866073144, 37.23482781437652989 ) ) ;
#60558=EDGE_LOOP ( 'NONE', ( #60031, #6684, #37590, #5266 ) ) ;
#60560=VECTOR ( 'NONE', #375, 1000.000000000000114 ) ;
#60561=ORIENTED_EDGE ( 'NONE', *, *, #23551, .F. ) ;
#60562=CARTESIAN_POINT ( 'NONE',  ( -6.016761891674564211, 4.873659902332621918, -18.20201388312090529 ) ) ;
#60564=CARTESIAN_POINT ( 'NONE',  ( 4.975801465491695552, 31.15993731089124097, -36.39623109580435312 ) ) ;
#60568=B_SPLINE_CURVE_WITH_KNOTS ( 'NONE', 3,
 ( #49174, #24441, #47954, #24132 ),
 .UNSPECIFIED., .F., .F.,
 ( 4, 4 ),
 ( 2.030239133983568861E-17, 0.004444306975806114161 ),
 .UNSPECIFIED. ) ;
#60570=CARTESIAN_POINT ( 'NONE',  ( 5.880360259849739535, 15.37531919565236116, -45.44137230084866275 ) ) ;
#60571=CARTESIAN_POINT ( 'NONE',  ( 0.2885697896453112143, -10.38006191081390917, -41.84838128162056847 ) ) ;
#60572=CARTESIAN_POINT ( 'NONE',  ( 0.1103878639767399278, 39.82320122342704138, -16.54784522866428986 ) ) ;
#60577=CARTESIAN_POINT ( 'NONE',  ( 0.7954190325252772364, 38.68220061605128279, 28.58653703871169682 ) ) ;
#60579=CARTESIAN_POINT ( 'NONE',  ( 0.5998501479064708430, -12.95623334615534716, 46.33007877220716608 ) ) ;
#60580=CARTESIAN_POINT ( 'NONE',  ( 0.6001305935487315502, -37.84751346122875759, 29.70149728382373056 ) ) ;
#60584=CARTESIAN_POINT ( 'NONE',  ( 2.643462169533600914, 40.89244134039076783, 25.20536747735794236 ) ) ;
#60595=DIRECTION ( 'NONE',  ( -1.000000000000000000, -0.000000000000000000, -0.000000000000000000 ) ) ;
#60596=CARTESIAN_POINT ( 'NONE',  ( -2.569797478183790229, 10.02484965418626395, 10.65947181927842990 ) ) ;
#60606=CARTESIAN_POINT ( 'NONE',  ( 5.880360259849739535, 47.04104239318766645, -9.405269135694755533 ) ) ;
#60607=CARTESIAN_POINT ( 'NONE',  ( -5.995132425357893702, 7.219211173946491478, 17.40647075750118944 ) ) ;
#60609=EDGE_CURVE ( 'NONE', #49088, #40811, #58628, .T. ) ;
#60614=CARTESIAN_POINT ( 'NONE',  ( 0.1103878639767399555, 5.580746265797033701, -42.76182653383951759 ) ) ;
#60615=ORIENTED_EDGE ( 'NONE', *, *, #30106, .T. ) ;
#60618=AXIS2_PLACEMENT_3D ( 'NONE', #17256, #2194, #21332 ) ;
#60619=CARTESIAN_POINT ( 'NONE',  ( -6.016489644550736315, -18.20227673842140348, -4.872725758886381264 ) ) ;
#60620=CARTESIAN_POINT ( 'NONE',  ( 0.5998501479064708430, 41.39809967730453621, 24.50586714782619424 ) ) ;
#60622=CARTESIAN_POINT ( 'NONE',  ( 0.7954196712028480665, -23.29293472883161442, -42.08256091708695124 ) ) ;
#60626=FACE_OUTER_BOUND ( 'NONE', #28582, .T. ) ;
#60628=CARTESIAN_POINT ( 'NONE',  ( 0.8760168074887090262, -47.80016357497245849, -5.394043284319338660 ) ) ;
#60629=B_SPLINE_CURVE_WITH_KNOTS ( 'NONE', 3,
 ( #41539, #25875, #11477, #30562, #12112, #16478, #2047, #50594, #21178, #35609, #7675, #31187, #54668, #11797, #49992, #45320 ),
 .UNSPECIFIED., .F., .F.,
 ( 4, 3, 3, 3, 3, 4 ),
 ( 2.501947744657918636E-17, 0.0002618515315864419768, 0.0003927756766342000512, 0.0005236998216950560468, 0.0007855159896329864293, 0.001047349442285929605 ),
 .UNSPECIFIED. ) ;
#60632=CARTESIAN_POINT ( 'NONE',  ( 0.1313383488274128263, 34.59671037481836464, 25.74310646082161824 ) ) ;
#60641=CARTESIAN_POINT ( 'NONE',  ( 0.3622758884714730732, 26.89560658783340585, 33.69533458712353280 ) ) ;
#60642=( BOUNDED_SURFACE ( )  B_SPLINE_SURFACE ( 3, 1, ( 
 ( #28643, #37457 ),
 ( #51825, #19268 ),
 ( #37778, #13960 ),
 ( #57432, #14266 ) ),
 .UNSPECIFIED., .F., .F., .F. ) 
 B_SPLINE_SURFACE_WITH_KNOTS ( ( 4, 4 ),
 ( 2, 2 ),
 ( 0.000000000000000000, 1.000000000000000000 ),
 ( 0.000000000000000000, 1.000000000000000000 ),
 .UNSPECIFIED. ) 
 GEOMETRIC_REPRESENTATION_ITEM ( )  RATIONAL_B_SPLINE_SURFACE ( (
 ( 1.000000000000000000, 1.000000000000000000),
 ( 0.7223157951917480446, 0.9931996967497186413),
 ( 0.7223157951917480446, 0.9931996967497186413),
 ( 1.000000000000000000, 1.000000000000000000) ) ) 
 REPRESENTATION_ITEM ( '' )  SURFACE ( )  );
#60649=CARTESIAN_POINT ( 'NONE',  ( 0.7954190325252785687, 44.09776758977471189, -19.20649988843073430 ) ) ;
#60650=B_SPLINE_CURVE_WITH_KNOTS ( 'NONE', 3,
 ( #18168, #4028, #13786, #32577, #14092, #47594, #57261, #61964, #37283, #47907, #23169, #13468, #51345, #9675, #56046, #28783, #19101, #42295, #8429 ),
 .UNSPECIFIED., .F., .F.,
 ( 4, 3, 3, 3, 3, 3, 4 ),
 ( 1.138109825968292890E-16, 0.0002618519381806302536, 0.0003927759815486006373, 0.0005237000248299482005, 0.0006546240681324976083, 0.0007855481115631354197, 0.0009699050456655131103 ),
 .UNSPECIFIED. ) ;
#60652=CARTESIAN_POINT ( 'NONE',  ( 0.6031356755852232965, 4.336951783013129340E-16, 48.10744332413860747 ) ) ;
#60657=EDGE_LOOP ( 'NONE', ( #52696, #48257, #48685, #2951 ) ) ;
#60661=CARTESIAN_POINT ( 'NONE',  ( 0.7246131072078556556, -37.65685186358372505, -29.92944207473638585 ) ) ;
#60668=EDGE_CURVE ( 'NONE', #61502, #29664, #61443, .T. ) ;
#60672=DIRECTION ( 'NONE',  ( -1.000000000000000000, -0.000000000000000000, -0.000000000000000000 ) ) ;
#60678=CARTESIAN_POINT ( 'NONE',  ( 0.6023142530420679819, 38.32506243004152680, 29.07781306567114754 ) ) ;
#60680=CARTESIAN_POINT ( 'NONE',  ( 0.6001305935487422083, 48.10757715638249010, -0.5236757026884415467 ) ) ;
#60688=CARTESIAN_POINT ( 'NONE',  ( 2.301529144917016545, -44.85388898587012818, -17.18548816179607996 ) ) ;
#60690=CARTESIAN_POINT ( 'NONE',  ( 0.8751705887134553219, -42.09020928323357680, -23.27176129838411001 ) ) ;
#60691=ORIENTED_EDGE ( 'NONE', *, *, #55858, .F. ) ;
#60699=CARTESIAN_POINT ( 'NONE',  ( 0.5998501479064708430, 24.50586714782604858, -41.39809967730462859 ) ) ;
#60703=EDGE_CURVE ( 'NONE', #45553, #8059, #18682, .T. ) ;
#60708=CARTESIAN_POINT ( 'NONE',  ( 0.1103744047535531458, 26.22174028894823650, 34.23648668783401661 ) ) ;
#60711=CARTESIAN_POINT ( 'NONE',  ( 0.2224561200757604607, -15.79689521915838135, -40.12166550582807645 ) ) ;
#60722=ORIENTED_EDGE ( 'NONE', *, *, #35309, .T. ) ;
#60742=CONICAL_SURFACE ( 'NONE', #28743, 47.91270532121795611, 0.04450589592585343229 ) ;
#60744=B_SPLINE_CURVE_WITH_KNOTS ( 'NONE', 3,
 ( #41807, #22994, #17991, #61179, #37108, #18298, #56480, #26753, #45888, #2935, #38643, #19528, #57386, #29214, #43656, #52399 ),
 .UNSPECIFIED., .F., .F.,
 ( 4, 3, 3, 3, 3, 4 ),
 ( 2.027574016683678720E-17, 0.0002618515315864419768, 0.0003927756766341985875, 0.0005236998216950574563, 0.0007855159896329904409, 0.001047349442285928304 ),
 .UNSPECIFIED. ) ;
#60753=VERTEX_POINT ( 'NONE', #57465 ) ;
#60760=EDGE_CURVE ( 'NONE', #7392, #1703, #33713, .T. ) ;
#60765=EDGE_CURVE ( 'NONE', #52785, #21034, #7641, .T. ) ;
#60766=B_SPLINE_CURVE_WITH_KNOTS ( 'NONE', 3,
 ( #48638, #18928, #5697, #24843, #1865, #37736, #56796, #13926, #33029, #4776, #4465, #19538, #23604, #47419, #38652, #38052, #14534, #29221, #14837 ),
 .UNSPECIFIED., .F., .F.,
 ( 4, 3, 3, 3, 3, 3, 4 ),
 ( 1.153344816771540786E-16, 0.0002618519381806257000, 0.0003927759815485966800, 0.0005237000248299429964, 0.0006546240681324979336, 0.0007855481115631330344, 0.0009699050456655101829 ),
 .UNSPECIFIED. ) ;
#60769=ORIENTED_EDGE ( 'NONE', *, *, #20697, .F. ) ;
#60772=CARTESIAN_POINT ( 'NONE',  ( 0.6254311100348659558, -38.58047947916347908, 28.73641524052507279 ) ) ;
#60778=VERTEX_POINT ( 'NONE', #21444 ) ;
#60787=CARTESIAN_POINT ( 'NONE',  ( 0.1064266379913940685, -42.82540706760018878, -5.071708164746911329 ) ) ;
#60792=EDGE_CURVE ( 'NONE', #10506, #38229, #40648, .T. ) ;
#60806=ORIENTED_EDGE ( 'NONE', *, *, #61164, .T. ) ;
#60809=( BOUNDED_SURFACE ( )  B_SPLINE_SURFACE ( 3, 1, ( 
 ( #60183, #46731 ),
 ( #22917, #46121 ),
 ( #17294, #36720 ),
 ( #61099, #17597 ) ),
 .UNSPECIFIED., .F., .F., .F. ) 
 B_SPLINE_SURFACE_WITH_KNOTS ( ( 4, 4 ),
 ( 2, 2 ),
 ( 0.000000000000000000, 1.000000000000000000 ),
 ( 0.000000000000000000, 1.000000000000000000 ),
 .UNSPECIFIED. ) 
 GEOMETRIC_REPRESENTATION_ITEM ( )  RATIONAL_B_SPLINE_SURFACE ( (
 ( 1.000000000000000000, 1.000000000000000000),
 ( 0.7223157951917476005, 0.9931996967497186413),
 ( 0.7223157951917476005, 0.9931996967497186413),
 ( 1.000000000000000000, 1.000000000000000000) ) ) 
 REPRESENTATION_ITEM ( '' )  SURFACE ( )  );
#60812=EDGE_CURVE ( 'NONE', #17449, #23651, #55462, .T. ) ;
#60813=CARTESIAN_POINT ( 'NONE',  ( 0.2885700199627521667, 11.93479339212609425, 41.43179222486424607 ) ) ;
#60816=CARTESIAN_POINT ( 'NONE',  ( -6.016761891674564211, -4.880293656734836283, -18.20023637398604066 ) ) ;
#60818=STYLED_ITEM ( 'NONE', ( #41382 ), #10540 ) ;
#60819=VERTEX_POINT ( 'NONE', #58397 ) ;
#60823=CARTESIAN_POINT ( 'NONE',  ( 0.6025881611877909050, 6.495537368245871690, -47.66695236827169424 ) ) ;
#60831=VECTOR ( 'NONE', #25643, 1000.000000000000114 ) ;
#60834=LINE ( 'NONE', #13252, #33074 ) ;
#60840=DIRECTION ( 'NONE',  ( 0.000000000000000000, 0.000000000000000000, 1.000000000000000000 ) ) ;
#60842=CARTESIAN_POINT ( 'NONE',  ( -2.569797478183783568, 3.352038560005916601, -14.24379821351254094 ) ) ;
#60843=CARTESIAN_POINT ( 'NONE',  ( 0.8760168074886960365, 11.58706983520261069, 46.68716261866180162 ) ) ;
#60846=EDGE_LOOP ( 'NONE', ( #26220, #16155, #23695, #33868 ) ) ;
#60847=ORIENTED_EDGE ( 'NONE', *, *, #60171, .T. ) ;
#60858=ORIENTED_EDGE ( 'NONE', *, *, #40466, .T. ) ;
#60868=CARTESIAN_POINT ( 'NONE',  ( 0.1084644655670282676, 21.90577137312941147, 37.14658555883740121 ) ) ;
#60875=AXIS2_PLACEMENT_3D ( 'NONE', #36655, #16933, #26614 ) ;
#60879=CARTESIAN_POINT ( 'NONE',  ( 0.6031356755773454870, 34.01708126935042031, -34.01711753073222866 ) ) ;
#60881=CARTESIAN_POINT ( 'NONE',  ( 0.6001305935487315502, -29.70149728382410714, -37.84751346122845916 ) ) ;
#60886=B_SPLINE_CURVE_WITH_KNOTS ( 'NONE', 3,
 ( #33735, #488, #34046, #9916 ),
 .UNSPECIFIED., .F., .F.,
 ( 4, 4 ),
 ( 0.000000000000000000, 0.005014147105413701254 ),
 .UNSPECIFIED. ) ;
#60887=CARTESIAN_POINT ( 'NONE',  ( 0.7048096507298635682, 47.58126109679103166, -7.115188260603352965 ) ) ;
#60889=EDGE_LOOP ( 'NONE', ( #17269, #42841, #25892, #40636 ) ) ;
#60895=EDGE_CURVE ( 'NONE', #23287, #5908, #23426, .T. ) ;
#60906=CARTESIAN_POINT ( 'NONE',  ( 0.6254311100348673991, -46.28443883864387942, -13.11433105842126601 ) ) ;
#60908=( BOUNDED_SURFACE ( )  B_SPLINE_SURFACE ( 3, 1, ( 
 ( #12955, #61747 ),
 ( #37070, #22958 ),
 ( #42688, #51430 ),
 ( #46462, #27958 ) ),
 .UNSPECIFIED., .F., .F., .F. ) 
 B_SPLINE_SURFACE_WITH_KNOTS ( ( 4, 4 ),
 ( 2, 2 ),
 ( 0.000000000000000000, 1.000000000000000000 ),
 ( 0.000000000000000000, 1.000000000000000000 ),
 .UNSPECIFIED. ) 
 GEOMETRIC_REPRESENTATION_ITEM ( )  RATIONAL_B_SPLINE_SURFACE ( (
 ( 1.000000000000000000, 1.000000000000000000),
 ( 0.7223157951917476005, 0.9931996967497186413),
 ( 0.7223157951917476005, 0.9931996967497186413),
 ( 1.000000000000000000, 1.000000000000000000) ) ) 
 REPRESENTATION_ITEM ( '' )  SURFACE ( )  );
#60910=EDGE_LOOP ( 'NONE', ( #3529, #27536, #38574, #29344 ) ) ;
#60917=B_SPLINE_CURVE_WITH_KNOTS ( 'NONE', 3,
 ( #36970, #21924, #50117, #22540 ),
 .UNSPECIFIED., .F., .F.,
 ( 4, 4 ),
 ( 0.000000000000000000, 0.004445488388166990781 ),
 .UNSPECIFIED. ) ;
#60920=B_SPLINE_CURVE_WITH_KNOTS ( 'NONE', 3,
 ( #42191, #60622, #51232, #3611, #8023, #61248 ),
 .UNSPECIFIED., .F., .F.,
 ( 4, 2, 4 ),
 ( 1.292312595306281327E-16, 0.0002450741128632353779, 0.0004901482257263415189 ),
 .UNSPECIFIED. ) ;
#60926=CARTESIAN_POINT ( 'NONE',  ( 0.6023142530420679819, -46.53533807097421260, -12.19802990522784469 ) ) ;
#60929=CARTESIAN_POINT ( 'NONE',  ( 0.1100053167205930771, -43.12409768020066281, 0.1794603581042977236 ) ) ;
#60937=CARTESIAN_POINT ( 'NONE',  ( 0.8760168074886960365, 33.37827814204077015, 34.63873394077499057 ) ) ;
#60939=VERTEX_POINT ( 'NONE', #13604 ) ;
#60943=CARTESIAN_POINT ( 'NONE',  ( 0.6017667736363749853, 41.48674115080369518, 24.35549005323431260 ) ) ;
#60947=CARTESIAN_POINT ( 'NONE',  ( -6.016104459813374383, -7.215917642689192668, 17.40682403289246238 ) ) ;
#60948=EDGE_CURVE ( 'NONE', #43360, #24504, #16659, .T. ) ;
#60952=ORIENTED_EDGE ( 'NONE', *, *, #60895, .T. ) ;
#60953=CARTESIAN_POINT ( 'NONE',  ( 0.6031357023905875581, -47.69018446756504659, -6.322524267548415011 ) ) ;
#60957=CARTESIAN_POINT ( 'NONE',  ( 0.7954196712028472893, -7.138712347928534818, 47.56618050291063327 ) ) ;
#60960=FACE_OUTER_BOUND ( 'NONE', #25899, .T. ) ;
#60971=CARTESIAN_POINT ( 'NONE',  ( 4.691466044806102964, 29.64918311951129226, -33.30232861642401332 ) ) ;
#60973=FACE_OUTER_BOUND ( 'NONE', #44666, .T. ) ;
#60983=DIRECTION ( 'NONE',  ( 0.09835009131224552170, 0.9951218349151971232, -0.007732607185420483503 ) ) ;
#60984=CARTESIAN_POINT ( 'NONE',  ( 0.8760168074887090262, -47.56749362999718045, 7.161346975772893586 ) ) ;
#60990=LINE ( 'NONE', #18098, #56998 ) ;
#60991=CARTESIAN_POINT ( 'NONE',  ( 4.691466044806102076, -33.30232861642411990, -29.64918311951117502 ) ) ;
#60992=CARTESIAN_POINT ( 'NONE',  ( 0.7245667037590741710, -41.24129124474318075, 24.75815201345775662 ) ) ;
#60995=CARTESIAN_POINT ( 'NONE',  ( 0.6029303876144825880, 47.67862422489724850, 6.409038528276291835 ) ) ;
#60997=DIRECTION ( 'NONE',  ( 0.000000000000000000, 0.000000000000000000, 1.000000000000000000 ) ) ;
#60999=CARTESIAN_POINT ( 'NONE',  ( 0.1073791018717483448, -5.147744207007177053, 42.81622261970985477 ) ) ;
#61000=ORIENTED_EDGE ( 'NONE', *, *, #47258, .F. ) ;
#61007=( BOUNDED_SURFACE ( )  B_SPLINE_SURFACE ( 3, 1, ( 
 ( #34489, #19164 ),
 ( #4701, #28529 ),
 ( #38275, #53560 ),
 ( #10677, #19462 ) ),
 .UNSPECIFIED., .F., .F., .F. ) 
 B_SPLINE_SURFACE_WITH_KNOTS ( ( 4, 4 ),
 ( 2, 2 ),
 ( 0.000000000000000000, 1.000000000000000000 ),
 ( 0.000000000000000000, 1.000000000000000000 ),
 .UNSPECIFIED. ) 
 GEOMETRIC_REPRESENTATION_ITEM ( )  RATIONAL_B_SPLINE_SURFACE ( (
 ( 1.000000000000000000, 1.000000000000000000),
 ( 0.7223157951917480446, 0.9931996967497186413),
 ( 0.7223157951917480446, 0.9931996967497186413),
 ( 1.000000000000000000, 1.000000000000000000) ) ) 
 REPRESENTATION_ITEM ( '' )  SURFACE ( )  );
#61012=CARTESIAN_POINT ( 'NONE',  ( 4.322998006666165516, -47.25487450103530307, -8.359821156456311186 ) ) ;
#61021=EDGE_CURVE ( 'NONE', #54056, #4316, #2942, .T. ) ;
#61023=CARTESIAN_POINT ( 'NONE',  ( -6.010958268070873523, -18.84344976839986785, -0.01451635840183061917 ) ) ;
#61025=LINE ( 'NONE', #8399, #45569 ) ;
#61028=CARTESIAN_POINT ( 'NONE',  ( 0.1087620492084205026, 25.96440931622084847, 34.43219573047441173 ) ) ;
#61040=ORIENTED_EDGE ( 'NONE', *, *, #15648, .F. ) ;
#61053=CARTESIAN_POINT ( 'NONE',  ( 0.1101816497532062955, -21.67974746580523870, -37.27878591512666162 ) ) ;
#61054=CARTESIAN_POINT ( 'NONE',  ( 0.5988103622719986863, 47.61318311633114320, 6.880137819455026005 ) ) ;
#61057=CARTESIAN_POINT ( 'NONE',  ( 0.6041374136657475802, 41.74951251761573445, -23.90252055111279716 ) ) ;
#61058=ORIENTED_EDGE ( 'NONE', *, *, #54278, .F. ) ;
#61065=ORIENTED_EDGE ( 'NONE', *, *, #44370, .T. ) ;
#61069=CARTESIAN_POINT ( 'NONE',  ( 3.238931869106855377, -1.828840280769088000, -42.95312220797016067 ) ) ;
#61074=CARTESIAN_POINT ( 'NONE',  ( 0.3622758884714600280, 41.85013935980101962, -10.35929834645879133 ) ) ;
#61082=CARTESIAN_POINT ( 'NONE',  ( 4.975801465491695552, 47.10002938642130488, 8.787181743660319455 ) ) ;
#61093=ORIENTED_EDGE ( 'NONE', *, *, #41396, .T. ) ;
#61096=EDGE_LOOP ( 'NONE', ( #38395, #36855, #46547, #35104 ) ) ;
#61099=CARTESIAN_POINT ( 'NONE',  ( -6.015611763856276717, 16.31561949997075445, 9.427003116184231146 ) ) ;
#61108=CARTESIAN_POINT ( 'NONE',  ( 4.975801465491695552, 0.000000000000000000, 0.000000000000000000 ) ) ;
#61109=ORIENTED_EDGE ( 'NONE', *, *, #32155, .T. ) ;
#61120=DIRECTION ( 'NONE',  ( 0.000000000000000000, 0.000000000000000000, 1.000000000000000000 ) ) ;
#61128=CARTESIAN_POINT ( 'NONE',  ( -6.016761891674564211, 18.68153697670645030, -2.462934516563616949 ) ) ;
#61138=CARTESIAN_POINT ( 'NONE',  ( 0.1097557419366048670, -21.36873056345920219, 37.45792859959189514 ) ) ;
#61141=FACE_OUTER_BOUND ( 'NONE', #21496, .T. ) ;
#61142=EDGE_CURVE ( 'NONE', #19392, #51621, #9194, .T. ) ;
#61147=CARTESIAN_POINT ( 'NONE',  ( 0.6017667736363749853, 46.55748817282775320, -12.11362382130087845 ) ) ;
#61149=CARTESIAN_POINT ( 'NONE',  ( 0.7048096507298635682, 24.78213711671542185, 41.23648859290934610 ) ) ;
#61150=ORIENTED_EDGE ( 'NONE', *, *, #28147, .T. ) ;
#61162=ORIENTED_EDGE ( 'NONE', *, *, #43575, .F. ) ;
#61164=EDGE_CURVE ( 'NONE', #21388, #22462, #45090, .T. ) ;
#61173=VERTEX_POINT ( 'NONE', #20760 ) ;
#61179=CARTESIAN_POINT ( 'NONE',  ( 0.6023143664670691511, -48.10676742339276046, -0.2618215695305907698 ) ) ;
#61185=CARTESIAN_POINT ( 'NONE',  ( 0.6041374136657476912, 33.89363087703046773, -34.14050483116103862 ) ) ;
#61190=B_SPLINE_CURVE_WITH_KNOTS ( 'NONE', 3,
 ( #20931, #50352, #30319, #55044 ),
 .UNSPECIFIED., .F., .F.,
 ( 4, 4 ),
 ( 4.670885906470169154E-18, 0.004566006591234647236 ),
 .UNSPECIFIED. ) ;
#61192=FACE_OUTER_BOUND ( 'NONE', #20845, .T. ) ;
#61197=EDGE_CURVE ( 'NONE', #34095, #30211, #6856, .T. ) ;
#61198=CARTESIAN_POINT ( 'NONE',  ( 4.975801465491695552, 36.39623109580423943, 31.15993731089136887 ) ) ;
#61214=VERTEX_POINT ( 'NONE', #11359 ) ;
#61217=CARTESIAN_POINT ( 'NONE',  ( -6.016104459813371719, -11.46679299034590827, 14.95258000663128328 ) ) ;
#61218=CARTESIAN_POINT ( 'NONE',  ( 0.8760168074886965917, -37.61398439004513961, -29.98565522133333516 ) ) ;
#61221=CARTESIAN_POINT ( 'NONE',  ( 0.1081432562775997558, 42.69830087850304068, 6.048481838666182497 ) ) ;
#61223=CARTESIAN_POINT ( 'NONE',  ( 0.8751705887134423323, -23.27176129838396790, -42.09020928323367627 ) ) ;
#61228=EDGE_CURVE ( 'NONE', #9105, #17449, #27000, .T. ) ;
#61229=CARTESIAN_POINT ( 'NONE',  ( 0.09136607875274982415, 0.000000000000000000, 43.12527911185304674 ) ) ;
#61232=CARTESIAN_POINT ( 'NONE',  ( 0.1084644655670282398, -43.12277244437005663, 0.3976617192056919881 ) ) ;
#61240=CIRCLE ( 'NONE', #14230, 42.92674063221959813 ) ;
#61247=CARTESIAN_POINT ( 'NONE',  ( 0.8760168074887076939, -34.63873394077464951, -33.37827814204112542 ) ) ;
#61248=CARTESIAN_POINT ( 'NONE',  ( 0.5998501479064708430, -23.59887241503325228, -41.92175333043611829 ) ) ;
#61249=B_SPLINE_CURVE_WITH_KNOTS ( 'NONE', 3,
 ( #2537, #59861, #53598, #48925, #5974, #11333 ),
 .UNSPECIFIED., .F., .F.,
 ( 4, 2, 4 ),
 ( 8.471125239557413953E-17, 0.0002293366620881436295, 0.0004586733241762025828 ),
 .UNSPECIFIED. ) ;
#61266=VERTEX_POINT ( 'NONE', #37044 ) ;
#61271=EDGE_LOOP ( 'NONE', ( #11741, #41203, #2136, #27126 ) ) ;
#61277=CARTESIAN_POINT ( 'NONE',  ( 0.6031356219577718170, -29.35521383643431292, -38.11305734842053283 ) ) ;
#61281=CARTESIAN_POINT ( 'NONE',  ( 0.6031356219577718170, 47.68448279784254851, -6.365832241666079305 ) ) ;
#61284=DIRECTION ( 'NONE',  ( 0.1024043820194936449, -0.5087173657443522234, -0.8548216096550979026 ) ) ;
#61293=CARTESIAN_POINT ( 'NONE',  ( 0.8751705887134423323, 37.60752970653787486, 29.98056538504974000 ) ) ;
#61297=CARTESIAN_POINT ( 'NONE',  ( 0.6025881611877910160, 47.66695236827166582, 6.495537368246036003 ) ) ;
#61302=EDGE_CURVE ( 'NONE', #593, #29811, #51695, .T. ) ;
#61303=CARTESIAN_POINT ( 'NONE',  ( -6.016761891674565099, -9.424569481870369358, 16.31696541414269319 ) ) ;
#61313=CARTESIAN_POINT ( 'NONE',  ( 3.238741278300273141, -12.88350628398768905, 41.01623499585991794 ) ) ;
#61314=EDGE_CURVE ( 'NONE', #33419, #32395, #32690, .T. ) ;
#61319=CARTESIAN_POINT ( 'NONE',  ( -6.015611763856276717, -4.870987357968047604, -18.20278301740941629 ) ) ;
#61325=CARTESIAN_POINT ( 'NONE',  ( 3.238741278300274029, -42.95313747363663026, -1.828728677531676228 ) ) ;
#61344=DIRECTION ( 'NONE',  ( 1.000000000000000000, 0.000000000000000000, 0.000000000000000000 ) ) ;
#61348=ORIENTED_EDGE ( 'NONE', *, *, #55727, .F. ) ;
#61351=LINE ( 'NONE', #23779, #8947 ) ;
#61358=CARTESIAN_POINT ( 'NONE',  ( 4.549368137175248350, 35.80950303116068056, 23.67244292351653101 ) ) ;
#61366=CARTESIAN_POINT ( 'NONE',  ( 0.1064266418746776799, 34.55203617814591155, -25.80493189480195326 ) ) ;
#61372=EDGE_CURVE ( 'NONE', #61502, #40551, #33260, .T. ) ;
#61373=CARTESIAN_POINT ( 'NONE',  ( 3.680882792899938583, -43.58303137875421385, 20.05474345988731955 ) ) ;
#61382=CARTESIAN_POINT ( 'NONE',  ( -6.016104459813374383, 16.32137543786095790, -9.416989654584133618 ) ) ;
#61387=DIRECTION ( 'NONE',  ( 0.000000000000000000, 0.000000000000000000, 1.000000000000000000 ) ) ;
#61390=CARTESIAN_POINT ( 'NONE',  ( 0.7048096507298635682, -47.80151517212783574, -5.442192462019296073 ) ) ;
#61392=ORIENTED_EDGE ( 'NONE', *, *, #50777, .T. ) ;
#61404=ORIENTED_EDGE ( 'NONE', *, *, #2763, .F. ) ;
#61409=ORIENTED_EDGE ( 'NONE', *, *, #16204, .F. ) ;
#61416=ORIENTED_EDGE ( 'NONE', *, *, #24626, .T. ) ;
#61423=DIRECTION ( 'NONE',  ( 0.000000000000000000, 0.000000000000000000, 1.000000000000000000 ) ) ;
#61424=ORIENTED_EDGE ( 'NONE', *, *, #52111, .T. ) ;
#61427=FACE_OUTER_BOUND ( 'NONE', #29045, .T. ) ;
#61428=CARTESIAN_POINT ( 'NONE',  ( 3.680882792899937250, -20.05474345988779561, -43.58303137875400068 ) ) ;
#61436=CARTESIAN_POINT ( 'NONE',  ( 0.1073791018717483448, -37.10214135362904386, 21.98088480513601795 ) ) ;
#61442=ADVANCED_FACE ( 'NONE', ( #59190 ), #4025, .F. ) ;
#61443=B_SPLINE_CURVE_WITH_KNOTS ( 'NONE', 3,
 ( #50624, #7714, #55627, #60632, #22445, #17751 ),
 .UNSPECIFIED., .F., .F.,
 ( 4, 2, 4 ),
 ( 8.542799345870747147E-17, 0.0002293366620881467195, 0.0004586733241762080038 ),
 .UNSPECIFIED. ) ;
#61451=FACE_OUTER_BOUND ( 'NONE', #7746, .T. ) ;
#61453=EDGE_LOOP ( 'NONE', ( #11326, #43505, #49705, #61638 ) ) ;
#61466=VERTEX_POINT ( 'NONE', #20083 ) ;
#61468=DIRECTION ( 'NONE',  ( 0.000000000000000000, 0.000000000000000000, -1.000000000000000000 ) ) ;
#61471=CARTESIAN_POINT ( 'NONE',  ( 4.322998006666165516, -27.50295597456424446, -39.32552843303840717 ) ) ;
#61481=CARTESIAN_POINT ( 'NONE',  ( -6.016761891674564211, 14.94721834528430371, -11.47373234755488092 ) ) ;
#61483=CARTESIAN_POINT ( 'NONE',  ( 5.880360259849739535, -45.41096578730658706, 15.46489389606675147 ) ) ;
#61489=ORIENTED_EDGE ( 'NONE', *, *, #25114, .T. ) ;
#61491=EDGE_CURVE ( 'NONE', #54789, #46497, #46507, .T. ) ;
#61502=VERTEX_POINT ( 'NONE', #29456 ) ;
#61504=CARTESIAN_POINT ( 'NONE',  ( 0.1087620492084205026, -42.80136086877936918, 5.269740196867194193 ) ) ;
#61506=AXIS2_PLACEMENT_3D ( 'NONE', #14066, #42569, #19076 ) ;
#61510=CARTESIAN_POINT ( 'NONE',  ( 3.238741278300274029, -32.96375560769479307, -27.59904135366523548 ) ) ;
#61518=EDGE_CURVE ( 'NONE', #4313, #17449, #18103, .T. ) ;
#61519=CARTESIAN_POINT ( 'NONE',  ( 0.6001305935487422083, -6.798494447612560165, 47.62765676940932025 ) ) ;
#61520=CARTESIAN_POINT ( 'NONE',  ( 0.1081432562775997835, -33.95357233988211476, -26.58728936586504688 ) ) ;
#61523=CARTESIAN_POINT ( 'NONE',  ( 3.680974057930773924, 44.99871514631792024, -16.63696281867813909 ) ) ;
#61526=ADVANCED_FACE ( 'NONE', ( #41660 ), #38469, .F. ) ;
#61535=EDGE_CURVE ( 'NONE', #38633, #20738, #51029, .T. ) ;
#61539=CARTESIAN_POINT ( 'NONE',  ( 0.6017666602106489515, -44.57804174182710000, -18.08695057064577583 ) ) ;
#61541=( BOUNDED_SURFACE ( )  B_SPLINE_SURFACE ( 3, 1, ( 
 ( #46919, #22167 ),
 ( #27786, #46295 ),
 ( #3955, #23095 ),
 ( #3339, #22468 ) ),
 .UNSPECIFIED., .F., .F., .F. ) 
 B_SPLINE_SURFACE_WITH_KNOTS ( ( 4, 4 ),
 ( 2, 2 ),
 ( 0.000000000000000000, 1.000000000000000000 ),
 ( 0.000000000000000000, 1.000000000000000000 ),
 .UNSPECIFIED. ) 
 GEOMETRIC_REPRESENTATION_ITEM ( )  RATIONAL_B_SPLINE_SURFACE ( (
 ( 1.000000000000000000, 1.000000000000000000),
 ( 0.9953040768229013402, 0.8617119497784988535),
 ( 0.9953040768229013402, 0.8617119497784988535),
 ( 1.000000000000000000, 1.000000000000000000) ) ) 
 REPRESENTATION_ITEM ( '' )  SURFACE ( )  );
#61544=ORIENTED_EDGE ( 'NONE', *, *, #34344, .T. ) ;
#61551=CARTESIAN_POINT ( 'NONE',  ( 0.5980894510889457338, -34.51330645350379456, -33.52121017007815595 ) ) ;
#61552=FACE_OUTER_BOUND ( 'NONE', #23056, .T. ) ;
#61554=CARTESIAN_POINT ( 'NONE',  ( -2.569797478183783568, 6.011723966603960356, 13.34095667500607085 ) ) ;
#61556=CARTESIAN_POINT ( 'NONE',  ( -6.010958268070873523, -9.434296419346321017, 16.31164801516939278 ) ) ;
#61558=EDGE_LOOP ( 'NONE', ( #39262, #29581, #20199, #46726 ) ) ;
#61560=DIRECTION ( 'NONE',  ( -1.000000000000000000, -0.000000000000000000, -0.000000000000000000 ) ) ;
#61568=EDGE_CURVE ( 'NONE', #50920, #31073, #7046, .T. ) ;
#61571=CARTESIAN_POINT ( 'NONE',  ( 0.6001305935487422083, -34.38748867424735778, 33.64689939321883116 ) ) ;
#61585=CARTESIAN_POINT ( 'NONE',  ( 0.6031357023905875581, 47.70157053127529423, -6.236038527293559675 ) ) ;
#61586=B_SPLINE_CURVE_WITH_KNOTS ( 'NONE', 3,
 ( #45993, #26856, #22772, #22163 ),
 .UNSPECIFIED., .F., .F.,
 ( 4, 4 ),
 ( 2.012794395885733147E-17, 0.004444306975806116763 ),
 .UNSPECIFIED. ) ;
#61587=CARTESIAN_POINT ( 'NONE',  ( 0.1101816497532063371, 16.37745527993589434, -39.89358705406968397 ) ) ;
#61589=CARTESIAN_POINT ( 'NONE',  ( 0.8760168074886960365, -37.61398439004513961, -29.98565522133333161 ) ) ;
#61606=CARTESIAN_POINT ( 'NONE',  ( 0.5980894510889457338, 23.44630161211586383, -42.01322166096895216 ) ) ;
#61607=ORIENTED_EDGE ( 'NONE', *, *, #36173, .F. ) ;
#61609=CARTESIAN_POINT ( 'NONE',  ( 0.8751705887134553219, -28.56654290188682666, 38.69254731947783199 ) ) ;
#61617=EDGE_LOOP ( 'NONE', ( #24578, #22296, #27844, #12898 ) ) ;
#61618=CARTESIAN_POINT ( 'NONE',  ( 4.975801465491694664, -15.94009207553080643, 45.18341283946430309 ) ) ;
#61619=CARTESIAN_POINT ( 'NONE',  ( 4.549368137175248350, 23.67244292351640667, -35.80950303116076583 ) ) ;
#61620=VERTEX_POINT ( 'NONE', #46063 ) ;
#61624=CARTESIAN_POINT ( 'NONE',  ( -6.016761891674564211, 17.40752468084793136, -7.214149619366169830 ) ) ;
#61627=ORIENTED_EDGE ( 'NONE', *, *, #49081, .F. ) ;
#61629=CARTESIAN_POINT ( 'NONE',  ( 0.1084644655670282398, 26.56696682929009867, 33.96951444491432426 ) ) ;
#61634=CARTESIAN_POINT ( 'NONE',  ( 2.301430502907646503, 33.04218380901171770, 34.86297247504486307 ) ) ;
#61636=ORIENTED_EDGE ( 'NONE', *, *, #50571, .F. ) ;
#61637=DIRECTION ( 'NONE',  ( -0.1024043820194934645, -0.6159418278945602010, 0.7811075516170060684 ) ) ;
#61638=ORIENTED_EDGE ( 'NONE', *, *, #57142, .T. ) ;
#61643=VECTOR ( 'NONE', #6968, 1000.000000000000114 ) ;
#61645=B_SPLINE_CURVE_WITH_KNOTS ( 'NONE', 3,
 ( #57119, #23630, #32734, #43066 ),
 .UNSPECIFIED., .F., .F.,
 ( 4, 4 ),
 ( 7.152448122690996019E-18, 0.005014147105413700387 ),
 .UNSPECIFIED. ) ;
#61648=VERTEX_POINT ( 'NONE', #28457 ) ;
#61654=VERTEX_POINT ( 'NONE', #52570 ) ;
#61681=CARTESIAN_POINT ( 'NONE',  ( 5.880360259849752858, -36.09847387447880607, 31.59460303415922411 ) ) ;
#61682=EDGE_LOOP ( 'NONE', ( #2176, #53792, #59003, #42099 ) ) ;
#61685=CARTESIAN_POINT ( 'NONE',  ( 0.6001305935487315502, 12.95698906763746017, 46.33281397023068138 ) ) ;
#61691=CARTESIAN_POINT ( 'NONE',  ( 0.3622758884714600280, -20.83792692158946025, -37.74294673546579304 ) ) ;
#61695=CARTESIAN_POINT ( 'NONE',  ( 0.1310142868023685681, -17.08943085418612995, 39.59283406808302885 ) ) ;
#61696=B_SPLINE_CURVE_WITH_KNOTS ( 'NONE', 3,
 ( #14561, #44311, #43379, #57733, #33976, #53050, #19874, #9844, #1339, #20180, #43693, #39293, #39605, #5422, #58659, #53962 ),
 .UNSPECIFIED., .F., .F.,
 ( 4, 3, 3, 3, 3, 4 ),
 ( 1.868480190406682863E-17, 0.0002618515315864450668, 0.0003927756766342005933, 0.0005236998216950575647, 0.0007855159896329933682, 0.001047349442285928738 ),
 .UNSPECIFIED. ) ;
#61697=ORIENTED_EDGE ( 'NONE', *, *, #42768, .T. ) ;
#61698=CARTESIAN_POINT ( 'NONE',  ( 2.643462169533613793, -43.83256147628748067, 19.65219740572111817 ) ) ;
#61699=ORIENTED_EDGE ( 'NONE', *, *, #13701, .F. ) ;
#61702=ORIENTED_EDGE ( 'NONE', *, *, #59781, .T. ) ;
#61708=EDGE_CURVE ( 'NONE', #21985, #868, #26481, .T. ) ;
#61719=CARTESIAN_POINT ( 'NONE',  ( 0.6001305935487422083, -24.50730504006429200, -41.40054608060284380 ) ) ;
#61732=EDGE_CURVE ( 'NONE', #60778, #36963, #8618, .T. ) ;
#61733=ORIENTED_EDGE ( 'NONE', *, *, #33627, .F. ) ;
#61739=CARTESIAN_POINT ( 'NONE',  ( 1.827326673878743701, -6.839036141888885645, 42.50320212329568648 ) ) ;
#61742=VECTOR ( 'NONE', #49603, 1000.000000000000000 ) ;
#61746=CARTESIAN_POINT ( 'NONE',  ( -6.010958268070873523, -16.31164801516948870, 9.434296419346148710 ) ) ;
#61747=CARTESIAN_POINT ( 'NONE',  ( 5.880360259849752858, 15.46489389606756149, -45.41096578730631705 ) ) ;
#61764=ORIENTED_EDGE ( 'NONE', *, *, #41078, .T. ) ;
#61768=B_SPLINE_CURVE_WITH_KNOTS ( 'NONE', 3,
 ( #50132, #45154, #6560, #44845 ),
 .UNSPECIFIED., .F., .F.,
 ( 4, 4 ),
 ( 2.030441771438897580E-17, 0.004444306975806115029 ),
 .UNSPECIFIED. ) ;
#61773=CARTESIAN_POINT ( 'NONE',  ( 4.549368137175248350, 0.000000000000000000, 0.000000000000000000 ) ) ;
#61776=DIRECTION ( 'NONE',  ( 0.000000000000000000, 0.000000000000000000, 1.000000000000000000 ) ) ;
#61779=CARTESIAN_POINT ( 'NONE',  ( 5.880360259849739535, -45.44137230084871248, -15.37531919565220129 ) ) ;
#61780=VERTEX_POINT ( 'NONE', #30528 ) ;
#61787=ORIENTED_EDGE ( 'NONE', *, *, #22492, .F. ) ;
#61788=CARTESIAN_POINT ( 'NONE',  ( 0.2230388203127586233, 41.44703429209685908, -11.89247826311231471 ) ) ;
#61789=CARTESIAN_POINT ( 'NONE',  ( 0.5980894510889457338, 5.583794302585253888, -47.78766676462070251 ) ) ;
#61796=EDGE_CURVE ( 'NONE', #56932, #53499, #55651, .T. ) ;
#61802=CARTESIAN_POINT ( 'NONE',  ( 0.5988103622719987973, 6.880137819454861692, -47.61318311633117872 ) ) ;
#61805=ORIENTED_EDGE ( 'NONE', *, *, #49580, .T. ) ;
#61806=ORIENTED_EDGE ( 'NONE', *, *, #42345, .T. ) ;
#61808=CARTESIAN_POINT ( 'NONE',  ( -6.015611763856276717, 14.95313250337445332, -11.46610900684707701 ) ) ;
#61811=CARTESIAN_POINT ( 'NONE',  ( -6.016761891674565099, 9.418621820384494470, 16.32039929810260048 ) ) ;
#61812=FACE_OUTER_BOUND ( 'NONE', #48854, .T. ) ;
#61813=CARTESIAN_POINT ( 'NONE',  ( 2.643462169533613793, 11.09243630552533055, -46.73820883660196301 ) ) ;
#61815=CARTESIAN_POINT ( 'NONE',  ( 0.2885700199627510010, -17.24062365614568293, -39.51953436244168216 ) ) ;
#61817=CARTESIAN_POINT ( 'NONE',  ( 4.549368137175248350, 0.000000000000000000, 0.000000000000000000 ) ) ;
#61824=DIRECTION ( 'NONE',  ( -1.000000000000000000, -0.000000000000000000, -0.000000000000000000 ) ) ;
#61833=ORIENTED_EDGE ( 'NONE', *, *, #24347, .T. ) ;
#61841=CARTESIAN_POINT ( 'NONE',  ( -2.708315649062916552, -4.041664582652708226, -14.06540004355481166 ) ) ;
#61845=ORIENTED_EDGE ( 'NONE', *, *, #7352, .F. ) ;
#61850=LINE ( 'NONE', #454, #25525 ) ;
#61855=ORIENTED_EDGE ( 'NONE', *, *, #30691, .F. ) ;
#61862=ADVANCED_FACE ( 'NONE', ( #31471 ), #25273, .F. ) ;
#61864=CARTESIAN_POINT ( 'NONE',  ( -6.015611763856276717, 9.427003116184170750, 16.31561949997079353 ) ) ;
#61873=EDGE_LOOP ( 'NONE', ( #6858, #3156, #36185, #20775 ) ) ;
#61880=CARTESIAN_POINT ( 'NONE',  ( -2.708315649062916552, 14.47261168455369607, -2.171184472130541998 ) ) ;
#61889=CARTESIAN_POINT ( 'NONE',  ( 4.975801465491694664, 9.906103548668228953, -46.87746200127445206 ) ) ;
#61896=CARTESIAN_POINT ( 'NONE',  ( -6.015611763856276717, -11.47596948473821321, 14.94556629257421498 ) ) ;
#61899=CARTESIAN_POINT ( 'NONE',  ( 0.8760168074887090262, -24.81951362746049483, -41.20610493656901241 ) ) ;
#61901=CARTESIAN_POINT ( 'NONE',  ( 3.238741278300274029, -24.69738534405286501, -35.19027457370170708 ) ) ;
#61905=DIRECTION ( 'NONE',  ( 1.000000000000000000, 0.000000000000000000, 0.000000000000000000 ) ) ;
#61907=CARTESIAN_POINT ( 'NONE',  ( 0.1310142868023678742, -25.74368468368911778, -34.59629828998408385 ) ) ;
#61925=CARTESIAN_POINT ( 'NONE',  ( 4.975801465491694664, 9.906103548668228953, -46.87746200127445206 ) ) ;
#61935=CARTESIAN_POINT ( 'NONE',  ( -6.016761891674564211, -13.32657647165345693, -13.32172022638605569 ) ) ;
#61939=CARTESIAN_POINT ( 'NONE',  ( -6.015611763856276717, -16.32183393015603556, 9.416239407363246272 ) ) ;
#61940=CARTESIAN_POINT ( 'NONE',  ( 2.301529144917016989, -40.93948199333351567, 25.12312032040438226 ) ) ;
#61941=CARTESIAN_POINT ( 'NONE',  ( 4.549368137175248350, -38.40568845698262379, -19.17571786012310753 ) ) ;
#61962=EDGE_CURVE ( 'NONE', #50661, #31157, #31046, .T. ) ;
#61964=CARTESIAN_POINT ( 'NONE',  ( 0.1103878639767399555, -34.18336104662756725, 26.29099398937389864 ) ) ;
ENDSEC;
END-ISO-10303-21;
